ISO-10303-21;
HEADER;
FILE_DESCRIPTION (('STEP AP214'),
    '1' );
FILE_NAME ('Injection Molded Chain Links 6.step',
    '2026-10-08T22:59:04',
    ( '' ),
    ( '' ),
    'SwSTEP 2.0',
    'SolidWorks 2020',
    '' );
FILE_SCHEMA (( 'AUTOMOTIVE_DESIGN' ));
ENDSEC;

DATA;
#17=CARTESIAN_POINT ( 'NONE',  ( -21.05000000000000071, 11.65000000001115232, -167.5999999999999659 ) ) ;
#26=TOROIDAL_SURFACE ( 'NONE', #183386, 0.4000000000000009104, 0.1000000000000000056 ) ;
#27=DIRECTION ( 'NONE',  ( -1.000000000000000000, -2.952720810173289112E-16, 0.000000000000000000 ) ) ;
#50=DIRECTION ( 'NONE',  ( -0.000000000000000000, -0.000000000000000000, 1.000000000000000000 ) ) ;
#112=CARTESIAN_POINT ( 'NONE',  ( 21.07928932188134397, 6.328516656404459262, -167.4011048543455615 ) ) ;
#116=EDGE_LOOP ( 'NONE', ( #122907, #87226, #174706, #3134 ) ) ;
#128=EDGE_CURVE ( 'NONE', #174631, #91171, #224322, .T. ) ;
#133=VERTEX_POINT ( 'NONE', #245061 ) ;
#135=DIRECTION ( 'NONE',  ( 0.000000000000000000, -1.000000000000000000, 0.000000000000000000 ) ) ;
#142=CARTESIAN_POINT ( 'NONE',  ( 20.12500000000000355, 10.24195072709382970, -175.3602037270860592 ) ) ;
#147=ORIENTED_EDGE ( 'NONE', *, *, #183774, .F. ) ;
#174=EDGE_CURVE ( 'NONE', #29202, #220627, #141140, .T. ) ;
#177=EDGE_LOOP ( 'NONE', ( #39245, #107994, #42022, #72538 ) ) ;
#182=EDGE_CURVE ( 'NONE', #9569, #208902, #126394, .T. ) ;
#186=DIRECTION ( 'NONE',  ( -0.000000000000000000, 0.1350103645451876666, 0.9908441862701600211 ) ) ;
#198=DIRECTION ( 'NONE',  ( 1.000000000000000000, 0.000000000000000000, 0.000000000000000000 ) ) ;
#213=CARTESIAN_POINT ( 'NONE',  ( 18.49999999999998934, 6.550000000011156231, -177.5170271704400022 ) ) ;
#251=CIRCLE ( 'NONE', #17030, 0.09999999999998898659 ) ;
#255=ORIENTED_EDGE ( 'NONE', *, *, #208280, .F. ) ;
#262=CYLINDRICAL_SURFACE ( 'NONE', #140052, 0.09999999999999939493 ) ;
#301=CARTESIAN_POINT ( 'NONE',  ( -21.59780538579341425, 6.847090529954407145, -167.4010213304019885 ) ) ;
#330=CARTESIAN_POINT ( 'NONE',  ( -20.54999999999999716, -8.999999999988844479, -191.1060308773475356 ) ) ;
#398=EDGE_CURVE ( 'NONE', #14558, #190027, #2320, .T. ) ;
#408=ORIENTED_EDGE ( 'NONE', *, *, #58975, .F. ) ;
#411=VERTEX_POINT ( 'NONE', #140497 ) ;
#429=VERTEX_POINT ( 'NONE', #64820 ) ;
#439=ORIENTED_EDGE ( 'NONE', *, *, #203304, .T. ) ;
#468=ORIENTED_EDGE ( 'NONE', *, *, #8297, .T. ) ;
#470=DIRECTION ( 'NONE',  ( 0.000000000000000000, 0.9998779222360096863, -0.01562500000001061998 ) ) ;
#482=CARTESIAN_POINT ( 'NONE',  ( -18.52643265882458579, 10.31973158071402530, -206.5505334713354273 ) ) ;
#493=VERTEX_POINT ( 'NONE', #148215 ) ;
#523=FILL_AREA_STYLE_COLOUR ( '', #40236 ) ;
#527=AXIS2_PLACEMENT_3D ( 'NONE', #46875, #130268, #126427 ) ;
#543=EDGE_CURVE ( 'NONE', #117026, #131456, #76254, .T. ) ;
#552=DIRECTION ( 'NONE',  ( 0.000000000000000000, 0.000000000000000000, -1.000000000000000000 ) ) ;
#553=ORIENTED_EDGE ( 'NONE', *, *, #95844, .F. ) ;
#573=CARTESIAN_POINT ( 'NONE',  ( 21.05000000000000071, 10.68429367439853905, -175.0266739386375150 ) ) ;
#667=EDGE_LOOP ( 'NONE', ( #215294, #148642, #179262, #17609, #245790 ) ) ;
#672=CARTESIAN_POINT ( 'NONE',  ( -23.15000000000000213, -8.999999999988846255, -176.8939691226524076 ) ) ;
#679=CARTESIAN_POINT ( 'NONE',  ( -23.25000000000000000, -1.835859311432481045, -212.6044391687984785 ) ) ;
#685=EDGE_CURVE ( 'NONE', #12588, #160946, #231620, .T. ) ;
#714=EDGE_LOOP ( 'NONE', ( #126745, #183780, #201751, #236755 ) ) ;
#763=ORIENTED_EDGE ( 'NONE', *, *, #124966, .T. ) ;
#805=ORIENTED_EDGE ( 'NONE', *, *, #207373, .F. ) ;
#806=FACE_OUTER_BOUND ( 'NONE', #236236, .T. ) ;
#808=EDGE_CURVE ( 'NONE', #17724, #122594, #59345, .T. ) ;
#814=DIRECTION ( 'NONE',  ( 0.000000000000000000, 0.000000000000000000, -1.000000000000000000 ) ) ;
#818=ORIENTED_EDGE ( 'NONE', *, *, #85034, .T. ) ;
#823=CARTESIAN_POINT ( 'NONE',  ( -22.59080734064478335, 11.75000000001115907, -167.4692502919029380 ) ) ;
#835=EDGE_CURVE ( 'NONE', #115342, #123667, #138878, .T. ) ;
#870=FACE_OUTER_BOUND ( 'NONE', #12758, .T. ) ;
#883=AXIS2_PLACEMENT_3D ( 'NONE', #48065, #246277, #168062 ) ;
#886=CIRCLE ( 'NONE', #254924, 0.09999999999998898659 ) ;
#888=ORIENTED_EDGE ( 'NONE', *, *, #177250, .T. ) ;
#906=CARTESIAN_POINT ( 'NONE',  ( -20.85000000000000142, -1.835859311432481045, -212.5044391687984842 ) ) ;
#921=CARTESIAN_POINT ( 'NONE',  ( 23.25000000000000000, -8.999999999988842703, -191.1060308773475072 ) ) ;
#963=DIRECTION ( 'NONE',  ( 0.000000000000000000, -1.734723475976997999E-14, 1.000000000000000000 ) ) ;
#972=DIRECTION ( 'NONE',  ( 6.938893903907991995E-14, 0.000000000000000000, 1.000000000000000000 ) ) ;
#1004=CARTESIAN_POINT ( 'NONE',  ( 21.05000000000000071, 1.115650877919449575E-11, -196.8999999999999773 ) ) ;
#1010=EDGE_CURVE ( 'NONE', #27613, #234902, #105062, .T. ) ;
#1020=DIRECTION ( 'NONE',  ( 0.000000000000000000, 0.000000000000000000, -1.000000000000000000 ) ) ;
#1033=CARTESIAN_POINT ( 'NONE',  ( 21.05000000000000071, 1.115600667400684642E-11, -200.9999999999999432 ) ) ;
#1034=TOROIDAL_SURFACE ( 'NONE', #80138, 7.800000000000000711, 0.1000000000000000056 ) ;
#1048=FACE_OUTER_BOUND ( 'NONE', #196732, .T. ) ;
#1050=ADVANCED_FACE ( 'NONE', ( #118760 ), #42562, .F. ) ;
#1079=CARTESIAN_POINT ( 'NONE',  ( 23.14999999999999503, 11.65000000001116298, -179.7499999999999716 ) ) ;
#1102=EDGE_LOOP ( 'NONE', ( #9288, #170503 ) ) ;
#1107=DIRECTION ( 'NONE',  ( -0.000000000000000000, 0.000000000000000000, 1.000000000000000000 ) ) ;
#1164=ORIENTED_EDGE ( 'NONE', *, *, #177190, .F. ) ;
#1208=CIRCLE ( 'NONE', #117918, 0.1999999999999987899 ) ;
#1227=CARTESIAN_POINT ( 'NONE',  ( -23.25000000000000000, -1.835859311432481045, -212.5044391687984842 ) ) ;
#1230=CIRCLE ( 'NONE', #21927, 11.80000000000000426 ) ;
#1307=CIRCLE ( 'NONE', #167950, 0.09999999999998898659 ) ;
#1315=DIRECTION ( 'NONE',  ( -1.000000000000000000, -0.000000000000000000, -0.000000000000000000 ) ) ;
#1326=ORIENTED_EDGE ( 'NONE', *, *, #86425, .F. ) ;
#1358=EDGE_LOOP ( 'NONE', ( #114954, #154136, #45014 ) ) ;
#1400=EDGE_CURVE ( 'NONE', #241874, #133509, #242653, .T. ) ;
#1539=ORIENTED_EDGE ( 'NONE', *, *, #4821, .T. ) ;
#1548=EDGE_CURVE ( 'NONE', #58178, #63249, #2309, .T. ) ;
#1555=DIRECTION ( 'NONE',  ( 0.000000000000000000, 0.000000000000000000, -1.000000000000000000 ) ) ;
#1564=DIRECTION ( 'NONE',  ( 0.000000000000000000, -2.664535259100430523E-15, -1.000000000000000000 ) ) ;
#1600=ORIENTED_EDGE ( 'NONE', *, *, #123794, .F. ) ;
#1606=DIRECTION ( 'NONE',  ( 1.000000000000000000, 7.304098846218134667E-16, -0.000000000000000000 ) ) ;
#1662=DIRECTION ( 'NONE',  ( 1.000000000000000000, 0.000000000000000000, 0.000000000000000000 ) ) ;
#1667=AXIS2_PLACEMENT_3D ( 'NONE', #224564, #87615, #44664 ) ;
#1689=VERTEX_POINT ( 'NONE', #90840 ) ;
#1695=CIRCLE ( 'NONE', #26674, 0.5000000000000013323 ) ;
#1699=DIRECTION ( 'NONE',  ( 0.000000000000000000, 0.5000000000000004441, 0.8660254037844384856 ) ) ;
#1708=ORIENTED_EDGE ( 'NONE', *, *, #138001, .F. ) ;
#1740=DIRECTION ( 'NONE',  ( 0.000000000000000000, -0.4999999999999478195, -0.8660254037844686836 ) ) ;
#1772=AXIS2_PLACEMENT_3D ( 'NONE', #171722, #253772, #95982 ) ;
#1773=CARTESIAN_POINT ( 'NONE',  ( -18.55121869061588669, 10.32747123227773045, -206.5774032850249000 ) ) ;
#1824=ORIENTED_EDGE ( 'NONE', *, *, #118042, .T. ) ;
#1829=LINE ( 'NONE', #244301, #75036 ) ;
#1844=CIRCLE ( 'NONE', #147615, 0.09999999999998898659 ) ;
#1846=CARTESIAN_POINT ( 'NONE',  ( 21.06600267594171783, 8.775166069211060460, -179.7042627823747125 ) ) ;
#1850=CARTESIAN_POINT ( 'NONE',  ( -23.15000000000000213, 11.65000000001115588, -179.6499999999999773 ) ) ;
#1861=CARTESIAN_POINT ( 'NONE',  ( -23.25000000000000000, 1.115600667400684642E-11, -200.9999999999999432 ) ) ;
#1924=TOROIDAL_SURFACE ( 'NONE', #35315, 0.2000000000000000111, 0.1000000000000000056 ) ;
#1931=ORIENTED_EDGE ( 'NONE', *, *, #44090, .T. ) ;
#1963=AXIS2_PLACEMENT_3D ( 'NONE', #187153, #72336, #107582 ) ;
#1975=CIRCLE ( 'NONE', #47763, 7.800000000000001599 ) ;
#1977=ADVANCED_FACE ( 'NONE', ( #106229 ), #130955, .F. ) ;
#1978=ORIENTED_EDGE ( 'NONE', *, *, #138333, .F. ) ;
#1995=CIRCLE ( 'NONE', #68659, 0.09999999999998898659 ) ;
#2022=CARTESIAN_POINT ( 'NONE',  ( -20.94999999999999929, -12.41227409413852811, -197.9999999999999432 ) ) ;
#2030=DIRECTION ( 'NONE',  ( -0.000000000000000000, 0.000000000000000000, 1.000000000000000000 ) ) ;
#2101=ORIENTED_EDGE ( 'NONE', *, *, #6458, .F. ) ;
#2115=DIRECTION ( 'NONE',  ( 0.000000000000000000, 0.000000000000000000, -1.000000000000000000 ) ) ;
#2120=DIRECTION ( 'NONE',  ( 0.000000000000000000, 0.9908441862701782288, -0.1350103645450542456 ) ) ;
#2124=CARTESIAN_POINT ( 'NONE',  ( -21.55000000000000071, 7.350000000011155166, -179.8499999999999943 ) ) ;
#2156=FACE_OUTER_BOUND ( 'NONE', #67120, .T. ) ;
#2169=CARTESIAN_POINT ( 'NONE',  ( 20.94999999999999574, -11.48912529306490349, -170.5999999999999659 ) ) ;
#2181=ORIENTED_EDGE ( 'NONE', *, *, #224044, .T. ) ;
#2199=EDGE_CURVE ( 'NONE', #166220, #129337, #219461, .T. ) ;
#2263=AXIS2_PLACEMENT_3D ( 'NONE', #76115, #20022, #117812 ) ;
#2288=DIRECTION ( 'NONE',  ( 0.000000000000000000, 0.000000000000000000, -1.000000000000000000 ) ) ;
#2301=CARTESIAN_POINT ( 'NONE',  ( -21.76363531954647357, 0.09900187431060442078, -160.4870634521282398 ) ) ;
#2309=LINE ( 'NONE', #81826, #246743 ) ;
#2312=DIRECTION ( 'NONE',  ( 0.000000000000000000, -0.8700118002898321601, 0.4930308989875230030 ) ) ;
#2320=CIRCLE ( 'NONE', #148096, 0.09999999999998898659 ) ;
#2345=DIRECTION ( 'NONE',  ( -0.000000000000000000, 0.1350103645451649625, -0.9908441862701631297 ) ) ;
#2363=ORIENTED_EDGE ( 'NONE', *, *, #1548, .T. ) ;
#2364=VERTEX_POINT ( 'NONE', #68113 ) ;
#2372=CARTESIAN_POINT ( 'NONE',  ( 23.14999999999998437, 1.115650265596050101E-11, -163.4499999999999886 ) ) ;
#2374=DIRECTION ( 'NONE',  ( 1.000000000000000000, 0.000000000000000000, 0.000000000000000000 ) ) ;
#2384=CARTESIAN_POINT ( 'NONE',  ( 23.15000000000000213, -9.599999999988842347, -191.1060308773475072 ) ) ;
#2391=DIRECTION ( 'NONE',  ( 0.000000000000000000, -1.000000000000000000, 0.000000000000000000 ) ) ;
#2392=ORIENTED_EDGE ( 'NONE', *, *, #12032, .T. ) ;
#2397=EDGE_CURVE ( 'NONE', #177487, #11610, #128089, .T. ) ;
#2398=AXIS2_PLACEMENT_3D ( 'NONE', #88626, #53379, #250294 ) ;
#2400=DIRECTION ( 'NONE',  ( 0.000000000000000000, 1.483188571960168804E-13, -1.000000000000000000 ) ) ;
#2418=ADVANCED_FACE ( 'NONE', ( #108518 ), #228484, .T. ) ;
#2425=AXIS2_PLACEMENT_3D ( 'NONE', #153513, #135160, #16531 ) ;
#2473=EDGE_CURVE ( 'NONE', #192876, #25429, #206345, .T. ) ;
#2487=DIRECTION ( 'NONE',  ( 0.000000000000000000, -0.1350103645451904977, 0.9908441862701596881 ) ) ;
#2495=CARTESIAN_POINT ( 'NONE',  ( 22.48660254037844197, 11.65000000001116298, -167.4499999999999602 ) ) ;
#2513=ORIENTED_EDGE ( 'NONE', *, *, #212335, .F. ) ;
#2522=DIRECTION ( 'NONE',  ( 2.952720810173289112E-16, -1.000000000000000000, -0.000000000000000000 ) ) ;
#2528=CARTESIAN_POINT ( 'NONE',  ( 22.47809213839789066, 0.03753706763967752658, -155.8500266652121695 ) ) ;
#2551=ORIENTED_EDGE ( 'NONE', *, *, #36169, .F. ) ;
#2559=CARTESIAN_POINT ( 'NONE',  ( 18.52928932188133970, 10.27928932189250411, -192.1499999999999488 ) ) ;
#2583=EDGE_CURVE ( 'NONE', #117760, #218080, #180668, .T. ) ;
#2594=CARTESIAN_POINT ( 'NONE',  ( -20.85000000000000142, 1.115600667400684642E-11, -200.9999999999999432 ) ) ;
#2599=DIRECTION ( 'NONE',  ( 1.000000000000000000, 0.000000000000000000, -0.000000000000000000 ) ) ;
#2696=DIRECTION ( 'NONE',  ( -1.000000000000000000, 0.000000000000000000, 0.000000000000000000 ) ) ;
#2713=CIRCLE ( 'NONE', #152790, 0.4000000000000114575 ) ;
#2714=AXIS2_PLACEMENT_3D ( 'NONE', #96080, #238160, #814 ) ;
#2719=CARTESIAN_POINT ( 'NONE',  ( -23.15000000000000213, 2.000000000011154189, -187.7753780772378889 ) ) ;
#2736=ORIENTED_EDGE ( 'NONE', *, *, #106681, .F. ) ;
#2740=AXIS2_PLACEMENT_3D ( 'NONE', #72863, #152397, #35025 ) ;
#2749=ORIENTED_EDGE ( 'NONE', *, *, #142897, .T. ) ;
#2754=DIRECTION ( 'NONE',  ( 0.000000000000000000, 0.000000000000000000, 1.000000000000000000 ) ) ;
#2757=CARTESIAN_POINT ( 'NONE',  ( -18.59999999999999787, 9.350000000011156942, -188.6499999999999488 ) ) ;
#2772=DIRECTION ( 'NONE',  ( 4.239556034732056743E-17, -0.1298341882520022972, -0.9915357197604853789 ) ) ;
#2799=DIRECTION ( 'NONE',  ( 1.000000000000000000, 3.265361837132813093E-16, -0.000000000000000000 ) ) ;
#2818=ADVANCED_FACE ( 'NONE', ( #179474 ), #193519, .T. ) ;
#2833=CARTESIAN_POINT ( 'NONE',  ( 18.59999999999999432, -1.299733671219632791, -157.5281295228693637 ) ) ;
#2849=ORIENTED_EDGE ( 'NONE', *, *, #229122, .T. ) ;
#2895=DIRECTION ( 'NONE',  ( 1.000000000000000000, -0.000000000000000000, -0.000000000000000000 ) ) ;
#2921=AXIS2_PLACEMENT_3D ( 'NONE', #248585, #85619, #146893 ) ;
#2934=DIRECTION ( 'NONE',  ( 0.000000000000000000, 0.000000000000000000, -1.000000000000000000 ) ) ;
#2943=CARTESIAN_POINT ( 'NONE',  ( 23.14999999999999858, 1.115600667400684642E-11, -202.9999999999999716 ) ) ;
#2949=CARTESIAN_POINT ( 'NONE',  ( 20.94999999999999929, -8.999999999988842703, -191.1060308773475072 ) ) ;
#2978=VERTEX_POINT ( 'NONE', #243259 ) ;
#2984=DIRECTION ( 'NONE',  ( 0.000000000000000000, 0.8700118002898321601, -0.4930308989875230585 ) ) ;
#3034=ORIENTED_EDGE ( 'NONE', *, *, #39800, .T. ) ;
#3051=DIRECTION ( 'NONE',  ( -1.000000000000000000, -2.952720810173289112E-16, 0.000000000000000000 ) ) ;
#3072=CIRCLE ( 'NONE', #36444, 0.09999999999998898659 ) ;
#3078=ORIENTED_EDGE ( 'NONE', *, *, #117560, .T. ) ;
#3097=LINE ( 'NONE', #184314, #70327 ) ;
#3134=ORIENTED_EDGE ( 'NONE', *, *, #46189, .F. ) ;
#3140=VECTOR ( 'NONE', #25579, 1000.000000000000000 ) ;
#3144=ORIENTED_EDGE ( 'NONE', *, *, #59982, .T. ) ;
#3164=AXIS2_PLACEMENT_3D ( 'NONE', #144993, #97845, #54883 ) ;
#3175=CARTESIAN_POINT ( 'NONE',  ( 18.52643265882457868, 10.31973158071402885, -206.5505334713354273 ) ) ;
#3198=VERTEX_POINT ( 'NONE', #56592 ) ;
#3200=CARTESIAN_POINT ( 'NONE',  ( -18.50000000000000000, 11.65000000001115588, -200.9999999999999432 ) ) ;
#3210=ORIENTED_EDGE ( 'NONE', *, *, #21143, .F. ) ;
#3230=EDGE_CURVE ( 'NONE', #75355, #172688, #14651, .T. ) ;
#3241=DIRECTION ( 'NONE',  ( 0.000000000000000000, 1.000000000000000000, -6.308085367188393199E-16 ) ) ;
#3252=VECTOR ( 'NONE', #158401, 1000.000000000000000 ) ;
#3261=DIRECTION ( 'NONE',  ( -1.000000000000000000, -2.952720810173289112E-16, 0.000000000000000000 ) ) ;
#3330=VECTOR ( 'NONE', #13475, 1000.000000000000000 ) ;
#3408=DIRECTION ( 'NONE',  ( 0.000000000000000000, 0.000000000000000000, -1.000000000000000000 ) ) ;
#3440=EDGE_LOOP ( 'NONE', ( #18861, #77108, #11709, #127194 ) ) ;
#3498=CARTESIAN_POINT ( 'NONE',  ( 23.24999999999999289, 6.650000000011155876, -179.6499999999999773 ) ) ;
#3532=ORIENTED_EDGE ( 'NONE', *, *, #224204, .T. ) ;
#3533=DIRECTION ( 'NONE',  ( -1.000000000000000000, -1.836970198721029934E-16, 0.000000000000000000 ) ) ;
#3589=EDGE_CURVE ( 'NONE', #13363, #127614, #172478, .T. ) ;
#3625=CIRCLE ( 'NONE', #190928, 0.09999999999998898659 ) ;
#3637=EDGE_CURVE ( 'NONE', #115507, #150045, #236250, .T. ) ;
#3647=CARTESIAN_POINT ( 'NONE',  ( -21.05000000000000071, 11.60000000001115517, -194.0717967697244717 ) ) ;
#3663=DIRECTION ( 'NONE',  ( 0.000000000000000000, -0.9893560106964500722, 0.1455152366551550613 ) ) ;
#3673=VERTEX_POINT ( 'NONE', #57599 ) ;
#3678=DIRECTION ( 'NONE',  ( 0.000000000000000000, 0.000000000000000000, -1.000000000000000000 ) ) ;
#3689=CARTESIAN_POINT ( 'NONE',  ( -18.59999999999999787, 11.65000000001115232, -174.5148057706539930 ) ) ;
#3720=CARTESIAN_POINT ( 'NONE',  ( 18.46163235739460973, -9.480150806907175820, -207.6576105398774530 ) ) ;
#3721=AXIS2_PLACEMENT_3D ( 'NONE', #28798, #106985, #228244 ) ;
#3731=DIRECTION ( 'NONE',  ( 0.000000000000000000, -1.000000000000000000, 0.000000000000000000 ) ) ;
#3733=DIRECTION ( 'NONE',  ( 0.000000000000000000, 0.000000000000000000, -1.000000000000000000 ) ) ;
#3739=CARTESIAN_POINT ( 'NONE',  ( -21.05000000000000071, 6.299230910103437608, -167.4015624999996703 ) ) ;
#3748=FACE_OUTER_BOUND ( 'NONE', #190198, .T. ) ;
#3764=LINE ( 'NONE', #113751, #157160 ) ;
#3784=EDGE_CURVE ( 'NONE', #34439, #163489, #243754, .T. ) ;
#3787=AXIS2_PLACEMENT_3D ( 'NONE', #105429, #165459, #242401 ) ;
#3797=CIRCLE ( 'NONE', #224540, 12.97499999999998721 ) ;
#3801=CARTESIAN_POINT ( 'NONE',  ( 22.50000000000000000, 11.64957080755595520, -167.3999999999999773 ) ) ;
#3802=EDGE_LOOP ( 'NONE', ( #9739, #90486, #211997, #23603 ) ) ;
#3821=CARTESIAN_POINT ( 'NONE',  ( -21.05000000000000071, 1.115600667400684642E-11, -167.4999999999999716 ) ) ;
#3828=CIRCLE ( 'NONE', #149595, 11.89999999999999325 ) ;
#3831=CARTESIAN_POINT ( 'NONE',  ( 20.94999999999999929, -12.41227409413852811, -197.9999999999999432 ) ) ;
#3854=ADVANCED_FACE ( 'NONE', ( #93540 ), #12753, .F. ) ;
#3866=CARTESIAN_POINT ( 'NONE',  ( 21.05000000000000071, 5.500000000011153745, -179.9052660189130677 ) ) ;
#3869=ORIENTED_EDGE ( 'NONE', *, *, #251492, .T. ) ;
#3874=ORIENTED_EDGE ( 'NONE', *, *, #30580, .F. ) ;
#3880=ORIENTED_EDGE ( 'NONE', *, *, #42529, .T. ) ;
#3902=CARTESIAN_POINT ( 'NONE',  ( -21.05000000000000071, 14.05000000001115623, -173.0136950707609458 ) ) ;
#3905=CARTESIAN_POINT ( 'NONE',  ( 21.14999999999999858, 10.71339244341104013, -179.7500000000000000 ) ) ;
#3919=ORIENTED_EDGE ( 'NONE', *, *, #245952, .T. ) ;
#3924=AXIS2_PLACEMENT_3D ( 'NONE', #6274, #153213, #187520 ) ;
#3951=ORIENTED_EDGE ( 'NONE', *, *, #210536, .F. ) ;
#3958=EDGE_CURVE ( 'NONE', #94619, #150045, #110663, .T. ) ;
#3974=CARTESIAN_POINT ( 'NONE',  ( 21.76363531954645936, 7.012936547882880234, -167.4009981257005393 ) ) ;
#3977=DIRECTION ( 'NONE',  ( 0.000000000000000000, -1.000000000000000000, 0.000000000000000000 ) ) ;
#3995=DIRECTION ( 'NONE',  ( -0.000000000000000000, -0.000000000000000000, -1.000000000000000000 ) ) ;
#4016=CARTESIAN_POINT ( 'NONE',  ( 20.94999999999999574, 1.835341550235567887, -179.0551512925629538 ) ) ;
#4021=DIRECTION ( 'NONE',  ( 0.000000000000000000, 0.000000000000000000, 1.000000000000000000 ) ) ;
#4060=CARTESIAN_POINT ( 'NONE',  ( 18.59999999999999432, 1.162701749949165642, -175.4999999999999716 ) ) ;
#4070=CARTESIAN_POINT ( 'NONE',  ( -18.59999999999999787, 1.261786168576181755, -175.5864989635454378 ) ) ;
#4086=EDGE_CURVE ( 'NONE', #103201, #133004, #31593, .T. ) ;
#4106=ORIENTED_EDGE ( 'NONE', *, *, #82251, .F. ) ;
#4193=ORIENTED_EDGE ( 'NONE', *, *, #40686, .F. ) ;
#4219=CARTESIAN_POINT ( 'NONE',  ( 20.94999999999999929, -1.835341550213257733, -179.0551512925629538 ) ) ;
#4264=VERTEX_POINT ( 'NONE', #16296 ) ;
#4287=LINE ( 'NONE', #179126, #207392 ) ;
#4296=VERTEX_POINT ( 'NONE', #150647 ) ;
#4297=AXIS2_PLACEMENT_3D ( 'NONE', #208281, #144409, #68762 ) ;
#4302=EDGE_CURVE ( 'NONE', #79726, #255690, #25842, .T. ) ;
#4307=CARTESIAN_POINT ( 'NONE',  ( 20.85000000000000142, 1.115600667400684642E-11, -208.7999999999999545 ) ) ;
#4310=CARTESIAN_POINT ( 'NONE',  ( -20.54999999999999716, -8.999999999988844479, -191.1060308773475356 ) ) ;
#4320=AXIS2_PLACEMENT_3D ( 'NONE', #130411, #206106, #245244 ) ;
#4322=AXIS2_PLACEMENT_3D ( 'NONE', #78111, #237208, #136805 ) ;
#4326=VERTEX_POINT ( 'NONE', #215732 ) ;
#4361=DIRECTION ( 'NONE',  ( 0.000000000000000000, 0.000000000000000000, -1.000000000000000000 ) ) ;
#4371=ADVANCED_FACE ( 'NONE', ( #59199 ), #236581, .F. ) ;
#4378=EDGE_LOOP ( 'NONE', ( #221382, #75733, #121298 ) ) ;
#4397=CIRCLE ( 'NONE', #229457, 0.5000000000000004441 ) ;
#4415=EDGE_CURVE ( 'NONE', #116285, #215160, #79963, .T. ) ;
#4440=CIRCLE ( 'NONE', #245878, 0.09999999999998898659 ) ;
#4442=AXIS2_PLACEMENT_3D ( 'NONE', #189892, #12560, #172941 ) ;
#4447=DIRECTION ( 'NONE',  ( 0.000000000000000000, 0.000000000000000000, -1.000000000000000000 ) ) ;
#4448=ORIENTED_EDGE ( 'NONE', *, *, #176572, .F. ) ;
#4453=CIRCLE ( 'NONE', #62735, 0.2000000000000057288 ) ;
#4480=DIRECTION ( 'NONE',  ( -0.000000000000000000, -0.8700118002898321601, 0.4930308989875230030 ) ) ;
#4495=VERTEX_POINT ( 'NONE', #77492 ) ;
#4496=CARTESIAN_POINT ( 'NONE',  ( -20.94999999999999929, 1.835341550235567887, -179.0551512925629538 ) ) ;
#4510=CARTESIAN_POINT ( 'NONE',  ( 18.59999999999999076, 11.65000000001115943, -192.3499999999999659 ) ) ;
#4511=DIRECTION ( 'NONE',  ( -1.000000000000000000, 0.000000000000000000, 0.000000000000000000 ) ) ;
#4571=ADVANCED_FACE ( 'NONE', ( #125636 ), #205153, .T. ) ;
#4599=CYLINDRICAL_SURFACE ( 'NONE', #219888, 0.09999999999999939493 ) ;
#4600=CIRCLE ( 'NONE', #66975, 0.2000000000000057288 ) ;
#4628=EDGE_LOOP ( 'NONE', ( #107414, #44209, #172063, #253771 ) ) ;
#4694=DIRECTION ( 'NONE',  ( 1.000000000000000000, 0.000000000000000000, 0.000000000000000000 ) ) ;
#4702=ADVANCED_FACE ( 'NONE', ( #141054 ), #1034, .T. ) ;
#4717=DIRECTION ( 'NONE',  ( 0.000000000000000000, 0.000000000000000000, -1.000000000000000000 ) ) ;
#4738=DIRECTION ( 'NONE',  ( -1.000000000000000000, 0.000000000000000000, 0.000000000000000000 ) ) ;
#4744=DIRECTION ( 'NONE',  ( 0.000000000000000000, 8.673617379884087537E-15, -1.000000000000000000 ) ) ;
#4745=DIRECTION ( 'NONE',  ( -1.000000000000000000, -0.000000000000000000, -0.000000000000000000 ) ) ;
#4790=DIRECTION ( 'NONE',  ( 0.000000000000000000, 0.000000000000000000, -1.000000000000000000 ) ) ;
#4793=CIRCLE ( 'NONE', #46499, 11.75000000000001066 ) ;
#4820=CARTESIAN_POINT ( 'NONE',  ( 20.84451136049651510, 10.62014191481791769, -174.9939245595323598 ) ) ;
#4821=EDGE_CURVE ( 'NONE', #146255, #134756, #167065, .T. ) ;
#4865=DIRECTION ( 'NONE',  ( 0.000000000000000000, -1.000000000000000000, 0.000000000000000000 ) ) ;
#4873=EDGE_CURVE ( 'NONE', #42259, #227290, #67711, .T. ) ;
#4875=PLANE ( 'NONE',  #142623 ) ;
#4881=FACE_OUTER_BOUND ( 'NONE', #132115, .T. ) ;
#4883=EDGE_LOOP ( 'NONE', ( #222595, #34866, #210855, #3951 ) ) ;
#4893=CARTESIAN_POINT ( 'NONE',  ( 21.14999999999999858, 6.257814610487280937, -167.4022097086911742 ) ) ;
#4899=ADVANCED_FACE ( 'NONE', ( #229581 ), #180157, .F. ) ;
#4938=FACE_OUTER_BOUND ( 'NONE', #210313, .T. ) ;
#4942=CYLINDRICAL_SURFACE ( 'NONE', #178171, 0.1000000000000101225 ) ;
#4948=DIRECTION ( 'NONE',  ( 0.000000000000000000, -0.9893560106964500722, 0.1455152366551550613 ) ) ;
#4982=EDGE_CURVE ( 'NONE', #20839, #87080, #213859, .T. ) ;
#4995=CARTESIAN_POINT ( 'NONE',  ( -22.00356870069946780, 1.195803586275321404E-11, -160.2457576382543323 ) ) ;
#5049=DIRECTION ( 'NONE',  ( -1.000000000000000000, 0.000000000000000000, 0.000000000000000000 ) ) ;
#5056=DIRECTION ( 'NONE',  ( 0.000000000000000000, 0.000000000000000000, 1.000000000000000000 ) ) ;
#5065=CARTESIAN_POINT ( 'NONE',  ( -18.50000000000000000, 9.150000000011157653, -155.7499999999999716 ) ) ;
#5072=CARTESIAN_POINT ( 'NONE',  ( 20.94999999999999574, -11.74999999998883560, -170.3999999999999773 ) ) ;
#5128=EDGE_CURVE ( 'NONE', #195513, #4326, #1230, .T. ) ;
#5135=AXIS2_PLACEMENT_3D ( 'NONE', #189164, #174783, #90046 ) ;
#5147=LINE ( 'NONE', #204648, #196811 ) ;
#5186=CIRCLE ( 'NONE', #175931, 0.09999999999999178990 ) ;
#5209=EDGE_CURVE ( 'NONE', #212963, #116440, #236687, .T. ) ;
#5216=ADVANCED_FACE ( 'NONE', ( #46761 ), #238579, .F. ) ;
#5217=ORIENTED_EDGE ( 'NONE', *, *, #209765, .T. ) ;
#5239=AXIS2_PLACEMENT_3D ( 'NONE', #172038, #151164, #134139 ) ;
#5304=CIRCLE ( 'NONE', #26380, 0.09999999999998898659 ) ;
#5317=DIRECTION ( 'NONE',  ( 0.7071067811865388020, -0.7071067811865561215, 0.000000000000000000 ) ) ;
#5321=CYLINDRICAL_SURFACE ( 'NONE', #138035, 0.09999999999998898659 ) ;
#5326=CYLINDRICAL_SURFACE ( 'NONE', #199567, 0.09999999999999864553 ) ;
#5349=AXIS2_PLACEMENT_3D ( 'NONE', #145713, #27099, #7497 ) ;
#5358=DIRECTION ( 'NONE',  ( 0.000000000000000000, 0.000000000000000000, 1.000000000000000000 ) ) ;
#5404=ORIENTED_EDGE ( 'NONE', *, *, #5739, .F. ) ;
#5422=LINE ( 'NONE', #25047, #40807 ) ;
#5454=AXIS2_PLACEMENT_3D ( 'NONE', #134936, #37173, #154569 ) ;
#5455=CARTESIAN_POINT ( 'NONE',  ( -23.25000000000000000, -1.835859311432481045, -212.5044391687984842 ) ) ;
#5488=EDGE_CURVE ( 'NONE', #224848, #11139, #90169, .T. ) ;
#5497=AXIS2_PLACEMENT_3D ( 'NONE', #49125, #45281, #7425 ) ;
#5511=ORIENTED_EDGE ( 'NONE', *, *, #72077, .F. ) ;
#5549=DIRECTION ( 'NONE',  ( 0.000000000000000000, -0.4999999999999413247, 0.8660254037844724584 ) ) ;
#5557=VERTEX_POINT ( 'NONE', #44865 ) ;
#5571=ORIENTED_EDGE ( 'NONE', *, *, #60961, .F. ) ;
#5578=ORIENTED_EDGE ( 'NONE', *, *, #156178, .F. ) ;
#5615=CARTESIAN_POINT ( 'NONE',  ( -18.59999999999999787, -1.164121893230052995, -208.7148480855715604 ) ) ;
#5687=TOROIDAL_SURFACE ( 'NONE', #51472, 3.899999999999999467, 0.1000000000000000056 ) ;
#5706=CARTESIAN_POINT ( 'NONE',  ( 20.94999999999999929, 1.835341550235569663, -179.0551512925629538 ) ) ;
#5732=EDGE_CURVE ( 'NONE', #34312, #177630, #90361, .T. ) ;
#5735=CARTESIAN_POINT ( 'NONE',  ( 18.51697539158856642, 10.31565961587946312, -206.5364194119177910 ) ) ;
#5739=EDGE_CURVE ( 'NONE', #218080, #156566, #112553, .T. ) ;
#5761=VERTEX_POINT ( 'NONE', #95538 ) ;
#5773=EDGE_CURVE ( 'NONE', #169487, #131901, #227722, .T. ) ;
#5818=EDGE_LOOP ( 'NONE', ( #54429, #182624, #172408, #107111 ) ) ;
#5822=CARTESIAN_POINT ( 'NONE',  ( -23.25000000000000000, 1.910280373842936141, -180.1313678551989028 ) ) ;
#5841=EDGE_LOOP ( 'NONE', ( #6235, #137887, #13606, #71947 ) ) ;
#5843=EDGE_CURVE ( 'NONE', #214983, #50484, #202785, .T. ) ;
#5852=CARTESIAN_POINT ( 'NONE',  ( 21.14999999999999858, -11.74999999998884448, -179.7499999999999716 ) ) ;
#5867=ORIENTED_EDGE ( 'NONE', *, *, #104362, .T. ) ;
#5900=DIRECTION ( 'NONE',  ( 0.000000000000000000, 0.4999999999999478195, -0.8660254037844686836 ) ) ;
#5940=AXIS2_PLACEMENT_3D ( 'NONE', #35010, #75408, #79205 ) ;
#5981=CARTESIAN_POINT ( 'NONE',  ( -23.15000000000000213, 1.115600667400684642E-11, -198.9999999999999432 ) ) ;
#5991=AXIS2_PLACEMENT_3D ( 'NONE', #4510, #204003, #64503 ) ;
#5997=VERTEX_POINT ( 'NONE', #76809 ) ;
#6028=AXIS2_PLACEMENT_3D ( 'NONE', #127679, #32457, #111975 ) ;
#6046=B_SPLINE_CURVE_WITH_KNOTS ( 'NONE', 3,
 ( #52130, #88677, #9171, #146104, #7908, #211220, #87408, #112145, #108281, #191697 ),
 .UNSPECIFIED., .F., .F.,
 ( 4, 2, 2, 2, 4 ),
 ( 0.000000000000000000, 0.0001584437871625804257, 0.0002376656807438308212, 0.0002772766275344220699, 0.0003168875743250132914 ),
 .UNSPECIFIED. ) ;
#6055=VERTEX_POINT ( 'NONE', #79363 ) ;
#6092=CARTESIAN_POINT ( 'NONE',  ( -23.15000000000000213, 1.115648428625851357E-11, -197.0999999999999659 ) ) ;
#6115=CARTESIAN_POINT ( 'NONE',  ( 20.30531438145591139, 10.09690106110208596, -175.2960178072733015 ) ) ;
#6119=DIRECTION ( 'NONE',  ( -2.940209281316621509E-16, 1.000000000000000000, -2.352167425053297207E-15 ) ) ;
#6156=ADVANCED_FACE ( 'NONE', ( #165689 ), #61339, .F. ) ;
#6188=CARTESIAN_POINT ( 'NONE',  ( -21.05000000000000071, 11.62071067812980907, -174.3684166523410113 ) ) ;
#6209=CIRCLE ( 'NONE', #76958, 0.1999999999999987899 ) ;
#6213=DIRECTION ( 'NONE',  ( -0.000000000000000000, 0.000000000000000000, 1.000000000000000000 ) ) ;
#6235=ORIENTED_EDGE ( 'NONE', *, *, #206955, .T. ) ;
#6237=ORIENTED_EDGE ( 'NONE', *, *, #150073, .F. ) ;
#6239=DIRECTION ( 'NONE',  ( 1.000000000000000000, 0.000000000000000000, 0.000000000000000000 ) ) ;
#6262=VERTEX_POINT ( 'NONE', #169565 ) ;
#6264=FACE_OUTER_BOUND ( 'NONE', #167475, .T. ) ;
#6274=CARTESIAN_POINT ( 'NONE',  ( 21.05000000000000071, 1.115600667400684642E-11, -167.4999999999999716 ) ) ;
#6289=DIRECTION ( 'NONE',  ( 0.000000000000000000, -0.000000000000000000, 1.000000000000000000 ) ) ;
#6384=CARTESIAN_POINT ( 'NONE',  ( -23.25000000000000000, 10.33248238083634440, -206.5948465439131496 ) ) ;
#6385=EDGE_CURVE ( 'NONE', #157944, #157060, #127976, .T. ) ;
#6407=AXIS2_PLACEMENT_3D ( 'NONE', #253710, #234151, #55485 ) ;
#6410=DIRECTION ( 'NONE',  ( 0.000000000000000000, 0.000000000000000000, -1.000000000000000000 ) ) ;
#6426=AXIS2_PLACEMENT_3D ( 'NONE', #87153, #48037, #84551 ) ;
#6434=LINE ( 'NONE', #49421, #102552 ) ;
#6442=LINE ( 'NONE', #229362, #56421 ) ;
#6458=EDGE_CURVE ( 'NONE', #81259, #130316, #85858, .T. ) ;
#6473=CARTESIAN_POINT ( 'NONE',  ( 23.14999999999999858, 2.000000000011158630, -200.9999999999999432 ) ) ;
#6483=CARTESIAN_POINT ( 'NONE',  ( 20.94999999999999929, 1.115625160336667635E-11, -198.9999999999999432 ) ) ;
#6520=VERTEX_POINT ( 'NONE', #22008 ) ;
#6533=AXIS2_PLACEMENT_3D ( 'NONE', #29911, #88553, #208540 ) ;
#6541=CARTESIAN_POINT ( 'NONE',  ( 23.14999999999999858, 1.115600667400684642E-11, -200.9999999999999432 ) ) ;
#6554=VERTEX_POINT ( 'NONE', #140651 ) ;
#6565=AXIS2_PLACEMENT_3D ( 'NONE', #138192, #239899, #83345 ) ;
#6608=CARTESIAN_POINT ( 'NONE',  ( 18.52928932188133970, 10.27928932189250411, -188.8499999999999659 ) ) ;
#6622=VERTEX_POINT ( 'NONE', #227898 ) ;
#6628=DIRECTION ( 'NONE',  ( -0.7071067811865475727, -0.7071067811865475727, -0.000000000000000000 ) ) ;
#6630=ORIENTED_EDGE ( 'NONE', *, *, #98151, .T. ) ;
#6654=DIRECTION ( 'NONE',  ( 0.000000000000000000, 0.000000000000000000, -1.000000000000000000 ) ) ;
#6667=ORIENTED_EDGE ( 'NONE', *, *, #215420, .T. ) ;
#6676=FACE_OUTER_BOUND ( 'NONE', #76516, .T. ) ;
#6681=ADVANCED_FACE ( 'NONE', ( #6264 ), #165361, .F. ) ;
#6709=EDGE_CURVE ( 'NONE', #135650, #132399, #15161, .T. ) ;
#6750=AXIS2_PLACEMENT_3D ( 'NONE', #154510, #219569, #159617 ) ;
#6752=AXIS2_PLACEMENT_3D ( 'NONE', #255201, #76617, #156192 ) ;
#6761=CARTESIAN_POINT ( 'NONE',  ( 18.54147908293604274, -9.463261657916875791, -174.5489488967558600 ) ) ;
#6770=CARTESIAN_POINT ( 'NONE',  ( 18.49999999999999289, 7.120270961708750512, -204.6595630418393057 ) ) ;
#6771=ORIENTED_EDGE ( 'NONE', *, *, #138555, .T. ) ;
#6805=CARTESIAN_POINT ( 'NONE',  ( 22.59999999999999432, 11.74956712350054566, -167.3991416309012550 ) ) ;
#6818=ORIENTED_EDGE ( 'NONE', *, *, #133684, .T. ) ;
#6834=EDGE_CURVE ( 'NONE', #252182, #254440, #127775, .T. ) ;
#6841=EDGE_CURVE ( 'NONE', #129705, #5761, #6956, .T. ) ;
#6894=DIRECTION ( 'NONE',  ( -0.000000000000000000, -0.1350103645451876666, 0.9908441862701600211 ) ) ;
#6942=LINE ( 'NONE', #9507, #138177 ) ;
#6948=FACE_OUTER_BOUND ( 'NONE', #54250, .T. ) ;
#6956=CIRCLE ( 'NONE', #235907, 0.09999999999998898659 ) ;
#6967=DIRECTION ( 'NONE',  ( 0.000000000000000000, 1.000000000000000000, 2.891205793294679805E-16 ) ) ;
#6977=EDGE_CURVE ( 'NONE', #165976, #221039, #131860, .T. ) ;
#6981=DIRECTION ( 'NONE',  ( 0.000000000000000000, 0.000000000000000000, 1.000000000000000000 ) ) ;
#6988=AXIS2_PLACEMENT_3D ( 'NONE', #27780, #242931, #224650 ) ;
#7016=CARTESIAN_POINT ( 'NONE',  ( 21.14999999999999858, 10.71339244341104013, -179.7499999999999716 ) ) ;
#7017=DIRECTION ( 'NONE',  ( 2.259780016855445309E-14, 0.9875055080513753802, -0.1575844902526748192 ) ) ;
#7024=AXIS2_PLACEMENT_3D ( 'NONE', #61529, #218002, #41980 ) ;
#7028=AXIS2_PLACEMENT_3D ( 'NONE', #46881, #89863, #188982 ) ;
#7074=CIRCLE ( 'NONE', #90458, 11.64999999999999325 ) ;
#7075=DIRECTION ( 'NONE',  ( 0.000000000000000000, -6.308085367188393199E-16, -1.000000000000000000 ) ) ;
#7099=DIRECTION ( 'NONE',  ( 0.000000000000000000, -0.000000000000000000, 1.000000000000000000 ) ) ;
#7112=CIRCLE ( 'NONE', #248750, 0.1000000000000002692 ) ;
#7119=ORIENTED_EDGE ( 'NONE', *, *, #224264, .F. ) ;
#7175=CARTESIAN_POINT ( 'NONE',  ( 20.94999999999999929, 1.115600667400684642E-11, -200.9999999999999432 ) ) ;
#7200=VERTEX_POINT ( 'NONE', #117591 ) ;
#7222=SPHERICAL_SURFACE ( 'NONE', #23073, 0.1000000000000000056 ) ;
#7239=CARTESIAN_POINT ( 'NONE',  ( 18.59999999999999076, 5.950000000011100632, -177.8057023050348278 ) ) ;
#7245=EDGE_CURVE ( 'NONE', #171611, #9569, #123682, .T. ) ;
#7261=FACE_OUTER_BOUND ( 'NONE', #253176, .T. ) ;
#7285=DIRECTION ( 'NONE',  ( -1.000000000000000000, 0.000000000000000000, 0.000000000000000000 ) ) ;
#7326=DIRECTION ( 'NONE',  ( 1.000000000000000000, -0.000000000000000000, -0.000000000000000000 ) ) ;
#7381=AXIS2_PLACEMENT_3D ( 'NONE', #14124, #233178, #149789 ) ;
#7397=EDGE_LOOP ( 'NONE', ( #70818, #194925, #149759, #111299 ) ) ;
#7413=CIRCLE ( 'NONE', #211441, 0.1000000000000111355 ) ;
#7425=DIRECTION ( 'NONE',  ( 0.000000000000000000, 0.000000000000000000, -1.000000000000000000 ) ) ;
#7447=DIRECTION ( 'NONE',  ( 1.000000000000000000, 0.000000000000000000, 0.000000000000000000 ) ) ;
#7452=VERTEX_POINT ( 'NONE', #4060 ) ;
#7456=CARTESIAN_POINT ( 'NONE',  ( 22.60000000000000142, 0.1008583691098682150, -155.7504328765105868 ) ) ;
#7474=DIRECTION ( 'NONE',  ( 1.000000000000000000, -0.000000000000000000, -0.000000000000000000 ) ) ;
#7491=ADVANCED_FACE ( 'NONE', ( #88712 ), #172179, .T. ) ;
#7497=DIRECTION ( 'NONE',  ( 0.000000000000000000, 0.000000000000000000, 1.000000000000000000 ) ) ;
#7516=VERTEX_POINT ( 'NONE', #127873 ) ;
#7542=DIRECTION ( 'NONE',  ( 0.000000000000000000, 0.8700118002898322711, -0.4930308989875231696 ) ) ;
#7548=DIRECTION ( 'NONE',  ( -0.000000000000000000, 1.000000000000000000, 1.734723475976807292E-15 ) ) ;
#7584=ORIENTED_EDGE ( 'NONE', *, *, #228816, .T. ) ;
#7588=DIRECTION ( 'NONE',  ( 1.000000000000000000, -0.000000000000000000, -0.000000000000000000 ) ) ;
#7590=CARTESIAN_POINT ( 'NONE',  ( -21.07016717457010913, 1.115541036281197940E-11, -161.1790591618990902 ) ) ;
#7632=AXIS2_PLACEMENT_3D ( 'NONE', #159756, #78899, #38524 ) ;
#7646=DIRECTION ( 'NONE',  ( -1.000000000000000000, -0.000000000000000000, -0.000000000000000000 ) ) ;
#7684=DIRECTION ( 'NONE',  ( 1.000000000000000000, 7.304098846218134667E-16, 0.000000000000000000 ) ) ;
#7699=VERTEX_POINT ( 'NONE', #95158 ) ;
#7732=DIRECTION ( 'NONE',  ( 0.000000000000000000, 0.9999631594459053030, 0.008583690987162899758 ) ) ;
#7750=VERTEX_POINT ( 'NONE', #242361 ) ;
#7784=ADVANCED_FACE ( 'NONE', ( #121178 ), #186412, .F. ) ;
#7801=AXIS2_PLACEMENT_3D ( 'NONE', #220657, #120312, #195007 ) ;
#7824=CARTESIAN_POINT ( 'NONE',  ( -22.50000000000088463, 0.04536165659882995804, -155.8494911657945750 ) ) ;
#7875=CARTESIAN_POINT ( 'NONE',  ( 19.88284271247461987, 11.69142135624847256, -192.2499999999999432 ) ) ;
#7885=AXIS2_PLACEMENT_3D ( 'NONE', #110637, #131483, #246303 ) ;
#7888=EDGE_CURVE ( 'NONE', #202001, #77719, #165409, .T. ) ;
#7898=ORIENTED_EDGE ( 'NONE', *, *, #118042, .F. ) ;
#7908=CARTESIAN_POINT ( 'NONE',  ( 18.46858270002951841, -9.474202674699414573, -174.6020219347037994 ) ) ;
#7911=ORIENTED_EDGE ( 'NONE', *, *, #185242, .T. ) ;
#8007=DIRECTION ( 'NONE',  ( 1.000000000000000000, 0.000000000000000000, 0.000000000000000000 ) ) ;
#8012=ORIENTED_EDGE ( 'NONE', *, *, #242193, .F. ) ;
#8022=ADVANCED_FACE ( 'NONE', ( #54430 ), #253208, .F. ) ;
#8043=CARTESIAN_POINT ( 'NONE',  ( -23.15000000000000213, 1.115600667400684642E-11, -167.4999999999999716 ) ) ;
#8060=DIRECTION ( 'NONE',  ( 1.000000000000000000, 0.000000000000000000, 0.000000000000000000 ) ) ;
#8084=EDGE_LOOP ( 'NONE', ( #68828, #88997 ) ) ;
#8092=CARTESIAN_POINT ( 'NONE',  ( -18.59999994787167310, -9.523637689750458435, -207.8824495347724337 ) ) ;
#8131=TOROIDAL_SURFACE ( 'NONE', #170676, 1.900000000000002576, 0.1000000000000000056 ) ;
#8153=CARTESIAN_POINT ( 'NONE',  ( 18.59999999999999076, 10.25000000001115552, -192.2499999999999716 ) ) ;
#8158=VERTEX_POINT ( 'NONE', #24317 ) ;
#8162=DIRECTION ( 'NONE',  ( -0.000000000000000000, 0.8660254037844383745, -0.5000000000000003331 ) ) ;
#8210=CARTESIAN_POINT ( 'NONE',  ( -18.59999999999999787, 1.115600667400684642E-11, -200.9999999999999432 ) ) ;
#8236=LINE ( 'NONE', #87741, #227715 ) ;
#8242=DIRECTION ( 'NONE',  ( -1.000000000000000000, 0.000000000000000000, 0.000000000000000000 ) ) ;
#8246=EDGE_CURVE ( 'NONE', #235498, #165951, #9863, .T. ) ;
#8275=DIRECTION ( 'NONE',  ( 1.000000000000000000, 0.000000000000000000, 0.000000000000000000 ) ) ;
#8297=EDGE_CURVE ( 'NONE', #233370, #89904, #230196, .T. ) ;
#8308=CARTESIAN_POINT ( 'NONE',  ( 21.08198257630413508, 6.336596734026219480, -167.4273566762153678 ) ) ;
#8343=CARTESIAN_POINT ( 'NONE',  ( 20.94999999999999929, 1.115600667400684642E-11, -200.9999999999999432 ) ) ;
#8369=VECTOR ( 'NONE', #108107, 1000.000000000000000 ) ;
#8377=PLANE ( 'NONE',  #43223 ) ;
#8387=DIRECTION ( 'NONE',  ( 0.000000000000000000, 0.4930308989874729320, 0.8700118002898605818 ) ) ;
#8397=DIRECTION ( 'NONE',  ( 1.000000000000000000, 0.000000000000000000, -0.000000000000000000 ) ) ;
#8405=CARTESIAN_POINT ( 'NONE',  ( -23.15000000000000213, 1.115600667400684642E-11, -167.4999999999999716 ) ) ;
#8413=ORIENTED_EDGE ( 'NONE', *, *, #8246, .F. ) ;
#8451=CYLINDRICAL_SURFACE ( 'NONE', #206298, 0.09999999999999817368 ) ;
#8484=DIRECTION ( 'NONE',  ( -1.000000000000000000, 0.000000000000000000, 0.000000000000000000 ) ) ;
#8499=LINE ( 'NONE', #245822, #165359 ) ;
#8504=ORIENTED_EDGE ( 'NONE', *, *, #84140, .F. ) ;
#8556=ADVANCED_FACE ( 'NONE', ( #103504 ), #200062, .T. ) ;
#8557=AXIS2_PLACEMENT_3D ( 'NONE', #226669, #45474, #147133 ) ;
#8582=CONICAL_SURFACE ( 'NONE', #129377, 4.299999999999970512, 0.7853981633974466137 ) ;
#8616=CARTESIAN_POINT ( 'NONE',  ( -18.59999999999999787, 9.350000000011156942, -179.8499999999999943 ) ) ;
#8633=CYLINDRICAL_SURFACE ( 'NONE', #97461, 0.09999999999998898659 ) ;
#8666=ORIENTED_EDGE ( 'NONE', *, *, #174058, .F. ) ;
#8681=DIRECTION ( 'NONE',  ( -2.952720810173289112E-16, 1.000000000000000000, 0.000000000000000000 ) ) ;
#8684=DIRECTION ( 'NONE',  ( 0.000000000000000000, -0.9876197685951252359, -0.1568667991644863424 ) ) ;
#8724=CIRCLE ( 'NONE', #192096, 0.09999999999999939493 ) ;
#8729=CIRCLE ( 'NONE', #104560, 2.100000000000002309 ) ;
#8775=CARTESIAN_POINT ( 'NONE',  ( -23.25000000000000000, -1.149570369564537842, -208.8159124845019221 ) ) ;
#8787=CARTESIAN_POINT ( 'NONE',  ( -18.59999999999999787, -1.164121893230052995, -208.9148480855715775 ) ) ;
#8815=ORIENTED_EDGE ( 'NONE', *, *, #3958, .T. ) ;
#8826=ORIENTED_EDGE ( 'NONE', *, *, #24379, .T. ) ;
#8832=DIRECTION ( 'NONE',  ( 1.000000000000000000, 0.000000000000000000, 0.000000000000000000 ) ) ;
#8833=CARTESIAN_POINT ( 'NONE',  ( 22.00411653962159164, 7.253442868381325681, -167.4009618942313580 ) ) ;
#8837=ORIENTED_EDGE ( 'NONE', *, *, #142433, .F. ) ;
#8838=DIRECTION ( 'NONE',  ( 0.000000000000000000, 0.000000000000000000, -1.000000000000000000 ) ) ;
#8860=VERTEX_POINT ( 'NONE', #96458 ) ;
#8876=AXIS2_PLACEMENT_3D ( 'NONE', #37847, #213888, #135622 ) ;
#8878=DIRECTION ( 'NONE',  ( -0.000000000000000000, 0.000000000000000000, 1.000000000000000000 ) ) ;
#8890=FACE_OUTER_BOUND ( 'NONE', #105921, .T. ) ;
#8917=ADVANCED_FACE ( 'NONE', ( #101580 ), #249505, .F. ) ;
#8922=ADVANCED_FACE ( 'NONE', ( #62502 ), #203700, .T. ) ;
#8926=ORIENTED_EDGE ( 'NONE', *, *, #241033, .T. ) ;
#8975=DIRECTION ( 'NONE',  ( 1.000000000000000000, 0.000000000000000000, 0.000000000000000000 ) ) ;
#8977=VERTEX_POINT ( 'NONE', #200723 ) ;
#8984=AXIS2_PLACEMENT_3D ( 'NONE', #11144, #138437, #90662 ) ;
#8985=CIRCLE ( 'NONE', #150633, 4.149999999999999467 ) ;
#8997=DIRECTION ( 'NONE',  ( -1.000000000000000000, -2.952720810173289112E-16, 0.000000000000000000 ) ) ;
#8999=CARTESIAN_POINT ( 'NONE',  ( -23.15000000000000213, 11.60000000001115517, -194.0717967697244717 ) ) ;
#9004=DIRECTION ( 'NONE',  ( 0.000000000000000000, 0.008583690987128059571, -0.9999631594459056361 ) ) ;
#9018=ADVANCED_FACE ( 'NONE', ( #182457 ), #162905, .F. ) ;
#9033=EDGE_CURVE ( 'NONE', #63695, #99579, #164170, .T. ) ;
#9037=DIRECTION ( 'NONE',  ( 0.000000000000000000, 0.000000000000000000, -1.000000000000000000 ) ) ;
#9099=FACE_OUTER_BOUND ( 'NONE', #191861, .T. ) ;
#9107=ORIENTED_EDGE ( 'NONE', *, *, #206594, .T. ) ;
#9123=LINE ( 'NONE', #241322, #88309 ) ;
#9143=EDGE_CURVE ( 'NONE', #232431, #170879, #78767, .T. ) ;
#9170=CARTESIAN_POINT ( 'NONE',  ( -23.15000000000000213, 4.350000000011156054, -188.7499999999999716 ) ) ;
#9171=CARTESIAN_POINT ( 'NONE',  ( 18.49505832270840600, -9.438028062771744331, -174.6984731748938486 ) ) ;
#9205=CARTESIAN_POINT ( 'NONE',  ( -23.15000000000000213, 1.115600667400684642E-11, -200.9999999999999432 ) ) ;
#9208=AXIS2_PLACEMENT_3D ( 'NONE', #207837, #29214, #9587 ) ;
#9234=CARTESIAN_POINT ( 'NONE',  ( 21.05000000000000071, 6.540656951712400691, -167.5999999999999659 ) ) ;
#9253=DIRECTION ( 'NONE',  ( 0.000000000000000000, 0.000000000000000000, -1.000000000000000000 ) ) ;
#9288=ORIENTED_EDGE ( 'NONE', *, *, #98804, .T. ) ;
#9320=EDGE_CURVE ( 'NONE', #127119, #14186, #63453, .T. ) ;
#9326=CARTESIAN_POINT ( 'NONE',  ( 18.39999999999999858, -9.499999999988844479, -174.5320693966996544 ) ) ;
#9344=FACE_OUTER_BOUND ( 'NONE', #223232, .T. ) ;
#9369=EDGE_CURVE ( 'NONE', #242139, #209946, #153869, .T. ) ;
#9380=VERTEX_POINT ( 'NONE', #107722 ) ;
#9394=EDGE_LOOP ( 'NONE', ( #140865, #151732, #121750 ) ) ;
#9418=ADVANCED_FACE ( 'NONE', ( #150707 ), #189836, .T. ) ;
#9421=AXIS2_PLACEMENT_3D ( 'NONE', #250287, #114625, #110769 ) ;
#9444=EDGE_LOOP ( 'NONE', ( #80988, #109614, #195871, #99520 ) ) ;
#9482=CARTESIAN_POINT ( 'NONE',  ( 20.94999999999999929, 1.115600667400684642E-11, -202.9999999999999716 ) ) ;
#9500=CARTESIAN_POINT ( 'NONE',  ( -20.64999999999999858, 1.115600667400684642E-11, -200.9999999999999432 ) ) ;
#9507=CARTESIAN_POINT ( 'NONE',  ( -23.25000000000000000, -11.64999999998884483, -155.7499999999999716 ) ) ;
#9534=FACE_BOUND ( 'NONE', #151284, .T. ) ;
#9569=VERTEX_POINT ( 'NONE', #97106 ) ;
#9579=EDGE_LOOP ( 'NONE', ( #79499, #154636, #156367, #240531 ) ) ;
#9587=DIRECTION ( 'NONE',  ( 0.000000000000000000, -0.1495327102803792052, -0.9887567792719320625 ) ) ;
#9605=DIRECTION ( 'NONE',  ( 0.000000000000000000, 0.000000000000000000, -1.000000000000000000 ) ) ;
#9643=DIRECTION ( 'NONE',  ( 0.7071067811865487940, 8.659560562354918067E-17, 0.7071067811865463515 ) ) ;
#9648=VERTEX_POINT ( 'NONE', #99685 ) ;
#9650=EDGE_CURVE ( 'NONE', #177551, #85751, #43602, .T. ) ;
#9669=CARTESIAN_POINT ( 'NONE',  ( 18.59999999999999787, 1.115600667400684642E-11, -167.4999999999999716 ) ) ;
#9720=DIRECTION ( 'NONE',  ( -0.000000000000000000, -2.891205793294679805E-16, 1.000000000000000000 ) ) ;
#9730=ORIENTED_EDGE ( 'NONE', *, *, #18824, .T. ) ;
#9739=ORIENTED_EDGE ( 'NONE', *, *, #212869, .F. ) ;
#9753=DIRECTION ( 'NONE',  ( 0.000000000000000000, 1.000000000000000000, 0.000000000000000000 ) ) ;
#9793=CIRCLE ( 'NONE', #180501, 0.09999999999999939493 ) ;
#9856=ORIENTED_EDGE ( 'NONE', *, *, #170160, .F. ) ;
#9863=LINE ( 'NONE', #46412, #182506 ) ;
#9868=CARTESIAN_POINT ( 'NONE',  ( -20.93975676684922504, 10.31104185824063002, -206.5204516983105236 ) ) ;
#9941=CARTESIAN_POINT ( 'NONE',  ( -22.48660254037843131, 11.75000000001115374, -167.4499999999999886 ) ) ;
#9946=ORIENTED_EDGE ( 'NONE', *, *, #239400, .F. ) ;
#9954=FACE_BOUND ( 'NONE', #177881, .T. ) ;
#9957=ORIENTED_EDGE ( 'NONE', *, *, #240631, .F. ) ;
#9965=ORIENTED_EDGE ( 'NONE', *, *, #102099, .T. ) ;
#9995=EDGE_CURVE ( 'NONE', #183962, #82856, #95893, .T. ) ;
#9999=ADVANCED_FACE ( 'NONE', ( #62764 ), #5321, .F. ) ;
#10029=CARTESIAN_POINT ( 'NONE',  ( -23.15000000000000213, -8.999999999988844479, -191.1060308773475356 ) ) ;
#10072=CARTESIAN_POINT ( 'NONE',  ( -22.44366136229477249, 0.009341569497225218552, -155.8502814425260397 ) ) ;
#10113=CYLINDRICAL_SURFACE ( 'NONE', #151866, 0.09999999999999939493 ) ;
#10123=AXIS2_PLACEMENT_3D ( 'NONE', #127697, #110688, #247635 ) ;
#10130=DIRECTION ( 'NONE',  ( 1.000000000000000000, -0.000000000000000000, -0.000000000000000000 ) ) ;
#10165=CARTESIAN_POINT ( 'NONE',  ( 21.05000000000000071, -0.09999999998884512298, -160.9593430482987344 ) ) ;
#10185=CARTESIAN_POINT ( 'NONE',  ( 20.85000000000000142, -1.835859311432481045, -212.5044391687984842 ) ) ;
#10205=CARTESIAN_POINT ( 'NONE',  ( -18.59999999999999787, -1.851028230129704522, -179.1539132694224463 ) ) ;
#10213=AXIS2_PLACEMENT_3D ( 'NONE', #190848, #206522, #228674 ) ;
#10251=CARTESIAN_POINT ( 'NONE',  ( 23.24999999999999289, 11.75000000001116263, -167.5999999999999659 ) ) ;
#10253=CARTESIAN_POINT ( 'NONE',  ( -21.05000000000000071, 1.115600667400684642E-11, -167.4999999999999716 ) ) ;
#10283=VERTEX_POINT ( 'NONE', #71771 ) ;
#10297=DIRECTION ( 'NONE',  ( 1.000000000000000000, 0.000000000000000000, 0.000000000000000000 ) ) ;
#10373=CARTESIAN_POINT ( 'NONE',  ( 21.05000000000000071, -1.849084418615859926, -179.1560105214470866 ) ) ;
#10374=DIRECTION ( 'NONE',  ( 1.000000000000000000, 0.000000000000000000, 0.000000000000000000 ) ) ;
#10380=VERTEX_POINT ( 'NONE', #211264 ) ;
#10408=DIRECTION ( 'NONE',  ( 0.000000000000000000, 0.000000000000000000, -1.000000000000000000 ) ) ;
#10430=CARTESIAN_POINT ( 'NONE',  ( 20.84999999999998721, 10.33248238083634440, -206.5948465439131496 ) ) ;
#10437=ORIENTED_EDGE ( 'NONE', *, *, #93816, .F. ) ;
#10445=VECTOR ( 'NONE', #9643, 1000.000000000000000 ) ;
#10509=FACE_OUTER_BOUND ( 'NONE', #170313, .T. ) ;
#10544=DIRECTION ( 'NONE',  ( 0.000000000000000000, 0.9915357197604971473, -0.1298341882519111479 ) ) ;
#10547=VECTOR ( 'NONE', #14070, 1000.000000000000000 ) ;
#10562=B_SPLINE_CURVE_WITH_KNOTS ( 'NONE', 3,
 ( #188506, #206791, #28186, #247187, #148105, #244622, #88090, #9868, #227623, #48992, #128537, #110247, #134918, #51527, #91968, #33327, #189798, #11157, #90679 ),
 .UNSPECIFIED., .F., .F.,
 ( 4, 3, 3, 3, 3, 3, 4 ),
 ( -2.000416914645579387E-06, 4.235164736271501695E-22, 4.714008503743245793E-05, 9.979203887776031420E-05, 0.0001372215519229365321, 0.0001635031576220883785, 0.0001900083748504048946 ),
 .UNSPECIFIED. ) ;
#10589=EDGE_CURVE ( 'NONE', #6520, #156141, #46630, .T. ) ;
#10613=CIRCLE ( 'NONE', #156377, 12.87500000000000000 ) ;
#10622=CARTESIAN_POINT ( 'NONE',  ( 18.39999999999999858, -9.519327731081279609, -174.4729763765593020 ) ) ;
#10652=CARTESIAN_POINT ( 'NONE',  ( -23.25000000000000000, 2.600000000011156054, -180.7246219227620543 ) ) ;
#10676=AXIS2_PLACEMENT_3D ( 'NONE', #98726, #217413, #235703 ) ;
#10742=EDGE_LOOP ( 'NONE', ( #73469, #51688, #92656, #252088 ) ) ;
#10755=CARTESIAN_POINT ( 'NONE',  ( -22.50000000000000000, 7.790779598384560245, -167.3999999999999773 ) ) ;
#10757=CARTESIAN_POINT ( 'NONE',  ( -23.25000000000000000, 1.115600667400684642E-11, -167.4999999999999716 ) ) ;
#10788=EDGE_CURVE ( 'NONE', #116826, #122253, #212254, .T. ) ;
#10819=ADVANCED_FACE ( 'NONE', ( #93569 ), #130017, .F. ) ;
#10833=VECTOR ( 'NONE', #82096, 1000.000000000000000 ) ;
#10853=CARTESIAN_POINT ( 'NONE',  ( 23.14999999999999858, 11.65000000001116298, -193.9851942293460070 ) ) ;
#10854=ADVANCED_FACE ( 'NONE', ( #99958 ), #20473, .F. ) ;
#10856=ORIENTED_EDGE ( 'NONE', *, *, #131843, .T. ) ;
#10865=CYLINDRICAL_SURFACE ( 'NONE', #26037, 0.09999999999998898659 ) ;
#10872=EDGE_CURVE ( 'NONE', #251277, #178255, #30287, .T. ) ;
#10905=CARTESIAN_POINT ( 'NONE',  ( -18.50000000000000000, 11.75000000001115197, -155.7499999999999716 ) ) ;
#10919=CARTESIAN_POINT ( 'NONE',  ( -21.46681500593269121, 6.857511159395801137, -167.4999999999999432 ) ) ;
#10941=AXIS2_PLACEMENT_3D ( 'NONE', #142106, #27, #159139 ) ;
#10957=CYLINDRICAL_SURFACE ( 'NONE', #187351, 0.09999999999998898659 ) ;
#10970=DIRECTION ( 'NONE',  ( 0.7071067811865487940, 0.000000000000000000, -0.7071067811865463515 ) ) ;
#10979=CIRCLE ( 'NONE', #185952, 0.09999999999998898659 ) ;
#10981=STYLED_ITEM ( 'NONE', ( #147766 ), #88633 ) ;
#10987=ORIENTED_EDGE ( 'NONE', *, *, #81364, .T. ) ;
#11013=DIRECTION ( 'NONE',  ( 0.000000000000000000, -0.9908441862701782288, -0.1350103645450542456 ) ) ;
#11031=DIRECTION ( 'NONE',  ( 1.000000000000000000, 2.952720810173289112E-16, -0.000000000000000000 ) ) ;
#11055=CARTESIAN_POINT ( 'NONE',  ( 18.49999999999999289, 11.75000000001115907, -155.7499999999999716 ) ) ;
#11059=CIRCLE ( 'NONE', #165181, 11.80000000000000426 ) ;
#11061=CYLINDRICAL_SURFACE ( 'NONE', #1963, 0.09999999999999939493 ) ;
#11070=EDGE_CURVE ( 'NONE', #249855, #181739, #10562, .T. ) ;
#11103=CARTESIAN_POINT ( 'NONE',  ( 21.12400222705959507, 8.778511907088271116, -179.7500000000000000 ) ) ;
#11139=VERTEX_POINT ( 'NONE', #55373 ) ;
#11144=CARTESIAN_POINT ( 'NONE',  ( -22.39999999999999858, 11.65000000001115588, -167.5999999999999659 ) ) ;
#11157=CARTESIAN_POINT ( 'NONE',  ( -20.85882249326303040, 10.33248238083634796, -206.5948465439131496 ) ) ;
#11180=CARTESIAN_POINT ( 'NONE',  ( 20.94999999999999574, 1.750000000011155743, -179.1695115579016147 ) ) ;
#11189=CARTESIAN_POINT ( 'NONE',  ( 21.13422380239053311, 6.493326514816903483, -167.4999999999999716 ) ) ;
#11196=EDGE_LOOP ( 'NONE', ( #133586, #58926 ) ) ;
#11204=VECTOR ( 'NONE', #101706, 1000.000000000000000 ) ;
#11234=CARTESIAN_POINT ( 'NONE',  ( -23.25000000000000000, 1.115626384983466744E-11, -198.8999999999999773 ) ) ;
#11247=ORIENTED_EDGE ( 'NONE', *, *, #153362, .T. ) ;
#11293=DIRECTION ( 'NONE',  ( -0.000000000000000000, 0.1350103645451876666, 0.9908441862701600211 ) ) ;
#11312=CARTESIAN_POINT ( 'NONE',  ( -18.59999999999999787, 5.900000000011102586, -177.7190997646563915 ) ) ;
#11316=CARTESIAN_POINT ( 'NONE',  ( 18.49999999999999289, 10.20857864377385127, -155.7499999999999716 ) ) ;
#11333=CARTESIAN_POINT ( 'NONE',  ( -21.05000000000000071, 11.75000000001115552, -193.9851942293460070 ) ) ;
#11356=DIRECTION ( 'NONE',  ( 1.000000000000000000, 0.000000000000000000, 0.000000000000000000 ) ) ;
#11408=CARTESIAN_POINT ( 'NONE',  ( 21.05000000000000071, 8.776282895303632259, -179.6499999999999773 ) ) ;
#11409=CARTESIAN_POINT ( 'NONE',  ( 22.47071067811865319, 7.720074744509197728, -167.4009075452973434 ) ) ;
#11443=CIRCLE ( 'NONE', #115463, 0.09999999999999982514 ) ;
#11447=DIRECTION ( 'NONE',  ( 0.000000000000000000, 0.1568667991644863147, 0.9876197685951252359 ) ) ;
#11458=CYLINDRICAL_SURFACE ( 'NONE', #190796, 0.09999999999999939493 ) ;
#11463=LINE ( 'NONE', #56957, #69824 ) ;
#11490=CARTESIAN_POINT ( 'NONE',  ( -18.59999999999999787, 3.912899247244609580, -178.9818229730109351 ) ) ;
#11509=CIRCLE ( 'NONE', #215497, 0.09999999999999907574 ) ;
#11533=ORIENTED_EDGE ( 'NONE', *, *, #177179, .T. ) ;
#11548=CARTESIAN_POINT ( 'NONE',  ( -18.50000000000000000, 11.65000000001115232, -188.8499999999999659 ) ) ;
#11559=DIRECTION ( 'NONE',  ( 0.000000000000000000, 0.000000000000000000, -1.000000000000000000 ) ) ;
#11562=CARTESIAN_POINT ( 'NONE',  ( -23.25000000000000000, -1.164121893230052995, -208.9148480855715775 ) ) ;
#11583=CARTESIAN_POINT ( 'NONE',  ( -21.05000000000000071, 1.261786168576181755, -175.5864989635454378 ) ) ;
#11610=VERTEX_POINT ( 'NONE', #194333 ) ;
#11612=LINE ( 'NONE', #229372, #206257 ) ;
#11658=CARTESIAN_POINT ( 'NONE',  ( 20.94999999999999574, -11.41227409413852989, -170.3999999999999773 ) ) ;
#11676=EDGE_LOOP ( 'NONE', ( #112299, #8926, #158428 ) ) ;
#11689=FACE_OUTER_BOUND ( 'NONE', #231774, .T. ) ;
#11707=EDGE_CURVE ( 'NONE', #104346, #64710, #192969, .T. ) ;
#11709=ORIENTED_EDGE ( 'NONE', *, *, #202258, .F. ) ;
#11714=CIRCLE ( 'NONE', #178318, 0.09999999999998898659 ) ;
#11726=ORIENTED_EDGE ( 'NONE', *, *, #17567, .F. ) ;
#11740=AXIS2_PLACEMENT_3D ( 'NONE', #38244, #201156, #102033 ) ;
#11763=DIRECTION ( 'NONE',  ( -1.000000000000000000, 0.000000000000000000, 0.000000000000000000 ) ) ;
#11764=DIRECTION ( 'NONE',  ( 1.000000000000000000, -0.000000000000000000, -0.000000000000000000 ) ) ;
#11828=EDGE_CURVE ( 'NONE', #35026, #145808, #188859, .T. ) ;
#11877=ORIENTED_EDGE ( 'NONE', *, *, #146118, .F. ) ;
#11895=ORIENTED_EDGE ( 'NONE', *, *, #124581, .T. ) ;
#11912=TOROIDAL_SURFACE ( 'NONE', #7801, 0.6000000000000015321, 0.1000000000000000056 ) ;
#11923=SPHERICAL_SURFACE ( 'NONE', #160622, 0.1000000000000000056 ) ;
#11951=DIRECTION ( 'NONE',  ( 0.000000000000000000, 0.000000000000000000, 1.000000000000000000 ) ) ;
#11966=ORIENTED_EDGE ( 'NONE', *, *, #58445, .F. ) ;
#12001=EDGE_LOOP ( 'NONE', ( #198106, #195753, #84223, #137689 ) ) ;
#12032=EDGE_CURVE ( 'NONE', #160190, #141186, #42619, .T. ) ;
#12041=AXIS2_PLACEMENT_3D ( 'NONE', #152676, #53544, #174824 ) ;
#12049=LINE ( 'NONE', #236199, #234659 ) ;
#12055=DIRECTION ( 'NONE',  ( 1.836970198721029934E-16, -1.000000000000000000, -0.000000000000000000 ) ) ;
#12067=CIRCLE ( 'NONE', #174406, 0.09999999999998898659 ) ;
#12107=CARTESIAN_POINT ( 'NONE',  ( -18.59999999999999787, -1.835341550213255957, -179.1551512925629197 ) ) ;
#12143=CARTESIAN_POINT ( 'NONE',  ( 19.86930884467607328, 11.68691006698174739, -192.2392226389382301 ) ) ;
#12181=ADVANCED_FACE ( 'NONE', ( #25629 ), #139115, .F. ) ;
#12193=EDGE_LOOP ( 'NONE', ( #166943, #71719, #227277 ) ) ;
#12196=EDGE_CURVE ( 'NONE', #54663, #61007, #206829, .T. ) ;
#12234=AXIS2_PLACEMENT_3D ( 'NONE', #186632, #63461, #80427 ) ;
#12237=DIRECTION ( 'NONE',  ( 0.000000000000000000, 6.308085367183347448E-16, 1.000000000000000000 ) ) ;
#12275=CIRCLE ( 'NONE', #249765, 0.4000000000000114575 ) ;
#12304=ORIENTED_EDGE ( 'NONE', *, *, #217181, .F. ) ;
#12339=VERTEX_POINT ( 'NONE', #155868 ) ;
#12342=CARTESIAN_POINT ( 'NONE',  ( -21.64999999999999858, 7.250000000011148416, -179.7499999999999716 ) ) ;
#12353=EDGE_CURVE ( 'NONE', #105545, #257429, #134963, .T. ) ;
#12361=DIRECTION ( 'NONE',  ( 0.000000000000000000, -1.000000000000000000, -0.000000000000000000 ) ) ;
#12379=CARTESIAN_POINT ( 'NONE',  ( 20.85000000000000142, -0.3238857010591806307, -200.9575895893139545 ) ) ;
#12385=CARTESIAN_POINT ( 'NONE',  ( 20.93975676684922504, 10.31104185824063002, -206.5204516983105236 ) ) ;
#12395=DIRECTION ( 'NONE',  ( 0.000000000000000000, 1.000000000000000000, 0.000000000000000000 ) ) ;
#12401=CARTESIAN_POINT ( 'NONE',  ( 20.12500000000000000, 9.750000000011153745, -175.6117712821142618 ) ) ;
#12408=AXIS2_PLACEMENT_3D ( 'NONE', #83961, #243080, #25350 ) ;
#12430=AXIS2_PLACEMENT_3D ( 'NONE', #60820, #199067, #99933 ) ;
#12446=CARTESIAN_POINT ( 'NONE',  ( -18.50000000000001066, -9.421308209727696337, -174.7423632140504708 ) ) ;
#12491=EDGE_CURVE ( 'NONE', #171236, #117217, #136246, .T. ) ;
#12496=ORIENTED_EDGE ( 'NONE', *, *, #212160, .T. ) ;
#12518=ADVANCED_FACE ( 'NONE', ( #257446 ), #68419, .T. ) ;
#12526=ADVANCED_FACE ( 'NONE', ( #138801 ), #214172, .T. ) ;
#12535=DIRECTION ( 'NONE',  ( 0.000000000000000000, 0.000000000000000000, -1.000000000000000000 ) ) ;
#12560=DIRECTION ( 'NONE',  ( 1.000000000000000000, 3.265361837132813093E-16, -0.000000000000000000 ) ) ;
#12563=EDGE_CURVE ( 'NONE', #131456, #168999, #134270, .T. ) ;
#12575=ORIENTED_EDGE ( 'NONE', *, *, #208067, .F. ) ;
#12588=VERTEX_POINT ( 'NONE', #47432 ) ;
#12596=DIRECTION ( 'NONE',  ( 0.000000000000000000, 0.9908441862701782288, 0.1350103645450542456 ) ) ;
#12612=VERTEX_POINT ( 'NONE', #83956 ) ;
#12647=EDGE_LOOP ( 'NONE', ( #76373, #126403, #48830, #42174 ) ) ;
#12650=EDGE_CURVE ( 'NONE', #160579, #234175, #63143, .T. ) ;
#12687=FACE_OUTER_BOUND ( 'NONE', #68965, .T. ) ;
#12713=DIRECTION ( 'NONE',  ( -4.239556034732056743E-17, 0.1298341882520022694, 0.9915357197604853789 ) ) ;
#12717=DIRECTION ( 'NONE',  ( 2.952720810173289112E-16, -1.000000000000000000, -0.000000000000000000 ) ) ;
#12731=CARTESIAN_POINT ( 'NONE',  ( 18.59999999999999076, 11.65000000001115943, -192.3499999999999659 ) ) ;
#12739=AXIS2_PLACEMENT_3D ( 'NONE', #114321, #109168, #193867 ) ;
#12752=DIRECTION ( 'NONE',  ( 1.000000000000000000, 0.000000000000000000, 0.000000000000000000 ) ) ;
#12753=CYLINDRICAL_SURFACE ( 'NONE', #160589, 0.09999999999998898659 ) ;
#12758=EDGE_LOOP ( 'NONE', ( #235315, #113092, #226535 ) ) ;
#12763=CARTESIAN_POINT ( 'NONE',  ( -18.59999999999999787, 7.120270961708750512, -204.6595630418393057 ) ) ;
#12777=VERTEX_POINT ( 'NONE', #91715 ) ;
#12796=CARTESIAN_POINT ( 'NONE',  ( 21.14999999999999858, 10.71339244341104013, -179.7499999999999716 ) ) ;
#12811=ADVANCED_FACE ( 'NONE', ( #30475 ), #189543, .F. ) ;
#12822=CARTESIAN_POINT ( 'NONE',  ( 23.24999999999999289, 6.450000000011156587, -155.7499999999999716 ) ) ;
#12827=VECTOR ( 'NONE', #197145, 1000.000000000000000 ) ;
#12844=CIRCLE ( 'NONE', #96189, 2.000000000000001776 ) ;
#12845=LINE ( 'NONE', #171938, #170411 ) ;
#12861=AXIS2_PLACEMENT_3D ( 'NONE', #244943, #165423, #46734 ) ;
#12863=VECTOR ( 'NONE', #126270, 1000.000000000000000 ) ;
#12877=VECTOR ( 'NONE', #209583, 1000.000000000000000 ) ;
#12882=CARTESIAN_POINT ( 'NONE',  ( -1.739115166359751801E-14, 11.65000000001114699, -192.3499999999999659 ) ) ;
#12893=EDGE_CURVE ( 'NONE', #20901, #66550, #81116, .T. ) ;
#12895=CARTESIAN_POINT ( 'NONE',  ( -21.45000000000000284, 7.708578643773852157, -188.6499999999999488 ) ) ;
#12906=EDGE_CURVE ( 'NONE', #91084, #84620, #197015, .T. ) ;
#12931=DIRECTION ( 'NONE',  ( 0.000000000000000000, 0.9908441862701782288, -0.1350103645450542456 ) ) ;
#12939=FACE_OUTER_BOUND ( 'NONE', #45957, .T. ) ;
#12940=VERTEX_POINT ( 'NONE', #198512 ) ;
#12957=DIRECTION ( 'NONE',  ( 1.000000000000000000, 0.000000000000000000, 0.000000000000000000 ) ) ;
#13001=EDGE_CURVE ( 'NONE', #42929, #63249, #213789, .T. ) ;
#13008=VERTEX_POINT ( 'NONE', #43301 ) ;
#13013=DIRECTION ( 'NONE',  ( 0.000000000000000000, 0.000000000000000000, -1.000000000000000000 ) ) ;
#13047=SPHERICAL_SURFACE ( 'NONE', #107630, 0.1000000000000000056 ) ;
#13060=CARTESIAN_POINT ( 'NONE',  ( 20.94999999999999574, 8.926614585098251453, -175.9716830192230930 ) ) ;
#13067=ORIENTED_EDGE ( 'NONE', *, *, #198514, .T. ) ;
#13093=ADVANCED_FACE ( 'NONE', ( #211361 ), #70591, .F. ) ;
#13106=DIRECTION ( 'NONE',  ( -1.000000000000000000, 0.000000000000000000, 0.000000000000000000 ) ) ;
#13118=CARTESIAN_POINT ( 'NONE',  ( 20.94999999999999929, -11.48912529306489994, -198.0999999999999659 ) ) ;
#13119=CARTESIAN_POINT ( 'NONE',  ( -23.15000000000000213, -8.999999999988844479, -191.1060308773475356 ) ) ;
#13156=LINE ( 'NONE', #90095, #67961 ) ;
#13176=CARTESIAN_POINT ( 'NONE',  ( -20.64999999999999858, 1.115600667400684642E-11, -200.9999999999999432 ) ) ;
#13186=FACE_OUTER_BOUND ( 'NONE', #198283, .T. ) ;
#13210=DIRECTION ( 'NONE',  ( 1.000000000000000000, -0.000000000000000000, 0.000000000000000000 ) ) ;
#13214=EDGE_CURVE ( 'NONE', #178378, #154754, #162617, .T. ) ;
#13216=DIRECTION ( 'NONE',  ( 0.000000000000000000, 0.000000000000000000, -1.000000000000000000 ) ) ;
#13220=ORIENTED_EDGE ( 'NONE', *, *, #179587, .F. ) ;
#13229=ORIENTED_EDGE ( 'NONE', *, *, #54044, .F. ) ;
#13272=ORIENTED_EDGE ( 'NONE', *, *, #229152, .T. ) ;
#13285=CARTESIAN_POINT ( 'NONE',  ( -21.08621493067320429, 0.05619483948720607747, -161.1507057088280419 ) ) ;
#13363=VERTEX_POINT ( 'NONE', #170358 ) ;
#13399=ORIENTED_EDGE ( 'NONE', *, *, #114358, .F. ) ;
#13404=DIRECTION ( 'NONE',  ( 0.000000000000000000, 0.9875055080513743810, -0.1575844902526802316 ) ) ;
#13432=DIRECTION ( 'NONE',  ( -0.000000000000000000, 3.469446951953635015E-14, 1.000000000000000000 ) ) ;
#13435=FACE_OUTER_BOUND ( 'NONE', #237299, .T. ) ;
#13465=EDGE_LOOP ( 'NONE', ( #198865, #48955, #17121, #240866 ) ) ;
#13475=DIRECTION ( 'NONE',  ( 1.000000000000000000, -0.000000000000000000, -0.000000000000000000 ) ) ;
#13476=AXIS2_PLACEMENT_3D ( 'NONE', #208301, #165307, #45357 ) ;
#13478=VECTOR ( 'NONE', #179711, 1000.000000000000000 ) ;
#13506=ORIENTED_EDGE ( 'NONE', *, *, #7245, .T. ) ;
#13548=AXIS2_PLACEMENT_3D ( 'NONE', #65966, #25568, #163795 ) ;
#13555=VECTOR ( 'NONE', #181087, 1000.000000000000000 ) ;
#13589=( BOUNDED_SURFACE ( )  B_SPLINE_SURFACE ( 3, 2, ( 
 ( #186224, #244898, #66274 ),
 ( #145790, #144498, #242330 ),
 ( #227913, #49266, #224043 ),
 ( #204480, #147070, #187523 ),
 ( #25873, #63691, #183661 ),
 ( #3720, #64974, #201932 ),
 ( #225317, #27179, #102800 ),
 ( #143223, #226608, #126230 ),
 ( #105351, #222758, #205770 ),
 ( #87092, #246194, #47976 ) ),
 .UNSPECIFIED., .F., .F., .F. ) 
 B_SPLINE_SURFACE_WITH_KNOTS ( ( 4, 2, 2, 2, 4 ),
 ( 3, 3 ),
 ( 0.0001701955120502393333, 0.0002247052511886148682, 0.0002792149903269904032, 0.0003882344686037414189, 0.0006062734251572434504 ),
 ( 0.000000000000000000, 1.000000000000000000 ),
 .UNSPECIFIED. ) 
 GEOMETRIC_REPRESENTATION_ITEM ( )  RATIONAL_B_SPLINE_SURFACE ( (
 ( 1.000000000000000000, 0.2966190024560962923, 1.000000000000000000),
 ( 1.000000000000000000, 0.2964522492697523326, 1.000000000000000000),
 ( 1.000000000000000000, 0.3059923531903553373, 1.000000000000000000),
 ( 1.000000000000000000, 0.3355751146924953465, 1.000000000000000000),
 ( 1.000000000000000000, 0.3550672384964631556, 1.000000000000000000),
 ( 1.000000000000000000, 0.4157034672184506396, 1.000000000000000000),
 ( 1.000000000000000000, 0.4588031877630285860, 1.000000000000000000),
 ( 1.000000000000000000, 0.5771441759709375896, 1.000000000000000000),
 ( 1.000000000000000000, 0.6469377121736774594, 1.000000000000000000),
 ( 1.000000000000000000, 0.7071067811865192621, 1.000000000000000000) ) ) 
 REPRESENTATION_ITEM ( '' )  SURFACE ( )  );
#13606=ORIENTED_EDGE ( 'NONE', *, *, #95705, .F. ) ;
#13610=EDGE_LOOP ( 'NONE', ( #58308, #146378, #226141, #11877 ) ) ;
#13615=EDGE_LOOP ( 'NONE', ( #239543, #218644, #141888, #110763 ) ) ;
#13642=EDGE_LOOP ( 'NONE', ( #3874, #147045, #45689, #134579 ) ) ;
#13647=EDGE_LOOP ( 'NONE', ( #64917, #4448, #244259 ) ) ;
#13657=ORIENTED_EDGE ( 'NONE', *, *, #20605, .T. ) ;
#13698=CARTESIAN_POINT ( 'NONE',  ( -20.94999999999999929, -11.41227409413852811, -198.0999999999999659 ) ) ;
#13711=CARTESIAN_POINT ( 'NONE',  ( 19.99999999999998934, 11.75000000001115907, -192.3499999999999659 ) ) ;
#13743=CARTESIAN_POINT ( 'NONE',  ( -23.15000000000000213, -9.499999999988848032, -177.3939691226524076 ) ) ;
#13757=CARTESIAN_POINT ( 'NONE',  ( 21.05000000000000071, 4.850467289730776344, -188.9657325909983001 ) ) ;
#13793=EDGE_CURVE ( 'NONE', #204622, #50484, #85110, .T. ) ;
#13800=EDGE_CURVE ( 'NONE', #55017, #233370, #189219, .T. ) ;
#13816=DIRECTION ( 'NONE',  ( 2.840903330521633255E-16, -0.8700118002898322711, 0.4930308989875231696 ) ) ;
#13820=CARTESIAN_POINT ( 'NONE',  ( -20.54999999999999716, 4.250000000011156409, -179.8499999999999943 ) ) ;
#13833=ORIENTED_EDGE ( 'NONE', *, *, #188288, .T. ) ;
#13929=CIRCLE ( 'NONE', #59873, 0.09999999999999939493 ) ;
#13936=DIRECTION ( 'NONE',  ( 0.000000000000000000, -1.000000000000000000, 0.000000000000000000 ) ) ;
#13943=EDGE_CURVE ( 'NONE', #46904, #1689, #218212, .T. ) ;
#13944=DIRECTION ( 'NONE',  ( 0.000000000000000000, 0.000000000000000000, -1.000000000000000000 ) ) ;
#13959=SPHERICAL_SURFACE ( 'NONE', #80100, 0.1000000000000000056 ) ;
#13962=EDGE_CURVE ( 'NONE', #142512, #204451, #243542, .T. ) ;
#13990=AXIS2_PLACEMENT_3D ( 'NONE', #123806, #139494, #144627 ) ;
#14000=CARTESIAN_POINT ( 'NONE',  ( 23.15000000000000213, -8.999999999988842703, -191.6060308773475072 ) ) ;
#14018=FACE_OUTER_BOUND ( 'NONE', #46852, .T. ) ;
#14052=CARTESIAN_POINT ( 'NONE',  ( -18.43707690579161351, -9.682403433465239573, -207.6568433774127129 ) ) ;
#14059=CYLINDRICAL_SURFACE ( 'NONE', #141824, 0.09999999999998898659 ) ;
#14070=DIRECTION ( 'NONE',  ( -1.000000000000000000, -0.000000000000000000, -0.000000000000000000 ) ) ;
#14072=LINE ( 'NONE', #191446, #115381 ) ;
#14095=VECTOR ( 'NONE', #105923, 999.9999999999998863 ) ;
#14124=CARTESIAN_POINT ( 'NONE',  ( -21.64999999999999858, 7.250000000011148416, -188.6499999999999488 ) ) ;
#14129=DIRECTION ( 'NONE',  ( -1.000000000000000000, 0.000000000000000000, 0.000000000000000000 ) ) ;
#14136=DIRECTION ( 'NONE',  ( -0.000000000000000000, 0.8660254037844411501, 0.4999999999999956146 ) ) ;
#14138=DIRECTION ( 'NONE',  ( 1.000000000000000000, 0.000000000000000000, 0.000000000000000000 ) ) ;
#14181=EDGE_CURVE ( 'NONE', #223514, #411, #93522, .T. ) ;
#14186=VERTEX_POINT ( 'NONE', #229353 ) ;
#14227=AXIS2_PLACEMENT_3D ( 'NONE', #112290, #113557, #251782 ) ;
#14294=EDGE_CURVE ( 'NONE', #190824, #95434, #252734, .T. ) ;
#14323=DIRECTION ( 'NONE',  ( -1.000000000000000000, -2.952720810173289112E-16, 0.000000000000000000 ) ) ;
#14362=SPHERICAL_SURFACE ( 'NONE', #160791, 0.1000000000000000056 ) ;
#14389=DIRECTION ( 'NONE',  ( 1.000000000000000000, 0.000000000000000000, 0.000000000000000000 ) ) ;
#14412=AXIS2_PLACEMENT_3D ( 'NONE', #115040, #212865, #253253 ) ;
#14470=CIRCLE ( 'NONE', #160215, 0.09999999999998898659 ) ;
#14488=EDGE_LOOP ( 'NONE', ( #18435, #61405, #137047, #257905 ) ) ;
#14498=EDGE_CURVE ( 'NONE', #4495, #33688, #77139, .T. ) ;
#14501=AXIS2_PLACEMENT_3D ( 'NONE', #196749, #54672, #153835 ) ;
#14558=VERTEX_POINT ( 'NONE', #150775 ) ;
#14573=ORIENTED_EDGE ( 'NONE', *, *, #129445, .F. ) ;
#14589=AXIS2_PLACEMENT_3D ( 'NONE', #76655, #36279, #57072 ) ;
#14590=CARTESIAN_POINT ( 'NONE',  ( 22.47007471830798764, 1.115784134737059924E-11, -159.7792893480734904 ) ) ;
#14619=CARTESIAN_POINT ( 'NONE',  ( 20.94999999999999929, 1.115600667400684642E-11, -167.4999999999999716 ) ) ;
#14639=ORIENTED_EDGE ( 'NONE', *, *, #67051, .T. ) ;
#14646=EDGE_CURVE ( 'NONE', #221039, #86050, #251927, .T. ) ;
#14647=EDGE_CURVE ( 'NONE', #55017, #12777, #222882, .T. ) ;
#14650=ORIENTED_EDGE ( 'NONE', *, *, #170640, .F. ) ;
#14651=CIRCLE ( 'NONE', #60401, 12.77500000000000036 ) ;
#14655=DIRECTION ( 'NONE',  ( 1.000000000000000000, 0.000000000000000000, 0.000000000000000000 ) ) ;
#14669=ORIENTED_EDGE ( 'NONE', *, *, #179698, .F. ) ;
#14674=CARTESIAN_POINT ( 'NONE',  ( 18.60000000000000142, -9.321008403350125704, -174.7359382490778614 ) ) ;
#14675=ORIENTED_EDGE ( 'NONE', *, *, #150073, .T. ) ;
#14700=EDGE_CURVE ( 'NONE', #142940, #226886, #125459, .T. ) ;
#14708=AXIS2_PLACEMENT_3D ( 'NONE', #147187, #149785, #25972 ) ;
#14710=CARTESIAN_POINT ( 'NONE',  ( 18.49999999999999289, 10.20857864377384239, -192.2671572875252934 ) ) ;
#14718=FACE_OUTER_BOUND ( 'NONE', #145533, .T. ) ;
#14738=DIRECTION ( 'NONE',  ( 0.000000000000000000, -3.339342691255721203E-13, 1.000000000000000000 ) ) ;
#14768=ORIENTED_EDGE ( 'NONE', *, *, #169629, .T. ) ;
#14774=DIRECTION ( 'NONE',  ( 1.713247197920696616E-14, 0.9876197685951252359, -0.1568667991644863424 ) ) ;
#14783=CARTESIAN_POINT ( 'NONE',  ( -23.15000000000000213, 2.500000000011154633, -187.7753780772378889 ) ) ;
#14809=EDGE_CURVE ( 'NONE', #255868, #192876, #102229, .T. ) ;
#14831=EDGE_CURVE ( 'NONE', #159614, #253024, #256312, .T. ) ;
#14833=VERTEX_POINT ( 'NONE', #51010 ) ;
#14855=CIRCLE ( 'NONE', #77188, 0.09999999999999939493 ) ;
#14880=VERTEX_POINT ( 'NONE', #154054 ) ;
#14897=AXIS2_PLACEMENT_3D ( 'NONE', #249356, #32907, #227205 ) ;
#14912=CIRCLE ( 'NONE', #119135, 0.09999999999999939493 ) ;
#14923=ADVANCED_FACE ( 'NONE', ( #137000 ), #36654, .T. ) ;
#14928=FACE_OUTER_BOUND ( 'NONE', #16453, .T. ) ;
#14930=AXIS2_PLACEMENT_3D ( 'NONE', #166278, #124561, #145385 ) ;
#14951=CIRCLE ( 'NONE', #160730, 0.09999999999998898659 ) ;
#14967=CARTESIAN_POINT ( 'NONE',  ( -23.25000000000000000, 1.910280373842930812, -188.3686321448010403 ) ) ;
#15018=ORIENTED_EDGE ( 'NONE', *, *, #89160, .F. ) ;
#15032=CIRCLE ( 'NONE', #181622, 0.09999999999998898659 ) ;
#15063=CARTESIAN_POINT ( 'NONE',  ( -20.85000000000000142, 1.115600667400684642E-11, -200.9999999999999432 ) ) ;
#15093=ORIENTED_EDGE ( 'NONE', *, *, #219532, .F. ) ;
#15150=ORIENTED_EDGE ( 'NONE', *, *, #215445, .T. ) ;
#15161=CIRCLE ( 'NONE', #40131, 0.09999999999998898659 ) ;
#15162=ADVANCED_FACE ( 'NONE', ( #164285 ), #194056, .T. ) ;
#15174=CARTESIAN_POINT ( 'NONE',  ( 18.49999999999998934, 10.25000000001115552, -192.2499999999999716 ) ) ;
#15175=ADVANCED_FACE ( 'NONE', ( #50710 ), #248957, .F. ) ;
#15178=CARTESIAN_POINT ( 'NONE',  ( 18.59999999999999076, 6.982009704867611077, -204.6961521182562649 ) ) ;
#15190=EDGE_LOOP ( 'NONE', ( #123367, #42656, #54340, #33180 ) ) ;
#15197=EDGE_CURVE ( 'NONE', #254577, #199182, #69044, .T. ) ;
#15209=CARTESIAN_POINT ( 'NONE',  ( -20.94560253601877164, 11.75000000001115197, -194.0100835125150240 ) ) ;
#15236=ORIENTED_EDGE ( 'NONE', *, *, #30883, .F. ) ;
#15284=LINE ( 'NONE', #111808, #180768 ) ;
#15287=ORIENTED_EDGE ( 'NONE', *, *, #13001, .F. ) ;
#15292=DIRECTION ( 'NONE',  ( 0.000000000000000000, 0.6728971962617388280, 0.7397360091702248619 ) ) ;
#15307=CARTESIAN_POINT ( 'NONE',  ( -18.59999999999999787, 11.65000000001115232, -179.6499999999999773 ) ) ;
#15335=ORIENTED_EDGE ( 'NONE', *, *, #174, .T. ) ;
#15369=ORIENTED_EDGE ( 'NONE', *, *, #21445, .F. ) ;
#15370=ORIENTED_EDGE ( 'NONE', *, *, #5732, .T. ) ;
#15398=LINE ( 'NONE', #234415, #58047 ) ;
#15405=CIRCLE ( 'NONE', #27889, 2.000000000000001776 ) ;
#15409=DIRECTION ( 'NONE',  ( -0.000000000000000000, -0.7397360091702755991, -0.6728971962616832059 ) ) ;
#15414=CARTESIAN_POINT ( 'NONE',  ( 20.85000000000000142, 1.115600667400684642E-11, -200.9999999999999432 ) ) ;
#15435=CARTESIAN_POINT ( 'NONE',  ( -23.25000000000000000, 4.250000000011156409, -179.6499999999999773 ) ) ;
#15450=CARTESIAN_POINT ( 'NONE',  ( 20.12481660106788084, 9.526343992285099205, -175.7261416690961937 ) ) ;
#15479=CARTESIAN_POINT ( 'NONE',  ( -18.40904629823844729, -9.499999999988851584, -207.6001895624822566 ) ) ;
#15497=CIRCLE ( 'NONE', #69835, 4.049999999999998934 ) ;
#15507=CARTESIAN_POINT ( 'NONE',  ( -20.85000000000000142, 1.115600667400684642E-11, -200.9999999999999432 ) ) ;
#15511=ORIENTED_EDGE ( 'NONE', *, *, #218929, .F. ) ;
#15539=VERTEX_POINT ( 'NONE', #28336 ) ;
#15574=EDGE_CURVE ( 'NONE', #8977, #27613, #119389, .T. ) ;
#15611=ORIENTED_EDGE ( 'NONE', *, *, #136692, .T. ) ;
#15629=ORIENTED_EDGE ( 'NONE', *, *, #102149, .T. ) ;
#15658=AXIS2_PLACEMENT_3D ( 'NONE', #175721, #235655, #51875 ) ;
#15666=DIRECTION ( 'NONE',  ( 0.000000000000000000, 1.000000000000000000, 0.000000000000000000 ) ) ;
#15667=EDGE_CURVE ( 'NONE', #250279, #75355, #227519, .T. ) ;
#15707=TOROIDAL_SURFACE ( 'NONE', #177998, 11.65000000000000036, 0.1000000000000000056 ) ;
#15717=DIRECTION ( 'NONE',  ( 1.000000000000000000, 0.000000000000000000, 0.000000000000000000 ) ) ;
#15762=FACE_OUTER_BOUND ( 'NONE', #80776, .T. ) ;
#15777=DIRECTION ( 'NONE',  ( 1.000000000000000000, 0.000000000000000000, 0.000000000000000000 ) ) ;
#15793=DIRECTION ( 'NONE',  ( 0.000000000000000000, 0.000000000000000000, -1.000000000000000000 ) ) ;
#15796=EDGE_CURVE ( 'NONE', #132728, #146076, #102595, .T. ) ;
#15802=DIRECTION ( 'NONE',  ( -0.000000000000000000, -0.1298341882519737922, -0.9915357197604890427 ) ) ;
#15806=DIRECTION ( 'NONE',  ( 0.000000000000000000, 0.9908441862701782288, -0.1350103645450542456 ) ) ;
#15811=ADVANCED_FACE ( 'NONE', ( #163654 ), #181933, .T. ) ;
#15863=VECTOR ( 'NONE', #183440, 1000.000000000000114 ) ;
#15878=ORIENTED_EDGE ( 'NONE', *, *, #138840, .F. ) ;
#15899=EDGE_CURVE ( 'NONE', #86132, #137741, #69523, .T. ) ;
#15914=DIRECTION ( 'NONE',  ( 0.000000000000000000, 0.000000000000000000, -1.000000000000000000 ) ) ;
#15923=VECTOR ( 'NONE', #149404, 1000.000000000000000 ) ;
#15943=CARTESIAN_POINT ( 'NONE',  ( -18.39999999999999858, -9.519327731081281385, -174.4729763765593020 ) ) ;
#15951=VECTOR ( 'NONE', #96532, 1000.000000000000114 ) ;
#15973=CARTESIAN_POINT ( 'NONE',  ( -18.59999999999999787, 11.65000000001115232, -200.9999999999999432 ) ) ;
#15995=CARTESIAN_POINT ( 'NONE',  ( 19.97071067695831559, 11.72071067696947644, -192.1762534328032075 ) ) ;
#16013=ORIENTED_EDGE ( 'NONE', *, *, #105266, .T. ) ;
#16039=CARTESIAN_POINT ( 'NONE',  ( -23.25000000000000000, 11.75000000001115552, -155.7499999999999716 ) ) ;
#16040=DIRECTION ( 'NONE',  ( -0.7071067811865475727, -0.7071067811865475727, -0.000000000000000000 ) ) ;
#16073=ORIENTED_EDGE ( 'NONE', *, *, #25509, .F. ) ;
#16080=FACE_OUTER_BOUND ( 'NONE', #157821, .T. ) ;
#16085=CARTESIAN_POINT ( 'NONE',  ( -2.995603634470891112E-16, 6.650000000011155876, -188.6499999999999488 ) ) ;
#16115=FACE_OUTER_BOUND ( 'NONE', #124654, .T. ) ;
#16154=EDGE_LOOP ( 'NONE', ( #249134, #251480, #185549, #8413 ) ) ;
#16193=VERTEX_POINT ( 'NONE', #124238 ) ;
#16201=TOROIDAL_SURFACE ( 'NONE', #28699, 3.899999999999999467, 0.1000000000000000056 ) ;
#16214=CIRCLE ( 'NONE', #136991, 0.09999999999999939493 ) ;
#16215=CARTESIAN_POINT ( 'NONE',  ( -20.64999999999999858, 1.115600667400684642E-11, -200.9999999999999432 ) ) ;
#16219=DIRECTION ( 'NONE',  ( 0.7071359030028113724, 0.000000000000000000, 0.7070776581708677622 ) ) ;
#16246=CARTESIAN_POINT ( 'NONE',  ( 20.85000000000000142, -11.74999999998883560, -197.9999999999999432 ) ) ;
#16272=VERTEX_POINT ( 'NONE', #249323 ) ;
#16283=VERTEX_POINT ( 'NONE', #228477 ) ;
#16296=CARTESIAN_POINT ( 'NONE',  ( 20.85000000000000142, 11.75000000001115907, -194.2161343370218560 ) ) ;
#16302=CARTESIAN_POINT ( 'NONE',  ( 20.94999999999999929, 6.450000000011156587, -177.5170271704400022 ) ) ;
#16323=ORIENTED_EDGE ( 'NONE', *, *, #69135, .F. ) ;
#16367=EDGE_CURVE ( 'NONE', #120605, #116285, #211346, .T. ) ;
#16371=ORIENTED_EDGE ( 'NONE', *, *, #136060, .T. ) ;
#16383=CIRCLE ( 'NONE', #107945, 12.97499999999998721 ) ;
#16438=ORIENTED_EDGE ( 'NONE', *, *, #95705, .T. ) ;
#16453=EDGE_LOOP ( 'NONE', ( #1931, #209899, #186178 ) ) ;
#16479=CARTESIAN_POINT ( 'NONE',  ( 21.05000000000000071, 8.876614585098254295, -175.8850804788446567 ) ) ;
#16497=CYLINDRICAL_SURFACE ( 'NONE', #98496, 0.1000000000000098310 ) ;
#16531=DIRECTION ( 'NONE',  ( 1.000000000000000000, 0.000000000000000000, 0.000000000000000000 ) ) ;
#16548=DIRECTION ( 'NONE',  ( 1.000000000000000000, 0.000000000000000000, 0.000000000000000000 ) ) ;
#16564=AXIS2_PLACEMENT_3D ( 'NONE', #82394, #43312, #122853 ) ;
#16599=CARTESIAN_POINT ( 'NONE',  ( 21.05000000000000071, -0.09999993529482809063, -161.0219217789056643 ) ) ;
#16601=CARTESIAN_POINT ( 'NONE',  ( -21.05000000000000071, 1.835341550235567887, -179.0551512925629538 ) ) ;
#16613=VERTEX_POINT ( 'NONE', #183571 ) ;
#16629=EDGE_LOOP ( 'NONE', ( #27848, #257461, #225904, #257985, #152776, #54003, #243282 ) ) ;
#16684=LINE ( 'NONE', #214861, #202128 ) ;
#16705=ORIENTED_EDGE ( 'NONE', *, *, #62797, .T. ) ;
#16706=DIRECTION ( 'NONE',  ( -0.000000000000000000, -2.891205793294679805E-16, 1.000000000000000000 ) ) ;
#16712=CARTESIAN_POINT ( 'NONE',  ( 23.24999999999999645, 4.775700934590584090, -179.3487681040459165 ) ) ;
#16730=CARTESIAN_POINT ( 'NONE',  ( 20.22516295850462598, 9.899364295461838381, -175.4100657120905566 ) ) ;
#16802=AXIS2_PLACEMENT_3D ( 'NONE', #139885, #43379, #59047 ) ;
#16831=ORIENTED_EDGE ( 'NONE', *, *, #29896, .F. ) ;
#16837=DIRECTION ( 'NONE',  ( 1.000000000000000000, 0.000000000000000000, 0.000000000000000000 ) ) ;
#16858=DIRECTION ( 'NONE',  ( 0.000000000000000000, -1.000000000000000000, -0.000000000000000000 ) ) ;
#16859=CARTESIAN_POINT ( 'NONE',  ( 21.05000000000000071, -0.09999999998884338825, -155.8504291924551808 ) ) ;
#16866=LINE ( 'NONE', #79370, #224661 ) ;
#16871=DIRECTION ( 'NONE',  ( 0.000000000000000000, -1.000000000000000000, -5.551115123125768187E-14 ) ) ;
#16901=CARTESIAN_POINT ( 'NONE',  ( 21.14999999999999858, 6.650000000011155876, -179.6499999999999773 ) ) ;
#16902=DIRECTION ( 'NONE',  ( 0.000000000000000000, 2.891205793294679805E-16, -1.000000000000000000 ) ) ;
#16912=CARTESIAN_POINT ( 'NONE',  ( -20.00857864376270001, 9.350000000011156942, -188.6499999999999488 ) ) ;
#16968=ADVANCED_FACE ( 'NONE', ( #103690 ), #4599, .F. ) ;
#16987=PLANE ( 'NONE',  #153421 ) ;
#17005=ADVANCED_FACE ( 'NONE', ( #149291 ), #47578, .F. ) ;
#17028=CARTESIAN_POINT ( 'NONE',  ( -18.59999999999999787, 9.350000000011156942, -188.7499999999999716 ) ) ;
#17030=AXIS2_PLACEMENT_3D ( 'NONE', #83102, #44018, #242211 ) ;
#17102=ORIENTED_EDGE ( 'NONE', *, *, #15197, .T. ) ;
#17106=EDGE_LOOP ( 'NONE', ( #121464, #123948, #247329, #171010 ) ) ;
#17107=FACE_OUTER_BOUND ( 'NONE', #48559, .T. ) ;
#17113=CARTESIAN_POINT ( 'NONE',  ( -23.25000000000000000, 11.65000000001115588, -188.7499999999999716 ) ) ;
#17121=ORIENTED_EDGE ( 'NONE', *, *, #126748, .F. ) ;
#17158=ORIENTED_EDGE ( 'NONE', *, *, #181541, .T. ) ;
#17179=ORIENTED_EDGE ( 'NONE', *, *, #45405, .F. ) ;
#17192=CARTESIAN_POINT ( 'NONE',  ( 18.59999999999999432, -1.736257131586239844, -179.0686523290174819 ) ) ;
#17200=ORIENTED_EDGE ( 'NONE', *, *, #168825, .F. ) ;
#17204=ORIENTED_EDGE ( 'NONE', *, *, #113665, .T. ) ;
#17212=DIRECTION ( 'NONE',  ( -0.7071067811865474617, -0.7071067811865474617, -0.000000000000000000 ) ) ;
#17217=DIRECTION ( 'NONE',  ( 1.000000000000000000, -0.000000000000000000, 0.000000000000000000 ) ) ;
#17255=CARTESIAN_POINT ( 'NONE',  ( 21.09610168723072832, 0.03358950690265592037, -161.1210442847751665 ) ) ;
#17258=CARTESIAN_POINT ( 'NONE',  ( 18.49999999999999289, 10.49142135624846439, -192.3499999999999659 ) ) ;
#17268=EDGE_LOOP ( 'NONE', ( #2749, #239736, #115345, #218782, #225574, #246458, #234271, #215721, #146737, #132893 ) ) ;
#17328=EDGE_LOOP ( 'NONE', ( #78792, #83146, #212480, #141607 ) ) ;
#17335=VERTEX_POINT ( 'NONE', #185551 ) ;
#17362=CYLINDRICAL_SURFACE ( 'NONE', #208655, 0.8750000000000007772 ) ;
#17373=ORIENTED_EDGE ( 'NONE', *, *, #205926, .F. ) ;
#17376=DIRECTION ( 'NONE',  ( 0.000000000000000000, 0.4999999999999348299, -0.8660254037844762331 ) ) ;
#17378=ORIENTED_EDGE ( 'NONE', *, *, #69726, .T. ) ;
#17415=VERTEX_POINT ( 'NONE', #231123 ) ;
#17417=ORIENTED_EDGE ( 'NONE', *, *, #65045, .F. ) ;
#17419=ORIENTED_EDGE ( 'NONE', *, *, #19029, .T. ) ;
#17459=AXIS2_PLACEMENT_3D ( 'NONE', #55700, #79139, #157452 ) ;
#17506=DIRECTION ( 'NONE',  ( 0.000000000000000000, 0.000000000000000000, -1.000000000000000000 ) ) ;
#17511=EDGE_LOOP ( 'NONE', ( #247274, #69847, #59187 ) ) ;
#17533=EDGE_LOOP ( 'NONE', ( #165661, #142729, #212435, #102755 ) ) ;
#17547=CARTESIAN_POINT ( 'NONE',  ( 20.94999999999999929, 1.115600667400684642E-11, -180.3749999999999716 ) ) ;
#17559=AXIS2_PLACEMENT_3D ( 'NONE', #200819, #203388, #2599 ) ;
#17565=ADVANCED_FACE ( 'NONE', ( #41915 ), #82260, .T. ) ;
#17567=EDGE_CURVE ( 'NONE', #4296, #64828, #182681, .T. ) ;
#17574=CARTESIAN_POINT ( 'NONE',  ( 21.05000000000251958, 10.50253167713809965, -175.0588298170762869 ) ) ;
#17580=DIRECTION ( 'NONE',  ( 1.000000000000000000, 0.000000000000000000, -0.000000000000000000 ) ) ;
#17594=AXIS2_PLACEMENT_3D ( 'NONE', #122665, #164352, #48239 ) ;
#17604=FACE_OUTER_BOUND ( 'NONE', #230299, .T. ) ;
#17609=ORIENTED_EDGE ( 'NONE', *, *, #125109, .F. ) ;
#17612=DIRECTION ( 'NONE',  ( 0.000000000000000000, 0.000000000000000000, 1.000000000000000000 ) ) ;
#17627=CIRCLE ( 'NONE', #146800, 0.09999999999998898659 ) ;
#17636=CARTESIAN_POINT ( 'NONE',  ( 20.94999999999999929, 1.115600667400684642E-11, -202.8999999999999773 ) ) ;
#17637=ORIENTED_EDGE ( 'NONE', *, *, #33114, .F. ) ;
#17640=CIRCLE ( 'NONE', #96736, 0.09999999999998898659 ) ;
#17663=DIRECTION ( 'NONE',  ( 0.000000000000000000, 0.000000000000000000, -1.000000000000000000 ) ) ;
#17724=VERTEX_POINT ( 'NONE', #13060 ) ;
#17740=CARTESIAN_POINT ( 'NONE',  ( -21.04386569057742307, 11.75000000001181277, -194.1428373517780130 ) ) ;
#17823=CARTESIAN_POINT ( 'NONE',  ( -20.54999999999999716, 7.150000000011155876, -188.6499999999999488 ) ) ;
#17863=ORIENTED_EDGE ( 'NONE', *, *, #245728, .F. ) ;
#17907=CARTESIAN_POINT ( 'NONE',  ( -20.54999999999999716, -8.999999999988846255, -176.8939691226524076 ) ) ;
#17940=CARTESIAN_POINT ( 'NONE',  ( 18.56579813702274961, 10.33025634372637924, -206.5870929282638429 ) ) ;
#17985=CARTESIAN_POINT ( 'NONE',  ( 20.75572585718237661, 8.882316728409755058, -175.9972583987020016 ) ) ;
#18010=FACE_OUTER_BOUND ( 'NONE', #47671, .T. ) ;
#18038=EDGE_CURVE ( 'NONE', #108161, #135650, #140566, .T. ) ;
#18050=DIRECTION ( 'NONE',  ( -1.000000000000000000, -1.836970198721029934E-16, 0.000000000000000000 ) ) ;
#18059=DIRECTION ( 'NONE',  ( 8.673617379884087537E-15, -0.000000000000000000, 1.000000000000000000 ) ) ;
#18071=ORIENTED_EDGE ( 'NONE', *, *, #81387, .F. ) ;
#18079=CARTESIAN_POINT ( 'NONE',  ( -21.12757541349819590, 0.005161215820883788274, -161.0266194287484041 ) ) ;
#18081=DIRECTION ( 'NONE',  ( -0.000000000000000000, 0.9876197685951279004, -0.1568667991644694115 ) ) ;
#18103=AXIS2_PLACEMENT_3D ( 'NONE', #22003, #101476, #181083 ) ;
#18108=LINE ( 'NONE', #140615, #248768 ) ;
#18140=ORIENTED_EDGE ( 'NONE', *, *, #179806, .T. ) ;
#18147=DIRECTION ( 'NONE',  ( 0.000000000000000000, 1.897661533703519897E-16, -1.000000000000000000 ) ) ;
#18172=ADVANCED_FACE ( 'NONE', ( #14018 ), #65933, .T. ) ;
#18177=VECTOR ( 'NONE', #2984, 1000.000000000000227 ) ;
#18187=ORIENTED_EDGE ( 'NONE', *, *, #104362, .F. ) ;
#18246=AXIS2_PLACEMENT_3D ( 'NONE', #65442, #180269, #142412 ) ;
#18293=AXIS2_PLACEMENT_3D ( 'NONE', #94622, #253692, #148185 ) ;
#18302=ORIENTED_EDGE ( 'NONE', *, *, #100533, .F. ) ;
#18312=CIRCLE ( 'NONE', #72488, 0.09999999999998898659 ) ;
#18317=ADVANCED_FACE ( 'NONE', ( #180787 ), #86753, .F. ) ;
#18320=EDGE_LOOP ( 'NONE', ( #109054, #117596, #136868, #162762 ) ) ;
#18326=EDGE_CURVE ( 'NONE', #223354, #69705, #232371, .T. ) ;
#18335=ADVANCED_FACE ( 'NONE', ( #206759 ), #232563, .T. ) ;
#18404=CARTESIAN_POINT ( 'NONE',  ( 22.32929514600007792, 7.578647565387638174, -167.4009243218860661 ) ) ;
#18428=ORIENTED_EDGE ( 'NONE', *, *, #93496, .F. ) ;
#18435=ORIENTED_EDGE ( 'NONE', *, *, #157878, .F. ) ;
#18486=DIRECTION ( 'NONE',  ( 0.000000000000000000, -2.602085213965497408E-13, 1.000000000000000000 ) ) ;
#18495=ORIENTED_EDGE ( 'NONE', *, *, #112962, .F. ) ;
#18541=VECTOR ( 'NONE', #46161, 1000.000000000000000 ) ;
#18545=ADVANCED_FACE ( 'NONE', ( #59191 ), #237874, .T. ) ;
#18583=CARTESIAN_POINT ( 'NONE',  ( 18.59999999999999076, 1.115600667400684642E-11, -200.9999999999999432 ) ) ;
#18584=FACE_OUTER_BOUND ( 'NONE', #51933, .T. ) ;
#18606=DIRECTION ( 'NONE',  ( 1.000000000000000000, 0.000000000000000000, 0.000000000000000000 ) ) ;
#18609=ORIENTED_EDGE ( 'NONE', *, *, #49124, .T. ) ;
#18638=DIRECTION ( 'NONE',  ( 1.000000000000000000, 0.000000000000000000, 0.000000000000000000 ) ) ;
#18650=AXIS2_PLACEMENT_3D ( 'NONE', #11562, #114495, #32426 ) ;
#18668=EDGE_CURVE ( 'NONE', #123667, #62433, #182663, .T. ) ;
#18670=AXIS2_PLACEMENT_3D ( 'NONE', #256272, #99804, #138923 ) ;
#18681=ORIENTED_EDGE ( 'NONE', *, *, #102099, .F. ) ;
#18694=DIRECTION ( 'NONE',  ( 0.000000000000000000, -0.9908441862701600211, -0.1350103645451876666 ) ) ;
#18710=EDGE_CURVE ( 'NONE', #140937, #58899, #186757, .T. ) ;
#18714=ORIENTED_EDGE ( 'NONE', *, *, #168436, .T. ) ;
#18718=ORIENTED_EDGE ( 'NONE', *, *, #191749, .T. ) ;
#18720=EDGE_CURVE ( 'NONE', #35026, #130077, #157760, .T. ) ;
#18764=FACE_OUTER_BOUND ( 'NONE', #133946, .T. ) ;
#18772=CARTESIAN_POINT ( 'NONE',  ( -23.25000000000000000, 1.115600667400684642E-11, -200.9999999999999432 ) ) ;
#18781=ORIENTED_EDGE ( 'NONE', *, *, #45954, .F. ) ;
#18821=AXIS2_PLACEMENT_3D ( 'NONE', #154933, #14136, #93646 ) ;
#18824=EDGE_CURVE ( 'NONE', #129423, #136769, #132959, .T. ) ;
#18852=CIRCLE ( 'NONE', #10676, 0.09999999999999939493 ) ;
#18861=ORIENTED_EDGE ( 'NONE', *, *, #78798, .F. ) ;
#18881=DIRECTION ( 'NONE',  ( 0.000000000000000000, 0.9999631594459053030, 0.008583690987162899758 ) ) ;
#18892=ORIENTED_EDGE ( 'NONE', *, *, #190249, .F. ) ;
#18957=CARTESIAN_POINT ( 'NONE',  ( -20.54999999999999716, 2.400000000011155432, -180.7246219227620543 ) ) ;
#19029=EDGE_CURVE ( 'NONE', #213934, #86243, #224519, .T. ) ;
#19093=CARTESIAN_POINT ( 'NONE',  ( -21.13614978966382196, 6.499104701844943044, -167.5000000000000000 ) ) ;
#19120=VERTEX_POINT ( 'NONE', #233124 ) ;
#19121=DIRECTION ( 'NONE',  ( 0.000000000000000000, 0.000000000000000000, -1.000000000000000000 ) ) ;
#19127=ORIENTED_EDGE ( 'NONE', *, *, #235833, .F. ) ;
#19146=ORIENTED_EDGE ( 'NONE', *, *, #152458, .T. ) ;
#19165=EDGE_CURVE ( 'NONE', #133, #86132, #144775, .T. ) ;
#19194=CARTESIAN_POINT ( 'NONE',  ( 21.97500000000000497, 9.750000000011153745, -179.7499999999999716 ) ) ;
#19246=VECTOR ( 'NONE', #30920, 1000.000000000000000 ) ;
#19288=ADVANCED_FACE ( 'NONE', ( #200387 ), #241906, .F. ) ;
#19299=ORIENTED_EDGE ( 'NONE', *, *, #227965, .T. ) ;
#19305=ORIENTED_EDGE ( 'NONE', *, *, #835, .T. ) ;
#19363=AXIS2_PLACEMENT_3D ( 'NONE', #11055, #47594, #48890 ) ;
#19390=DIRECTION ( 'NONE',  ( 0.000000000000000000, 1.000000000000000000, 0.000000000000000000 ) ) ;
#19395=DIRECTION ( 'NONE',  ( 1.000000000000000000, 0.000000000000000000, 0.000000000000000000 ) ) ;
#19401=CARTESIAN_POINT ( 'NONE',  ( -23.15000000000000213, -11.64999999998884483, -197.8999999999999773 ) ) ;
#19406=ORIENTED_EDGE ( 'NONE', *, *, #137839, .T. ) ;
#19411=ORIENTED_EDGE ( 'NONE', *, *, #161900, .T. ) ;
#19426=CIRCLE ( 'NONE', #140190, 0.09999999999999907574 ) ;
#19435=DIRECTION ( 'NONE',  ( 0.000000000000000000, -4.336808689942494997E-15, -1.000000000000000000 ) ) ;
#19439=EDGE_LOOP ( 'NONE', ( #156077, #253588, #94106, #203531, #6667, #245333, #98860, #16013, #17419, #153224, #61679, #76511, #30616, #114956 ) ) ;
#19475=CARTESIAN_POINT ( 'NONE',  ( 19.58285714285715073, 10.38499851036257837, -175.1296846673899097 ) ) ;
#19496=CARTESIAN_POINT ( 'NONE',  ( 20.94999999999999929, 5.400000000011154988, -179.9052660189130677 ) ) ;
#19508=CYLINDRICAL_SURFACE ( 'NONE', #8557, 0.09999999999998898659 ) ;
#19514=AXIS2_PLACEMENT_3D ( 'NONE', #67265, #7285, #248478 ) ;
#19536=ORIENTED_EDGE ( 'NONE', *, *, #209469, .F. ) ;
#19548=DIRECTION ( 'NONE',  ( -1.836970198721029934E-16, 1.000000000000000000, 0.000000000000000000 ) ) ;
#19573=DIRECTION ( 'NONE',  ( 1.000000000000000000, 0.000000000000000000, 0.000000000000000000 ) ) ;
#19575=DIRECTION ( 'NONE',  ( 0.000000000000000000, -1.000000000000000000, 0.000000000000000000 ) ) ;
#19604=DIRECTION ( 'NONE',  ( -1.000000000000000000, -0.000000000000000000, 0.000000000000000000 ) ) ;
#19616=CARTESIAN_POINT ( 'NONE',  ( 21.05000000000000071, 1.115600667400684642E-11, -167.4999999999999716 ) ) ;
#19628=CIRCLE ( 'NONE', #144493, 0.1000000000000002554 ) ;
#19652=CARTESIAN_POINT ( 'NONE',  ( -21.51976009735018991, 6.910458441670358276, -167.4999999999999716 ) ) ;
#19672=CARTESIAN_POINT ( 'NONE',  ( -20.94999999999999929, 1.115600667400684642E-11, -200.9999999999999432 ) ) ;
#19690=EDGE_CURVE ( 'NONE', #231547, #90736, #66743, .T. ) ;
#19720=TOROIDAL_SURFACE ( 'NONE', #240293, 4.099999999999999645, 0.1000000000000000056 ) ;
#19742=CIRCLE ( 'NONE', #203055, 0.5000000000000004441 ) ;
#19743=EDGE_CURVE ( 'NONE', #96608, #152513, #71253, .T. ) ;
#19778=CARTESIAN_POINT ( 'NONE',  ( 22.60000000000000142, 11.74956712350054744, -167.3991416309012550 ) ) ;
#19793=DIRECTION ( 'NONE',  ( 0.000000000000000000, 0.000000000000000000, -1.000000000000000000 ) ) ;
#19800=DIRECTION ( 'NONE',  ( 0.000000000000000000, 0.000000000000000000, -1.000000000000000000 ) ) ;
#19807=EDGE_CURVE ( 'NONE', #210872, #220110, #96337, .T. ) ;
#19823=CIRCLE ( 'NONE', #53116, 11.64999999999999325 ) ;
#19824=CARTESIAN_POINT ( 'NONE',  ( -18.40000000000000213, -9.499999999988851584, -174.5320693966996259 ) ) ;
#19858=CARTESIAN_POINT ( 'NONE',  ( 21.05000000000000071, 5.850000000011156942, -190.8675027757220448 ) ) ;
#19930=CIRCLE ( 'NONE', #165675, 0.09999999999999939493 ) ;
#19947=VERTEX_POINT ( 'NONE', #55092 ) ;
#19965=CARTESIAN_POINT ( 'NONE',  ( -18.59999999999999787, 1.835341550235567887, -179.0551512925629538 ) ) ;
#19988=VECTOR ( 'NONE', #176276, 1000.000000000000000 ) ;
#20022=DIRECTION ( 'NONE',  ( -0.000000000000000000, -1.000000000000000000, 0.000000000000000000 ) ) ;
#20042=DIRECTION ( 'NONE',  ( 0.000000000000000000, 0.000000000000000000, -1.000000000000000000 ) ) ;
#20055=FACE_OUTER_BOUND ( 'NONE', #157628, .T. ) ;
#20075=CARTESIAN_POINT ( 'NONE',  ( 20.94999027547553894, 10.29326151435327219, -206.4592822510414578 ) ) ;
#20076=AXIS2_PLACEMENT_3D ( 'NONE', #167985, #229218, #191397 ) ;
#20080=CIRCLE ( 'NONE', #28500, 0.1000000000000043493 ) ;
#20100=CARTESIAN_POINT ( 'NONE',  ( 22.47071067811865319, 0.09909245471376171288, -159.7799252555019223 ) ) ;
#20170=CARTESIAN_POINT ( 'NONE',  ( 21.05000000000000071, 10.72371710471868056, -175.1649135690875880 ) ) ;
#20215=ADVANCED_FACE ( 'NONE', ( #241473 ), #26280, .F. ) ;
#20224=VECTOR ( 'NONE', #14129, 1000.000000000000000 ) ;
#20232=ORIENTED_EDGE ( 'NONE', *, *, #13793, .F. ) ;
#20266=CARTESIAN_POINT ( 'NONE',  ( -21.05000000000000071, 6.270085863700304962, -167.4651319969869121 ) ) ;
#20288=EDGE_CURVE ( 'NONE', #141132, #223911, #61467, .T. ) ;
#20303=AXIS2_PLACEMENT_3D ( 'NONE', #67682, #207214, #191517 ) ;
#20305=ORIENTED_EDGE ( 'NONE', *, *, #138840, .T. ) ;
#20367=LINE ( 'NONE', #21637, #244067 ) ;
#20370=CIRCLE ( 'NONE', #83033, 0.09999999999998898659 ) ;
#20374=LINE ( 'NONE', #77732, #127758 ) ;
#20424=ADVANCED_FACE ( 'NONE', ( #4938 ), #167930, .F. ) ;
#20447=FACE_OUTER_BOUND ( 'NONE', #160786, .T. ) ;
#20453=CARTESIAN_POINT ( 'NONE',  ( -21.14999999999999858, 6.540656951712397138, -167.5999999999999659 ) ) ;
#20454=ORIENTED_EDGE ( 'NONE', *, *, #45954, .T. ) ;
#20457=PLANE ( 'NONE',  #176863 ) ;
#20465=ORIENTED_EDGE ( 'NONE', *, *, #114546, .F. ) ;
#20473=PLANE ( 'NONE',  #92618 ) ;
#20474=ORIENTED_EDGE ( 'NONE', *, *, #71904, .T. ) ;
#20479=VECTOR ( 'NONE', #177934, 1000.000000000000114 ) ;
#20513=DIRECTION ( 'NONE',  ( -0.000000000000000000, -0.8660254037844411501, -0.4999999999999956701 ) ) ;
#20537=AXIS2_PLACEMENT_3D ( 'NONE', #135315, #178337, #234422 ) ;
#20571=EDGE_CURVE ( 'NONE', #104346, #67428, #74155, .T. ) ;
#20572=CARTESIAN_POINT ( 'NONE',  ( -20.64999999999999858, -8.999999999988844479, -191.6060308773475356 ) ) ;
#20605=EDGE_CURVE ( 'NONE', #128403, #32139, #82457, .T. ) ;
#20607=FACE_OUTER_BOUND ( 'NONE', #146843, .T. ) ;
#20615=CARTESIAN_POINT ( 'NONE',  ( 20.94999999999999929, 8.776282895303632259, -179.6499999999999773 ) ) ;
#20674=CARTESIAN_POINT ( 'NONE',  ( -21.14250536705909411, 1.115652671863510454E-11, -160.9818278231192039 ) ) ;
#20690=CARTESIAN_POINT ( 'NONE',  ( -18.59999999999999787, 6.846123162363745074, -204.7377262668498190 ) ) ;
#20700=( GEOMETRIC_REPRESENTATION_CONTEXT ( 3 ) GLOBAL_UNCERTAINTY_ASSIGNED_CONTEXT ( ( #200530 ) ) GLOBAL_UNIT_ASSIGNED_CONTEXT ( ( #205219, #47431, #106112 ) ) REPRESENTATION_CONTEXT ( 'NONE', 'WORKASPACE' ) );
#20715=VERTEX_POINT ( 'NONE', #202454 ) ;
#20718=DIRECTION ( 'NONE',  ( 0.000000000000000000, 0.000000000000000000, -1.000000000000000000 ) ) ;
#20746=ORIENTED_EDGE ( 'NONE', *, *, #126822, .T. ) ;
#20765=EDGE_LOOP ( 'NONE', ( #98316, #231911, #253830 ) ) ;
#20766=DIRECTION ( 'NONE',  ( 0.000000000000000000, 0.000000000000000000, -1.000000000000000000 ) ) ;
#20767=FACE_OUTER_BOUND ( 'NONE', #4378, .T. ) ;
#20774=VERTEX_POINT ( 'NONE', #191592 ) ;
#20833=ADVANCED_FACE ( 'NONE', ( #214965 ), #178441, .T. ) ;
#20839=VERTEX_POINT ( 'NONE', #100125 ) ;
#20888=CARTESIAN_POINT ( 'NONE',  ( 20.94999999999999929, 1.115600667400684642E-11, -200.9999999999999432 ) ) ;
#20901=VERTEX_POINT ( 'NONE', #160159 ) ;
#20942=DIRECTION ( 'NONE',  ( -1.000000000000000000, 0.000000000000000000, 0.000000000000000000 ) ) ;
#20956=DIRECTION ( 'NONE',  ( -1.000000000000000000, -0.000000000000000000, -0.000000000000000000 ) ) ;
#21025=EDGE_LOOP ( 'NONE', ( #205902, #209442, #88330, #29246 ) ) ;
#21031=ORIENTED_EDGE ( 'NONE', *, *, #25208, .T. ) ;
#21041=SPHERICAL_SURFACE ( 'NONE', #175248, 0.1000000000000000056 ) ;
#21068=VERTEX_POINT ( 'NONE', #16479 ) ;
#21087=ORIENTED_EDGE ( 'NONE', *, *, #15796, .F. ) ;
#21089=CARTESIAN_POINT ( 'NONE',  ( 20.94999999999999929, 1.115600667400684642E-11, -200.9999999999999432 ) ) ;
#21100=DIRECTION ( 'NONE',  ( -1.000000000000000000, 0.000000000000000000, 0.000000000000000000 ) ) ;
#21101=DIRECTION ( 'NONE',  ( 1.000000000000000000, 3.265361837132813093E-16, -0.000000000000000000 ) ) ;
#21117=AXIS2_PLACEMENT_3D ( 'NONE', #122420, #161562, #61154 ) ;
#21143=EDGE_CURVE ( 'NONE', #203019, #242139, #120320, .T. ) ;
#21159=AXIS2_PLACEMENT_3D ( 'NONE', #146468, #8275, #145189 ) ;
#21179=DIRECTION ( 'NONE',  ( -1.000000000000000000, 0.000000000000000000, 0.000000000000000000 ) ) ;
#21202=CARTESIAN_POINT ( 'NONE',  ( -21.05000000000000071, 1.115600667400684642E-11, -167.4999999999999716 ) ) ;
#21211=DIRECTION ( 'NONE',  ( -0.000000000000000000, -0.000000000000000000, 1.000000000000000000 ) ) ;
#21222=DIRECTION ( 'NONE',  ( 0.000000000000000000, 0.000000000000000000, -1.000000000000000000 ) ) ;
#21224=CARTESIAN_POINT ( 'NONE',  ( 18.59999994388910238, -9.363566187059905843, -174.6811172368009863 ) ) ;
#21244=DIRECTION ( 'NONE',  ( -0.000000000000000000, 0.000000000000000000, 1.000000000000000000 ) ) ;
#21253=CARTESIAN_POINT ( 'NONE',  ( 20.94999999999999574, 1.851028230152016674, -179.1539132694224463 ) ) ;
#21283=DIRECTION ( 'NONE',  ( -1.000000000000000000, 0.000000000000000000, 0.000000000000000000 ) ) ;
#21293=EDGE_CURVE ( 'NONE', #175396, #63066, #85375, .T. ) ;
#21299=ORIENTED_EDGE ( 'NONE', *, *, #89789, .F. ) ;
#21333=ORIENTED_EDGE ( 'NONE', *, *, #147446, .T. ) ;
#21352=DIRECTION ( 'NONE',  ( -1.000000000000000000, 0.000000000000000000, 0.000000000000000000 ) ) ;
#21376=CARTESIAN_POINT ( 'NONE',  ( -18.57399277249657032, 10.33112638556969465, -206.5901228926974227 ) ) ;
#21384=DIRECTION ( 'NONE',  ( 1.000000000000000000, 2.952720810173289112E-16, -0.000000000000000000 ) ) ;
#21404=CIRCLE ( 'NONE', #217164, 0.09999999999999892308 ) ;
#21438=LINE ( 'NONE', #22722, #195826 ) ;
#21445=EDGE_CURVE ( 'NONE', #232936, #82222, #136418, .T. ) ;
#21447=DIRECTION ( 'NONE',  ( -1.000000000000000000, -7.304098846218133681E-16, 4.217023435051677994E-16 ) ) ;
#21460=CARTESIAN_POINT ( 'NONE',  ( 21.05543885634738643, 8.775771046858691804, -179.6843844707146616 ) ) ;
#21466=CYLINDRICAL_SURFACE ( 'NONE', #241959, 0.09999999999998898659 ) ;
#21479=AXIS2_PLACEMENT_3D ( 'NONE', #167669, #171529, #91955 ) ;
#21506=ORIENTED_EDGE ( 'NONE', *, *, #187639, .F. ) ;
#21509=ORIENTED_EDGE ( 'NONE', *, *, #166302, .T. ) ;
#21527=CIRCLE ( 'NONE', #42183, 0.2000000000000057288 ) ;
#21561=ORIENTED_EDGE ( 'NONE', *, *, #253632, .F. ) ;
#21579=ORIENTED_EDGE ( 'NONE', *, *, #149518, .F. ) ;
#21585=CARTESIAN_POINT ( 'NONE',  ( 20.94999999999999929, -11.64999999998883595, -200.9999999999999432 ) ) ;
#21637=CARTESIAN_POINT ( 'NONE',  ( 23.25000000000000000, 11.75000000001116263, -188.8499999999999659 ) ) ;
#21640=CARTESIAN_POINT ( 'NONE',  ( 21.05000000000000071, 1.115600667400684642E-11, -167.4999999999999716 ) ) ;
#21666=CARTESIAN_POINT ( 'NONE',  ( -23.15000000000000213, 4.350000000011156054, -188.6499999999999488 ) ) ;
#21672=CARTESIAN_POINT ( 'NONE',  ( -21.14999999999999858, 1.115600667400684642E-11, -167.4999999999999716 ) ) ;
#21697=ORIENTED_EDGE ( 'NONE', *, *, #61779, .F. ) ;
#21713=LINE ( 'NONE', #226297, #30131 ) ;
#21718=CARTESIAN_POINT ( 'NONE',  ( 18.50000000000000000, -9.399999999988843058, -207.8820418481726620 ) ) ;
#21741=EDGE_CURVE ( 'NONE', #138184, #252796, #40811, .T. ) ;
#21748=CARTESIAN_POINT ( 'NONE',  ( -21.05000000000000071, 1.750000000011155743, -179.1695115579016147 ) ) ;
#21788=ORIENTED_EDGE ( 'NONE', *, *, #201465, .F. ) ;
#21796=VERTEX_POINT ( 'NONE', #194509 ) ;
#21863=ADVANCED_FACE ( 'NONE', ( #120123 ), #86720, .F. ) ;
#21904=ORIENTED_EDGE ( 'NONE', *, *, #168872, .F. ) ;
#21917=AXIS2_PLACEMENT_3D ( 'NONE', #33683, #113167, #149754 ) ;
#21919=DIRECTION ( 'NONE',  ( 0.000000000000000000, 0.000000000000000000, 1.000000000000000000 ) ) ;
#21927=AXIS2_PLACEMENT_3D ( 'NONE', #22094, #101577, #121219 ) ;
#21930=AXIS2_PLACEMENT_3D ( 'NONE', #192938, #14323, #95113 ) ;
#21937=AXIS2_PLACEMENT_3D ( 'NONE', #82667, #7017, #224769 ) ;
#21963=ORIENTED_EDGE ( 'NONE', *, *, #225802, .F. ) ;
#21976=DIRECTION ( 'NONE',  ( 1.000000000000000000, 0.000000000000000000, 0.000000000000000000 ) ) ;
#21990=FACE_OUTER_BOUND ( 'NONE', #161629, .T. ) ;
#21997=DIRECTION ( 'NONE',  ( -0.000000000000000000, 1.000000000000000000, -0.000000000000000000 ) ) ;
#22003=CARTESIAN_POINT ( 'NONE',  ( 20.94999999999999929, 1.115600667400684642E-11, -200.9999999999999432 ) ) ;
#22008=CARTESIAN_POINT ( 'NONE',  ( -20.64999999999999858, -8.999999999988846255, -176.8939691226524076 ) ) ;
#22021=ADVANCED_FACE ( 'NONE', ( #250853 ), #232617, .F. ) ;
#22036=FACE_OUTER_BOUND ( 'NONE', #9579, .T. ) ;
#22039=EDGE_LOOP ( 'NONE', ( #232880, #100746, #245149, #227658 ) ) ;
#22049=CARTESIAN_POINT ( 'NONE',  ( -18.59999999999999787, -1.362429037182155023, -208.8888812479211765 ) ) ;
#22094=CARTESIAN_POINT ( 'NONE',  ( 21.05000000000000071, 1.115600667400684642E-11, -200.9999999999999432 ) ) ;
#22123=VECTOR ( 'NONE', #201454, 999.9999999999998863 ) ;
#22129=EDGE_CURVE ( 'NONE', #91307, #242283, #74516, .T. ) ;
#22147=FACE_BOUND ( 'NONE', #232017, .T. ) ;
#22167=CARTESIAN_POINT ( 'NONE',  ( 23.14999999999998437, 1.115600667400684642E-11, -171.5499999999999829 ) ) ;
#22201=CARTESIAN_POINT ( 'NONE',  ( 22.50000000000000000, 1.115600667400684642E-11, -167.4999999999999716 ) ) ;
#22234=ADVANCED_FACE ( 'NONE', ( #121546 ), #135920, .F. ) ;
#22236=CARTESIAN_POINT ( 'NONE',  ( -23.25000000000000000, -11.74999999998884448, -170.5999999999999659 ) ) ;
#22246=DIRECTION ( 'NONE',  ( -1.000000000000000000, -0.000000000000000000, -0.000000000000000000 ) ) ;
#22257=CYLINDRICAL_SURFACE ( 'NONE', #228994, 0.09999999999999939493 ) ;
#22290=ORIENTED_EDGE ( 'NONE', *, *, #113794, .T. ) ;
#22304=EDGE_CURVE ( 'NONE', #72109, #12777, #207759, .T. ) ;
#22393=DIRECTION ( 'NONE',  ( 1.000000000000000000, 0.000000000000000000, 0.000000000000000000 ) ) ;
#22400=DIRECTION ( 'NONE',  ( 0.000000000000000000, -0.4930308989874729320, -0.8700118002898605818 ) ) ;
#22435=CARTESIAN_POINT ( 'NONE',  ( -20.64999999999999858, -9.399999999988850163, -177.3939691226524076 ) ) ;
#22443=CYLINDRICAL_SURFACE ( 'NONE', #85630, 0.09999999999999817368 ) ;
#22459=ORIENTED_EDGE ( 'NONE', *, *, #59141, .T. ) ;
#22521=CARTESIAN_POINT ( 'NONE',  ( -21.05000000000000071, 1.115600667400684642E-11, -200.9999999999999432 ) ) ;
#22523=ORIENTED_EDGE ( 'NONE', *, *, #12353, .T. ) ;
#22535=ORIENTED_EDGE ( 'NONE', *, *, #171744, .T. ) ;
#22536=CIRCLE ( 'NONE', #97499, 0.09999999999998898659 ) ;
#22563=ORIENTED_EDGE ( 'NONE', *, *, #212869, .T. ) ;
#22572=CIRCLE ( 'NONE', #110039, 4.049999999999998046 ) ;
#22593=EDGE_CURVE ( 'NONE', #145347, #185004, #195477, .T. ) ;
#22594=VERTEX_POINT ( 'NONE', #236011 ) ;
#22646=EDGE_LOOP ( 'NONE', ( #11247, #94298, #179848, #144607 ) ) ;
#22658=VECTOR ( 'NONE', #205432, 1000.000000000000000 ) ;
#22668=VERTEX_POINT ( 'NONE', #42959 ) ;
#22685=EDGE_CURVE ( 'NONE', #214983, #182339, #104190, .T. ) ;
#22706=DIRECTION ( 'NONE',  ( 0.000000000000000000, 0.000000000000000000, 1.000000000000000000 ) ) ;
#22708=DIRECTION ( 'NONE',  ( 2.952720810173289112E-16, -1.000000000000000000, 0.000000000000000000 ) ) ;
#22709=CARTESIAN_POINT ( 'NONE',  ( 18.50000000000000000, -9.499999999988842703, -174.5320693966996259 ) ) ;
#22715=DIRECTION ( 'NONE',  ( 1.000000000000000000, 0.000000000000000000, 0.000000000000000000 ) ) ;
#22716=VERTEX_POINT ( 'NONE', #251422 ) ;
#22722=CARTESIAN_POINT ( 'NONE',  ( -23.25000000000000000, -0.1008583690875562017, -155.7504328765105868 ) ) ;
#22747=CARTESIAN_POINT ( 'NONE',  ( 21.08832698747859169, 8.775364393428372267, -179.7287174664641327 ) ) ;
#22757=ORIENTED_EDGE ( 'NONE', *, *, #173304, .T. ) ;
#22779=CARTESIAN_POINT ( 'NONE',  ( 20.95132126680579887, 10.48994987015794322, -175.0703245384344768 ) ) ;
#22820=CARTESIAN_POINT ( 'NONE',  ( -22.50000000000000000, 11.75000000001115552, -167.4999999999999716 ) ) ;
#22852=DIRECTION ( 'NONE',  ( 0.000000000000000000, -0.000000000000000000, -1.000000000000000000 ) ) ;
#22881=DIRECTION ( 'NONE',  ( 0.000000000000000000, 0.000000000000000000, -1.000000000000000000 ) ) ;
#22903=ORIENTED_EDGE ( 'NONE', *, *, #192163, .F. ) ;
#22907=EDGE_CURVE ( 'NONE', #493, #135423, #59608, .T. ) ;
#22913=ORIENTED_EDGE ( 'NONE', *, *, #126748, .T. ) ;
#22923=DIRECTION ( 'NONE',  ( 0.000000000000000000, 0.000000000000000000, -1.000000000000000000 ) ) ;
#22932=AXIS2_PLACEMENT_3D ( 'NONE', #52616, #211720, #132162 ) ;
#22943=DIRECTION ( 'NONE',  ( 1.000000000000000000, 0.000000000000000000, 0.000000000000000000 ) ) ;
#22946=EDGE_CURVE ( 'NONE', #239004, #77358, #15398, .T. ) ;
#22972=DIRECTION ( 'NONE',  ( 0.000000000000000000, -0.9654727137038715545, 0.2605042016806676242 ) ) ;
#22985=VERTEX_POINT ( 'NONE', #216135 ) ;
#22986=CARTESIAN_POINT ( 'NONE',  ( 21.14999999999999858, 6.650000000011155876, -179.6499999999999773 ) ) ;
#23011=CIRCLE ( 'NONE', #64845, 0.09999999999999939493 ) ;
#23016=CARTESIAN_POINT ( 'NONE',  ( -21.14999999999999858, 1.115600667400684642E-11, -160.9593430482987344 ) ) ;
#23065=DIRECTION ( 'NONE',  ( -0.8660254037843277963, 0.000000000000000000, -0.5000000000001921796 ) ) ;
#23073=AXIS2_PLACEMENT_3D ( 'NONE', #245853, #183313, #67211 ) ;
#23103=CARTESIAN_POINT ( 'NONE',  ( -20.94999999999999929, 1.835341550235569663, -179.0551512925629538 ) ) ;
#23134=CARTESIAN_POINT ( 'NONE',  ( 21.05000000000000071, 5.500000000011153745, -188.5947339810868755 ) ) ;
#23190=ORIENTED_EDGE ( 'NONE', *, *, #53760, .F. ) ;
#23197=VERTEX_POINT ( 'NONE', #167752 ) ;
#23223=DIRECTION ( 'NONE',  ( 1.000000000000000000, -0.000000000000000000, -0.000000000000000000 ) ) ;
#23242=DIRECTION ( 'NONE',  ( 0.000000000000000000, -0.9908441862701782288, -0.1350103645450539402 ) ) ;
#23266=SPHERICAL_SURFACE ( 'NONE', #136958, 0.1000000000000000056 ) ;
#23284=FACE_OUTER_BOUND ( 'NONE', #17533, .T. ) ;
#23318=B_SPLINE_CURVE_WITH_KNOTS ( 'NONE', 3,
 ( #222048, #42178, #44741, #139956, #43449, #219500 ),
 .UNSPECIFIED., .F., .F.,
 ( 4, 2, 4 ),
 ( 0.000000000000000000, 0.0001568709654583421050, 0.0003137419309166842099 ),
 .UNSPECIFIED. ) ;
#23320=ORIENTED_EDGE ( 'NONE', *, *, #152203, .T. ) ;
#23339=CARTESIAN_POINT ( 'NONE',  ( -21.04999999999998295, 6.344723404101382691, -167.4852821434760131 ) ) ;
#23346=DIRECTION ( 'NONE',  ( 0.000000000000000000, 0.000000000000000000, -1.000000000000000000 ) ) ;
#23359=AXIS2_PLACEMENT_3D ( 'NONE', #224471, #246606, #67975 ) ;
#23389=DIRECTION ( 'NONE',  ( 0.000000000000000000, 1.000000000000000000, 0.000000000000000000 ) ) ;
#23402=ORIENTED_EDGE ( 'NONE', *, *, #48133, .T. ) ;
#23414=ORIENTED_EDGE ( 'NONE', *, *, #113626, .T. ) ;
#23420=CARTESIAN_POINT ( 'NONE',  ( -21.05000000000000071, -11.64999999998884306, -198.0999999999999659 ) ) ;
#23440=CARTESIAN_POINT ( 'NONE',  ( -18.50000000000000000, -1.162701749926853712, -175.5999999999999659 ) ) ;
#23471=DIRECTION ( 'NONE',  ( -0.7071067811865475727, -0.7071067811865475727, 0.000000000000000000 ) ) ;
#23565=CARTESIAN_POINT ( 'NONE',  ( 18.59999999999998721, 6.933893972137497030, -204.7856458343735255 ) ) ;
#23574=EDGE_LOOP ( 'NONE', ( #57058, #59760, #110394 ) ) ;
#23603=ORIENTED_EDGE ( 'NONE', *, *, #112417, .T. ) ;
#23614=ADVANCED_FACE ( 'NONE', ( #157852 ), #195679, .T. ) ;
#23636=LINE ( 'NONE', #199697, #209910 ) ;
#23637=CIRCLE ( 'NONE', #135997, 0.09999999999999939493 ) ;
#23664=CARTESIAN_POINT ( 'NONE',  ( -2.995603634470891112E-16, -11.74999999998884448, -179.7499999999999716 ) ) ;
#23676=DIRECTION ( 'NONE',  ( 0.000000000000000000, 0.000000000000000000, -1.000000000000000000 ) ) ;
#23677=CARTESIAN_POINT ( 'NONE',  ( 18.44444291854882678, -9.490101180932073888, -207.6289039648910091 ) ) ;
#23689=ADVANCED_FACE ( 'NONE', ( #255569 ), #108510, .T. ) ;
#23690=ORIENTED_EDGE ( 'NONE', *, *, #60606, .F. ) ;
#23724=SPHERICAL_SURFACE ( 'NONE', #196498, 0.1000000000000000056 ) ;
#23736=DIRECTION ( 'NONE',  ( 0.000000000000000000, 0.9908441862701782288, 0.1350103645450542456 ) ) ;
#23741=CARTESIAN_POINT ( 'NONE',  ( 21.05000000000000071, 11.75000000001116263, -193.9851942293460070 ) ) ;
#23765=FACE_OUTER_BOUND ( 'NONE', #144898, .T. ) ;
#23779=EDGE_CURVE ( 'NONE', #200909, #62075, #241785, .T. ) ;
#23804=ORIENTED_EDGE ( 'NONE', *, *, #187803, .F. ) ;
#23824=ORIENTED_EDGE ( 'NONE', *, *, #174058, .T. ) ;
#23836=ORIENTED_EDGE ( 'NONE', *, *, #64973, .T. ) ;
#23847=AXIS2_PLACEMENT_3D ( 'NONE', #220195, #237192, #16871 ) ;
#23864=VERTEX_POINT ( 'NONE', #154272 ) ;
#23911=ORIENTED_EDGE ( 'NONE', *, *, #144941, .F. ) ;
#24000=CARTESIAN_POINT ( 'NONE',  ( 18.59999999999999076, 1.835341550235567887, -179.0551512925629538 ) ) ;
#24034=CARTESIAN_POINT ( 'NONE',  ( 23.14999999999999503, 6.650000000011155876, -188.6499999999999488 ) ) ;
#24044=CARTESIAN_POINT ( 'NONE',  ( 18.59999999999999432, -1.162701749926853712, -175.5999999999999659 ) ) ;
#24082=ORIENTED_EDGE ( 'NONE', *, *, #122929, .T. ) ;
#24105=DIRECTION ( 'NONE',  ( 0.000000000000000000, 1.000000000000000000, -6.308085367188393199E-16 ) ) ;
#24125=ORIENTED_EDGE ( 'NONE', *, *, #78888, .F. ) ;
#24171=DIRECTION ( 'NONE',  ( -0.000000000000000000, 1.000000000000000000, -0.000000000000000000 ) ) ;
#24181=ORIENTED_EDGE ( 'NONE', *, *, #70841, .T. ) ;
#24203=AXIS2_PLACEMENT_3D ( 'NONE', #64219, #246698, #225826 ) ;
#24258=AXIS2_PLACEMENT_3D ( 'NONE', #257683, #240762, #141646 ) ;
#24292=DIRECTION ( 'NONE',  ( -0.7071067811865389130, 8.659560562355038861E-17, -0.7071067811865561215 ) ) ;
#24306=CARTESIAN_POINT ( 'NONE',  ( -23.25000000000000000, 11.75000000001115552, -167.4999999999999716 ) ) ;
#24317=CARTESIAN_POINT ( 'NONE',  ( 23.14999999999999503, 6.650000000011155876, -188.7499999999999716 ) ) ;
#24329=CARTESIAN_POINT ( 'NONE',  ( 18.50000000000281730, 10.44006789215406705, -192.2671177488813896 ) ) ;
#24338=LINE ( 'NONE', #85532, #110035 ) ;
#24361=CARTESIAN_POINT ( 'NONE',  ( -20.64999999999999858, 1.115600667400684642E-11, -167.4999999999999716 ) ) ;
#24363=CARTESIAN_POINT ( 'NONE',  ( 23.24999999999999289, 6.550000000011156231, -188.8499999999999659 ) ) ;
#24364=ADVANCED_FACE ( 'NONE', ( #105543 ), #224237, .F. ) ;
#24379=EDGE_CURVE ( 'NONE', #103201, #218583, #154520, .T. ) ;
#24385=EDGE_CURVE ( 'NONE', #167246, #236853, #204666, .T. ) ;
#24410=EDGE_CURVE ( 'NONE', #76299, #171611, #112982, .T. ) ;
#24439=ORIENTED_EDGE ( 'NONE', *, *, #227057, .F. ) ;
#24460=ORIENTED_EDGE ( 'NONE', *, *, #101457, .T. ) ;
#24524=ORIENTED_EDGE ( 'NONE', *, *, #108814, .T. ) ;
#24534=CARTESIAN_POINT ( 'NONE',  ( -21.05000000000000071, -0.09999999998884338825, -155.8499999999999659 ) ) ;
#24539=ORIENTED_EDGE ( 'NONE', *, *, #168346, .T. ) ;
#24564=CARTESIAN_POINT ( 'NONE',  ( 23.24999999999999289, 11.65000000001116298, -167.4999999999999716 ) ) ;
#24571=CARTESIAN_POINT ( 'NONE',  ( -20.85000000000000142, -1.135018845899022466, -208.7169768834322952 ) ) ;
#24586=CARTESIAN_POINT ( 'NONE',  ( 21.14999999999999858, 1.115600667400684642E-11, -179.6499999999999773 ) ) ;
#24620=CARTESIAN_POINT ( 'NONE',  ( -22.39999999999999503, 1.115541036281197940E-11, -159.7092204016265384 ) ) ;
#24653=DIRECTION ( 'NONE',  ( -3.265361837132813093E-16, 1.000000000000000000, 0.000000000000000000 ) ) ;
#24656=DIRECTION ( 'NONE',  ( 1.000000000000000000, 0.000000000000000000, 0.000000000000000000 ) ) ;
#24679=DIRECTION ( 'NONE',  ( 0.000000000000000000, 0.000000000000000000, -1.000000000000000000 ) ) ;
#24710=VECTOR ( 'NONE', #132311, 1000.000000000000000 ) ;
#24730=TOROIDAL_SURFACE ( 'NONE', #141395, 1.900000000000002576, 0.1000000000000000056 ) ;
#24751=DIRECTION ( 'NONE',  ( -1.000000000000000000, 0.000000000000000000, 0.000000000000000000 ) ) ;
#24759=DIRECTION ( 'NONE',  ( 0.000000000000000000, 0.000000000000000000, -1.000000000000000000 ) ) ;
#24785=AXIS2_PLACEMENT_3D ( 'NONE', #170909, #206132, #91324 ) ;
#24792=ORIENTED_EDGE ( 'NONE', *, *, #180367, .T. ) ;
#24796=CARTESIAN_POINT ( 'NONE',  ( -22.39999999999999858, 1.115600667400684642E-11, -161.2499999999999716 ) ) ;
#24832=AXIS2_PLACEMENT_3D ( 'NONE', #58885, #21101, #138420 ) ;
#24839=CARTESIAN_POINT ( 'NONE',  ( -21.05000000000000071, 5.900000000011102586, -177.7190997646563915 ) ) ;
#24850=ADVANCED_FACE ( 'NONE', ( #41473 ), #200520, .T. ) ;
#24870=EDGE_LOOP ( 'NONE', ( #218649, #218131, #124842, #171679 ) ) ;
#24886=CARTESIAN_POINT ( 'NONE',  ( -18.59999999999999787, 14.05000000001115623, -173.0136950707609458 ) ) ;
#24912=CIRCLE ( 'NONE', #258067, 0.09999999999999939493 ) ;
#24926=LINE ( 'NONE', #62750, #218143 ) ;
#24944=DIRECTION ( 'NONE',  ( 1.000000000000000000, 2.952720810173289112E-16, -0.000000000000000000 ) ) ;
#25013=DIRECTION ( 'NONE',  ( -0.000000000000000000, -0.000000000000000000, 1.000000000000000000 ) ) ;
#25024=DIRECTION ( 'NONE',  ( 0.000000000000000000, 0.000000000000000000, -1.000000000000000000 ) ) ;
#25033=ADVANCED_FACE ( 'NONE', ( #34744 ), #174280, .F. ) ;
#25038=FACE_OUTER_BOUND ( 'NONE', #219925, .T. ) ;
#25047=CARTESIAN_POINT ( 'NONE',  ( 23.25000000000000000, -11.64999999998883595, -155.7499999999999716 ) ) ;
#25094=EDGE_CURVE ( 'NONE', #76299, #42612, #39877, .T. ) ;
#25135=CARTESIAN_POINT ( 'NONE',  ( 22.39999999999999503, 7.790779598384535376, -167.4999999999999716 ) ) ;
#25176=LINE ( 'NONE', #100789, #40808 ) ;
#25196=CARTESIAN_POINT ( 'NONE',  ( 21.05000000000000071, 5.850000000011156942, -190.8675027757220448 ) ) ;
#25208=EDGE_CURVE ( 'NONE', #231547, #143070, #64544, .T. ) ;
#25210=AXIS2_PLACEMENT_3D ( 'NONE', #88976, #250624, #205070 ) ;
#25216=CARTESIAN_POINT ( 'NONE',  ( 21.05000000000000071, 1.115600667400684642E-11, -200.9999999999999432 ) ) ;
#25311=CARTESIAN_POINT ( 'NONE',  ( 21.12802099929860589, 8.780552590233368093, -179.7481899849315994 ) ) ;
#25324=CARTESIAN_POINT ( 'NONE',  ( 21.07888907270776002, 10.72506921352637654, -179.7211935868331807 ) ) ;
#25344=DIRECTION ( 'NONE',  ( 0.000000000000000000, 1.000000000000000000, 0.000000000000000000 ) ) ;
#25350=DIRECTION ( 'NONE',  ( 6.938893903907991995E-14, 0.000000000000000000, 1.000000000000000000 ) ) ;
#25385=DIRECTION ( 'NONE',  ( 0.000000000000000000, -0.9908441862701782288, -0.1350103645450542456 ) ) ;
#25387=ORIENTED_EDGE ( 'NONE', *, *, #42030, .F. ) ;
#25394=FACE_OUTER_BOUND ( 'NONE', #28441, .T. ) ;
#25429=VERTEX_POINT ( 'NONE', #244721 ) ;
#25430=VECTOR ( 'NONE', #27265, 1000.000000000000000 ) ;
#25436=DIRECTION ( 'NONE',  ( 1.000000000000000000, -0.000000000000000000, -0.000000000000000000 ) ) ;
#25444=CARTESIAN_POINT ( 'NONE',  ( 21.07928932188134397, 6.328516656404459262, -167.4011048543455615 ) ) ;
#25492=CARTESIAN_POINT ( 'NONE',  ( 21.00000000000000000, 9.750000000011153745, -188.7499999999999716 ) ) ;
#25499=VECTOR ( 'NONE', #111562, 1000.000000000000000 ) ;
#25509=EDGE_CURVE ( 'NONE', #183971, #177551, #227735, .T. ) ;
#25511=CARTESIAN_POINT ( 'NONE',  ( 20.94999999999999929, -9.399999999988844834, -191.1060308773475072 ) ) ;
#25550=DIRECTION ( 'NONE',  ( -4.336808689942053235E-15, -0.8660254037844482555, -0.4999999999999836797 ) ) ;
#25551=CIRCLE ( 'NONE', #221325, 0.1999999999999987899 ) ;
#25568=DIRECTION ( 'NONE',  ( 7.304098846218134667E-16, -1.000000000000000000, 0.000000000000000000 ) ) ;
#25579=DIRECTION ( 'NONE',  ( 1.000000000000000000, -0.000000000000000000, -0.000000000000000000 ) ) ;
#25588=DIRECTION ( 'NONE',  ( 0.000000000000000000, -0.1350103645451904977, -0.9908441862701596881 ) ) ;
#25602=CARTESIAN_POINT ( 'NONE',  ( 18.49999999999996447, 10.49142135624846439, -192.2499999999999716 ) ) ;
#25629=FACE_OUTER_BOUND ( 'NONE', #139328, .T. ) ;
#25636=AXIS2_PLACEMENT_3D ( 'NONE', #100595, #221837, #257089 ) ;
#25661=FACE_OUTER_BOUND ( 'NONE', #137684, .T. ) ;
#25683=CARTESIAN_POINT ( 'NONE',  ( 23.14999999999999503, 11.75000000001115552, -188.7499999999999716 ) ) ;
#25705=CARTESIAN_POINT ( 'NONE',  ( 18.60000000000000497, 1.115600667400684642E-11, -167.4999999999999716 ) ) ;
#25732=ORIENTED_EDGE ( 'NONE', *, *, #72592, .F. ) ;
#25771=ORIENTED_EDGE ( 'NONE', *, *, #122440, .F. ) ;
#25782=AXIS2_PLACEMENT_3D ( 'NONE', #71193, #192408, #251078 ) ;
#25813=AXIS2_PLACEMENT_3D ( 'NONE', #167085, #83617, #245312 ) ;
#25827=DIRECTION ( 'NONE',  ( 0.000000000000000000, 0.000000000000000000, -1.000000000000000000 ) ) ;
#25839=FACE_OUTER_BOUND ( 'NONE', #143418, .T. ) ;
#25842=CIRCLE ( 'NONE', #63225, 0.1000000000000089567 ) ;
#25857=AXIS2_PLACEMENT_3D ( 'NONE', #124711, #162569, #204233 ) ;
#25873=CARTESIAN_POINT ( 'NONE',  ( 18.44206774312977259, -9.491027357528896147, -207.6262275046982211 ) ) ;
#25885=DIRECTION ( 'NONE',  ( 1.000000000000000000, 0.000000000000000000, 0.000000000000000000 ) ) ;
#25891=CARTESIAN_POINT ( 'NONE',  ( -21.11825140030082792, 6.445407565431271024, -167.4927963793673200 ) ) ;
#25915=EDGE_CURVE ( 'NONE', #22985, #180615, #113691, .T. ) ;
#25941=ORIENTED_EDGE ( 'NONE', *, *, #107506, .F. ) ;
#25944=DIRECTION ( 'NONE',  ( 0.000000000000000000, 0.000000000000000000, -1.000000000000000000 ) ) ;
#25949=CARTESIAN_POINT ( 'NONE',  ( -21.37071067811865532, 8.070710678129811910, -179.7499999999999716 ) ) ;
#25965=DIRECTION ( 'NONE',  ( 1.000000000000000000, 0.000000000000000000, 0.000000000000000000 ) ) ;
#25972=DIRECTION ( 'NONE',  ( 0.000000000000000000, 0.000000000000000000, -1.000000000000000000 ) ) ;
#26007=AXIS2_PLACEMENT_3D ( 'NONE', #56181, #236118, #60037 ) ;
#26010=DIRECTION ( 'NONE',  ( 0.000000000000000000, 0.000000000000000000, -1.000000000000000000 ) ) ;
#26018=EDGE_LOOP ( 'NONE', ( #163896, #203149, #73598, #62250 ) ) ;
#26028=VECTOR ( 'NONE', #85485, 1000.000000000000000 ) ;
#26037=AXIS2_PLACEMENT_3D ( 'NONE', #171267, #89102, #90380 ) ;
#26060=ORIENTED_EDGE ( 'NONE', *, *, #158614, .F. ) ;
#26084=DIRECTION ( 'NONE',  ( -0.000000000000000000, -0.000000000000000000, -1.000000000000000000 ) ) ;
#26099=AXIS2_PLACEMENT_3D ( 'NONE', #188539, #172880, #249801 ) ;
#26136=CARTESIAN_POINT ( 'NONE',  ( -21.13422380239137510, 1.115580863182033025E-11, -161.0066734851942556 ) ) ;
#26142=EDGE_CURVE ( 'NONE', #103174, #254691, #147200, .T. ) ;
#26144=ORIENTED_EDGE ( 'NONE', *, *, #136555, .F. ) ;
#26171=ORIENTED_EDGE ( 'NONE', *, *, #210310, .F. ) ;
#26178=FACE_OUTER_BOUND ( 'NONE', #78469, .T. ) ;
#26222=VECTOR ( 'NONE', #53503, 1000.000000000000000 ) ;
#26224=CARTESIAN_POINT ( 'NONE',  ( -21.00250684356849362, 11.75000000001115197, -174.5148057687579808 ) ) ;
#26240=AXIS2_PLACEMENT_3D ( 'NONE', #129020, #88577, #188986 ) ;
#26241=ORIENTED_EDGE ( 'NONE', *, *, #142104, .T. ) ;
#26246=CYLINDRICAL_SURFACE ( 'NONE', #148675, 0.09999999999998898659 ) ;
#26277=DIRECTION ( 'NONE',  ( -0.000000000000000000, 1.000000000000000000, -0.000000000000000000 ) ) ;
#26280=CYLINDRICAL_SURFACE ( 'NONE', #228068, 0.09999999999999939493 ) ;
#26353=EDGE_CURVE ( 'NONE', #6520, #236406, #196549, .T. ) ;
#26369=CARTESIAN_POINT ( 'NONE',  ( -21.05000000000000071, 6.540656951712397138, -167.5999999999999659 ) ) ;
#26379=AXIS2_PLACEMENT_3D ( 'NONE', #90528, #249631, #170128 ) ;
#26380=AXIS2_PLACEMENT_3D ( 'NONE', #221401, #187139, #147993 ) ;
#26381=AXIS2_PLACEMENT_3D ( 'NONE', #64936, #6239, #25827 ) ;
#26391=CYLINDRICAL_SURFACE ( 'NONE', #24203, 12.87499999999999822 ) ;
#26394=EDGE_CURVE ( 'NONE', #52759, #218080, #13929, .T. ) ;
#26404=AXIS2_PLACEMENT_3D ( 'NONE', #167111, #129238, #33705 ) ;
#26410=ADVANCED_FACE ( 'NONE', ( #122163 ), #8633, .T. ) ;
#26424=DIRECTION ( 'NONE',  ( 0.000000000000000000, 0.000000000000000000, -1.000000000000000000 ) ) ;
#26455=EDGE_CURVE ( 'NONE', #130308, #251611, #134874, .T. ) ;
#26461=EDGE_CURVE ( 'NONE', #178866, #250208, #226456, .T. ) ;
#26504=DIRECTION ( 'NONE',  ( 0.000000000000000000, 0.000000000000000000, -1.000000000000000000 ) ) ;
#26521=CIRCLE ( 'NONE', #238894, 0.09999999999999939493 ) ;
#26529=LINE ( 'NONE', #222112, #230884 ) ;
#26556=CARTESIAN_POINT ( 'NONE',  ( 20.85000000000000142, 11.65000000001115943, -200.9999999999999432 ) ) ;
#26557=VERTEX_POINT ( 'NONE', #157145 ) ;
#26563=DIRECTION ( 'NONE',  ( 0.7071067811865475727, 0.7071067811865475727, 0.000000000000000000 ) ) ;
#26566=CARTESIAN_POINT ( 'NONE',  ( 18.59999999999999076, 14.05000000001116689, -173.0136950707609458 ) ) ;
#26621=VECTOR ( 'NONE', #22881, 1000.000000000000000 ) ;
#26628=CARTESIAN_POINT ( 'NONE',  ( 18.60000000000000497, -9.364236010355609707, -174.6802544007245501 ) ) ;
#26674=AXIS2_PLACEMENT_3D ( 'NONE', #146924, #167825, #184779 ) ;
#26685=DIRECTION ( 'NONE',  ( 0.000000000000000000, 0.000000000000000000, -1.000000000000000000 ) ) ;
#26722=DIRECTION ( 'NONE',  ( 2.952720810173289112E-16, -1.000000000000000000, 0.000000000000000000 ) ) ;
#26762=VERTEX_POINT ( 'NONE', #226046 ) ;
#26778=CYLINDRICAL_SURFACE ( 'NONE', #31160, 0.09999999999999892308 ) ;
#26812=DIRECTION ( 'NONE',  ( 1.000000000000000000, -0.000000000000000000, -0.000000000000000000 ) ) ;
#26826=ADVANCED_FACE ( 'NONE', ( #87832 ), #150424, .T. ) ;
#26873=CARTESIAN_POINT ( 'NONE',  ( 21.05000000000000071, 11.75000000001116263, -193.9851942293460070 ) ) ;
#26890=DIRECTION ( 'NONE',  ( 0.000000000000000000, 1.000000000000000000, 0.000000000000000000 ) ) ;
#26907=EDGE_CURVE ( 'NONE', #237038, #123700, #251617, .T. ) ;
#26914=DIRECTION ( 'NONE',  ( 0.000000000000000000, 0.000000000000000000, -1.000000000000000000 ) ) ;
#26955=AXIS2_PLACEMENT_3D ( 'NONE', #187925, #151377, #8007 ) ;
#27012=EDGE_CURVE ( 'NONE', #42929, #246745, #189271, .T. ) ;
#27016=EDGE_CURVE ( 'NONE', #196712, #215838, #86986, .T. ) ;
#27029=ORIENTED_EDGE ( 'NONE', *, *, #20288, .T. ) ;
#27099=DIRECTION ( 'NONE',  ( -1.000000000000000000, -0.000000000000000000, -0.000000000000000000 ) ) ;
#27100=EDGE_LOOP ( 'NONE', ( #96839, #248408, #162742 ) ) ;
#27122=ORIENTED_EDGE ( 'NONE', *, *, #43279, .T. ) ;
#27134=ORIENTED_EDGE ( 'NONE', *, *, #12353, .F. ) ;
#27168=VERTEX_POINT ( 'NONE', #199821 ) ;
#27170=ORIENTED_EDGE ( 'NONE', *, *, #171744, .F. ) ;
#27171=ADVANCED_FACE ( 'NONE', ( #81114 ), #163254, .T. ) ;
#27179=CARTESIAN_POINT ( 'NONE',  ( 18.37172112093692888, -9.570961652232536920, -207.8167344534829510 ) ) ;
#27195=CARTESIAN_POINT ( 'NONE',  ( -21.05000000000000071, 6.300179817925902981, -167.4485171181181897 ) ) ;
#27219=DIRECTION ( 'NONE',  ( -1.000000000000000000, -3.265361837132813093E-16, 0.000000000000000000 ) ) ;
#27247=AXIS2_PLACEMENT_3D ( 'NONE', #216298, #135471, #78071 ) ;
#27256=EDGE_CURVE ( 'NONE', #204622, #52856, #1975, .T. ) ;
#27265=DIRECTION ( 'NONE',  ( -1.000000000000000000, 0.000000000000000000, 0.000000000000000000 ) ) ;
#27293=CARTESIAN_POINT ( 'NONE',  ( -20.94999999999999929, -0.2561057920810652089, -167.4651035583276553 ) ) ;
#27300=CARTESIAN_POINT ( 'NONE',  ( -23.15000000000000213, 11.75000000001115552, -197.8999999999999773 ) ) ;
#27306=B_SPLINE_CURVE_WITH_KNOTS ( 'NONE', 3,
 ( #149105, #164802, #65689, #146493, #46121, #125662, #106073, #185647, #47397, #166120, #126954, #107378, #8308, #167391, #254573, #112539, #173839, #70866, #253311 ),
 .UNSPECIFIED., .F., .F.,
 ( 4, 3, 3, 3, 3, 3, 4 ),
 ( 0.000000000000000000, 7.110282409890013474E-05, 0.0001508797727291402539, 0.0002027344179858551164, 0.0002343294522349084557, 0.0002454816334821245888, 0.0002619873080085767438 ),
 .UNSPECIFIED. ) ;
#27347=EDGE_CURVE ( 'NONE', #118647, #36019, #31264, .T. ) ;
#27364=CARTESIAN_POINT ( 'NONE',  ( 21.05000000000000071, 10.72371711693665652, -179.6762396011382066 ) ) ;
#27379=ORIENTED_EDGE ( 'NONE', *, *, #47782, .F. ) ;
#27415=DIRECTION ( 'NONE',  ( 0.000000000000000000, 0.000000000000000000, 1.000000000000000000 ) ) ;
#27426=DIRECTION ( 'NONE',  ( 0.000000000000000000, 0.000000000000000000, 1.000000000000000000 ) ) ;
#27459=AXIS2_PLACEMENT_3D ( 'NONE', #108380, #72806, #245325 ) ;
#27476=CARTESIAN_POINT ( 'NONE',  ( -21.05000000000000071, 1.115600667400684642E-11, -189.1999999999999602 ) ) ;
#27478=ADVANCED_FACE ( 'NONE', ( #191167 ), #170346, .T. ) ;
#27481=VERTEX_POINT ( 'NONE', #231562 ) ;
#27521=ORIENTED_EDGE ( 'NONE', *, *, #191749, .F. ) ;
#27528=DIRECTION ( 'NONE',  ( -1.000000000000000000, -2.952720810173289112E-16, 0.000000000000000000 ) ) ;
#27535=DIRECTION ( 'NONE',  ( -0.000000000000000000, -0.000000000000000000, 1.000000000000000000 ) ) ;
#27554=CARTESIAN_POINT ( 'NONE',  ( -20.64999999999999858, -8.663551401858001100, -191.4758988819326646 ) ) ;
#27613=VERTEX_POINT ( 'NONE', #137568 ) ;
#27631=ORIENTED_EDGE ( 'NONE', *, *, #126451, .F. ) ;
#27665=CARTESIAN_POINT ( 'NONE',  ( -20.64999999999999858, 7.250000000011155521, -179.8499999999999943 ) ) ;
#27678=DIRECTION ( 'NONE',  ( 1.836970198721029934E-16, -1.000000000000000000, -0.000000000000000000 ) ) ;
#27683=LINE ( 'NONE', #169760, #185902 ) ;
#27700=CARTESIAN_POINT ( 'NONE',  ( 22.39999999999999858, 7.790779598384538929, -167.3999999999999773 ) ) ;
#27721=CARTESIAN_POINT ( 'NONE',  ( 21.14999999999999858, 6.550000000011156231, -179.8499999999999943 ) ) ;
#27738=EDGE_LOOP ( 'NONE', ( #198966, #54479, #162243, #203953, #41886, #92477, #143610, #111856, #252632, #23414, #107548, #161082 ) ) ;
#27740=CARTESIAN_POINT ( 'NONE',  ( -21.05000000000000071, -1.261786168553869603, -175.5864989635454378 ) ) ;
#27780=CARTESIAN_POINT ( 'NONE',  ( -20.64999999999999858, 1.115600667400684642E-11, -167.4999999999999716 ) ) ;
#27826=CARTESIAN_POINT ( 'NONE',  ( 18.59999999999999787, -1.736705739456431807, -212.5174225876236846 ) ) ;
#27848=ORIENTED_EDGE ( 'NONE', *, *, #148829, .F. ) ;
#27862=CARTESIAN_POINT ( 'NONE',  ( 21.05000000000000071, -11.48912529306489994, -197.8999999999999773 ) ) ;
#27878=CARTESIAN_POINT ( 'NONE',  ( 22.50000000000000000, 0.1000000000111554016, -155.7499999999999716 ) ) ;
#27889=AXIS2_PLACEMENT_3D ( 'NONE', #248133, #106029, #185593 ) ;
#27913=CARTESIAN_POINT ( 'NONE',  ( -20.94999999999999929, 1.115600667400684642E-11, -189.1999999999999602 ) ) ;
#27963=AXIS2_PLACEMENT_3D ( 'NONE', #246457, #67816, #187785 ) ;
#27974=ORIENTED_EDGE ( 'NONE', *, *, #91537, .T. ) ;
#27976=ADVANCED_FACE ( 'NONE', ( #93024 ), #134702, .F. ) ;
#27994=ORIENTED_EDGE ( 'NONE', *, *, #80269, .F. ) ;
#28063=EDGE_CURVE ( 'NONE', #171236, #232431, #81440, .T. ) ;
#28120=CARTESIAN_POINT ( 'NONE',  ( 21.05000000000000071, 8.776282889879928106, -179.6762151410682975 ) ) ;
#28176=DIRECTION ( 'NONE',  ( -4.701977403289178058E-30, 1.734723475976807094E-14, -1.000000000000000000 ) ) ;
#28186=CARTESIAN_POINT ( 'NONE',  ( -20.94999675878240808, 10.29307482169071264, -206.4586421466939896 ) ) ;
#28196=AXIS2_PLACEMENT_3D ( 'NONE', #171279, #132103, #209069 ) ;
#28212=CARTESIAN_POINT ( 'NONE',  ( -20.94999999999999929, -11.48912529306489994, -197.9999999999999432 ) ) ;
#28233=ADVANCED_FACE ( 'NONE', ( #144971 ), #92106, .T. ) ;
#28243=CARTESIAN_POINT ( 'NONE',  ( -20.85000000000000142, 11.75000000001115197, -194.2161343370218560 ) ) ;
#28247=ORIENTED_EDGE ( 'NONE', *, *, #155904, .F. ) ;
#28258=ADVANCED_FACE ( 'NONE', ( #167158 ), #11923, .T. ) ;
#28263=DIRECTION ( 'NONE',  ( 0.000000000000000000, 2.851451713636794872E-13, 1.000000000000000000 ) ) ;
#28272=CARTESIAN_POINT ( 'NONE',  ( -20.94999999999999929, 1.115600667400684642E-11, -200.9999999999999432 ) ) ;
#28275=ADVANCED_FACE ( 'NONE', ( #207546 ), #90128, .T. ) ;
#28278=LINE ( 'NONE', #222565, #185444 ) ;
#28290=CARTESIAN_POINT ( 'NONE',  ( -21.64999999999999858, 7.250000000011148416, -188.7499999999999716 ) ) ;
#28336=CARTESIAN_POINT ( 'NONE',  ( 21.05000000000000071, 11.60000000001116227, -194.0717967697244717 ) ) ;
#28345=EDGE_LOOP ( 'NONE', ( #200354, #23836, #212849, #113937 ) ) ;
#28366=VECTOR ( 'NONE', #49966, 1000.000000000000000 ) ;
#28367=CLOSED_SHELL ( 'NONE', ( #85171, #225757, #59979, #8922, #34384, #222781, #6156, #137693, #195828, #18317, #84682, #213387, #171641, #41237, #183770, #8917, #216929, #84126, #168912, #51494, #160944, #152412, #47626, #257186, #179686, #3854, #175599, #193667, #144443, #81661, #77805, #165092, #116227, #31666, #184112, #214809, #54397, #94849, #196901, #109992, #50992, #63126, #146222, #219546, #169203, #75931, #102043, #157875, #213294, #240558, #183087, #9018, #255474, #221547, #224614, #75302, #116199, #27171, #44988, #55305, #133034, #214441, #102277, #168699, #159117, #220203, #210398, #1977, #171647, #25033, #154998, #54040, #24850, #31155, #109078, #12811, #15811, #181680, #185735, #121269, #159621, #182142, #2418, #35257, #100985, #233115, #164739, #253595, #203935, #220931, #123739, #10854, #63401, #17005, #51531, #50339, #66110, #122471, #175383, #239572, #121617, #244577, #158532, #82793, #121821, #240233, #110129, #183215, #223834, #86482, #182936, #31418, #31411, #76185, #6681, #130737, #13093, #225335, #109278, #178425, #108022, #162659, #49702, #96649, #229052, #223039, #246495, #82029, #143550, #145153, #202137, #123291, #207509, #102686, #171851, #253261, #125573, #74196, #85892, #98172, #69377, #236654, #185969, #190896, #182141, #228432, #134655, #235158, #34281, #125898, #5216, #77095, #83088, #245672, #47811, #77654, #12181, #246563, #4371, #225245, #220250, #39657, #49961, #202641, #203403, #10819, #79791, #172060, #100357, #191165, #86587, #240946, #220113, #154448, #210091, #47044, #196504, #112966, #170838, #72213, #78599, #41570, #142069, #249602, #232410, #173362, #257361, #185408, #24364, #84092, #44197, #105341, #105476, #142076, #8556, #215184, #32577, #145400, #162259, #100659, #208562, #209185, #4899, #95014, #250461, #95260, #12518, #205175, #43817, #172504, #88482, #161769, #74084, #14923, #96605, #157399, #27478, #218660, #189764, #149446, #37840, #23614, #130038, #4571, #200769, #155136, #241572, #110554, #64131, #225406, #190092, #234216, #205349, #206864, #229907, #95641, #200467, #112534, #93040, #49781, #20833, #257398, #238716, #202712, #100991, #100254, #63927, #191122, #54318, #17565, #257959, #207612, #145321, #9418, #233566, #231438, #106509, #88117, #124055, #93026, #19288, #79676, #98525, #159101, #15162, #55240, #74898, #81624, #217755, #230039, #184786, #217662, #134425, #105511, #177310, #156260, #41653, #32038, #134362, #43498, #65067, #20215, #214086, #106351, #237908, #47587, #102880, #134589, #73387, #9999, #82982, #165125, #120669, #36065, #246394, #142336, #72053, #106686, #243944, #78494, #188990, #143585, #226024, #23689, #211939, #26826, #12526, #254531, #156914, #4702, #28258, #106500, #157021, #117347, #232228, #174774, #254716, #145968, #208622, #47388, #258006, #167517, #121834, #87209, #251149, #36758, #91124, #193167, #242603, #210077, #164005, #164882, #158984, #147560, #104498, #28275, #56099, #96470, #73428, #18335, #187543, #132911, #209008, #21863, #78850, #120069, #173107, #100662, #116646, #238936, #93928, #52052, #18172, #26410, #117466, #245965, #234237, #227814, #8022, #142848, #28233, #182796, #154479, #242499, #119414, #51539, #100755, #7491, #22021, #20424, #112613, #46427, #7784, #124078, #15175, #59371, #89768, #77496, #41987, #194498, #112865, #180714, #212189, #181003, #124821, #219493, #88107, #252214, #119373, #94043, #232176, #136902, #228979, #87720, #105853, #194846, #246188, #32008, #57879, #186883, #175989, #44690, #171259, #221969, #75550, #43712, #132953, #1050, #85849, #211648, #242643, #29112, #238384, #253994, #178404, #83210, #93598, #228356, #41433, #122977, #162229, #34258, #100867, #80921, #107262, #98022, #256714, #165254, #87603, #164617, #155716, #54466, #81074, #2818, #42858, #114785, #188534, #145166, #256366, #27976, #100801, #157815, #249517, #202158, #83326, #236504, #109908, #16968, #69911, #106646, #142434, #107155, #121959, #18545, #115936, #166552, #96166, #161586, #214381, #44269, #255606, #36897, #72892, #45282, #22234, #72147, #232686, #119679, #231871, #244469, #167961, #186139, #245176, #69738, #243941, #161852, #211673, #30540 ) ) ;
#28394=FACE_OUTER_BOUND ( 'NONE', #16629, .T. ) ;
#28395=TOROIDAL_SURFACE ( 'NONE', #215602, 0.6000000000000017542, 0.1000000000000000056 ) ;
#28414=DIRECTION ( 'NONE',  ( 0.000000000000000000, 1.000000000000000000, 0.000000000000000000 ) ) ;
#28441=EDGE_LOOP ( 'NONE', ( #17417, #39199, #171847, #255 ) ) ;
#28456=EDGE_CURVE ( 'NONE', #245309, #157060, #177559, .T. ) ;
#28460=ORIENTED_EDGE ( 'NONE', *, *, #124780, .F. ) ;
#28481=EDGE_CURVE ( 'NONE', #21796, #39612, #227399, .T. ) ;
#28500=AXIS2_PLACEMENT_3D ( 'NONE', #239558, #256483, #36245 ) ;
#28512=CARTESIAN_POINT ( 'NONE',  ( 20.84999999999998721, 11.75000000001115552, -200.9999999999999432 ) ) ;
#28513=DIRECTION ( 'NONE',  ( 1.000000000000000000, 0.000000000000000000, 0.000000000000000000 ) ) ;
#28540=DIRECTION ( 'NONE',  ( 0.000000000000000000, 0.000000000000000000, -1.000000000000000000 ) ) ;
#28558=EDGE_CURVE ( 'NONE', #142940, #64487, #135802, .T. ) ;
#28570=DIRECTION ( 'NONE',  ( 0.000000000000000000, 0.000000000000000000, -1.000000000000000000 ) ) ;
#28572=SPHERICAL_SURFACE ( 'NONE', #140887, 0.1000000000000000056 ) ;
#28623=CARTESIAN_POINT ( 'NONE',  ( 21.14999999999999503, -11.74999999998883560, -155.7499999999999716 ) ) ;
#28644=ORIENTED_EDGE ( 'NONE', *, *, #45510, .T. ) ;
#28667=CARTESIAN_POINT ( 'NONE',  ( -20.54999999999999716, 1.925233644870967487, -188.2697564668738153 ) ) ;
#28699=AXIS2_PLACEMENT_3D ( 'NONE', #9205, #168334, #70505 ) ;
#28707=CARTESIAN_POINT ( 'NONE',  ( -22.50000000000094147, 0.1008583691097610646, -155.7504328765105583 ) ) ;
#28710=CIRCLE ( 'NONE', #195285, 0.5999999999999894307 ) ;
#28775=DIRECTION ( 'NONE',  ( -1.000000000000000000, -0.000000000000000000, -0.000000000000000000 ) ) ;
#28798=CARTESIAN_POINT ( 'NONE',  ( -18.59999999999999787, -1.835859311432481045, -212.5044391687984842 ) ) ;
#28808=EDGE_CURVE ( 'NONE', #141200, #169154, #2713, .T. ) ;
#28816=LINE ( 'NONE', #225647, #189512 ) ;
#28829=AXIS2_PLACEMENT_3D ( 'NONE', #205555, #144284, #163890 ) ;
#28844=CIRCLE ( 'NONE', #49633, 0.09999999999999939493 ) ;
#28858=( BOUNDED_CURVE ( )  B_SPLINE_CURVE ( 3, ( #255211, #142995, #165157, #28243 ),
 .UNSPECIFIED., .F., .F. ) 
 B_SPLINE_CURVE_WITH_KNOTS ( ( 4, 4 ),
 ( 3.141592653589791784, 4.712388980384688786 ),
 .UNSPECIFIED. ) 
 CURVE ( )  GEOMETRIC_REPRESENTATION_ITEM ( )  RATIONAL_B_SPLINE_CURVE ( ( 1.000000000000000000, 0.8047378541243649375, 0.8047378541243649375, 1.000000000000000000 ) ) 
 REPRESENTATION_ITEM ( '' )  );
#28871=DIRECTION ( 'NONE',  ( -1.000000000000000000, 0.000000000000000000, 0.000000000000000000 ) ) ;
#28910=ORIENTED_EDGE ( 'NONE', *, *, #231577, .T. ) ;
#28926=DIRECTION ( 'NONE',  ( 1.000000000000000000, 3.265361837132813093E-16, -0.000000000000000000 ) ) ;
#28937=DIRECTION ( 'NONE',  ( 1.000000000000000000, 0.000000000000000000, 0.000000000000000000 ) ) ;
#28953=VECTOR ( 'NONE', #165742, 1000.000000000000000 ) ;
#28954=ORIENTED_EDGE ( 'NONE', *, *, #12491, .F. ) ;
#29011=ORIENTED_EDGE ( 'NONE', *, *, #164931, .T. ) ;
#29024=VERTEX_POINT ( 'NONE', #147916 ) ;
#29040=CARTESIAN_POINT ( 'NONE',  ( -18.39999999999999858, -9.499999999988849808, -207.6001893912220169 ) ) ;
#29041=ORIENTED_EDGE ( 'NONE', *, *, #198237, .T. ) ;
#29051=DIRECTION ( 'NONE',  ( 1.000000000000000000, 0.000000000000000000, 0.000000000000000000 ) ) ;
#29074=LINE ( 'NONE', #249378, #186930 ) ;
#29112=ADVANCED_FACE ( 'NONE', ( #119059 ), #77912, .F. ) ;
#29117=EDGE_LOOP ( 'NONE', ( #1824, #190933 ) ) ;
#29140=ORIENTED_EDGE ( 'NONE', *, *, #166302, .F. ) ;
#29143=EDGE_LOOP ( 'NONE', ( #121915, #90277, #38265, #95311, #150795, #143227, #131386, #172057, #113780, #11726, #190775, #134159, #35143, #62986, #86744, #242107, #121146, #16323 ) ) ;
#29172=CARTESIAN_POINT ( 'NONE',  ( -21.55000000000000426, 7.750000000011155521, -179.8499999999999943 ) ) ;
#29175=DIRECTION ( 'NONE',  ( 0.000000000000000000, 0.000000000000000000, -1.000000000000000000 ) ) ;
#29176=CARTESIAN_POINT ( 'NONE',  ( 18.59999999999999432, 1.162701749949165642, -175.5999999999999659 ) ) ;
#29181=DIRECTION ( 'NONE',  ( -0.000000000000000000, -0.000000000000000000, -1.000000000000000000 ) ) ;
#29191=CARTESIAN_POINT ( 'NONE',  ( -22.39999999999999858, -0.09999999998884338825, -155.8504291924551808 ) ) ;
#29202=VERTEX_POINT ( 'NONE', #65484 ) ;
#29206=CARTESIAN_POINT ( 'NONE',  ( -23.25000000000000000, -11.48912529306489994, -197.8999999999999773 ) ) ;
#29214=DIRECTION ( 'NONE',  ( 1.296989514748957922E-15, -0.9887567792719341719, 0.1495327102803664099 ) ) ;
#29246=ORIENTED_EDGE ( 'NONE', *, *, #48453, .F. ) ;
#29250=TOROIDAL_SURFACE ( 'NONE', #41693, 12.97499999999999787, 0.1000000000000000056 ) ;
#29289=FACE_OUTER_BOUND ( 'NONE', #235852, .T. ) ;
#29314=EDGE_CURVE ( 'NONE', #8860, #60251, #227755, .T. ) ;
#29346=CARTESIAN_POINT ( 'NONE',  ( -21.05000000000000071, 1.115600667400684642E-11, -167.4999999999999716 ) ) ;
#29349=EDGE_LOOP ( 'NONE', ( #224367, #37568, #169751, #244990 ) ) ;
#29393=CARTESIAN_POINT ( 'NONE',  ( 20.88420186297724612, 10.33025634372637391, -206.5870929282638429 ) ) ;
#29394=CIRCLE ( 'NONE', #41859, 11.75000000000001066 ) ;
#29415=CARTESIAN_POINT ( 'NONE',  ( 21.06277459767431282, 8.872862438279383923, -179.7039991923569460 ) ) ;
#29430=EDGE_CURVE ( 'NONE', #185664, #81259, #208859, .T. ) ;
#29444=ORIENTED_EDGE ( 'NONE', *, *, #28456, .F. ) ;
#29465=AXIS2_PLACEMENT_3D ( 'NONE', #93126, #111421, #230081 ) ;
#29468=DIRECTION ( 'NONE',  ( 1.000000000000000000, 0.000000000000000000, 0.000000000000000000 ) ) ;
#29511=DIRECTION ( 'NONE',  ( -1.000000000000000000, -2.952720810173289112E-16, 0.000000000000000000 ) ) ;
#29517=CYLINDRICAL_SURFACE ( 'NONE', #170473, 0.09999999999998898659 ) ;
#29538=CARTESIAN_POINT ( 'NONE',  ( -22.59066674512259709, 11.75000000001115552, -167.4694958763693364 ) ) ;
#29586=LINE ( 'NONE', #68686, #131633 ) ;
#29590=ORIENTED_EDGE ( 'NONE', *, *, #78932, .F. ) ;
#29604=ORIENTED_EDGE ( 'NONE', *, *, #64078, .T. ) ;
#29615=CARTESIAN_POINT ( 'NONE',  ( -21.05000000000000071, 11.65000000001115588, -167.5999999999999659 ) ) ;
#29624=DIRECTION ( 'NONE',  ( -0.000000000000000000, -0.000000000000000000, -1.000000000000000000 ) ) ;
#29625=VERTEX_POINT ( 'NONE', #237411 ) ;
#29632=DIRECTION ( 'NONE',  ( 1.000000000000000000, 0.000000000000000000, 0.000000000000000000 ) ) ;
#29662=CARTESIAN_POINT ( 'NONE',  ( 22.50000000000000000, 0.1000000000111554016, -159.7092204016265669 ) ) ;
#29680=EDGE_LOOP ( 'NONE', ( #203067, #17204, #83641, #127531, #254085, #3078, #167925, #246431, #183943, #52755 ) ) ;
#29725=CARTESIAN_POINT ( 'NONE',  ( 18.49999999999999645, 1.115600667400684642E-11, -200.9999999999999432 ) ) ;
#29763=ORIENTED_EDGE ( 'NONE', *, *, #114474, .T. ) ;
#29764=CARTESIAN_POINT ( 'NONE',  ( -20.64999999999999858, 1.940186915899004161, -188.1708807889466470 ) ) ;
#29776=EDGE_LOOP ( 'NONE', ( #152648, #252013, #29011, #94555, #77714, #248126 ) ) ;
#29783=ORIENTED_EDGE ( 'NONE', *, *, #104002, .F. ) ;
#29787=CARTESIAN_POINT ( 'NONE',  ( -20.64999999999999858, -8.999999999988846255, -177.3939691226524076 ) ) ;
#29810=DIRECTION ( 'NONE',  ( -1.000000000000000000, -2.952720810173289112E-16, 0.000000000000000000 ) ) ;
#29838=EDGE_CURVE ( 'NONE', #226886, #51917, #18312, .T. ) ;
#29881=CARTESIAN_POINT ( 'NONE',  ( 22.59999999999999787, 11.64957080755595520, -167.3999999999999773 ) ) ;
#29896=EDGE_CURVE ( 'NONE', #66806, #214983, #205740, .T. ) ;
#29911=CARTESIAN_POINT ( 'NONE',  ( 20.94999999999999574, 14.00000000001115730, -172.9270925303825095 ) ) ;
#29922=CARTESIAN_POINT ( 'NONE',  ( 20.94999999999999574, -1.349084418615859482, -175.4864989635454435 ) ) ;
#29956=CARTESIAN_POINT ( 'NONE',  ( 20.94999999999999929, -8.999999999988842703, -191.6060308773475072 ) ) ;
#30007=EDGE_LOOP ( 'NONE', ( #7584, #193070 ) ) ;
#30025=EDGE_CURVE ( 'NONE', #249855, #19947, #122286, .T. ) ;
#30030=EDGE_CURVE ( 'NONE', #179090, #213186, #143392, .T. ) ;
#30037=CARTESIAN_POINT ( 'NONE',  ( -18.50000000000000711, -9.419203418015495544, -174.7477858104286952 ) ) ;
#30052=CIRCLE ( 'NONE', #142439, 12.77500000000000924 ) ;
#30118=DIRECTION ( 'NONE',  ( -1.000000000000000000, -0.000000000000000000, 0.000000000000000000 ) ) ;
#30122=TOROIDAL_SURFACE ( 'NONE', #209153, 0.6000000000000006439, 0.1000000000000000056 ) ;
#30131=VECTOR ( 'NONE', #222438, 1000.000000000000000 ) ;
#30139=AXIS2_PLACEMENT_3D ( 'NONE', #166222, #244434, #22852 ) ;
#30149=CARTESIAN_POINT ( 'NONE',  ( 23.14999999999999147, 1.115600667400684642E-11, -167.4999999999999716 ) ) ;
#30155=CARTESIAN_POINT ( 'NONE',  ( 23.14999999999999858, 5.500000000011153745, -179.9052660189130677 ) ) ;
#30163=DIRECTION ( 'NONE',  ( -1.000000000000000000, -0.000000000000000000, -0.000000000000000000 ) ) ;
#30168=AXIS2_PLACEMENT_3D ( 'NONE', #88083, #29468, #45138 ) ;
#30182=CIRCLE ( 'NONE', #50975, 0.09999999999999158173 ) ;
#30198=CARTESIAN_POINT ( 'NONE',  ( 18.52165635395202870, -9.481150711271050469, -174.5248375828624035 ) ) ;
#30204=CARTESIAN_POINT ( 'NONE',  ( -20.07928932188135107, 9.220710678129810489, -179.8499999999999943 ) ) ;
#30205=ORIENTED_EDGE ( 'NONE', *, *, #122331, .T. ) ;
#30211=DIRECTION ( 'NONE',  ( -0.000000000000000000, 1.000000000000000000, 0.000000000000000000 ) ) ;
#30235=AXIS2_PLACEMENT_3D ( 'NONE', #227531, #128443, #207999 ) ;
#30241=CARTESIAN_POINT ( 'NONE',  ( 20.95512820512820440, 10.62384868372303615, -179.6499999999999773 ) ) ;
#30242=CARTESIAN_POINT ( 'NONE',  ( 23.14999999999999503, 11.65000000001116298, -188.8499999999999659 ) ) ;
#30272=CARTESIAN_POINT ( 'NONE',  ( 21.14999999999999858, 11.65000000001115943, -179.6499999999999773 ) ) ;
#30279=ORIENTED_EDGE ( 'NONE', *, *, #73845, .T. ) ;
#30287=CIRCLE ( 'NONE', #196857, 11.64999999999999325 ) ;
#30386=CIRCLE ( 'NONE', #142763, 0.09999999999998898659 ) ;
#30430=AXIS2_PLACEMENT_3D ( 'NONE', #27300, #46803, #248887 ) ;
#30474=AXIS2_PLACEMENT_3D ( 'NONE', #96663, #249372, #51127 ) ;
#30475=FACE_OUTER_BOUND ( 'NONE', #233291, .T. ) ;
#30479=CARTESIAN_POINT ( 'NONE',  ( -23.25000000000000000, 11.75000000001115552, -200.9999999999999432 ) ) ;
#30481=FACE_OUTER_BOUND ( 'NONE', #91563, .T. ) ;
#30483=AXIS2_PLACEMENT_3D ( 'NONE', #79357, #3678, #162780 ) ;
#30518=CARTESIAN_POINT ( 'NONE',  ( 18.59999999999999076, 11.75000000001115907, -192.3499999999999659 ) ) ;
#30525=AXIS2_PLACEMENT_3D ( 'NONE', #65792, #142742, #82745 ) ;
#30540=ADVANCED_FACE ( 'NONE', ( #189337 ), #111073, .T. ) ;
#30559=EDGE_CURVE ( 'NONE', #223911, #23864, #102035, .T. ) ;
#30563=EDGE_CURVE ( 'NONE', #252182, #215011, #188054, .T. ) ;
#30576=EDGE_CURVE ( 'NONE', #127119, #163489, #146926, .T. ) ;
#30580=EDGE_CURVE ( 'NONE', #253024, #73463, #214483, .T. ) ;
#30615=ORIENTED_EDGE ( 'NONE', *, *, #6834, .F. ) ;
#30616=ORIENTED_EDGE ( 'NONE', *, *, #248342, .T. ) ;
#30622=AXIS2_PLACEMENT_3D ( 'NONE', #47089, #26277, #88783 ) ;
#30629=CARTESIAN_POINT ( 'NONE',  ( 21.05000000000000071, 1.115600667400684642E-11, -200.9999999999999432 ) ) ;
#30646=FACE_OUTER_BOUND ( 'NONE', #252076, .T. ) ;
#30666=CIRCLE ( 'NONE', #84771, 0.09999999999999939493 ) ;
#30675=ORIENTED_EDGE ( 'NONE', *, *, #208631, .F. ) ;
#30690=CARTESIAN_POINT ( 'NONE',  ( -20.94999999999999929, 11.60000000001115161, -174.4282032302755283 ) ) ;
#30745=CARTESIAN_POINT ( 'NONE',  ( -20.85000000000000142, -1.149570369564537842, -208.8159124845019221 ) ) ;
#30755=CIRCLE ( 'NONE', #13990, 0.09999999999998898659 ) ;
#30785=DIRECTION ( 'NONE',  ( 0.000000000000000000, 1.000000000000000000, 0.000000000000000000 ) ) ;
#30807=CIRCLE ( 'NONE', #234799, 11.70000000000001528 ) ;
#30845=DIRECTION ( 'NONE',  ( -0.000000000000000000, 0.000000000000000000, -1.000000000000000000 ) ) ;
#30875=EDGE_CURVE ( 'NONE', #39669, #171236, #143747, .T. ) ;
#30879=ORIENTED_EDGE ( 'NONE', *, *, #30025, .F. ) ;
#30883=EDGE_CURVE ( 'NONE', #197017, #16283, #18852, .T. ) ;
#30889=EDGE_CURVE ( 'NONE', #43643, #214529, #136593, .T. ) ;
#30912=EDGE_LOOP ( 'NONE', ( #97921, #154695, #41431, #238469 ) ) ;
#30920=DIRECTION ( 'NONE',  ( 1.000000000000000000, -0.000000000000000000, -0.000000000000000000 ) ) ;
#30984=ORIENTED_EDGE ( 'NONE', *, *, #184685, .T. ) ;
#30988=ORIENTED_EDGE ( 'NONE', *, *, #225438, .F. ) ;
#30995=LINE ( 'NONE', #89633, #157330 ) ;
#31017=DIRECTION ( 'NONE',  ( 1.000000000000000000, -0.000000000000000000, -0.000000000000000000 ) ) ;
#31028=EDGE_CURVE ( 'NONE', #228990, #176585, #164614, .T. ) ;
#31040=DIRECTION ( 'NONE',  ( 0.000000000000000000, 0.000000000000000000, -1.000000000000000000 ) ) ;
#31081=CIRCLE ( 'NONE', #47762, 0.09999999999998807065 ) ;
#31099=FACE_OUTER_BOUND ( 'NONE', #714, .T. ) ;
#31101=DIRECTION ( 'NONE',  ( 0.000000000000000000, 1.000000000000000000, 1.626303258728238113E-15 ) ) ;
#31117=LINE ( 'NONE', #12822, #83818 ) ;
#31128=DIRECTION ( 'NONE',  ( 0.000000000000000000, -2.664535259100396996E-15, 1.000000000000000000 ) ) ;
#31137=CARTESIAN_POINT ( 'NONE',  ( 22.50000000000000000, 0.1000000000111554016, -155.8504291924551808 ) ) ;
#31155=ADVANCED_FACE ( 'NONE', ( #129240 ), #229625, .T. ) ;
#31160=AXIS2_PLACEMENT_3D ( 'NONE', #245800, #247065, #104958 ) ;
#31206=DIRECTION ( 'NONE',  ( -0.000000000000000000, -0.000000000000000000, -1.000000000000000000 ) ) ;
#31207=ORIENTED_EDGE ( 'NONE', *, *, #117733, .T. ) ;
#31223=AXIS2_PLACEMENT_3D ( 'NONE', #9669, #128348, #228740 ) ;
#31257=DIRECTION ( 'NONE',  ( 0.000000000000000000, 0.000000000000000000, -1.000000000000000000 ) ) ;
#31264=CIRCLE ( 'NONE', #60252, 0.09999999999999939493 ) ;
#31315=ORIENTED_EDGE ( 'NONE', *, *, #146602, .T. ) ;
#31319=ORIENTED_EDGE ( 'NONE', *, *, #128961, .T. ) ;
#31320=CIRCLE ( 'NONE', #177053, 0.5000000000000004441 ) ;
#31331=CARTESIAN_POINT ( 'NONE',  ( -18.39999999999999858, -9.499999999988849808, -174.5320693966996259 ) ) ;
#31345=CIRCLE ( 'NONE', #164585, 0.09999999999999939493 ) ;
#31369=VERTEX_POINT ( 'NONE', #23440 ) ;
#31411=ADVANCED_FACE ( 'NONE', ( #99061 ), #160380, .F. ) ;
#31418=ADVANCED_FACE ( 'NONE', ( #123799, #22147 ), #122522, .F. ) ;
#31443=DIRECTION ( 'NONE',  ( 0.000000000000000000, 0.000000000000000000, -1.000000000000000000 ) ) ;
#31498=CIRCLE ( 'NONE', #35586, 12.77500000000000036 ) ;
#31519=EDGE_CURVE ( 'NONE', #48993, #185664, #70268, .T. ) ;
#31521=EDGE_LOOP ( 'NONE', ( #100059, #5867, #129879, #236300 ) ) ;
#31561=ORIENTED_EDGE ( 'NONE', *, *, #193042, .F. ) ;
#31562=DIRECTION ( 'NONE',  ( 0.000000000000000000, 0.000000000000000000, -1.000000000000000000 ) ) ;
#31573=CARTESIAN_POINT ( 'NONE',  ( -21.14999999999999858, 1.115600667400684642E-11, -155.8504291924551808 ) ) ;
#31579=CARTESIAN_POINT ( 'NONE',  ( -20.00857864376270001, 9.250000000011157297, -179.8499999999999943 ) ) ;
#31593=CIRCLE ( 'NONE', #85679, 0.09999999999998898659 ) ;
#31608=DIRECTION ( 'NONE',  ( 0.000000000000000000, 0.000000000000000000, -1.000000000000000000 ) ) ;
#31628=DIRECTION ( 'NONE',  ( 0.000000000000000000, -4.440892098500570153E-15, 1.000000000000000000 ) ) ;
#31665=ORIENTED_EDGE ( 'NONE', *, *, #75390, .F. ) ;
#31666=ADVANCED_FACE ( 'NONE', ( #92356 ), #35446, .T. ) ;
#31704=DIRECTION ( 'NONE',  ( 0.000000000000000000, 0.1575844902526876978, 0.9875055080513731598 ) ) ;
#31721=EDGE_CURVE ( 'NONE', #172688, #105032, #97736, .T. ) ;
#31737=FACE_OUTER_BOUND ( 'NONE', #1358, .T. ) ;
#31739=DIRECTION ( 'NONE',  ( 1.000000000000000000, 0.000000000000000000, 0.000000000000000000 ) ) ;
#31754=CARTESIAN_POINT ( 'NONE',  ( 20.99551997958312199, 11.75000000001053913, -194.1516591376895349 ) ) ;
#31758=DIRECTION ( 'NONE',  ( -0.7071067811865388020, 0.7071067811865561215, 0.000000000000000000 ) ) ;
#31787=ORIENTED_EDGE ( 'NONE', *, *, #27016, .T. ) ;
#31799=ORIENTED_EDGE ( 'NONE', *, *, #18710, .T. ) ;
#31805=ORIENTED_EDGE ( 'NONE', *, *, #163670, .T. ) ;
#31819=DIRECTION ( 'NONE',  ( 0.000000000000000000, 1.000000000000000000, 0.000000000000000000 ) ) ;
#31824=ORIENTED_EDGE ( 'NONE', *, *, #209416, .F. ) ;
#31884=FACE_OUTER_BOUND ( 'NONE', #78038, .T. ) ;
#31925=EDGE_CURVE ( 'NONE', #140846, #220457, #177081, .T. ) ;
#31930=CARTESIAN_POINT ( 'NONE',  ( -20.94999999999999929, -11.64999999998884483, -197.9999999999999432 ) ) ;
#31938=ORIENTED_EDGE ( 'NONE', *, *, #122329, .T. ) ;
#32007=CARTESIAN_POINT ( 'NONE',  ( 21.98333005346336222, 1.115600667400684642E-11, -160.1259246709433057 ) ) ;
#32008=ADVANCED_FACE ( 'NONE', ( #137273 ), #243698, .F. ) ;
#32009=CARTESIAN_POINT ( 'NONE',  ( 18.59999999999999076, 1.250000000011167511, -175.4999999999999716 ) ) ;
#32038=ADVANCED_FACE ( 'NONE', ( #34364 ), #193425, .F. ) ;
#32054=DIRECTION ( 'NONE',  ( -1.000000000000000000, 0.000000000000000000, 0.000000000000000000 ) ) ;
#32058=DIRECTION ( 'NONE',  ( 1.000000000000000000, 0.000000000000000000, 0.000000000000000000 ) ) ;
#32061=CARTESIAN_POINT ( 'NONE',  ( 21.04999999999999716, 6.299230910098046365, -167.4015624999999829 ) ) ;
#32068=DIRECTION ( 'NONE',  ( 0.000000000000000000, 0.000000000000000000, -1.000000000000000000 ) ) ;
#32086=CARTESIAN_POINT ( 'NONE',  ( 18.59999999999999432, 1.261786168576181755, -175.5864989635454378 ) ) ;
#32097=CARTESIAN_POINT ( 'NONE',  ( -22.50000000000000000, 11.64957080755595520, -167.3999999999999773 ) ) ;
#32114=CIRCLE ( 'NONE', #244467, 11.64999999999999325 ) ;
#32118=VERTEX_POINT ( 'NONE', #61600 ) ;
#32136=DIRECTION ( 'NONE',  ( 1.000000000000000000, 0.000000000000000000, 0.000000000000000000 ) ) ;
#32139=VERTEX_POINT ( 'NONE', #219376 ) ;
#32146=LINE ( 'NONE', #254951, #48602 ) ;
#32172=VECTOR ( 'NONE', #30211, 1000.000000000000000 ) ;
#32227=ORIENTED_EDGE ( 'NONE', *, *, #133972, .T. ) ;
#32248=DIRECTION ( 'NONE',  ( 1.000000000000000000, 0.000000000000000000, 0.000000000000000000 ) ) ;
#32271=CARTESIAN_POINT ( 'NONE',  ( 22.00356870140516463, 7.254242362509886632, -167.4999999999999716 ) ) ;
#32293=DIRECTION ( 'NONE',  ( -1.000000000000000000, 0.000000000000000000, 0.000000000000000000 ) ) ;
#32300=CARTESIAN_POINT ( 'NONE',  ( 22.45305468355010703, -0.1008583690885486023, -155.7504328765102457 ) ) ;
#32331=DIRECTION ( 'NONE',  ( 0.000000000000000000, 6.505213034913742890E-15, -1.000000000000000000 ) ) ;
#32345=CARTESIAN_POINT ( 'NONE',  ( -20.94999999999999929, -11.48912529306490349, -170.4999999999999716 ) ) ;
#32364=CARTESIAN_POINT ( 'NONE',  ( 21.04999999999999716, -0.03753606327451274732, -161.1677277260643564 ) ) ;
#32426=DIRECTION ( 'NONE',  ( 0.000000000000000000, 0.000000000000000000, -1.000000000000000000 ) ) ;
#32427=FACE_OUTER_BOUND ( 'NONE', #164096, .T. ) ;
#32440=AXIS2_PLACEMENT_3D ( 'NONE', #124258, #73289, #109800 ) ;
#32457=DIRECTION ( 'NONE',  ( -1.000000000000000000, -0.000000000000000000, 0.000000000000000000 ) ) ;
#32496=CARTESIAN_POINT ( 'NONE',  ( -18.48179518609192229, -9.518325300483091667, -207.8897055767644133 ) ) ;
#32542=ORIENTED_EDGE ( 'NONE', *, *, #230813, .T. ) ;
#32557=CIRCLE ( 'NONE', #236516, 0.09999999999999939493 ) ;
#32570=ORIENTED_EDGE ( 'NONE', *, *, #148095, .T. ) ;
#32577=ADVANCED_FACE ( 'NONE', ( #168140 ), #48245, .T. ) ;
#32591=DIRECTION ( 'NONE',  ( 0.000000000000000000, 0.000000000000000000, -1.000000000000000000 ) ) ;
#32608=CIRCLE ( 'NONE', #11740, 0.09999999999998898659 ) ;
#32652=EDGE_CURVE ( 'NONE', #190860, #118040, #6442, .T. ) ;
#32655=AXIS2_PLACEMENT_3D ( 'NONE', #164792, #86496, #241749 ) ;
#32656=CARTESIAN_POINT ( 'NONE',  ( -23.15000000000000213, 1.115600667400684642E-11, -167.4999999999999716 ) ) ;
#32658=CARTESIAN_POINT ( 'NONE',  ( 22.40000000000020819, -0.1008583690885111045, -155.7504328765102457 ) ) ;
#32669=EDGE_LOOP ( 'NONE', ( #255588, #20746, #15018, #45547, #38966, #204075, #152049, #35069, #46255, #144096, #150895, #127112, #83547, #232887, #79013, #84282 ) ) ;
#32678=AXIS2_PLACEMENT_3D ( 'NONE', #47095, #126656, #184057 ) ;
#32695=EDGE_CURVE ( 'NONE', #167246, #138331, #123251, .T. ) ;
#32718=DIRECTION ( 'NONE',  ( -1.000000000000000000, -0.000000000000000000, 0.000000000000000000 ) ) ;
#32727=TOROIDAL_SURFACE ( 'NONE', #149225, 4.149999999999999467, 0.1000000000000000056 ) ;
#32745=EDGE_LOOP ( 'NONE', ( #163859, #77482, #121420, #176805 ) ) ;
#32772=DIRECTION ( 'NONE',  ( 1.000000000000000000, 0.000000000000000000, 0.000000000000000000 ) ) ;
#32778=CYLINDRICAL_SURFACE ( 'NONE', #14227, 0.09999999999999881206 ) ;
#32781=VECTOR ( 'NONE', #7548, 1000.000000000000000 ) ;
#32809=EDGE_LOOP ( 'NONE', ( #144487, #36061, #251282, #100000 ) ) ;
#32831=DIRECTION ( 'NONE',  ( -1.000000000000000000, 0.000000000000000000, 0.000000000000000000 ) ) ;
#32838=CARTESIAN_POINT ( 'NONE',  ( -18.50000000000000000, 11.65000000001115232, -179.7499999999999716 ) ) ;
#32854=ORIENTED_EDGE ( 'NONE', *, *, #36553, .T. ) ;
#32876=ORIENTED_EDGE ( 'NONE', *, *, #137508, .F. ) ;
#32907=DIRECTION ( 'NONE',  ( 1.000000000000000000, 0.000000000000000000, 0.000000000000000000 ) ) ;
#32917=EDGE_LOOP ( 'NONE', ( #78405, #21904, #147763, #86234 ) ) ;
#32921=DIRECTION ( 'NONE',  ( 1.000000000000000000, -0.000000000000000000, -0.000000000000000000 ) ) ;
#32992=ORIENTED_EDGE ( 'NONE', *, *, #68707, .F. ) ;
#33022=EDGE_CURVE ( 'NONE', #87151, #236886, #29586, .T. ) ;
#33058=CARTESIAN_POINT ( 'NONE',  ( -20.64999999999999858, 4.350000000011156054, -179.8499999999999943 ) ) ;
#33089=ORIENTED_EDGE ( 'NONE', *, *, #185154, .F. ) ;
#33093=DIRECTION ( 'NONE',  ( 1.000000000000000000, -0.000000000000000000, -0.000000000000000000 ) ) ;
#33106=CIRCLE ( 'NONE', #178837, 0.2000000000000057288 ) ;
#33108=EDGE_LOOP ( 'NONE', ( #36034, #133092, #213330, #47975 ) ) ;
#33114=EDGE_CURVE ( 'NONE', #6554, #131901, #102748, .T. ) ;
#33126=EDGE_CURVE ( 'NONE', #39669, #48866, #32146, .T. ) ;
#33159=CARTESIAN_POINT ( 'NONE',  ( -20.94999999999999929, 1.162701749949165642, -175.5999999999999659 ) ) ;
#33180=ORIENTED_EDGE ( 'NONE', *, *, #147342, .F. ) ;
#33185=CARTESIAN_POINT ( 'NONE',  ( -18.59999999999999787, 11.65000000001115232, -155.7499999999999716 ) ) ;
#33218=DIRECTION ( 'NONE',  ( -0.000000000000000000, 0.000000000000000000, -1.000000000000000000 ) ) ;
#33255=ORIENTED_EDGE ( 'NONE', *, *, #238373, .F. ) ;
#33261=DIRECTION ( 'NONE',  ( -0.7071067811865388020, 0.7071067811865561215, 0.000000000000000000 ) ) ;
#33299=DIRECTION ( 'NONE',  ( 1.000000000000000000, 0.000000000000000000, 0.000000000000000000 ) ) ;
#33306=ORIENTED_EDGE ( 'NONE', *, *, #101379, .F. ) ;
#33311=CARTESIAN_POINT ( 'NONE',  ( -18.45037301276657971, -9.490200447530781958, -174.5126741364145175 ) ) ;
#33327=CARTESIAN_POINT ( 'NONE',  ( -20.87600722750343252, 10.33112638556969465, -206.5901228926974227 ) ) ;
#33359=CARTESIAN_POINT ( 'NONE',  ( 21.05000000000000071, 6.477552182504824785, -167.5999999652990482 ) ) ;
#33360=AXIS2_PLACEMENT_3D ( 'NONE', #213172, #136174, #158381 ) ;
#33419=CYLINDRICAL_SURFACE ( 'NONE', #100392, 0.1000000000000101225 ) ;
#33548=AXIS2_PLACEMENT_3D ( 'NONE', #194298, #58588, #15666 ) ;
#33559=FACE_OUTER_BOUND ( 'NONE', #200078, .T. ) ;
#33574=CARTESIAN_POINT ( 'NONE',  ( 21.53699400381851703, 6.787711793190427834, -167.4999999999999432 ) ) ;
#33590=EDGE_CURVE ( 'NONE', #38886, #99286, #189616, .T. ) ;
#33619=DIRECTION ( 'NONE',  ( -1.000000000000000000, 0.000000000000000000, 0.000000000000000000 ) ) ;
#33641=ORIENTED_EDGE ( 'NONE', *, *, #241072, .T. ) ;
#33650=CARTESIAN_POINT ( 'NONE',  ( -20.64999999999999858, 7.250000000011155521, -179.7499999999999716 ) ) ;
#33683=CARTESIAN_POINT ( 'NONE',  ( 22.59999999999999432, 0.1000000000111554016, -155.8504291924551808 ) ) ;
#33688=VERTEX_POINT ( 'NONE', #144704 ) ;
#33705=DIRECTION ( 'NONE',  ( 0.000000000000000000, 0.000000000000000000, 1.000000000000000000 ) ) ;
#33740=EDGE_CURVE ( 'NONE', #72236, #36747, #185132, .T. ) ;
#33750=CARTESIAN_POINT ( 'NONE',  ( -18.50000000000000000, 7.021664781911246322, -204.8335654018972605 ) ) ;
#33762=DIRECTION ( 'NONE',  ( 0.000000000000000000, 0.000000000000000000, 1.000000000000000000 ) ) ;
#33774=ORIENTED_EDGE ( 'NONE', *, *, #165580, .F. ) ;
#33784=CARTESIAN_POINT ( 'NONE',  ( -18.43634282235129618, -9.679787199916868090, -207.6606518854537740 ) ) ;
#33800=CYLINDRICAL_SURFACE ( 'NONE', #54229, 0.09999999999998898659 ) ;
#33844=VERTEX_POINT ( 'NONE', #205977 ) ;
#33854=LINE ( 'NONE', #190329, #130615 ) ;
#33880=EDGE_LOOP ( 'NONE', ( #80884, #183811, #94453, #239212, #128418, #86979, #158219, #94411, #18718, #178150, #143311, #143260, #221612, #21509, #155570, #159359, #171116, #135735, #155681, #249851, #31938, #203133, #253153 ) ) ;
#33882=DIRECTION ( 'NONE',  ( -1.000000000000000000, -0.000000000000000000, 0.000000000000000000 ) ) ;
#33914=CARTESIAN_POINT ( 'NONE',  ( -18.49499033040907037, -9.438148771733517961, -174.6981532259234200 ) ) ;
#33918=DIRECTION ( 'NONE',  ( -1.000000000000000000, 0.000000000000000000, 0.000000000000000000 ) ) ;
#33931=ORIENTED_EDGE ( 'NONE', *, *, #136023, .F. ) ;
#33998=DIRECTION ( 'NONE',  ( 0.000000000000000000, 0.000000000000000000, 1.000000000000000000 ) ) ;
#34030=ORIENTED_EDGE ( 'NONE', *, *, #222061, .T. ) ;
#34064=EDGE_CURVE ( 'NONE', #85452, #242283, #161427, .T. ) ;
#34087=DIRECTION ( 'NONE',  ( -1.000000000000000000, 0.000000000000000000, 0.000000000000000000 ) ) ;
#34100=DIRECTION ( 'NONE',  ( -1.000000000000000000, 0.000000000000000000, 0.000000000000000000 ) ) ;
#34121=EDGE_CURVE ( 'NONE', #86058, #194468, #230351, .T. ) ;
#34126=ORIENTED_EDGE ( 'NONE', *, *, #165055, .F. ) ;
#34129=CARTESIAN_POINT ( 'NONE',  ( -23.15000000000000213, -11.39257802169451139, -197.9260504201680249 ) ) ;
#34138=ORIENTED_EDGE ( 'NONE', *, *, #184151, .T. ) ;
#34140=ORIENTED_EDGE ( 'NONE', *, *, #168708, .F. ) ;
#34141=VERTEX_POINT ( 'NONE', #7456 ) ;
#34185=AXIS2_PLACEMENT_3D ( 'NONE', #5706, #202645, #244335 ) ;
#34196=DIRECTION ( 'NONE',  ( -1.000000000000000000, 0.000000000000000000, 0.000000000000000000 ) ) ;
#34258=ADVANCED_FACE ( 'NONE', ( #170440 ), #40820, .T. ) ;
#34281=ADVANCED_FACE ( 'NONE', ( #116829 ), #154703, .F. ) ;
#34308=CARTESIAN_POINT ( 'NONE',  ( 21.05000000000000071, 1.115600667400684642E-11, -167.5999999999999659 ) ) ;
#34312=VERTEX_POINT ( 'NONE', #157267 ) ;
#34316=CARTESIAN_POINT ( 'NONE',  ( 23.14999999999999503, 11.65000000001116298, -179.6499999999999773 ) ) ;
#34324=ORIENTED_EDGE ( 'NONE', *, *, #38475, .T. ) ;
#34347=DIRECTION ( 'NONE',  ( 0.000000000000000000, 0.000000000000000000, -1.000000000000000000 ) ) ;
#34364=FACE_OUTER_BOUND ( 'NONE', #223106, .T. ) ;
#34375=VERTEX_POINT ( 'NONE', #60683 ) ;
#34382=CARTESIAN_POINT ( 'NONE',  ( 21.00000000000000000, 9.750000000011153745, -188.7499999999999716 ) ) ;
#34384=ADVANCED_FACE ( 'NONE', ( #178107 ), #219837, .T. ) ;
#34439=VERTEX_POINT ( 'NONE', #138916 ) ;
#34442=FACE_OUTER_BOUND ( 'NONE', #115047, .T. ) ;
#34465=LINE ( 'NONE', #53989, #68815 ) ;
#34499=DIRECTION ( 'NONE',  ( 1.000000000000000000, -7.304098846218134667E-16, -4.217023435051625732E-16 ) ) ;
#34541=CARTESIAN_POINT ( 'NONE',  ( -21.55000000000000426, 7.708578643773852157, -179.8499999999999943 ) ) ;
#34560=DIRECTION ( 'NONE',  ( 0.000000000000000000, 0.000000000000000000, -1.000000000000000000 ) ) ;
#34591=AXIS2_PLACEMENT_3D ( 'NONE', #54095, #236574, #57934 ) ;
#34606=PLANE ( 'NONE',  #76805 ) ;
#34619=CYLINDRICAL_SURFACE ( 'NONE', #185951, 0.09999999999999939493 ) ;
#34674=ORIENTED_EDGE ( 'NONE', *, *, #199622, .T. ) ;
#34681=AXIS2_PLACEMENT_3D ( 'NONE', #1033, #79300, #257902 ) ;
#34684=FACE_OUTER_BOUND ( 'NONE', #214055, .T. ) ;
#34744=FACE_OUTER_BOUND ( 'NONE', #214921, .T. ) ;
#34749=EDGE_CURVE ( 'NONE', #234902, #224848, #111699, .T. ) ;
#34803=DIRECTION ( 'NONE',  ( 1.000000000000000000, -0.000000000000000000, -0.000000000000000000 ) ) ;
#34804=CARTESIAN_POINT ( 'NONE',  ( -22.41119224318417125, 1.115600667400684642E-11, -155.8504291924551808 ) ) ;
#34817=DIRECTION ( 'NONE',  ( 0.000000000000000000, 0.000000000000000000, -1.000000000000000000 ) ) ;
#34818=DIRECTION ( 'NONE',  ( 0.000000000000000000, 0.8700118002898321601, -0.4930308989875230030 ) ) ;
#34842=DIRECTION ( 'NONE',  ( 0.000000000000000000, 0.9876197685951252359, -0.1568667991644863424 ) ) ;
#34845=DIRECTION ( 'NONE',  ( 0.000000000000000000, 4.440892098500631684E-15, -1.000000000000000000 ) ) ;
#34858=ORIENTED_EDGE ( 'NONE', *, *, #236285, .F. ) ;
#34866=ORIENTED_EDGE ( 'NONE', *, *, #4086, .T. ) ;
#34875=EDGE_CURVE ( 'NONE', #133529, #75581, #192277, .T. ) ;
#34879=CIRCLE ( 'NONE', #247220, 0.09999999999998898659 ) ;
#34921=DIRECTION ( 'NONE',  ( 0.000000000000000000, 0.000000000000000000, 1.000000000000000000 ) ) ;
#34957=CARTESIAN_POINT ( 'NONE',  ( 21.05000000000000071, -8.999999999988842703, -191.1060308773475072 ) ) ;
#34963=EDGE_CURVE ( 'NONE', #196712, #237038, #116192, .T. ) ;
#34975=EDGE_CURVE ( 'NONE', #119689, #72236, #236974, .T. ) ;
#35010=CARTESIAN_POINT ( 'NONE',  ( -20.54999999999999716, -8.999999999988846255, -177.3939691226524076 ) ) ;
#35019=CARTESIAN_POINT ( 'NONE',  ( -20.00857864376270001, 9.250000000011157297, -188.7499999999999716 ) ) ;
#35025=DIRECTION ( 'NONE',  ( 0.000000000000000000, 0.000000000000000000, -1.000000000000000000 ) ) ;
#35026=VERTEX_POINT ( 'NONE', #193556 ) ;
#35035=CARTESIAN_POINT ( 'NONE',  ( 20.22894356738451194, 9.278498222849622223, -175.7685229062464600 ) ) ;
#35063=CARTESIAN_POINT ( 'NONE',  ( -18.39999999999999858, -9.499999999988851584, -207.6001893912219884 ) ) ;
#35069=ORIENTED_EDGE ( 'NONE', *, *, #685, .T. ) ;
#35095=CARTESIAN_POINT ( 'NONE',  ( -23.15000000000000213, -11.64999999998884483, -197.9999999999999432 ) ) ;
#35096=DIRECTION ( 'NONE',  ( 0.000000000000000000, 1.000000000000000000, 0.000000000000000000 ) ) ;
#35123=AXIS2_PLACEMENT_3D ( 'NONE', #154015, #233517, #173579 ) ;
#35143=ORIENTED_EDGE ( 'NONE', *, *, #175416, .T. ) ;
#35164=DIRECTION ( 'NONE',  ( 0.000000000000000000, 0.8660254037844384856, -0.5000000000000003331 ) ) ;
#35170=AXIS2_PLACEMENT_3D ( 'NONE', #163720, #43765, #123313 ) ;
#35208=DIRECTION ( 'NONE',  ( 0.000000000000000000, 0.7397360091702755991, -0.6728971962616832059 ) ) ;
#35216=CARTESIAN_POINT ( 'NONE',  ( -18.59999999999999787, -1.162701749926853712, -175.5999999999999659 ) ) ;
#35240=CIRCLE ( 'NONE', #226726, 1.900000000000012790 ) ;
#35257=ADVANCED_FACE ( 'NONE', ( #229795 ), #171162, .T. ) ;
#35275=CARTESIAN_POINT ( 'NONE',  ( -23.15000000000000213, 4.350000000011156054, -188.8499999999999659 ) ) ;
#35283=EDGE_CURVE ( 'NONE', #86816, #64487, #29074, .T. ) ;
#35289=VECTOR ( 'NONE', #219068, 1000.000000000000000 ) ;
#35290=DIRECTION ( 'NONE',  ( 0.000000000000000000, 1.000000000000000000, 0.000000000000000000 ) ) ;
#35315=AXIS2_PLACEMENT_3D ( 'NONE', #134116, #170752, #96272 ) ;
#35316=CARTESIAN_POINT ( 'NONE',  ( -22.39999999999999858, 11.65000000001115588, -167.3999999999999773 ) ) ;
#35340=DIRECTION ( 'NONE',  ( 0.000000000000000000, 0.000000000000000000, 1.000000000000000000 ) ) ;
#35359=DIRECTION ( 'NONE',  ( 0.000000000000000000, 1.000000000000000000, 0.000000000000000000 ) ) ;
#35377=DIRECTION ( 'NONE',  ( 1.000000000000000000, 0.000000000000000000, 0.000000000000000000 ) ) ;
#35414=CARTESIAN_POINT ( 'NONE',  ( 20.94999999999999929, 5.000000000011153745, -188.9947339810868812 ) ) ;
#35446=TOROIDAL_SURFACE ( 'NONE', #89376, 7.800000000000000711, 0.1000000000000000056 ) ;
#35487=AXIS2_PLACEMENT_3D ( 'NONE', #35978, #115491, #118063 ) ;
#35506=DIRECTION ( 'NONE',  ( 0.000000000000000000, 0.000000000000000000, -1.000000000000000000 ) ) ;
#35516=DIRECTION ( 'NONE',  ( 1.000000000000000000, 0.000000000000000000, 0.000000000000000000 ) ) ;
#35533=LINE ( 'NONE', #150318, #131883 ) ;
#35558=CARTESIAN_POINT ( 'NONE',  ( 19.94784844284930969, 11.71308993304057999, -192.2021987172990407 ) ) ;
#35560=LINE ( 'NONE', #216728, #177374 ) ;
#35568=ORIENTED_EDGE ( 'NONE', *, *, #11070, .T. ) ;
#35580=CARTESIAN_POINT ( 'NONE',  ( 23.14999999999999858, 1.115600667400684642E-11, -200.9999999999999432 ) ) ;
#35581=CARTESIAN_POINT ( 'NONE',  ( 23.24999999999999289, 11.75000000001116263, -155.7499999999999716 ) ) ;
#35586=AXIS2_PLACEMENT_3D ( 'NONE', #50139, #11031, #185807 ) ;
#35589=AXIS2_PLACEMENT_3D ( 'NONE', #98786, #58385, #217471 ) ;
#35591=EDGE_CURVE ( 'NONE', #64290, #63066, #212033, .T. ) ;
#35668=DIRECTION ( 'NONE',  ( -0.000000000000000000, -0.000000000000000000, 1.000000000000000000 ) ) ;
#35683=EDGE_LOOP ( 'NONE', ( #160800, #55527, #110988, #85239 ) ) ;
#35706=DIRECTION ( 'NONE',  ( 0.000000000000000000, 0.000000000000000000, -1.000000000000000000 ) ) ;
#35719=EDGE_CURVE ( 'NONE', #226840, #225164, #104030, .T. ) ;
#35738=DIRECTION ( 'NONE',  ( 0.000000000000000000, 0.000000000000000000, -1.000000000000000000 ) ) ;
#35808=CARTESIAN_POINT ( 'NONE',  ( -20.64999999999999858, 7.250000000011155521, -188.7499999999999716 ) ) ;
#35811=AXIS2_PLACEMENT_3D ( 'NONE', #67935, #30118, #48369 ) ;
#35813=LINE ( 'NONE', #253538, #249984 ) ;
#35825=EDGE_LOOP ( 'NONE', ( #179931, #37151, #236753 ) ) ;
#35837=CIRCLE ( 'NONE', #44213, 2.100000000000002309 ) ;
#35838=EDGE_LOOP ( 'NONE', ( #48241, #232953, #44014, #122025 ) ) ;
#35894=FACE_OUTER_BOUND ( 'NONE', #118634, .T. ) ;
#35955=ORIENTED_EDGE ( 'NONE', *, *, #183774, .T. ) ;
#35978=CARTESIAN_POINT ( 'NONE',  ( -20.64999999999999858, -8.730841121484170131, -191.4019252810156217 ) ) ;
#35980=EDGE_LOOP ( 'NONE', ( #6630, #27379, #122585, #218785 ) ) ;
#36019=VERTEX_POINT ( 'NONE', #153210 ) ;
#36032=AXIS2_PLACEMENT_3D ( 'NONE', #81378, #120568, #243053 ) ;
#36034=ORIENTED_EDGE ( 'NONE', *, *, #49517, .T. ) ;
#36061=ORIENTED_EDGE ( 'NONE', *, *, #218231, .F. ) ;
#36065=ADVANCED_FACE ( 'NONE', ( #110186 ), #48700, .F. ) ;
#36105=VERTEX_POINT ( 'NONE', #155776 ) ;
#36143=EDGE_CURVE ( 'NONE', #239004, #245309, #66066, .T. ) ;
#36166=CYLINDRICAL_SURFACE ( 'NONE', #146161, 0.09999999999999939493 ) ;
#36169=EDGE_CURVE ( 'NONE', #131901, #41100, #28710, .T. ) ;
#36172=CIRCLE ( 'NONE', #56968, 0.4000000000000114575 ) ;
#36182=CARTESIAN_POINT ( 'NONE',  ( -20.54999999999999716, 1.940186915899009490, -180.3291192110532961 ) ) ;
#36189=CARTESIAN_POINT ( 'NONE',  ( -21.05000000000000071, -11.48912529306490349, -170.5999999999999659 ) ) ;
#36203=DIRECTION ( 'NONE',  ( 1.000000000000000000, -7.304098846218133681E-16, 0.000000000000000000 ) ) ;
#36214=CARTESIAN_POINT ( 'NONE',  ( -18.59999999999999787, 1.115600667400684642E-11, -208.8999999999999488 ) ) ;
#36234=AXIS2_PLACEMENT_3D ( 'NONE', #3821, #247566, #205866 ) ;
#36243=DIRECTION ( 'NONE',  ( 0.000000000000000000, 0.000000000000000000, -1.000000000000000000 ) ) ;
#36245=DIRECTION ( 'NONE',  ( 0.000000000000000000, 0.008583690987127625890, 0.9999631594459055250 ) ) ;
#36263=LINE ( 'NONE', #192756, #20224 ) ;
#36279=DIRECTION ( 'NONE',  ( 0.000000000000000000, -0.8700118002898359348, 0.4930308989875165082 ) ) ;
#36297=DIRECTION ( 'NONE',  ( -1.000000000000000000, 0.000000000000000000, 0.000000000000000000 ) ) ;
#36306=AXIS2_PLACEMENT_3D ( 'NONE', #153021, #232546, #34347 ) ;
#36321=CARTESIAN_POINT ( 'NONE',  ( 18.39999999999999858, -9.682403433465241349, -207.6568433774127413 ) ) ;
#36345=EDGE_LOOP ( 'NONE', ( #65662, #168322, #21506, #68213 ) ) ;
#36368=CARTESIAN_POINT ( 'NONE',  ( -18.59999999999999787, 11.65000000001115232, -179.6499999999999773 ) ) ;
#36444=AXIS2_PLACEMENT_3D ( 'NONE', #131438, #31101, #213534 ) ;
#36457=EDGE_LOOP ( 'NONE', ( #43068, #134019, #117982, #228813, #53937 ) ) ;
#36506=CARTESIAN_POINT ( 'NONE',  ( -20.94999999999999929, 11.75000000001115197, -174.5148057706539930 ) ) ;
#36518=( BOUNDED_CURVE ( )  B_SPLINE_CURVE ( 3, ( #241389, #67867, #105684, #163140 ),
 .UNSPECIFIED., .F., .F. ) 
 B_SPLINE_CURVE_WITH_KNOTS ( ( 4, 4 ),
 ( 4.712388980384689674, 6.283185307179586232 ),
 .UNSPECIFIED. ) 
 CURVE ( )  GEOMETRIC_REPRESENTATION_ITEM ( )  RATIONAL_B_SPLINE_CURVE ( ( 1.000000000000000000, 0.8047378541243649375, 0.8047378541243649375, 1.000000000000000000 ) ) 
 REPRESENTATION_ITEM ( '' )  );
#36523=CIRCLE ( 'NONE', #165500, 0.09999999999998898659 ) ;
#36553=EDGE_CURVE ( 'NONE', #178255, #156566, #182980, .T. ) ;
#36584=CARTESIAN_POINT ( 'NONE',  ( -21.65000000000000213, 7.708578643773852157, -188.7499999999999716 ) ) ;
#36603=ORIENTED_EDGE ( 'NONE', *, *, #61390, .T. ) ;
#36638=DIRECTION ( 'NONE',  ( 0.000000000000000000, -0.000000000000000000, 1.000000000000000000 ) ) ;
#36654=CYLINDRICAL_SURFACE ( 'NONE', #210597, 0.09999999999999939493 ) ;
#36675=EDGE_CURVE ( 'NONE', #180615, #66806, #107958, .T. ) ;
#36703=EDGE_LOOP ( 'NONE', ( #121744, #16073, #169454, #56547 ) ) ;
#36747=VERTEX_POINT ( 'NONE', #202281 ) ;
#36758=ADVANCED_FACE ( 'NONE', ( #159318 ), #5326, .T. ) ;
#36824=DIRECTION ( 'NONE',  ( 0.000000000000000000, 0.000000000000000000, -1.000000000000000000 ) ) ;
#36831=DIRECTION ( 'NONE',  ( 0.000000000000000000, 0.9908441862701600211, -0.1350103645451876666 ) ) ;
#36848=CARTESIAN_POINT ( 'NONE',  ( 20.00000000000000355, 11.75000000001116263, -192.1499999999999488 ) ) ;
#36855=CYLINDRICAL_SURFACE ( 'NONE', #87637, 0.09999999999999939493 ) ;
#36871=EDGE_CURVE ( 'NONE', #50484, #80866, #191378, .T. ) ;
#36881=CARTESIAN_POINT ( 'NONE',  ( -23.15000000000000213, -11.41227409413852811, -197.9999999999999432 ) ) ;
#36895=PLANE ( 'NONE',  #84153 ) ;
#36897=ADVANCED_FACE ( 'NONE', ( #10509 ), #213965, .T. ) ;
#36913=AXIS2_PLACEMENT_3D ( 'NONE', #101917, #116389, #195936 ) ;
#36924=CARTESIAN_POINT ( 'NONE',  ( 20.02499999999999858, 9.750000000011153745, -188.7499999999999716 ) ) ;
#36950=ORIENTED_EDGE ( 'NONE', *, *, #168436, .F. ) ;
#36997=CARTESIAN_POINT ( 'NONE',  ( -20.64999999999999858, -8.999999999988844479, -191.1060308773475356 ) ) ;
#37041=DIRECTION ( 'NONE',  ( -1.000000000000000000, -3.265361837132813093E-16, 0.000000000000000000 ) ) ;
#37059=LINE ( 'NONE', #182656, #143278 ) ;
#37092=EDGE_LOOP ( 'NONE', ( #28954, #181901, #214703, #29041 ) ) ;
#37093=CARTESIAN_POINT ( 'NONE',  ( 23.24999999999999645, 1.115600667400684642E-11, -167.4999999999999716 ) ) ;
#37142=EDGE_LOOP ( 'NONE', ( #154522, #105486, #231738, #148627 ) ) ;
#37151=ORIENTED_EDGE ( 'NONE', *, *, #242193, .T. ) ;
#37173=DIRECTION ( 'NONE',  ( 3.469446951953635015E-14, -0.000000000000000000, 1.000000000000000000 ) ) ;
#37179=CARTESIAN_POINT ( 'NONE',  ( -23.15000000000000213, 1.115600667400684642E-11, -200.9999999999999432 ) ) ;
#37184=CARTESIAN_POINT ( 'NONE',  ( -20.64999999999999858, 2.000000000011154189, -180.7246219227620543 ) ) ;
#37190=DIRECTION ( 'NONE',  ( 0.000000000000000000, 0.008583690987128059571, -0.9999631594459056361 ) ) ;
#37227=ORIENTED_EDGE ( 'NONE', *, *, #26353, .T. ) ;
#37235=CARTESIAN_POINT ( 'NONE',  ( 18.59999999999999076, 1.835341550235567887, -179.1551512925629197 ) ) ;
#37386=ORIENTED_EDGE ( 'NONE', *, *, #245045, .T. ) ;
#37393=CIRCLE ( 'NONE', #112230, 0.09999999999999939493 ) ;
#37419=ORIENTED_EDGE ( 'NONE', *, *, #44960, .F. ) ;
#37461=DIRECTION ( 'NONE',  ( 1.000000000000000000, 0.000000000000000000, 0.000000000000000000 ) ) ;
#37470=DIRECTION ( 'NONE',  ( 0.000000000000000000, -0.000000000000000000, -1.000000000000000000 ) ) ;
#37496=ORIENTED_EDGE ( 'NONE', *, *, #228508, .F. ) ;
#37540=EDGE_CURVE ( 'NONE', #234897, #48993, #1829, .T. ) ;
#37543=AXIS2_PLACEMENT_3D ( 'NONE', #175703, #80390, #141676 ) ;
#37561=EDGE_CURVE ( 'NONE', #139380, #202001, #254053, .T. ) ;
#37568=ORIENTED_EDGE ( 'NONE', *, *, #76993, .F. ) ;
#37589=ORIENTED_EDGE ( 'NONE', *, *, #12032, .F. ) ;
#37594=VECTOR ( 'NONE', #217442, 1000.000000000000000 ) ;
#37637=CARTESIAN_POINT ( 'NONE',  ( -20.94999999999999929, 7.070967871809997973, -204.7465642218682547 ) ) ;
#37650=EDGE_CURVE ( 'NONE', #190860, #154754, #4440, .T. ) ;
#37674=CARTESIAN_POINT ( 'NONE',  ( -21.08884785362073089, 0.04978309507788075683, -161.1428066325743487 ) ) ;
#37737=ORIENTED_EDGE ( 'NONE', *, *, #110029, .T. ) ;
#37836=ORIENTED_EDGE ( 'NONE', *, *, #193503, .F. ) ;
#37840=ADVANCED_FACE ( 'NONE', ( #214177 ), #36855, .T. ) ;
#37841=DIRECTION ( 'NONE',  ( -1.000000000000000000, -2.952720810173289112E-16, 0.000000000000000000 ) ) ;
#37847=CARTESIAN_POINT ( 'NONE',  ( 20.94999999999999929, 1.115600667400684642E-11, -167.4999999999999716 ) ) ;
#37904=CIRCLE ( 'NONE', #116990, 0.09999999999998898659 ) ;
#37906=CIRCLE ( 'NONE', #92595, 11.64999999999999325 ) ;
#37975=EDGE_CURVE ( 'NONE', #214529, #3198, #200263, .T. ) ;
#37983=ORIENTED_EDGE ( 'NONE', *, *, #49809, .F. ) ;
#37996=ORIENTED_EDGE ( 'NONE', *, *, #5732, .F. ) ;
#38013=DIRECTION ( 'NONE',  ( 1.000000000000000000, -0.000000000000000000, -0.000000000000000000 ) ) ;
#38021=ORIENTED_EDGE ( 'NONE', *, *, #134465, .F. ) ;
#38028=ORIENTED_EDGE ( 'NONE', *, *, #5773, .F. ) ;
#38037=DIRECTION ( 'NONE',  ( 0.000000000000000000, 0.000000000000000000, -1.000000000000000000 ) ) ;
#38070=DIRECTION ( 'NONE',  ( 1.000000000000000000, 0.000000000000000000, 0.000000000000000000 ) ) ;
#38101=CARTESIAN_POINT ( 'NONE',  ( -18.50000000000000000, -9.399999999988850163, -207.9146583429696307 ) ) ;
#38185=EDGE_CURVE ( 'NONE', #76578, #156526, #8729, .T. ) ;
#38207=DIRECTION ( 'NONE',  ( 0.000000000000000000, -1.000000000000000000, -0.000000000000000000 ) ) ;
#38244=CARTESIAN_POINT ( 'NONE',  ( -21.44999999999999929, 7.150000000011155876, -188.6499999999999488 ) ) ;
#38251=CIRCLE ( 'NONE', #163166, 0.2000000000000057288 ) ;
#38253=CIRCLE ( 'NONE', #113258, 0.09999999999998898659 ) ;
#38265=ORIENTED_EDGE ( 'NONE', *, *, #144059, .T. ) ;
#38271=ORIENTED_EDGE ( 'NONE', *, *, #236125, .F. ) ;
#38313=AXIS2_PLACEMENT_3D ( 'NONE', #85798, #87106, #3731 ) ;
#38359=FACE_OUTER_BOUND ( 'NONE', #11676, .T. ) ;
#38378=AXIS2_PLACEMENT_3D ( 'NONE', #170951, #130477, #165783 ) ;
#38405=ORIENTED_EDGE ( 'NONE', *, *, #65045, .T. ) ;
#38416=ORIENTED_EDGE ( 'NONE', *, *, #192329, .T. ) ;
#38464=CARTESIAN_POINT ( 'NONE',  ( 20.95575313997065336, 10.61455330328599089, -175.1212907019447869 ) ) ;
#38475=EDGE_CURVE ( 'NONE', #64282, #138184, #63534, .T. ) ;
#38476=VERTEX_POINT ( 'NONE', #236615 ) ;
#38499=TOROIDAL_SURFACE ( 'NONE', #21930, 4.149999999999999467, 0.1000000000000000056 ) ;
#38502=EDGE_CURVE ( 'NONE', #135423, #119397, #197446, .T. ) ;
#38509=ORIENTED_EDGE ( 'NONE', *, *, #142255, .T. ) ;
#38511=CIRCLE ( 'NONE', #113522, 0.09999999999998898659 ) ;
#38517=CIRCLE ( 'NONE', #42609, 0.09999999999999817368 ) ;
#38522=CARTESIAN_POINT ( 'NONE',  ( 19.75857864376268935, 11.75000000001115907, -192.3499999999999659 ) ) ;
#38524=DIRECTION ( 'NONE',  ( -0.7071067811865388020, 0.7071067811865561215, 0.000000000000000000 ) ) ;
#38606=PLANE ( 'NONE',  #81723 ) ;
#38626=DIRECTION ( 'NONE',  ( 0.000000000000000000, 0.000000000000000000, 1.000000000000000000 ) ) ;
#38647=CARTESIAN_POINT ( 'NONE',  ( 20.85000000000000142, -1.851617760457748618, -212.6031897196036198 ) ) ;
#38695=EDGE_CURVE ( 'NONE', #100214, #16283, #64418, .T. ) ;
#38715=CARTESIAN_POINT ( 'NONE',  ( 21.04999999999999716, -0.01454569055804403460, -161.0029822135684867 ) ) ;
#38722=CARTESIAN_POINT ( 'NONE',  ( -18.59999999999999787, 1.637172712981537659, -179.0821533654719815 ) ) ;
#38733=VECTOR ( 'NONE', #4480, 1000.000000000000227 ) ;
#38746=DIRECTION ( 'NONE',  ( 0.000000000000000000, -1.000000000000000000, 0.000000000000000000 ) ) ;
#38754=DIRECTION ( 'NONE',  ( 0.000000000000000000, 1.000000000000000000, 0.000000000000000000 ) ) ;
#38784=AXIS2_PLACEMENT_3D ( 'NONE', #170332, #131150, #210691 ) ;
#38811=DIRECTION ( 'NONE',  ( 0.000000000000000000, -2.255140518769784599E-13, 1.000000000000000000 ) ) ;
#38827=CARTESIAN_POINT ( 'NONE',  ( -23.15000000000000213, 1.115600667400684642E-11, -200.9999999999999432 ) ) ;
#38884=CARTESIAN_POINT ( 'NONE',  ( 18.60000000000000142, -9.523946312306554418, -207.8820279953382055 ) ) ;
#38886=VERTEX_POINT ( 'NONE', #109950 ) ;
#38888=CARTESIAN_POINT ( 'NONE',  ( 18.59999999999999076, 11.65000000001115943, -200.9999999999999432 ) ) ;
#38900=VECTOR ( 'NONE', #191208, 1000.000000000000000 ) ;
#38904=DIRECTION ( 'NONE',  ( 1.000000000000000000, 0.000000000000000000, 0.000000000000000000 ) ) ;
#38909=CARTESIAN_POINT ( 'NONE',  ( 23.14999999999999858, 1.115600667400684642E-11, -200.9999999999999432 ) ) ;
#38963=CARTESIAN_POINT ( 'NONE',  ( -23.15000000000000213, -11.48912529306489994, -197.8999999999999773 ) ) ;
#38966=ORIENTED_EDGE ( 'NONE', *, *, #184685, .F. ) ;
#39003=LINE ( 'NONE', #118547, #96982 ) ;
#39022=AXIS2_PLACEMENT_3D ( 'NONE', #2757, #236246, #40666 ) ;
#39072=LINE ( 'NONE', #98987, #165430 ) ;
#39074=VECTOR ( 'NONE', #33218, 1000.000000000000000 ) ;
#39079=ORIENTED_EDGE ( 'NONE', *, *, #33590, .F. ) ;
#39139=DIRECTION ( 'NONE',  ( -0.000000000000000000, -0.000000000000000000, 1.000000000000000000 ) ) ;
#39147=DIRECTION ( 'NONE',  ( -2.952720810173288619E-16, 1.000000000000000000, 0.000000000000000000 ) ) ;
#39156=EDGE_CURVE ( 'NONE', #83655, #57200, #113975, .T. ) ;
#39170=DIRECTION ( 'NONE',  ( 0.000000000000000000, 1.000000000000000000, 0.000000000000000000 ) ) ;
#39199=ORIENTED_EDGE ( 'NONE', *, *, #63270, .F. ) ;
#39205=CARTESIAN_POINT ( 'NONE',  ( -23.15000000000000213, -8.999999999988846255, -177.3939691226524076 ) ) ;
#39220=ORIENTED_EDGE ( 'NONE', *, *, #88663, .T. ) ;
#39245=ORIENTED_EDGE ( 'NONE', *, *, #49482, .T. ) ;
#39294=CARTESIAN_POINT ( 'NONE',  ( -21.07954763557309619, 0.06587591862965960776, -161.1707090099635593 ) ) ;
#39400=CARTESIAN_POINT ( 'NONE',  ( -18.54159361262948380, -9.463132135481973961, -174.5491222162928580 ) ) ;
#39439=DIRECTION ( 'NONE',  ( 1.000000000000000000, 0.000000000000000000, 0.000000000000000000 ) ) ;
#39478=CARTESIAN_POINT ( 'NONE',  ( -22.24259225415828567, 7.491937870576586889, -167.4009341165471199 ) ) ;
#39511=CARTESIAN_POINT ( 'NONE',  ( 18.59999999999999787, -9.321008403350148797, -174.7359382490778330 ) ) ;
#39521=DIRECTION ( 'NONE',  ( -1.000000000000000000, 0.000000000000000000, 0.000000000000000000 ) ) ;
#39529=AXIS2_PLACEMENT_3D ( 'NONE', #77050, #156636, #236130 ) ;
#39532=TOROIDAL_SURFACE ( 'NONE', #93658, 11.70000000000000107, 0.1000000000000000056 ) ;
#39550=ORIENTED_EDGE ( 'NONE', *, *, #237255, .F. ) ;
#39596=CARTESIAN_POINT ( 'NONE',  ( 20.94999999999999929, 14.05000000001115623, -195.4863049292390542 ) ) ;
#39612=VERTEX_POINT ( 'NONE', #225422 ) ;
#39627=EDGE_LOOP ( 'NONE', ( #18681, #30988, #38405, #203410 ) ) ;
#39644=SPHERICAL_SURFACE ( 'NONE', #97639, 0.1000000000000000056 ) ;
#39657=ADVANCED_FACE ( 'NONE', ( #252692 ), #228016, .F. ) ;
#39663=CARTESIAN_POINT ( 'NONE',  ( -18.50596464788227635, 10.30632246271647112, -206.5041836778895572 ) ) ;
#39669=VERTEX_POINT ( 'NONE', #251428 ) ;
#39672=CARTESIAN_POINT ( 'NONE',  ( -22.49806830649814415, 11.64988965485023620, -167.4225356836744538 ) ) ;
#39691=ORIENTED_EDGE ( 'NONE', *, *, #36553, .F. ) ;
#39702=AXIS2_PLACEMENT_3D ( 'NONE', #80625, #2374, #221415 ) ;
#39714=DIRECTION ( 'NONE',  ( -2.952720810173289112E-16, 1.000000000000000000, 0.000000000000000000 ) ) ;
#39721=AXIS2_PLACEMENT_3D ( 'NONE', #59108, #240365, #139946 ) ;
#39729=CIRCLE ( 'NONE', #2263, 0.09999999999998898659 ) ;
#39752=DIRECTION ( 'NONE',  ( 0.000000000000000000, 1.000000000000000000, 0.000000000000000000 ) ) ;
#39754=CARTESIAN_POINT ( 'NONE',  ( 20.94999999999999929, 10.47338541492405106, -175.0786544642485012 ) ) ;
#39767=AXIS2_PLACEMENT_3D ( 'NONE', #79258, #177129, #77986 ) ;
#39770=EDGE_CURVE ( 'NONE', #95048, #184932, #112908, .T. ) ;
#39777=DIRECTION ( 'NONE',  ( -1.000000000000000000, 0.000000000000000000, 0.000000000000000000 ) ) ;
#39778=LINE ( 'NONE', #137544, #241282 ) ;
#39779=DIRECTION ( 'NONE',  ( -1.000000000000000000, -2.952720810173289112E-16, 0.000000000000000000 ) ) ;
#39785=EDGE_CURVE ( 'NONE', #5557, #17415, #202674, .T. ) ;
#39800=EDGE_CURVE ( 'NONE', #45677, #83250, #184392, .T. ) ;
#39834=CARTESIAN_POINT ( 'NONE',  ( -18.50000000000000000, -1.866714910046153308, -179.2526752462819672 ) ) ;
#39846=AXIS2_PLACEMENT_3D ( 'NONE', #65868, #84093, #64577 ) ;
#39877=LINE ( 'NONE', #21585, #26621 ) ;
#39891=DIRECTION ( 'NONE',  ( -0.000000000000000000, -1.000000000000000000, -0.000000000000000000 ) ) ;
#39935=CARTESIAN_POINT ( 'NONE',  ( -18.50000000000000000, 7.021664781911246322, -204.6335654018972434 ) ) ;
#39969=CARTESIAN_POINT ( 'NONE',  ( -20.94999999999999929, -1.135018845899022466, -208.7169768834322952 ) ) ;
#39982=FACE_OUTER_BOUND ( 'NONE', #149172, .T. ) ;
#40003=ORIENTED_EDGE ( 'NONE', *, *, #110922, .T. ) ;
#40019=DIRECTION ( 'NONE',  ( 1.000000000000000000, -0.000000000000000000, -0.000000000000000000 ) ) ;
#40040=ORIENTED_EDGE ( 'NONE', *, *, #196112, .T. ) ;
#40043=FACE_OUTER_BOUND ( 'NONE', #53070, .T. ) ;
#40057=CIRCLE ( 'NONE', #114856, 0.5000000000000004441 ) ;
#40061=DIRECTION ( 'NONE',  ( 0.000000000000000000, 0.000000000000000000, -1.000000000000000000 ) ) ;
#40083=CARTESIAN_POINT ( 'NONE',  ( 21.05000000000000071, 10.72371710471867701, -179.6499999999999773 ) ) ;
#40087=ORIENTED_EDGE ( 'NONE', *, *, #119145, .F. ) ;
#40110=EDGE_CURVE ( 'NONE', #236598, #411, #32557, .T. ) ;
#40116=DIRECTION ( 'NONE',  ( -0.000000000000000000, -0.1298341882520022694, -0.9915357197604853789 ) ) ;
#40120=EDGE_LOOP ( 'NONE', ( #153878, #142177, #50541, #162915 ) ) ;
#40127=AXIS2_PLACEMENT_3D ( 'NONE', #29922, #74199, #12931 ) ;
#40131=AXIS2_PLACEMENT_3D ( 'NONE', #12731, #32293, #114371 ) ;
#40152=ORIENTED_EDGE ( 'NONE', *, *, #153434, .T. ) ;
#40158=ORIENTED_EDGE ( 'NONE', *, *, #146497, .T. ) ;
#40162=AXIS2_PLACEMENT_3D ( 'NONE', #71353, #150866, #99846 ) ;
#40224=VECTOR ( 'NONE', #51513, 1000.000000000000000 ) ;
#40236=COLOUR_RGB ( '', 0.09019608, 0.27058824, 0.51372549) ;
#40260=CARTESIAN_POINT ( 'NONE',  ( -23.25000000000000000, 1.115600667400684642E-11, -167.4999999999999716 ) ) ;
#40262=DIRECTION ( 'NONE',  ( 1.000000000000000000, 0.000000000000000000, 0.000000000000000000 ) ) ;
#40302=EDGE_CURVE ( 'NONE', #56169, #82821, #82550, .T. ) ;
#40346=DIRECTION ( 'NONE',  ( -1.000000000000000000, 0.000000000000000000, 0.000000000000000000 ) ) ;
#40348=DIRECTION ( 'NONE',  ( 1.000000000000000000, 0.000000000000000000, 0.000000000000000000 ) ) ;
#40369=DIRECTION ( 'NONE',  ( 0.000000000000000000, 0.000000000000000000, -1.000000000000000000 ) ) ;
#40398=CARTESIAN_POINT ( 'NONE',  ( -20.94999999999999929, 6.846123162363745074, -204.7377262668498190 ) ) ;
#40405=DIRECTION ( 'NONE',  ( 0.000000000000000000, 0.000000000000000000, 1.000000000000000000 ) ) ;
#40412=FACE_OUTER_BOUND ( 'NONE', #169665, .T. ) ;
#40482=FACE_OUTER_BOUND ( 'NONE', #255571, .T. ) ;
#40488=DIRECTION ( 'NONE',  ( 1.000000000000000000, 0.000000000000000000, 0.000000000000000000 ) ) ;
#40558=EDGE_LOOP ( 'NONE', ( #162912, #206672, #220961, #132691, #30279, #226450, #160997, #118471 ) ) ;
#40560=FACE_OUTER_BOUND ( 'NONE', #226939, .T. ) ;
#40579=CARTESIAN_POINT ( 'NONE',  ( 21.30740335185486245, 6.556657922039159203, -167.4010654742241115 ) ) ;
#40648=VECTOR ( 'NONE', #79576, 1000.000000000000000 ) ;
#40661=LINE ( 'NONE', #97992, #178891 ) ;
#40666=DIRECTION ( 'NONE',  ( 0.000000000000000000, 0.000000000000000000, 1.000000000000000000 ) ) ;
#40683=VECTOR ( 'NONE', #106084, 1000.000000000000000 ) ;
#40686=EDGE_CURVE ( 'NONE', #177487, #131118, #128570, .T. ) ;
#40714=ORIENTED_EDGE ( 'NONE', *, *, #241883, .T. ) ;
#40725=FACE_OUTER_BOUND ( 'NONE', #54511, .T. ) ;
#40789=CARTESIAN_POINT ( 'NONE',  ( 18.50000000000000355, -9.421456145484540912, -174.7419820840196110 ) ) ;
#40807=VECTOR ( 'NONE', #122850, 1000.000000000000000 ) ;
#40808=VECTOR ( 'NONE', #182959, 1000.000000000000000 ) ;
#40810=DIRECTION ( 'NONE',  ( 0.000000000000000000, 0.000000000000000000, 1.000000000000000000 ) ) ;
#40811=CIRCLE ( 'NONE', #32440, 0.09999999999999158173 ) ;
#40813=CIRCLE ( 'NONE', #161617, 4.299999999999970512 ) ;
#40820=TOROIDAL_SURFACE ( 'NONE', #165713, 0.6000000000000004219, 0.1000000000000000056 ) ;
#40908=CIRCLE ( 'NONE', #207488, 0.09999999999999939493 ) ;
#40909=VECTOR ( 'NONE', #34803, 1000.000000000000000 ) ;
#40983=CIRCLE ( 'NONE', #27963, 0.09999999999999817368 ) ;
#40986=DIRECTION ( 'NONE',  ( 1.000000000000000000, 0.000000000000000000, 0.000000000000000000 ) ) ;
#40991=FACE_OUTER_BOUND ( 'NONE', #183377, .T. ) ;
#41020=AXIS2_PLACEMENT_3D ( 'NONE', #238593, #117369, #119965 ) ;
#41024=CARTESIAN_POINT ( 'NONE',  ( 21.05281448260627641, 8.776010158548784190, -179.6735579118114003 ) ) ;
#41030=EDGE_CURVE ( 'NONE', #16193, #44391, #12067, .T. ) ;
#41040=CARTESIAN_POINT ( 'NONE',  ( -23.25000000000000000, 1.115600667400684642E-11, -171.6499999999999773 ) ) ;
#41045=VECTOR ( 'NONE', #46263, 1000.000000000000000 ) ;
#41078=CARTESIAN_POINT ( 'NONE',  ( -23.15000000000000213, -4.831324760611774849, -184.4696969421987376 ) ) ;
#41091=CARTESIAN_POINT ( 'NONE',  ( 20.94999999999999574, 1.736257131608553550, -179.0686523290174819 ) ) ;
#41100=VERTEX_POINT ( 'NONE', #144322 ) ;
#41136=DIRECTION ( 'NONE',  ( 1.000000000000000000, -0.000000000000000000, -0.000000000000000000 ) ) ;
#41138=ORIENTED_EDGE ( 'NONE', *, *, #2397, .F. ) ;
#41149=EDGE_LOOP ( 'NONE', ( #212661, #54918, #78325, #77571 ) ) ;
#41171=DIRECTION ( 'NONE',  ( 1.000000000000000000, 0.000000000000000000, -0.000000000000000000 ) ) ;
#41181=DIRECTION ( 'NONE',  ( 0.000000000000000000, -1.000000000000000000, 0.000000000000000000 ) ) ;
#41197=DIRECTION ( 'NONE',  ( 0.000000000000000000, 0.000000000000000000, -1.000000000000000000 ) ) ;
#41210=ORIENTED_EDGE ( 'NONE', *, *, #244547, .F. ) ;
#41237=ADVANCED_FACE ( 'NONE', ( #51639 ), #24730, .F. ) ;
#41250=VERTEX_POINT ( 'NONE', #234150 ) ;
#41275=VECTOR ( 'NONE', #157476, 1000.000000000000000 ) ;
#41296=ORIENTED_EDGE ( 'NONE', *, *, #224557, .F. ) ;
#41301=DIRECTION ( 'NONE',  ( 1.000000000000000000, 0.000000000000000000, -0.000000000000000000 ) ) ;
#41304=CARTESIAN_POINT ( 'NONE',  ( 21.05000000000000071, -0.08559286335121364664, -161.0863372651298846 ) ) ;
#41324=CYLINDRICAL_SURFACE ( 'NONE', #106975, 0.1000000000000001443 ) ;
#41328=DIRECTION ( 'NONE',  ( 0.000000000000000000, -0.9908441862701600211, -0.1350103645451876666 ) ) ;
#41338=DIRECTION ( 'NONE',  ( 1.000000000000000000, 0.000000000000000000, 0.000000000000000000 ) ) ;
#41347=AXIS2_PLACEMENT_3D ( 'NONE', #142998, #227683, #49050 ) ;
#41367=ORIENTED_EDGE ( 'NONE', *, *, #101645, .T. ) ;
#41416=DIRECTION ( 'NONE',  ( 3.469446951953635015E-14, -0.000000000000000000, 1.000000000000000000 ) ) ;
#41431=ORIENTED_EDGE ( 'NONE', *, *, #21741, .T. ) ;
#41433=ADVANCED_FACE ( 'NONE', ( #125759 ), #170490, .T. ) ;
#41453=EDGE_CURVE ( 'NONE', #160579, #6554, #79002, .T. ) ;
#41473=FACE_OUTER_BOUND ( 'NONE', #29680, .T. ) ;
#41476=CARTESIAN_POINT ( 'NONE',  ( -22.37643362114956602, 0.09908137369253962323, -159.8742100060415794 ) ) ;
#41492=ORIENTED_EDGE ( 'NONE', *, *, #152746, .F. ) ;
#41495=DIRECTION ( 'NONE',  ( -1.000000000000000000, -1.836970198721029934E-16, 0.000000000000000000 ) ) ;
#41510=AXIS2_PLACEMENT_3D ( 'NONE', #159114, #156558, #194391 ) ;
#41525=CARTESIAN_POINT ( 'NONE',  ( -21.07933241753356413, 0.09337959043041976770, -161.1713540516202272 ) ) ;
#41536=VECTOR ( 'NONE', #237558, 1000.000000000000114 ) ;
#41541=FACE_OUTER_BOUND ( 'NONE', #179097, .T. ) ;
#41568=DIRECTION ( 'NONE',  ( 3.469446951953498700E-14, -0.7899159663865300551, -0.6132151058540831201 ) ) ;
#41570=ADVANCED_FACE ( 'NONE', ( #29289 ), #176154, .T. ) ;
#41592=CARTESIAN_POINT ( 'NONE',  ( -18.59999999999999787, 7.021664781911246322, -204.8335654018972605 ) ) ;
#41653=ADVANCED_FACE ( 'NONE', ( #138263 ), #79573, .T. ) ;
#41691=CARTESIAN_POINT ( 'NONE',  ( 22.43288208788031568, 0.004899854896538673524, -155.8503481562808872 ) ) ;
#41693=AXIS2_PLACEMENT_3D ( 'NONE', #113207, #8975, #148495 ) ;
#41697=DIRECTION ( 'NONE',  ( 0.000000000000000000, 0.000000000000000000, 1.000000000000000000 ) ) ;
#41724=CYLINDRICAL_SURFACE ( 'NONE', #145325, 12.87499999999999822 ) ;
#41744=EDGE_CURVE ( 'NONE', #208902, #71184, #198251, .T. ) ;
#41753=ORIENTED_EDGE ( 'NONE', *, *, #119145, .T. ) ;
#41757=AXIS2_PLACEMENT_3D ( 'NONE', #219132, #100457, #108202 ) ;
#41794=ORIENTED_EDGE ( 'NONE', *, *, #170429, .T. ) ;
#41810=VERTEX_POINT ( 'NONE', #125157 ) ;
#41820=TOROIDAL_SURFACE ( 'NONE', #21159, 12.97499999999999609, 0.1000000000000000056 ) ;
#41823=( BOUNDED_SURFACE ( )  B_SPLINE_SURFACE ( 3, 2, ( 
 ( #162837, #143239, #24620 ),
 ( #183673, #4995, #246207 ),
 ( #50539, #130094, #68868 ),
 ( #111836, #7590, #49278 ) ),
 .UNSPECIFIED., .F., .F., .F. ) 
 B_SPLINE_SURFACE_WITH_KNOTS ( ( 4, 4 ),
 ( 3, 3 ),
 ( -1.908195823574487804E-17, 0.001979672783031562362 ),
 ( 0.000000000000000000, 1.000000000000000000 ),
 .UNSPECIFIED. ) 
 GEOMETRIC_REPRESENTATION_ITEM ( )  RATIONAL_B_SPLINE_SURFACE ( (
 ( 1.000000000000000000, 0.7103081912008197829, 1.000000000000000000),
 ( 1.000000000000000000, 0.7104998333558621981, 1.000000000000000000),
 ( 1.000000000000000000, 0.7107238315755282088, 1.000000000000000000),
 ( 1.000000000000000000, 0.7110073749539377319, 1.000000000000000000) ) ) 
 REPRESENTATION_ITEM ( '' )  SURFACE ( )  );
#41832=ORIENTED_EDGE ( 'NONE', *, *, #90309, .F. ) ;
#41859=AXIS2_PLACEMENT_3D ( 'NONE', #147904, #252120, #130890 ) ;
#41878=ORIENTED_EDGE ( 'NONE', *, *, #127673, .T. ) ;
#41884=DIRECTION ( 'NONE',  ( 1.000000000000000000, 0.000000000000000000, 0.000000000000000000 ) ) ;
#41885=ORIENTED_EDGE ( 'NONE', *, *, #200702, .F. ) ;
#41886=ORIENTED_EDGE ( 'NONE', *, *, #253274, .T. ) ;
#41892=DIRECTION ( 'NONE',  ( -1.000000000000000000, -0.000000000000000000, -0.000000000000000000 ) ) ;
#41915=FACE_OUTER_BOUND ( 'NONE', #88704, .T. ) ;
#41927=ORIENTED_EDGE ( 'NONE', *, *, #191536, .T. ) ;
#41946=CARTESIAN_POINT ( 'NONE',  ( 18.49999999999999645, -9.419078080838366063, -207.8299253502082706 ) ) ;
#41959=CIRCLE ( 'NONE', #21117, 0.09999999999998898659 ) ;
#41966=DIRECTION ( 'NONE',  ( -3.265361837132813093E-16, 1.000000000000000000, 0.000000000000000000 ) ) ;
#41967=ORIENTED_EDGE ( 'NONE', *, *, #173643, .F. ) ;
#41980=DIRECTION ( 'NONE',  ( 0.000000000000000000, 0.000000000000000000, -1.000000000000000000 ) ) ;
#41981=ORIENTED_EDGE ( 'NONE', *, *, #218304, .T. ) ;
#41984=DIRECTION ( 'NONE',  ( 0.000000000000000000, 0.9654727137038715545, -0.2605042016806676242 ) ) ;
#41987=ADVANCED_FACE ( 'NONE', ( #195199 ), #153529, .T. ) ;
#42022=ORIENTED_EDGE ( 'NONE', *, *, #127389, .F. ) ;
#42030=EDGE_CURVE ( 'NONE', #112737, #90934, #50009, .T. ) ;
#42036=CARTESIAN_POINT ( 'NONE',  ( -23.15000000000000213, 1.115600667400684642E-11, -188.1249999999999716 ) ) ;
#42087=ORIENTED_EDGE ( 'NONE', *, *, #37650, .F. ) ;
#42095=VERTEX_POINT ( 'NONE', #124621 ) ;
#42103=DIRECTION ( 'NONE',  ( 0.000000000000000000, -1.000000000000000000, 0.000000000000000000 ) ) ;
#42128=EDGE_LOOP ( 'NONE', ( #66182, #226781, #145223, #39079 ) ) ;
#42157=CARTESIAN_POINT ( 'NONE',  ( 20.94999999999999574, -11.74999999998883560, -170.5999999999999659 ) ) ;
#42174=ORIENTED_EDGE ( 'NONE', *, *, #113665, .F. ) ;
#42175=AXIS2_PLACEMENT_3D ( 'NONE', #199106, #36203, #59554 ) ;
#42178=CARTESIAN_POINT ( 'NONE',  ( -22.45305610364634674, -0.1008583690875579503, -155.7504328765105583 ) ) ;
#42183=AXIS2_PLACEMENT_3D ( 'NONE', #209717, #130163, #104175 ) ;
#42213=FACE_OUTER_BOUND ( 'NONE', #180415, .T. ) ;
#42217=DIRECTION ( 'NONE',  ( -0.000000000000000000, 0.000000000000000000, 1.000000000000000000 ) ) ;
#42254=LINE ( 'NONE', #22709, #49021 ) ;
#42259=VERTEX_POINT ( 'NONE', #226252 ) ;
#42330=EDGE_CURVE ( 'NONE', #254440, #64828, #232721, .T. ) ;
#42359=FACE_OUTER_BOUND ( 'NONE', #149403, .T. ) ;
#42371=DIRECTION ( 'NONE',  ( -1.000000000000000000, 0.000000000000000000, 0.000000000000000000 ) ) ;
#42375=EDGE_CURVE ( 'NONE', #138430, #54663, #61456, .T. ) ;
#42404=CIRCLE ( 'NONE', #188166, 0.1000000000000060701 ) ;
#42406=EDGE_CURVE ( 'NONE', #130316, #43467, #250961, .T. ) ;
#42423=CIRCLE ( 'NONE', #188181, 11.75000000000001066 ) ;
#42459=LINE ( 'NONE', #138963, #109762 ) ;
#42461=APPLICATION_CONTEXT ( 'automotive_design' ) ;
#42517=CARTESIAN_POINT ( 'NONE',  ( 21.05000000000000071, 1.835341550235569663, -179.0551512925629538 ) ) ;
#42529=EDGE_CURVE ( 'NONE', #75238, #182666, #33106, .T. ) ;
#42559=EDGE_CURVE ( 'NONE', #165621, #9380, #190412, .T. ) ;
#42562=TOROIDAL_SURFACE ( 'NONE', #26007, 0.4000000000000012990, 0.1000000000000000056 ) ;
#42582=AXIS2_PLACEMENT_3D ( 'NONE', #206158, #107038, #186609 ) ;
#42600=DIRECTION ( 'NONE',  ( -0.000000000000000000, 0.000000000000000000, 1.000000000000000000 ) ) ;
#42602=DIRECTION ( 'NONE',  ( 0.000000000000000000, 0.000000000000000000, 1.000000000000000000 ) ) ;
#42609=AXIS2_PLACEMENT_3D ( 'NONE', #193696, #157152, #155870 ) ;
#42612=VERTEX_POINT ( 'NONE', #212541 ) ;
#42619=LINE ( 'NONE', #142975, #172158 ) ;
#42647=AXIS2_PLACEMENT_3D ( 'NONE', #102237, #185675, #223497 ) ;
#42650=ORIENTED_EDGE ( 'NONE', *, *, #227737, .T. ) ;
#42656=ORIENTED_EDGE ( 'NONE', *, *, #177110, .F. ) ;
#42663=CIRCLE ( 'NONE', #96810, 0.09999999999999939493 ) ;
#42680=AXIS2_PLACEMENT_3D ( 'NONE', #132884, #70364, #10374 ) ;
#42691=CARTESIAN_POINT ( 'NONE',  ( 20.54374330479337374, 10.50501031423420351, -175.2256836348880711 ) ) ;
#42696=CARTESIAN_POINT ( 'NONE',  ( -20.94999999999999929, -11.64999999998884306, -170.5999999999999659 ) ) ;
#42703=EDGE_CURVE ( 'NONE', #183962, #249855, #149788, .T. ) ;
#42715=VERTEX_POINT ( 'NONE', #119866 ) ;
#42730=EDGE_CURVE ( 'NONE', #13008, #204451, #124820, .T. ) ;
#42731=CARTESIAN_POINT ( 'NONE',  ( -22.47071067811865319, 0.09909245471376171288, -159.7799252555019223 ) ) ;
#42732=EDGE_LOOP ( 'NONE', ( #216306, #184945, #187242, #139078 ) ) ;
#42757=CARTESIAN_POINT ( 'NONE',  ( -21.05000000000000071, -1.835341550213255957, -179.0551512925629538 ) ) ;
#42765=DIRECTION ( 'NONE',  ( 1.000000000000000000, 0.000000000000000000, 0.000000000000000000 ) ) ;
#42775=CARTESIAN_POINT ( 'NONE',  ( -20.94999999999999929, 1.835341550235569663, -179.0551512925629538 ) ) ;
#42776=ORIENTED_EDGE ( 'NONE', *, *, #214270, .F. ) ;
#42794=CIRCLE ( 'NONE', #155262, 4.000000000000003553 ) ;
#42818=ORIENTED_EDGE ( 'NONE', *, *, #234152, .F. ) ;
#42820=DIRECTION ( 'NONE',  ( -5.603264701231743991E-32, 1.897661533703520143E-16, -1.000000000000000000 ) ) ;
#42830=ORIENTED_EDGE ( 'NONE', *, *, #198237, .F. ) ;
#42851=DIRECTION ( 'NONE',  ( 4.504528286903032433E-15, -0.1298341882520124002, -0.9915357197604841577 ) ) ;
#42858=ADVANCED_FACE ( 'NONE', ( #81957 ), #124109, .T. ) ;
#42874=ORIENTED_EDGE ( 'NONE', *, *, #241963, .T. ) ;
#42878=CARTESIAN_POINT ( 'NONE',  ( -21.05000000000000071, -1.835341550213255957, -179.0551512925629538 ) ) ;
#42899=CARTESIAN_POINT ( 'NONE',  ( -18.59999999999999787, 9.350000000011156942, -188.8499999999999659 ) ) ;
#42929=VERTEX_POINT ( 'NONE', #250057 ) ;
#42932=TOROIDAL_SURFACE ( 'NONE', #30474, 0.2000000000000000111, 0.1000000000000000056 ) ;
#42939=DIRECTION ( 'NONE',  ( 1.000000000000000000, -0.000000000000000000, -0.000000000000000000 ) ) ;
#42959=CARTESIAN_POINT ( 'NONE',  ( -21.29999999999995808, 1.115650265596050101E-11, -163.4499999999999886 ) ) ;
#43010=ORIENTED_EDGE ( 'NONE', *, *, #13800, .F. ) ;
#43030=AXIS2_PLACEMENT_3D ( 'NONE', #140850, #63877, #139543 ) ;
#43032=ORIENTED_EDGE ( 'NONE', *, *, #219311, .T. ) ;
#43040=CARTESIAN_POINT ( 'NONE',  ( 21.09551895715245706, 10.62143732718000244, -179.7371246658989037 ) ) ;
#43068=ORIENTED_EDGE ( 'NONE', *, *, #244944, .F. ) ;
#43115=DIRECTION ( 'NONE',  ( 0.7071067811865474617, 0.7071067811865474617, -0.000000000000000000 ) ) ;
#43117=ORIENTED_EDGE ( 'NONE', *, *, #177579, .F. ) ;
#43129=AXIS2_PLACEMENT_3D ( 'NONE', #136708, #112043, #55872 ) ;
#43155=EDGE_LOOP ( 'NONE', ( #81197, #225301, #216675, #213159 ) ) ;
#43157=CARTESIAN_POINT ( 'NONE',  ( -23.15000000000000213, -11.64999999998884483, -197.8999999999999773 ) ) ;
#43160=CARTESIAN_POINT ( 'NONE',  ( 22.47071067811865319, 1.115600667400684642E-11, -167.4999999999999716 ) ) ;
#43178=CARTESIAN_POINT ( 'NONE',  ( -21.05000000000000071, -1.162701749926853712, -175.5999999999999659 ) ) ;
#43217=CIRCLE ( 'NONE', #255532, 0.09999999999998898659 ) ;
#43223=AXIS2_PLACEMENT_3D ( 'NONE', #22820, #7075, #24105 ) ;
#43238=DIRECTION ( 'NONE',  ( -0.000000000000000000, -0.000000000000000000, -1.000000000000000000 ) ) ;
#43252=CARTESIAN_POINT ( 'NONE',  ( 22.39999999999999858, 1.115600667400684642E-11, -167.4999999999999716 ) ) ;
#43258=VECTOR ( 'NONE', #61223, 1000.000000000000000 ) ;
#43260=DIRECTION ( 'NONE',  ( -1.000000000000000000, 0.000000000000000000, 0.000000000000000000 ) ) ;
#43279=EDGE_CURVE ( 'NONE', #215160, #172274, #90021, .T. ) ;
#43300=CIRCLE ( 'NONE', #222309, 0.09999999999999062417 ) ;
#43301=CARTESIAN_POINT ( 'NONE',  ( -21.65000000000000213, 7.708578643773852157, -179.7499999999999716 ) ) ;
#43309=DIRECTION ( 'NONE',  ( 0.000000000000000000, 0.000000000000000000, -1.000000000000000000 ) ) ;
#43312=DIRECTION ( 'NONE',  ( 1.000000000000000000, 0.000000000000000000, -0.000000000000000000 ) ) ;
#43333=CARTESIAN_POINT ( 'NONE',  ( 18.49999999999998579, -9.321008403350155902, -174.7359382490778046 ) ) ;
#43346=CARTESIAN_POINT ( 'NONE',  ( -23.15000000000000213, 1.115600667400684642E-11, -200.9999999999999432 ) ) ;
#43354=VECTOR ( 'NONE', #128658, 1000.000000000000000 ) ;
#43377=PLANE ( 'NONE',  #1667 ) ;
#43378=ORIENTED_EDGE ( 'NONE', *, *, #43396, .T. ) ;
#43379=DIRECTION ( 'NONE',  ( 0.000000000000000000, -1.000000000000000000, 0.000000000000000000 ) ) ;
#43396=EDGE_CURVE ( 'NONE', #202583, #195513, #98326, .T. ) ;
#43414=FACE_OUTER_BOUND ( 'NONE', #174579, .T. ) ;
#43415=ORIENTED_EDGE ( 'NONE', *, *, #15899, .T. ) ;
#43426=ORIENTED_EDGE ( 'NONE', *, *, #18824, .F. ) ;
#43435=EDGE_CURVE ( 'NONE', #50174, #177630, #154536, .T. ) ;
#43449=CARTESIAN_POINT ( 'NONE',  ( -22.60000000000080789, 0.04781698047652397504, -155.7499775688472710 ) ) ;
#43467=VERTEX_POINT ( 'NONE', #54104 ) ;
#43482=ORIENTED_EDGE ( 'NONE', *, *, #125220, .T. ) ;
#43498=ADVANCED_FACE ( 'NONE', ( #196191 ), #176649, .T. ) ;
#43500=CARTESIAN_POINT ( 'NONE',  ( 21.05000000000000071, 4.813084112160684214, -189.0584822434761634 ) ) ;
#43517=TOROIDAL_SURFACE ( 'NONE', #14501, 0.2000000000000000111, 0.1000000000000000056 ) ;
#43531=( LENGTH_UNIT ( ) NAMED_UNIT ( * ) SI_UNIT ( .MILLI., .METRE. ) );
#43575=ORIENTED_EDGE ( 'NONE', *, *, #51067, .T. ) ;
#43577=FACE_OUTER_BOUND ( 'NONE', #64575, .T. ) ;
#43602=LINE ( 'NONE', #181824, #78939 ) ;
#43603=CARTESIAN_POINT ( 'NONE',  ( 18.60000000000000142, -9.321008403350125704, -174.7359382490778614 ) ) ;
#43605=CARTESIAN_POINT ( 'NONE',  ( 20.95325940946048249, 10.52339007070744614, -175.0644621292400416 ) ) ;
#43625=ORIENTED_EDGE ( 'NONE', *, *, #93239, .T. ) ;
#43643=VERTEX_POINT ( 'NONE', #243009 ) ;
#43712=ADVANCED_FACE ( 'NONE', ( #128216 ), #41820, .F. ) ;
#43713=CARTESIAN_POINT ( 'NONE',  ( 21.05000000000000071, -8.730841121484166578, -191.4019252810156217 ) ) ;
#43736=EDGE_LOOP ( 'NONE', ( #240023, #71699, #155675, #123802 ) ) ;
#43746=LINE ( 'NONE', #186805, #223429 ) ;
#43752=CIRCLE ( 'NONE', #48031, 0.09999999999999939493 ) ;
#43765=DIRECTION ( 'NONE',  ( 1.000000000000000000, 2.952720810173289112E-16, -0.000000000000000000 ) ) ;
#43775=DIRECTION ( 'NONE',  ( 0.000000000000000000, 1.897661533703519897E-16, -1.000000000000000000 ) ) ;
#43791=FACE_OUTER_BOUND ( 'NONE', #57093, .T. ) ;
#43817=ADVANCED_FACE ( 'NONE', ( #154242 ), #127142, .T. ) ;
#43820=ORIENTED_EDGE ( 'NONE', *, *, #180419, .F. ) ;
#43834=EDGE_CURVE ( 'NONE', #162728, #232247, #96751, .T. ) ;
#43838=EDGE_CURVE ( 'NONE', #4264, #108752, #52507, .T. ) ;
#43883=CARTESIAN_POINT ( 'NONE',  ( 18.49999999999998934, 6.450000000011156587, -177.5170271704400022 ) ) ;
#43912=ORIENTED_EDGE ( 'NONE', *, *, #133728, .F. ) ;
#43932=CARTESIAN_POINT ( 'NONE',  ( 21.05000000000000071, 8.815201804577398548, -175.9205374966817033 ) ) ;
#43962=LINE ( 'NONE', #80480, #214157 ) ;
#43989=CARTESIAN_POINT ( 'NONE',  ( -21.14999999999999858, -11.74999999998884448, -167.4999999999999432 ) ) ;
#44014=ORIENTED_EDGE ( 'NONE', *, *, #9650, .T. ) ;
#44018=DIRECTION ( 'NONE',  ( -0.000000000000000000, 1.000000000000000000, -0.000000000000000000 ) ) ;
#44022=DIRECTION ( 'NONE',  ( 0.000000000000000000, 1.000000000000000000, -1.224646799147353207E-16 ) ) ;
#44039=ORIENTED_EDGE ( 'NONE', *, *, #107512, .T. ) ;
#44053=DIRECTION ( 'NONE',  ( 0.000000000000000000, 0.01562499999998609446, -0.9998779222360101304 ) ) ;
#44058=AXIS2_PLACEMENT_3D ( 'NONE', #247930, #169730, #171025 ) ;
#44060=ORIENTED_EDGE ( 'NONE', *, *, #109471, .F. ) ;
#44090=EDGE_CURVE ( 'NONE', #208426, #116862, #158718, .T. ) ;
#44094=EDGE_CURVE ( 'NONE', #122253, #194728, #151004, .T. ) ;
#44115=CARTESIAN_POINT ( 'NONE',  ( -21.05000000000000071, 1.116121084443477685E-11, -170.3999999999999488 ) ) ;
#44129=EDGE_CURVE ( 'NONE', #83250, #185463, #50325, .T. ) ;
#44197=ADVANCED_FACE ( 'NONE', ( #135263 ), #214811, .T. ) ;
#44209=ORIENTED_EDGE ( 'NONE', *, *, #144059, .F. ) ;
#44213=AXIS2_PLACEMENT_3D ( 'NONE', #129653, #106213, #245755 ) ;
#44222=CARTESIAN_POINT ( 'NONE',  ( 22.49999999999999645, 11.64976291804307884, -167.4111900236130452 ) ) ;
#44260=CARTESIAN_POINT ( 'NONE',  ( 20.85000000000000142, -1.263275465206102233, -208.9018646667463770 ) ) ;
#44267=DIRECTION ( 'NONE',  ( -1.000000000000000000, -0.000000000000000000, -0.000000000000000000 ) ) ;
#44269=ADVANCED_FACE ( 'NONE', ( #257735 ), #80400, .T. ) ;
#44286=CARTESIAN_POINT ( 'NONE',  ( -20.64999999999999858, -8.999999999988844479, -191.1060308773475356 ) ) ;
#44315=ORIENTED_EDGE ( 'NONE', *, *, #238079, .T. ) ;
#44332=CARTESIAN_POINT ( 'NONE',  ( -20.54999999999999716, 1.115600667400684642E-11, -202.8999999999999773 ) ) ;
#44336=AXIS2_PLACEMENT_3D ( 'NONE', #60541, #157109, #115385 ) ;
#44361=CARTESIAN_POINT ( 'NONE',  ( -20.94999999999999929, -1.261786168553869603, -175.5864989635454378 ) ) ;
#44363=DIRECTION ( 'NONE',  ( 0.000000000000000000, 0.000000000000000000, -1.000000000000000000 ) ) ;
#44391=VERTEX_POINT ( 'NONE', #105100 ) ;
#44405=DIRECTION ( 'NONE',  ( 2.952720810173289112E-16, -1.000000000000000000, 0.000000000000000000 ) ) ;
#44406=DIRECTION ( 'NONE',  ( -1.000000000000000000, -1.836970198721029934E-16, -3.186635328391151676E-31 ) ) ;
#44448=DIRECTION ( 'NONE',  ( 1.000000000000000000, 0.000000000000000000, 0.000000000000000000 ) ) ;
#44457=DIRECTION ( 'NONE',  ( 0.000000000000000000, 0.000000000000000000, 1.000000000000000000 ) ) ;
#44460=CARTESIAN_POINT ( 'NONE',  ( 23.14999999999999858, 4.813084112160680661, -179.4415177565237798 ) ) ;
#44469=ORIENTED_EDGE ( 'NONE', *, *, #231307, .T. ) ;
#44475=DIRECTION ( 'NONE',  ( 0.000000000000000000, -5.204170427930272346E-14, -1.000000000000000000 ) ) ;
#44505=DIRECTION ( 'NONE',  ( -1.000000000000000000, -2.952720810173289112E-16, 0.000000000000000000 ) ) ;
#44542=AXIS2_PLACEMENT_3D ( 'NONE', #214530, #112877, #115432 ) ;
#44543=CARTESIAN_POINT ( 'NONE',  ( 18.49999999999998934, 6.550000000011156231, -188.6499999999999488 ) ) ;
#44544=DIRECTION ( 'NONE',  ( 0.000000000000000000, 0.000000000000000000, -1.000000000000000000 ) ) ;
#44564=ORIENTED_EDGE ( 'NONE', *, *, #180396, .F. ) ;
#44572=EDGE_CURVE ( 'NONE', #133004, #168057, #225661, .T. ) ;
#44584=EDGE_CURVE ( 'NONE', #151116, #80866, #38253, .T. ) ;
#44631=AXIS2_PLACEMENT_3D ( 'NONE', #246888, #29181, #31739 ) ;
#44632=CARTESIAN_POINT ( 'NONE',  ( -20.64999999999999858, -9.399999999988846611, -191.1060308773475356 ) ) ;
#44652=CARTESIAN_POINT ( 'NONE',  ( 22.39999999999999503, 11.75000000001116263, -167.5999999999999659 ) ) ;
#44655=EDGE_CURVE ( 'NONE', #86816, #48432, #150676, .T. ) ;
#44664=DIRECTION ( 'NONE',  ( 0.000000000000000000, 0.000000000000000000, -1.000000000000000000 ) ) ;
#44686=CIRCLE ( 'NONE', #232141, 0.09999999999999817368 ) ;
#44690=ADVANCED_FACE ( 'NONE', ( #104797 ), #184360, .F. ) ;
#44741=CARTESIAN_POINT ( 'NONE',  ( -22.50485643085239928, -0.07878633906603053905, -155.7502050608275965 ) ) ;
#44823=DIRECTION ( 'NONE',  ( 0.000000000000000000, 1.734723475976997999E-14, -1.000000000000000000 ) ) ;
#44829=CARTESIAN_POINT ( 'NONE',  ( -22.39999999999999858, 11.65000000001115588, -167.3999999999999773 ) ) ;
#44840=EDGE_LOOP ( 'NONE', ( #95796, #14639, #24792, #161158, #168774 ) ) ;
#44865=CARTESIAN_POINT ( 'NONE',  ( -20.94999999999999929, -1.162701749926853712, -175.4999999999999716 ) ) ;
#44868=CARTESIAN_POINT ( 'NONE',  ( 21.10642757222115051, 10.72315628916975250, -179.7406975237851725 ) ) ;
#44871=ORIENTED_EDGE ( 'NONE', *, *, #64860, .F. ) ;
#44888=CARTESIAN_POINT ( 'NONE',  ( 18.52130828395270612, -9.481395502614638815, -174.5245067238836043 ) ) ;
#44912=DIRECTION ( 'NONE',  ( 0.000000000000000000, 0.4999999999999478195, 0.8660254037844686836 ) ) ;
#44942=DIRECTION ( 'NONE',  ( 0.000000000000000000, 0.000000000000000000, -1.000000000000000000 ) ) ;
#44960=EDGE_CURVE ( 'NONE', #234897, #20839, #125894, .T. ) ;
#44988=ADVANCED_FACE ( 'NONE', ( #98077, #75986, #18584 ), #36895, .F. ) ;
#45008=TOROIDAL_SURFACE ( 'NONE', #240834, 0.2000000000000000111, 0.1000000000000000056 ) ;
#45014=ORIENTED_EDGE ( 'NONE', *, *, #81113, .F. ) ;
#45079=EDGE_CURVE ( 'NONE', #57491, #11139, #138359, .T. ) ;
#45138=DIRECTION ( 'NONE',  ( 0.000000000000000000, 0.000000000000000000, -1.000000000000000000 ) ) ;
#45139=EDGE_LOOP ( 'NONE', ( #166836, #43117, #133927 ) ) ;
#45189=TOROIDAL_SURFACE ( 'NONE', #190973, 0.2000000000000000111, 0.1000000000000000056 ) ;
#45228=PLANE ( 'NONE',  #239196 ) ;
#45258=CARTESIAN_POINT ( 'NONE',  ( 18.49999999999999645, -1.362429037182155023, -208.8888812479211765 ) ) ;
#45281=DIRECTION ( 'NONE',  ( 1.000000000000000000, -0.000000000000000000, 0.000000000000000000 ) ) ;
#45282=ADVANCED_FACE ( 'NONE', ( #201901 ), #243591, .T. ) ;
#45287=ORIENTED_EDGE ( 'NONE', *, *, #12893, .T. ) ;
#45309=EDGE_CURVE ( 'NONE', #204695, #131456, #51046, .T. ) ;
#45312=CIRCLE ( 'NONE', #191088, 0.09999999999999939493 ) ;
#45322=DIRECTION ( 'NONE',  ( 0.000000000000000000, 0.000000000000000000, -1.000000000000000000 ) ) ;
#45357=DIRECTION ( 'NONE',  ( 0.000000000000000000, 0.000000000000000000, 1.000000000000000000 ) ) ;
#45364=EDGE_LOOP ( 'NONE', ( #31665, #137170, #59008, #169476 ) ) ;
#45389=DIRECTION ( 'NONE',  ( 1.000000000000000000, 0.000000000000000000, 0.000000000000000000 ) ) ;
#45393=FACE_OUTER_BOUND ( 'NONE', #106753, .T. ) ;
#45404=EDGE_LOOP ( 'NONE', ( #92987, #134621, #76804, #128507 ) ) ;
#45405=EDGE_CURVE ( 'NONE', #227290, #158852, #250972, .T. ) ;
#45454=DIRECTION ( 'NONE',  ( -0.000000000000000000, -1.000000000000000000, -1.734723475976807292E-15 ) ) ;
#45464=DIRECTION ( 'NONE',  ( 1.000000000000000000, 3.265361837132813093E-16, -0.000000000000000000 ) ) ;
#45474=DIRECTION ( 'NONE',  ( 0.000000000000000000, -1.000000000000000000, -2.891205793294679805E-16 ) ) ;
#45477=AXIS2_PLACEMENT_3D ( 'NONE', #24361, #4745, #32068 ) ;
#45495=DIRECTION ( 'NONE',  ( 1.000000000000000000, 0.000000000000000000, -0.000000000000000000 ) ) ;
#45496=EDGE_CURVE ( 'NONE', #78009, #95420, #255020, .T. ) ;
#45510=EDGE_CURVE ( 'NONE', #67305, #135358, #192748, .T. ) ;
#45547=ORIENTED_EDGE ( 'NONE', *, *, #219347, .T. ) ;
#45571=ORIENTED_EDGE ( 'NONE', *, *, #167142, .F. ) ;
#45602=CARTESIAN_POINT ( 'NONE',  ( 21.05000012384916275, 10.62872029888669978, -179.6779773300349632 ) ) ;
#45619=ORIENTED_EDGE ( 'NONE', *, *, #21143, .T. ) ;
#45620=FACE_OUTER_BOUND ( 'NONE', #176601, .T. ) ;
#45624=CARTESIAN_POINT ( 'NONE',  ( -20.64999999999999858, 1.925233644870972816, -180.2302435331260995 ) ) ;
#45663=AXIS2_PLACEMENT_3D ( 'NONE', #53375, #151203, #134182 ) ;
#45672=DIRECTION ( 'NONE',  ( 0.000000000000000000, -1.000000000000000000, 0.000000000000000000 ) ) ;
#45677=VERTEX_POINT ( 'NONE', #171563 ) ;
#45689=ORIENTED_EDGE ( 'NONE', *, *, #256763, .T. ) ;
#45693=FACE_OUTER_BOUND ( 'NONE', #170287, .T. ) ;
#45709=ORIENTED_EDGE ( 'NONE', *, *, #835, .F. ) ;
#45716=CARTESIAN_POINT ( 'NONE',  ( -21.07946286933445279, 6.329037319018850916, -167.4233161567435673 ) ) ;
#45727=VECTOR ( 'NONE', #50, 1000.000000000000000 ) ;
#45733=ORIENTED_EDGE ( 'NONE', *, *, #103222, .T. ) ;
#45769=CARTESIAN_POINT ( 'NONE',  ( 18.39999999999999858, -9.499999999988842703, -207.6001893912220169 ) ) ;
#45803=EDGE_CURVE ( 'NONE', #138430, #68978, #84541, .T. ) ;
#45863=EDGE_CURVE ( 'NONE', #155258, #77947, #147475, .T. ) ;
#45887=CARTESIAN_POINT ( 'NONE',  ( 18.47073956224746993, -9.471729412460748065, -174.6086857528181326 ) ) ;
#45942=DIRECTION ( 'NONE',  ( 1.000000000000000000, 0.000000000000000000, 0.000000000000000000 ) ) ;
#45952=ORIENTED_EDGE ( 'NONE', *, *, #141192, .T. ) ;
#45954=EDGE_CURVE ( 'NONE', #52860, #50099, #193117, .T. ) ;
#45957=EDGE_LOOP ( 'NONE', ( #215532, #18714, #219963, #243119 ) ) ;
#45975=DIRECTION ( 'NONE',  ( 0.000000000000000000, 0.000000000000000000, -1.000000000000000000 ) ) ;
#45982=DIRECTION ( 'NONE',  ( 0.000000000000000000, -1.000000000000000000, 0.000000000000000000 ) ) ;
#45985=ORIENTED_EDGE ( 'NONE', *, *, #153999, .T. ) ;
#46043=DIRECTION ( 'NONE',  ( 0.000000000000000000, 1.000000000000000000, 0.000000000000000000 ) ) ;
#46050=CYLINDRICAL_SURFACE ( 'NONE', #231531, 0.09999999999999939493 ) ;
#46082=DIRECTION ( 'NONE',  ( 0.000000000000000000, 0.9915357197604971473, -0.1298341882519111479 ) ) ;
#46092=EDGE_CURVE ( 'NONE', #152331, #135750, #136907, .T. ) ;
#46098=DIRECTION ( 'NONE',  ( -1.000000000000000000, 0.000000000000000000, 0.000000000000000000 ) ) ;
#46111=AXIS2_PLACEMENT_3D ( 'NONE', #110897, #92600, #151330 ) ;
#46121=CARTESIAN_POINT ( 'NONE',  ( 21.11927991906888025, 6.448493118502573118, -167.4909163205260541 ) ) ;
#46124=ORIENTED_EDGE ( 'NONE', *, *, #199590, .F. ) ;
#46145=TOROIDAL_SURFACE ( 'NONE', #4442, 11.90000000000000213, 0.1000000000000000056 ) ;
#46150=FACE_OUTER_BOUND ( 'NONE', #46340, .T. ) ;
#46161=DIRECTION ( 'NONE',  ( -0.000000000000000000, -1.265107689135680095E-16, 1.000000000000000000 ) ) ;
#46162=ORIENTED_EDGE ( 'NONE', *, *, #60433, .F. ) ;
#46189=EDGE_CURVE ( 'NONE', #104346, #23197, #83319, .T. ) ;
#46203=EDGE_CURVE ( 'NONE', #123667, #133882, #104182, .T. ) ;
#46232=EDGE_CURVE ( 'NONE', #7200, #179560, #26521, .T. ) ;
#46255=ORIENTED_EDGE ( 'NONE', *, *, #124244, .T. ) ;
#46263=DIRECTION ( 'NONE',  ( -0.000000000000000000, -0.000000000000000000, 1.000000000000000000 ) ) ;
#46264=AXIS2_PLACEMENT_3D ( 'NONE', #3831, #46789, #222868 ) ;
#46275=TOROIDAL_SURFACE ( 'NONE', #87956, 12.77500000000000036, 0.1000000000000000056 ) ;
#46278=ORIENTED_EDGE ( 'NONE', *, *, #107512, .F. ) ;
#46285=AXIS2_PLACEMENT_3D ( 'NONE', #151012, #208435, #67609 ) ;
#46304=CIRCLE ( 'NONE', #217001, 0.4000000000000114575 ) ;
#46340=EDGE_LOOP ( 'NONE', ( #22913, #200283, #237475, #8012, #133537 ) ) ;
#46411=ORIENTED_EDGE ( 'NONE', *, *, #228139, .T. ) ;
#46412=CARTESIAN_POINT ( 'NONE',  ( -21.05000000000000071, 1.162701749949165642, -175.4999999999999716 ) ) ;
#46416=DIRECTION ( 'NONE',  ( -1.000000000000000000, -1.836970198721029934E-16, 0.000000000000000000 ) ) ;
#46427=ADVANCED_FACE ( 'NONE', ( #253963 ), #76749, .F. ) ;
#46454=DIRECTION ( 'NONE',  ( 1.000000000000000000, 0.000000000000000000, 0.000000000000000000 ) ) ;
#46499=AXIS2_PLACEMENT_3D ( 'NONE', #162911, #42939, #5056 ) ;
#46630=CIRCLE ( 'NONE', #71626, 0.5000000000000004441 ) ;
#46654=DIRECTION ( 'NONE',  ( 0.000000000000000000, 0.000000000000000000, -1.000000000000000000 ) ) ;
#46667=AXIS2_PLACEMENT_3D ( 'NONE', #159012, #4694, #223746 ) ;
#46698=DIRECTION ( 'NONE',  ( -1.000000000000000000, 0.000000000000000000, 0.000000000000000000 ) ) ;
#46700=CYLINDRICAL_SURFACE ( 'NONE', #80047, 2.000000000000001776 ) ;
#46730=ORIENTED_EDGE ( 'NONE', *, *, #227513, .T. ) ;
#46731=CARTESIAN_POINT ( 'NONE',  ( -23.15000000000000213, 4.250000000011156409, -179.7499999999999716 ) ) ;
#46734=DIRECTION ( 'NONE',  ( 0.000000000000000000, -1.000000000000000000, 5.551115123125768187E-14 ) ) ;
#46742=EDGE_CURVE ( 'NONE', #221039, #220454, #134613, .T. ) ;
#46761=FACE_OUTER_BOUND ( 'NONE', #196088, .T. ) ;
#46764=CARTESIAN_POINT ( 'NONE',  ( 21.05000000000000071, 1.115600667400684642E-11, -200.9999999999999432 ) ) ;
#46774=ORIENTED_EDGE ( 'NONE', *, *, #238373, .T. ) ;
#46780=AXIS2_PLACEMENT_3D ( 'NONE', #135688, #75743, #155303 ) ;
#46789=DIRECTION ( 'NONE',  ( 0.000000000000000000, -0.000000000000000000, 1.000000000000000000 ) ) ;
#46799=SPHERICAL_SURFACE ( 'NONE', #137504, 0.1000000000000000056 ) ;
#46803=DIRECTION ( 'NONE',  ( 0.000000000000000000, 1.000000000000000000, 0.000000000000000000 ) ) ;
#46835=DIRECTION ( 'NONE',  ( 0.000000000000000000, -1.000000000000000000, 0.000000000000000000 ) ) ;
#46836=CIRCLE ( 'NONE', #184210, 0.5000000000000004441 ) ;
#46839=DIRECTION ( 'NONE',  ( -2.915501640297153790E-16, 1.000000000000000000, 0.000000000000000000 ) ) ;
#46852=EDGE_LOOP ( 'NONE', ( #130708, #7119, #25387, #137766 ) ) ;
#46875=CARTESIAN_POINT ( 'NONE',  ( 21.05000000000000071, -11.64999999998883595, -198.0999999999999659 ) ) ;
#46881=CARTESIAN_POINT ( 'NONE',  ( -23.15000000000000213, 1.115600667400684642E-11, -204.8999999999999488 ) ) ;
#46889=DIRECTION ( 'NONE',  ( -0.000000000000000000, 1.000000000000000000, 0.000000000000000000 ) ) ;
#46891=VERTEX_POINT ( 'NONE', #239254 ) ;
#46892=DIRECTION ( 'NONE',  ( -1.000000000000000000, -0.000000000000000000, -0.000000000000000000 ) ) ;
#46904=VERTEX_POINT ( 'NONE', #95863 ) ;
#46925=FACE_OUTER_BOUND ( 'NONE', #152446, .T. ) ;
#46933=CARTESIAN_POINT ( 'NONE',  ( -23.15000000000000213, 1.115600667400684642E-11, -180.2749999999999773 ) ) ;
#46949=ORIENTED_EDGE ( 'NONE', *, *, #113626, .F. ) ;
#46964=DIRECTION ( 'NONE',  ( 1.000000000000000000, -0.000000000000000000, -0.000000000000000000 ) ) ;
#46969=AXIS2_PLACEMENT_3D ( 'NONE', #101462, #181072, #2391 ) ;
#46974=ORIENTED_EDGE ( 'NONE', *, *, #221940, .F. ) ;
#46999=FACE_OUTER_BOUND ( 'NONE', #195833, .T. ) ;
#47020=CARTESIAN_POINT ( 'NONE',  ( 18.59999999999999787, 1.866714910068465239, -179.2526752462819672 ) ) ;
#47040=EDGE_CURVE ( 'NONE', #50465, #163390, #72189, .T. ) ;
#47044=ADVANCED_FACE ( 'NONE', ( #48743 ), #50033, .T. ) ;
#47061=ORIENTED_EDGE ( 'NONE', *, *, #177419, .F. ) ;
#47084=DIRECTION ( 'NONE',  ( 0.000000000000000000, 0.4999999999999543698, 0.8660254037844650199 ) ) ;
#47089=CARTESIAN_POINT ( 'NONE',  ( -18.59999999999999787, 9.350000000011156942, -179.6499999999999773 ) ) ;
#47095=CARTESIAN_POINT ( 'NONE',  ( 21.97500000000000497, 9.750000000011153745, -188.6499999999999488 ) ) ;
#47096=DIRECTION ( 'NONE',  ( 1.000000000000000000, 0.000000000000000000, 0.000000000000000000 ) ) ;
#47111=CARTESIAN_POINT ( 'NONE',  ( -21.05000000000000071, -1.835341550213255957, -179.1551512925629197 ) ) ;
#47131=ORIENTED_EDGE ( 'NONE', *, *, #229262, .T. ) ;
#47145=CIRCLE ( 'NONE', #88653, 0.2000000000000057288 ) ;
#47175=CIRCLE ( 'NONE', #197023, 11.70000000000001528 ) ;
#47180=CARTESIAN_POINT ( 'NONE',  ( -18.40000000000000213, -9.499999999988936850, -207.9221498493300828 ) ) ;
#47324=VECTOR ( 'NONE', #165176, 1000.000000000000227 ) ;
#47371=FACE_OUTER_BOUND ( 'NONE', #209935, .T. ) ;
#47384=DIRECTION ( 'NONE',  ( -3.469446951953635015E-14, 1.000000000000000000, 0.000000000000000000 ) ) ;
#47388=ADVANCED_FACE ( 'NONE', ( #86264 ), #88832, .F. ) ;
#47397=CARTESIAN_POINT ( 'NONE',  ( 21.09316766718127667, 6.370153312485570929, -167.4607365976852691 ) ) ;
#47421=LINE ( 'NONE', #27913, #163335 ) ;
#47431=( NAMED_UNIT ( * ) PLANE_ANGLE_UNIT ( ) SI_UNIT ( $, .RADIAN. ) );
#47432=CARTESIAN_POINT ( 'NONE',  ( -23.15000000000000213, -11.74999999998884448, -167.4999999999999432 ) ) ;
#47470=CYLINDRICAL_SURFACE ( 'NONE', #205519, 0.09999999999999817368 ) ;
#47472=ORIENTED_EDGE ( 'NONE', *, *, #210310, .T. ) ;
#47494=CARTESIAN_POINT ( 'NONE',  ( -20.85000000000000142, -1.835859311432481045, -212.6044391687984785 ) ) ;
#47519=EDGE_LOOP ( 'NONE', ( #2363, #213518, #116344, #204562 ) ) ;
#47528=ORIENTED_EDGE ( 'NONE', *, *, #125328, .T. ) ;
#47531=ORIENTED_EDGE ( 'NONE', *, *, #141602, .F. ) ;
#47542=AXIS2_PLACEMENT_3D ( 'NONE', #10905, #252067, #231247 ) ;
#47578=PLANE ( 'NONE',  #161661 ) ;
#47587=ADVANCED_FACE ( 'NONE', ( #13186 ), #32778, .T. ) ;
#47594=DIRECTION ( 'NONE',  ( 1.000000000000000000, 3.265361837132813093E-16, -0.000000000000000000 ) ) ;
#47626=ADVANCED_FACE ( 'NONE', ( #40482 ), #179964, .F. ) ;
#47645=ORIENTED_EDGE ( 'NONE', *, *, #193984, .F. ) ;
#47671=EDGE_LOOP ( 'NONE', ( #201643, #123597, #170792, #74288 ) ) ;
#47673=CARTESIAN_POINT ( 'NONE',  ( 21.56666275994540172, 1.115600667400684642E-11, -160.5426315931066483 ) ) ;
#47748=DIRECTION ( 'NONE',  ( 1.000000000000000000, -0.000000000000000000, -0.000000000000000000 ) ) ;
#47759=DIRECTION ( 'NONE',  ( 0.000000000000000000, 0.000000000000000000, 1.000000000000000000 ) ) ;
#47762=AXIS2_PLACEMENT_3D ( 'NONE', #243565, #3663, #84442 ) ;
#47763=AXIS2_PLACEMENT_3D ( 'NONE', #83656, #67984, #150116 ) ;
#47776=CIRCLE ( 'NONE', #193561, 7.720710678118663850 ) ;
#47782=EDGE_CURVE ( 'NONE', #245420, #190860, #99102, .T. ) ;
#47795=ORIENTED_EDGE ( 'NONE', *, *, #76201, .F. ) ;
#47796=ORIENTED_EDGE ( 'NONE', *, *, #177913, .F. ) ;
#47811=ADVANCED_FACE ( 'NONE', ( #174215 ), #90765, .F. ) ;
#47818=VERTEX_POINT ( 'NONE', #212032 ) ;
#47858=EDGE_CURVE ( 'NONE', #171611, #42095, #193739, .T. ) ;
#47875=DIRECTION ( 'NONE',  ( -0.000000000000000000, 1.000000000000000000, -0.000000000000000000 ) ) ;
#47950=DIRECTION ( 'NONE',  ( -1.000000000000000000, -3.265361837132813093E-16, 0.000000000000000000 ) ) ;
#47975=ORIENTED_EDGE ( 'NONE', *, *, #19029, .F. ) ;
#47976=CARTESIAN_POINT ( 'NONE',  ( 18.60000000000000142, -9.480686695267790398, -207.9411151687578183 ) ) ;
#48031=AXIS2_PLACEMENT_3D ( 'NONE', #252933, #130425, #169609 ) ;
#48033=CARTESIAN_POINT ( 'NONE',  ( 20.94999999999999929, 1.115600667400684642E-11, -200.9999999999999432 ) ) ;
#48037=DIRECTION ( 'NONE',  ( -1.000000000000000000, 0.000000000000000000, 0.000000000000000000 ) ) ;
#48065=CARTESIAN_POINT ( 'NONE',  ( 23.14999999999999858, -3.899999999988843502, -200.9999999999999432 ) ) ;
#48129=ORIENTED_EDGE ( 'NONE', *, *, #68707, .T. ) ;
#48133=EDGE_CURVE ( 'NONE', #108161, #132399, #51766, .T. ) ;
#48147=CIRCLE ( 'NONE', #89832, 11.80000000000000426 ) ;
#48184=EDGE_CURVE ( 'NONE', #176585, #9648, #50859, .T. ) ;
#48239=DIRECTION ( 'NONE',  ( 0.000000000000000000, -0.1455152366551721865, -0.9893560106964475187 ) ) ;
#48241=ORIENTED_EDGE ( 'NONE', *, *, #229122, .F. ) ;
#48245=TOROIDAL_SURFACE ( 'NONE', #227306, 11.65000000000000036, 0.1000000000000000056 ) ;
#48281=EDGE_CURVE ( 'NONE', #14558, #253941, #189361, .T. ) ;
#48284=DIRECTION ( 'NONE',  ( -1.000000000000000000, -0.000000000000000000, -0.000000000000000000 ) ) ;
#48291=DIRECTION ( 'NONE',  ( -1.000000000000000000, -0.000000000000000000, -0.000000000000000000 ) ) ;
#48294=DIRECTION ( 'NONE',  ( 1.000000000000000000, -0.000000000000000000, -0.000000000000000000 ) ) ;
#48369=DIRECTION ( 'NONE',  ( 0.000000000000000000, -2.428612866367527723E-14, -1.000000000000000000 ) ) ;
#48396=DIRECTION ( 'NONE',  ( 2.952720810173289112E-16, -1.000000000000000000, 0.000000000000000000 ) ) ;
#48415=DIRECTION ( 'NONE',  ( 0.000000000000000000, 0.000000000000000000, -1.000000000000000000 ) ) ;
#48432=VERTEX_POINT ( 'NONE', #21253 ) ;
#48452=AXIS2_PLACEMENT_3D ( 'NONE', #173694, #54946, #253163 ) ;
#48453=EDGE_CURVE ( 'NONE', #66095, #142512, #103303, .T. ) ;
#48467=AXIS2_PLACEMENT_3D ( 'NONE', #241059, #141933, #104071 ) ;
#48476=AXIS2_PLACEMENT_3D ( 'NONE', #172406, #71988, #94093 ) ;
#48483=DIRECTION ( 'NONE',  ( 0.000000000000000000, 0.000000000000000000, -1.000000000000000000 ) ) ;
#48485=VECTOR ( 'NONE', #48291, 1000.000000000000000 ) ;
#48505=ORIENTED_EDGE ( 'NONE', *, *, #247632, .T. ) ;
#48538=AXIS2_PLACEMENT_3D ( 'NONE', #29881, #9004, #7732 ) ;
#48559=EDGE_LOOP ( 'NONE', ( #98119, #70413 ) ) ;
#48572=TOROIDAL_SURFACE ( 'NONE', #165107, 0.2000000000000000111, 0.1000000000000000056 ) ;
#48585=DIRECTION ( 'NONE',  ( 1.000000000000000000, 0.000000000000000000, 0.000000000000000000 ) ) ;
#48602=VECTOR ( 'NONE', #135044, 1000.000000000000000 ) ;
#48603=VECTOR ( 'NONE', #43775, 1000.000000000000000 ) ;
#48610=TOROIDAL_SURFACE ( 'NONE', #194400, 1.900000000000002576, 0.1000000000000000056 ) ;
#48612=CARTESIAN_POINT ( 'NONE',  ( 18.49999999999999645, -1.835341550213255957, -179.0551512925629538 ) ) ;
#48616=VECTOR ( 'NONE', #175440, 1000.000000000000000 ) ;
#48648=EDGE_CURVE ( 'NONE', #223514, #4495, #27683, .T. ) ;
#48695=DIRECTION ( 'NONE',  ( -1.000000000000000000, -0.000000000000000000, -0.000000000000000000 ) ) ;
#48698=DIRECTION ( 'NONE',  ( -1.000000000000000000, 0.000000000000000000, 0.000000000000000000 ) ) ;
#48700=( BOUNDED_SURFACE ( )  B_SPLINE_SURFACE ( 3, 2, ( 
 ( #249713, #54068, #189739 ),
 ( #191046, #231447, #11103 ),
 ( #91908, #71090, #150615 ),
 ( #206728, #29415, #167628 ),
 ( #112769, #89332, #28120 ),
 ( #230145, #107622, #72376 ) ),
 .UNSPECIFIED., .F., .F., .F. ) 
 B_SPLINE_SURFACE_WITH_KNOTS ( ( 4, 2, 4 ),
 ( 3, 3 ),
 ( 0.0001381104793128107321, 0.0002947094729387620326, 0.0004513084665647133873 ),
 ( 0.000000000000000000, 1.000000000000000000 ),
 .UNSPECIFIED. ) 
 GEOMETRIC_REPRESENTATION_ITEM ( )  RATIONAL_B_SPLINE_SURFACE ( (
 ( 1.000000000000000000, 0.7071067811865475727, 1.000000000000000000),
 ( 1.000000000000000000, 0.6919563088098478199, 1.000000000000000000),
 ( 1.000000000000000000, 0.6959445945718057969, 1.000000000000000000),
 ( 1.000000000000000000, 0.7137882985313904749, 1.000000000000000000),
 ( 1.000000000000000000, 0.7257496306095887473, 1.000000000000000000),
 ( 1.000000000000000000, 0.7250110520819876836, 1.000000000000000000) ) ) 
 REPRESENTATION_ITEM ( '' )  SURFACE ( )  );
#48708=ORIENTED_EDGE ( 'NONE', *, *, #103401, .T. ) ;
#48712=DIRECTION ( 'NONE',  ( 1.000000000000000000, -0.000000000000000000, -0.000000000000000000 ) ) ;
#48736=CARTESIAN_POINT ( 'NONE',  ( -21.07016717456945543, 6.320940838111416049, -167.4999999999999432 ) ) ;
#48737=ORIENTED_EDGE ( 'NONE', *, *, #99000, .F. ) ;
#48743=FACE_OUTER_BOUND ( 'NONE', #13615, .T. ) ;
#48797=DIRECTION ( 'NONE',  ( 0.000000000000000000, 1.000000000000000000, 0.000000000000000000 ) ) ;
#48828=CARTESIAN_POINT ( 'NONE',  ( 20.94999999999999574, -1.736257131586239844, -179.0686523290174819 ) ) ;
#48830=ORIENTED_EDGE ( 'NONE', *, *, #195454, .F. ) ;
#48866=VERTEX_POINT ( 'NONE', #122604 ) ;
#48880=VERTEX_POINT ( 'NONE', #45624 ) ;
#48890=DIRECTION ( 'NONE',  ( -3.265361837132813093E-16, 1.000000000000000000, 0.000000000000000000 ) ) ;
#48895=VECTOR ( 'NONE', #241803, 1000.000000000000000 ) ;
#48898=DIRECTION ( 'NONE',  ( 0.000000000000000000, 0.000000000000000000, -1.000000000000000000 ) ) ;
#48908=CARTESIAN_POINT ( 'NONE',  ( 20.87600722750343252, 10.33112638556969465, -206.5901228926974227 ) ) ;
#48955=ORIENTED_EDGE ( 'NONE', *, *, #112100, .F. ) ;
#48984=PLANE ( 'NONE',  #30168 ) ;
#48992=CARTESIAN_POINT ( 'NONE',  ( -20.92356734117541706, 10.31973158071402175, -206.5505334713353989 ) ) ;
#48993=VERTEX_POINT ( 'NONE', #127731 ) ;
#49005=EDGE_CURVE ( 'NONE', #99065, #224509, #194492, .T. ) ;
#49021=VECTOR ( 'NONE', #102179, 1000.000000000000000 ) ;
#49033=EDGE_CURVE ( 'NONE', #177021, #48432, #50717, .T. ) ;
#49050=DIRECTION ( 'NONE',  ( 0.000000000000000000, 0.1350103645451876666, 0.9908441862701600211 ) ) ;
#49060=CARTESIAN_POINT ( 'NONE',  ( -22.50014994444008565, 11.74971973190334218, -167.4169198432813346 ) ) ;
#49072=DIRECTION ( 'NONE',  ( 0.000000000000000000, 6.505213034913742890E-15, 1.000000000000000000 ) ) ;
#49079=CARTESIAN_POINT ( 'NONE',  ( 21.05000000000000071, -12.41227409413852811, -197.9999999999999432 ) ) ;
#49094=DIRECTION ( 'NONE',  ( 0.000000000000000000, 1.000000000000000000, -0.000000000000000000 ) ) ;
#49116=EDGE_LOOP ( 'NONE', ( #250804, #91037, #201564, #68220 ) ) ;
#49119=AXIS2_PLACEMENT_3D ( 'NONE', #129901, #8684, #188594 ) ;
#49124=EDGE_CURVE ( 'NONE', #132941, #199601, #148701, .T. ) ;
#49125=CARTESIAN_POINT ( 'NONE',  ( 23.14999999999999503, 11.65000000001116298, -179.6499999999999773 ) ) ;
#49206=CARTESIAN_POINT ( 'NONE',  ( 20.95512820512820440, 8.876151316299271343, -179.6499999999999773 ) ) ;
#49233=CARTESIAN_POINT ( 'NONE',  ( 22.39999999999999858, 7.790779598384538041, -167.4999999999999432 ) ) ;
#49236=CARTESIAN_POINT ( 'NONE',  ( -21.45000000000000284, 7.708578643773852157, -188.7499999999999716 ) ) ;
#49257=DIRECTION ( 'NONE',  ( 0.000000000000000000, 0.7397360091702755991, -0.6728971962616832059 ) ) ;
#49266=CARTESIAN_POINT ( 'NONE',  ( 18.33683296300592147, -9.511149971122062396, -207.9057074127082956 ) ) ;
#49269=AXIS2_PLACEMENT_3D ( 'NONE', #71391, #148340, #209600 ) ;
#49278=CARTESIAN_POINT ( 'NONE',  ( -21.00023020733502932, 1.115541036281197940E-11, -161.1091307547316376 ) ) ;
#49294=AXIS2_PLACEMENT_3D ( 'NONE', #209727, #231878, #31128 ) ;
#49302=ORIENTED_EDGE ( 'NONE', *, *, #78739, .F. ) ;
#49307=DIRECTION ( 'NONE',  ( 0.000000000000000000, 0.000000000000000000, -1.000000000000000000 ) ) ;
#49389=AXIS2_PLACEMENT_3D ( 'NONE', #256369, #161196, #238144 ) ;
#49409=AXIS2_PLACEMENT_3D ( 'NONE', #184740, #146885, #247279 ) ;
#49421=CARTESIAN_POINT ( 'NONE',  ( 18.49999999999999289, 11.75000000001115552, -192.3499999999999659 ) ) ;
#49482=EDGE_CURVE ( 'NONE', #156141, #10283, #140915, .T. ) ;
#49484=AXIS2_PLACEMENT_3D ( 'NONE', #130331, #112085, #115925 ) ;
#49486=DIRECTION ( 'NONE',  ( 5.603264701231745086E-32, -1.897661533703520636E-16, 1.000000000000000000 ) ) ;
#49491=AXIS2_PLACEMENT_3D ( 'NONE', #126202, #247438, #8838 ) ;
#49506=DIRECTION ( 'NONE',  ( -1.000000000000000000, 0.000000000000000000, 0.000000000000000000 ) ) ;
#49517=EDGE_CURVE ( 'NONE', #213934, #4326, #53429, .T. ) ;
#49520=DIRECTION ( 'NONE',  ( 0.000000000000000000, 1.000000000000000000, -6.308085367188393199E-16 ) ) ;
#49527=ORIENTED_EDGE ( 'NONE', *, *, #211051, .F. ) ;
#49571=VERTEX_POINT ( 'NONE', #127936 ) ;
#49584=FACE_OUTER_BOUND ( 'NONE', #247336, .T. ) ;
#49619=CARTESIAN_POINT ( 'NONE',  ( -21.03571358705729111, 11.75000000001115197, -174.3251068220585580 ) ) ;
#49627=VECTOR ( 'NONE', #12395, 1000.000000000000000 ) ;
#49633=AXIS2_PLACEMENT_3D ( 'NONE', #252947, #170912, #153917 ) ;
#49664=EDGE_CURVE ( 'NONE', #116440, #22716, #111887, .T. ) ;
#49702=ADVANCED_FACE ( 'NONE', ( #191786 ), #16987, .T. ) ;
#49724=AXIS2_PLACEMENT_3D ( 'NONE', #185682, #25344, #67013 ) ;
#49742=EDGE_LOOP ( 'NONE', ( #258013, #24460, #142901, #75698 ) ) ;
#49745=CIRCLE ( 'NONE', #24832, 11.90000000000000213 ) ;
#49750=EDGE_CURVE ( 'NONE', #213316, #257624, #74314, .T. ) ;
#49753=LINE ( 'NONE', #112309, #114125 ) ;
#49781=ADVANCED_FACE ( 'NONE', ( #199477 ), #101596, .T. ) ;
#49784=ORIENTED_EDGE ( 'NONE', *, *, #146215, .T. ) ;
#49796=CIRCLE ( 'NONE', #12408, 0.09999999999998898659 ) ;
#49808=ORIENTED_EDGE ( 'NONE', *, *, #20571, .F. ) ;
#49809=EDGE_CURVE ( 'NONE', #254925, #75581, #16214, .T. ) ;
#49853=DIRECTION ( 'NONE',  ( 0.000000000000000000, -1.734723475983309083E-15, 1.000000000000000000 ) ) ;
#49887=AXIS2_PLACEMENT_3D ( 'NONE', #54380, #10130, #150922 ) ;
#49892=ORIENTED_EDGE ( 'NONE', *, *, #194937, .F. ) ;
#49939=CARTESIAN_POINT ( 'NONE',  ( -21.05000000000000071, -1.162701749926853712, -175.5999999999999659 ) ) ;
#49961=ADVANCED_FACE ( 'NONE', ( #183750 ), #128914, .F. ) ;
#49966=DIRECTION ( 'NONE',  ( -6.938893903907222067E-15, 1.000000000000000000, 2.891205793294679805E-16 ) ) ;
#49967=ORIENTED_EDGE ( 'NONE', *, *, #251446, .F. ) ;
#49994=CARTESIAN_POINT ( 'NONE',  ( 21.05000000000000071, -11.48912529306490349, -170.5999999999999659 ) ) ;
#50009=CIRCLE ( 'NONE', #116636, 0.1000000000000001860 ) ;
#50033=CYLINDRICAL_SURFACE ( 'NONE', #151795, 0.09999999999999939493 ) ;
#50056=CARTESIAN_POINT ( 'NONE',  ( -21.14999999999999858, -0.09999999998884338825, -155.8504291924551808 ) ) ;
#50077=CARTESIAN_POINT ( 'NONE',  ( -18.50000000000000000, 5.950000000011100632, -177.8057023050348278 ) ) ;
#50088=ORIENTED_EDGE ( 'NONE', *, *, #163175, .T. ) ;
#50093=CARTESIAN_POINT ( 'NONE',  ( 20.94999999999999574, 1.250000000011155299, -175.3999999999999773 ) ) ;
#50099=VERTEX_POINT ( 'NONE', #114475 ) ;
#50102=PLANE ( 'NONE',  #184030 ) ;
#50109=EDGE_LOOP ( 'NONE', ( #152524, #219159, #41967, #205414 ) ) ;
#50118=CIRCLE ( 'NONE', #75101, 0.09999999999999939493 ) ;
#50139=CARTESIAN_POINT ( 'NONE',  ( 23.24999999999999645, 1.115600667400684642E-11, -167.4999999999999716 ) ) ;
#50166=FACE_OUTER_BOUND ( 'NONE', #84171, .T. ) ;
#50174=VERTEX_POINT ( 'NONE', #3498 ) ;
#50191=AXIS2_PLACEMENT_3D ( 'NONE', #67574, #247497, #66300 ) ;
#50212=VERTEX_POINT ( 'NONE', #118341 ) ;
#50242=CARTESIAN_POINT ( 'NONE',  ( 22.39999999999999503, 1.115600667400684642E-11, -159.7092204016265669 ) ) ;
#50258=DIRECTION ( 'NONE',  ( -1.000000000000000000, -0.000000000000000000, -0.000000000000000000 ) ) ;
#50291=CARTESIAN_POINT ( 'NONE',  ( 21.09096482362069835, 6.363544365415760851, -167.4605517212258974 ) ) ;
#50325=CIRCLE ( 'NONE', #125546, 0.5000000000000004441 ) ;
#50339=ADVANCED_FACE ( 'NONE', ( #103869 ), #148152, .F. ) ;
#50381=CARTESIAN_POINT ( 'NONE',  ( -20.94999999999999929, -11.64999999998884483, -200.9999999999999432 ) ) ;
#50442=ORIENTED_EDGE ( 'NONE', *, *, #78351, .F. ) ;
#50455=DIRECTION ( 'NONE',  ( 0.000000000000000000, -1.000000000000000000, 0.000000000000000000 ) ) ;
#50465=VERTEX_POINT ( 'NONE', #58019 ) ;
#50468=CARTESIAN_POINT ( 'NONE',  ( 21.05000000000000071, 10.72371710471867701, -175.1649135690875880 ) ) ;
#50484=VERTEX_POINT ( 'NONE', #136267 ) ;
#50485=ORIENTED_EDGE ( 'NONE', *, *, #247532, .F. ) ;
#50539=CARTESIAN_POINT ( 'NONE',  ( -21.53752568622130070, 0.09897446127749365274, -160.7131921254514282 ) ) ;
#50541=ORIENTED_EDGE ( 'NONE', *, *, #250232, .F. ) ;
#50598=CARTESIAN_POINT ( 'NONE',  ( -21.05000000000000071, 1.162701749949165642, -175.5999999999999659 ) ) ;
#50650=ORIENTED_EDGE ( 'NONE', *, *, #96220, .T. ) ;
#50680=DIRECTION ( 'NONE',  ( -0.000000000000000000, -1.000000000000000000, 6.308085367188393199E-16 ) ) ;
#50681=CARTESIAN_POINT ( 'NONE',  ( 18.49999999999999645, 1.115600667400684642E-11, -167.4999999999999716 ) ) ;
#50682=CARTESIAN_POINT ( 'NONE',  ( -22.47071067811865319, 7.720074744509219933, -167.4009075452973434 ) ) ;
#50690=DIRECTION ( 'NONE',  ( -1.000000000000000000, 0.000000000000000000, 0.000000000000000000 ) ) ;
#50693=ORIENTED_EDGE ( 'NONE', *, *, #247018, .F. ) ;
#50710=FACE_OUTER_BOUND ( 'NONE', #114997, .T. ) ;
#50717=LINE ( 'NONE', #130274, #152811 ) ;
#50720=ORIENTED_EDGE ( 'NONE', *, *, #182228, .F. ) ;
#50722=EDGE_CURVE ( 'NONE', #185627, #63695, #179088, .T. ) ;
#50754=ORIENTED_EDGE ( 'NONE', *, *, #233309, .T. ) ;
#50760=LINE ( 'NONE', #146028, #246767 ) ;
#50764=DIRECTION ( 'NONE',  ( 0.000000000000000000, 0.000000000000000000, -1.000000000000000000 ) ) ;
#50772=FACE_OUTER_BOUND ( 'NONE', #110101, .T. ) ;
#50811=ORIENTED_EDGE ( 'NONE', *, *, #215643, .F. ) ;
#50845=( BOUNDED_SURFACE ( )  B_SPLINE_SURFACE ( 3, 2, ( 
 ( #249496, #188225, #252046 ),
 ( #210367, #144254, #89120 ),
 ( #223805, #90398, #189521 ),
 ( #129544, #31754, #70878 ),
 ( #209072, #248203, #72149 ),
 ( #231226, #52551, #132108 ) ),
 .UNSPECIFIED., .F., .F., .F. ) 
 B_SPLINE_SURFACE_WITH_KNOTS ( ( 4, 2, 4 ),
 ( 3, 3 ),
 ( -1.776356839400250465E-15, 0.7853981633974468357, 1.570796326794895448 ),
 ( 0.000000000000000000, 1.000000000000000000 ),
 .UNSPECIFIED. ) 
 GEOMETRIC_REPRESENTATION_ITEM ( )  RATIONAL_B_SPLINE_SURFACE ( (
 ( 1.000000000000000000, 0.5000000000000260902, 1.000000000000000000),
 ( 1.000000000000000000, 0.4993418825348700518, 1.000000000000000000),
 ( 1.000000000000000000, 0.5278258667036815899, 1.000000000000000000),
 ( 1.000000000000000000, 0.6092287576718847797, 1.000000000000000000),
 ( 1.000000000000000000, 0.6611148371761672582, 1.000000000000000000),
 ( 1.000000000000000000, 0.7071067811865597852, 1.000000000000000000) ) ) 
 REPRESENTATION_ITEM ( '' )  SURFACE ( )  );
#50859=B_SPLINE_CURVE_WITH_KNOTS ( 'NONE', 3,
 ( #190903, #72222, #132181, #188291, #207892, #246979, #150474, #210449 ),
 .UNSPECIFIED., .F., .F.,
 ( 4, 2, 2, 4 ),
 ( 0.000000000000000000, 0.0001049670497870194505, 0.0002099340995740389009, 0.0004198681991480204476 ),
 .UNSPECIFIED. ) ;
#50862=ORIENTED_EDGE ( 'NONE', *, *, #144488, .T. ) ;
#50893=TOROIDAL_SURFACE ( 'NONE', #196662, 11.65000000000000036, 0.1000000000000000056 ) ;
#50917=CYLINDRICAL_SURFACE ( 'NONE', #38378, 0.09999999999999892308 ) ;
#50923=ORIENTED_EDGE ( 'NONE', *, *, #179466, .T. ) ;
#50925=CARTESIAN_POINT ( 'NONE',  ( -20.64999999999999858, -8.999999999988844479, -191.1060308773475356 ) ) ;
#50949=CARTESIAN_POINT ( 'NONE',  ( 21.30000000000002558, 1.115600667400684642E-11, -167.4999999999999716 ) ) ;
#50975=AXIS2_PLACEMENT_3D ( 'NONE', #29764, #109249, #126248 ) ;
#50977=DIRECTION ( 'NONE',  ( 0.000000000000000000, -3.552713678800554572E-15, -1.000000000000000000 ) ) ;
#50991=CARTESIAN_POINT ( 'NONE',  ( 18.49713797159841633, -9.446482327567903070, -174.5714581216104477 ) ) ;
#50992=ADVANCED_FACE ( 'NONE', ( #82086 ), #95826, .F. ) ;
#50996=AXIS2_PLACEMENT_3D ( 'NONE', #254866, #234076, #235358 ) ;
#51010=CARTESIAN_POINT ( 'NONE',  ( -21.05000000000000071, -11.74999999998884448, -197.8999999999999773 ) ) ;
#51017=AXIS2_PLACEMENT_3D ( 'NONE', #242343, #61142, #140677 ) ;
#51046=CIRCLE ( 'NONE', #159440, 0.1000000000000033223 ) ;
#51048=DIRECTION ( 'NONE',  ( 0.000000000000000000, -1.000000000000000000, 0.000000000000000000 ) ) ;
#51067=EDGE_CURVE ( 'NONE', #222295, #7200, #58402, .T. ) ;
#51068=CARTESIAN_POINT ( 'NONE',  ( 23.15000000000000213, -8.999999999988842703, -191.1060308773475072 ) ) ;
#51088=CIRCLE ( 'NONE', #84382, 3.899999999999987033 ) ;
#51127=DIRECTION ( 'NONE',  ( 0.000000000000000000, 0.000000000000000000, 1.000000000000000000 ) ) ;
#51140=AXIS2_PLACEMENT_3D ( 'NONE', #149914, #211149, #50764 ) ;
#51171=DIRECTION ( 'NONE',  ( 0.000000000000000000, 0.000000000000000000, -1.000000000000000000 ) ) ;
#51227=VECTOR ( 'NONE', #141374, 1000.000000000000114 ) ;
#51261=AXIS2_PLACEMENT_3D ( 'NONE', #95451, #152899, #55020 ) ;
#51263=CARTESIAN_POINT ( 'NONE',  ( -23.25000000000000000, 1.115600667400684642E-11, -167.4999999999999716 ) ) ;
#51305=AXIS2_PLACEMENT_3D ( 'NONE', #202350, #103228, #25024 ) ;
#51321=CYLINDRICAL_SURFACE ( 'NONE', #161229, 0.1000000000000101918 ) ;
#51424=ORIENTED_EDGE ( 'NONE', *, *, #58228, .F. ) ;
#51472=AXIS2_PLACEMENT_3D ( 'NONE', #138017, #115917, #160199 ) ;
#51494=ADVANCED_FACE ( 'NONE', ( #54218 ), #62723, .F. ) ;
#51513=DIRECTION ( 'NONE',  ( -0.000000000000000000, 1.000000000000000000, -0.000000000000000000 ) ) ;
#51515=CARTESIAN_POINT ( 'NONE',  ( -18.48550754432035959, -9.463399778548783559, -174.5487897524151037 ) ) ;
#51526=DIRECTION ( 'NONE',  ( 0.000000000000000000, 0.000000000000000000, -1.000000000000000000 ) ) ;
#51527=CARTESIAN_POINT ( 'NONE',  ( -20.89192007715127986, 10.32898536001801304, -206.5826683222763904 ) ) ;
#51531=ADVANCED_FACE ( 'NONE', ( #234142 ), #71249, .F. ) ;
#51539=ADVANCED_FACE ( 'NONE', ( #155925 ), #46145, .T. ) ;
#51557=CARTESIAN_POINT ( 'NONE',  ( 21.07928932188134397, 6.328516656404468144, -167.4011048543455615 ) ) ;
#51563=DIRECTION ( 'NONE',  ( 1.000000000000000000, 3.265361837132813093E-16, -0.000000000000000000 ) ) ;
#51577=ORIENTED_EDGE ( 'NONE', *, *, #181541, .F. ) ;
#51607=ORIENTED_EDGE ( 'NONE', *, *, #159789, .F. ) ;
#51615=DIRECTION ( 'NONE',  ( 0.000000000000000000, 0.000000000000000000, -1.000000000000000000 ) ) ;
#51620=DIRECTION ( 'NONE',  ( 0.000000000000000000, 0.000000000000000000, -1.000000000000000000 ) ) ;
#51631=VECTOR ( 'NONE', #44267, 1000.000000000000000 ) ;
#51639=FACE_OUTER_BOUND ( 'NONE', #144763, .T. ) ;
#51660=ORIENTED_EDGE ( 'NONE', *, *, #112100, .T. ) ;
#51681=CARTESIAN_POINT ( 'NONE',  ( -20.05000000000000426, 9.250000000011157297, -188.7499999999999716 ) ) ;
#51683=ORIENTED_EDGE ( 'NONE', *, *, #183844, .F. ) ;
#51688=ORIENTED_EDGE ( 'NONE', *, *, #60474, .F. ) ;
#51719=ORIENTED_EDGE ( 'NONE', *, *, #184448, .F. ) ;
#51720=CARTESIAN_POINT ( 'NONE',  ( -21.29999999999995808, 1.115600667400684642E-11, -167.4999999999999716 ) ) ;
#51725=EDGE_CURVE ( 'NONE', #237228, #411, #245716, .T. ) ;
#51754=CARTESIAN_POINT ( 'NONE',  ( 21.04999999999999716, 10.68430915749624077, -175.0266967903268096 ) ) ;
#51757=SPHERICAL_SURFACE ( 'NONE', #210122, 0.1000000000000000056 ) ;
#51766=CIRCLE ( 'NONE', #5991, 0.09999999999999939493 ) ;
#51842=ORIENTED_EDGE ( 'NONE', *, *, #218304, .F. ) ;
#51843=VERTEX_POINT ( 'NONE', #154366 ) ;
#51872=DIRECTION ( 'NONE',  ( -1.000000000000000000, 0.000000000000000000, 0.000000000000000000 ) ) ;
#51875=DIRECTION ( 'NONE',  ( 0.000000000000000000, 0.000000000000000000, -1.000000000000000000 ) ) ;
#51891=EDGE_CURVE ( 'NONE', #246179, #57491, #46304, .T. ) ;
#51904=FACE_OUTER_BOUND ( 'NONE', #20765, .T. ) ;
#51917=VERTEX_POINT ( 'NONE', #111346 ) ;
#51933=EDGE_LOOP ( 'NONE', ( #43912, #75406, #159397, #250886, #20305, #98681, #178848, #45985, #164430, #199635, #43482, #223047 ) ) ;
#51937=AXIS2_PLACEMENT_3D ( 'NONE', #250014, #233043, #72692 ) ;
#51972=CARTESIAN_POINT ( 'NONE',  ( 20.94999999999999574, -1.835341550213255957, -179.0551512925629538 ) ) ;
#51982=ORIENTED_EDGE ( 'NONE', *, *, #240256, .F. ) ;
#51986=ORIENTED_EDGE ( 'NONE', *, *, #180508, .T. ) ;
#52020=ORIENTED_EDGE ( 'NONE', *, *, #54044, .T. ) ;
#52028=CYLINDRICAL_SURFACE ( 'NONE', #109309, 0.09999999999999939493 ) ;
#52052=ADVANCED_FACE ( 'NONE', ( #120365 ), #76060, .T. ) ;
#52130=CARTESIAN_POINT ( 'NONE',  ( 18.50000000000000000, -9.399999999988843058, -174.7972597596632625 ) ) ;
#52136=CIRCLE ( 'NONE', #27247, 0.09999999999998898659 ) ;
#52149=CIRCLE ( 'NONE', #210394, 0.09999999999998898659 ) ;
#52151=ORIENTED_EDGE ( 'NONE', *, *, #159789, .T. ) ;
#52157=CARTESIAN_POINT ( 'NONE',  ( -23.15000000000000213, 4.350000000011156054, -179.8499999999999943 ) ) ;
#52159=CARTESIAN_POINT ( 'NONE',  ( 22.45380639572245585, 1.426796592706731485E-07, -155.7495671089028804 ) ) ;
#52185=CARTESIAN_POINT ( 'NONE',  ( 22.39999999999999503, -0.09999999998884338825, -155.8504291924551808 ) ) ;
#52199=DIRECTION ( 'NONE',  ( 0.000000000000000000, 0.000000000000000000, 1.000000000000000000 ) ) ;
#52206=ORIENTED_EDGE ( 'NONE', *, *, #236230, .F. ) ;
#52245=ORIENTED_EDGE ( 'NONE', *, *, #200962, .T. ) ;
#52289=CIRCLE ( 'NONE', #235452, 0.1000000000000000472 ) ;
#52306=DIRECTION ( 'NONE',  ( -0.000000000000000000, 0.1350103645451904977, 0.9908441862701597991 ) ) ;
#52397=ORIENTED_EDGE ( 'NONE', *, *, #38185, .T. ) ;
#52419=FACE_OUTER_BOUND ( 'NONE', #113284, .T. ) ;
#52435=B_SPLINE_CURVE_WITH_KNOTS ( 'NONE', 3,
 ( #220563, #41946, #158068, #101869, #237561, #127888, #23677, #223117, #126597, #45769 ),
 .UNSPECIFIED., .F., .F.,
 ( 4, 2, 2, 2, 4 ),
 ( 0.000000000000000000, 0.0001660831991681999738, 0.0002491247987522991476, 0.0002906455985443850824, 0.0003321663983364709629 ),
 .UNSPECIFIED. ) ;
#52452=ORIENTED_EDGE ( 'NONE', *, *, #193984, .T. ) ;
#52470=EDGE_CURVE ( 'NONE', #86456, #7699, #225741, .T. ) ;
#52507=LINE ( 'NONE', #177640, #141923 ) ;
#52532=FACE_OUTER_BOUND ( 'NONE', #152270, .T. ) ;
#52533=DIRECTION ( 'NONE',  ( 0.000000000000000000, 1.000000000000000000, 0.000000000000000000 ) ) ;
#52551=CARTESIAN_POINT ( 'NONE',  ( 20.94999999999999929, 11.75000000001115552, -194.2161343370218844 ) ) ;
#52582=LINE ( 'NONE', #151727, #216397 ) ;
#52586=ORIENTED_EDGE ( 'NONE', *, *, #18710, .F. ) ;
#52609=EDGE_CURVE ( 'NONE', #235213, #252182, #246605, .T. ) ;
#52616=CARTESIAN_POINT ( 'NONE',  ( -20.54999999999999716, 2.000000000011154189, -180.7246219227620543 ) ) ;
#52702=VERTEX_POINT ( 'NONE', #135170 ) ;
#52746=ORIENTED_EDGE ( 'NONE', *, *, #177579, .T. ) ;
#52747=ORIENTED_EDGE ( 'NONE', *, *, #195130, .T. ) ;
#52755=ORIENTED_EDGE ( 'NONE', *, *, #211614, .T. ) ;
#52759=VERTEX_POINT ( 'NONE', #138996 ) ;
#52817=FACE_OUTER_BOUND ( 'NONE', #17328, .T. ) ;
#52833=DIRECTION ( 'NONE',  ( 0.000000000000000000, 0.000000000000000000, -1.000000000000000000 ) ) ;
#52839=EDGE_CURVE ( 'NONE', #257429, #33688, #17640, .T. ) ;
#52849=FACE_OUTER_BOUND ( 'NONE', #27738, .T. ) ;
#52856=VERTEX_POINT ( 'NONE', #39969 ) ;
#52860=VERTEX_POINT ( 'NONE', #99873 ) ;
#52879=EDGE_CURVE ( 'NONE', #236598, #145192, #38511, .T. ) ;
#52995=DIRECTION ( 'NONE',  ( 0.7071067811865474617, 0.7071067811865474617, 0.000000000000000000 ) ) ;
#53045=CARTESIAN_POINT ( 'NONE',  ( -22.45372860728439690, 0.01492061955964466002, -155.8502028652960973 ) ) ;
#53070=EDGE_LOOP ( 'NONE', ( #157225, #93377, #150849, #97364, #180005 ) ) ;
#53082=CARTESIAN_POINT ( 'NONE',  ( 22.47007471830799474, 7.720710651937603863, -167.4999999999999432 ) ) ;
#53116=AXIS2_PLACEMENT_3D ( 'NONE', #73698, #33299, #34560 ) ;
#53117=ORIENTED_EDGE ( 'NONE', *, *, #3637, .F. ) ;
#53135=EDGE_LOOP ( 'NONE', ( #98201, #220013, #58423, #167546 ) ) ;
#53211=DIRECTION ( 'NONE',  ( 1.000000000000000000, 7.304098846218134667E-16, -0.000000000000000000 ) ) ;
#53225=EDGE_CURVE ( 'NONE', #163390, #122995, #194876, .T. ) ;
#53301=FACE_OUTER_BOUND ( 'NONE', #53135, .T. ) ;
#53311=EDGE_CURVE ( 'NONE', #135750, #90736, #241684, .T. ) ;
#53346=FACE_OUTER_BOUND ( 'NONE', #159183, .T. ) ;
#53359=ORIENTED_EDGE ( 'NONE', *, *, #25094, .F. ) ;
#53375=CARTESIAN_POINT ( 'NONE',  ( 21.14999999999999858, -0.09999999998884338825, -155.8504291924551808 ) ) ;
#53379=DIRECTION ( 'NONE',  ( 1.000000000000000000, 0.000000000000000000, 0.000000000000000000 ) ) ;
#53417=ORIENTED_EDGE ( 'NONE', *, *, #213163, .F. ) ;
#53429=CIRCLE ( 'NONE', #82604, 0.1000000000000102612 ) ;
#53438=AXIS2_PLACEMENT_3D ( 'NONE', #220490, #101774, #2696 ) ;
#53453=CARTESIAN_POINT ( 'NONE',  ( -18.59999999999999787, 1.162701749949165642, -175.5999999999999659 ) ) ;
#53462=CARTESIAN_POINT ( 'NONE',  ( 22.49999999999999645, 0.1008583691098678403, -155.7504328765105868 ) ) ;
#53468=EDGE_CURVE ( 'NONE', #100214, #12612, #113138, .T. ) ;
#53475=LINE ( 'NONE', #170908, #61970 ) ;
#53492=AXIS2_PLACEMENT_3D ( 'NONE', #49939, #129492, #250708 ) ;
#53503=DIRECTION ( 'NONE',  ( 0.000000000000000000, 0.000000000000000000, -1.000000000000000000 ) ) ;
#53519=EDGE_CURVE ( 'NONE', #182339, #117379, #84032, .T. ) ;
#53520=FACE_OUTER_BOUND ( 'NONE', #160077, .T. ) ;
#53524=FACE_OUTER_BOUND ( 'NONE', #87128, .T. ) ;
#53526=DIRECTION ( 'NONE',  ( -0.8660254037844653530, 0.000000000000000000, 0.4999999999999539257 ) ) ;
#53536=ORIENTED_EDGE ( 'NONE', *, *, #157329, .T. ) ;
#53544=DIRECTION ( 'NONE',  ( 0.000000000000000000, -1.000000000000000000, 6.308085367188393199E-16 ) ) ;
#53548=CARTESIAN_POINT ( 'NONE',  ( 20.94999999999999929, 1.115650877919449413E-11, -196.8999999999999773 ) ) ;
#53580=AXIS2_PLACEMENT_3D ( 'NONE', #46933, #45672, #223009 ) ;
#53583=ORIENTED_EDGE ( 'NONE', *, *, #30875, .T. ) ;
#53642=TOROIDAL_SURFACE ( 'NONE', #107604, 7.791421356237316687, 0.1000000000000000056 ) ;
#53686=ORIENTED_EDGE ( 'NONE', *, *, #206835, .T. ) ;
#53689=EDGE_CURVE ( 'NONE', #152331, #150045, #75734, .T. ) ;
#53706=ORIENTED_EDGE ( 'NONE', *, *, #12491, .T. ) ;
#53739=AXIS2_PLACEMENT_3D ( 'NONE', #223389, #143856, #162174 ) ;
#53760=EDGE_CURVE ( 'NONE', #209946, #56169, #182388, .T. ) ;
#53824=DIRECTION ( 'NONE',  ( -0.000000000000000000, 0.000000000000000000, 1.000000000000000000 ) ) ;
#53866=AXIS2_PLACEMENT_3D ( 'NONE', #216602, #200890, #237454 ) ;
#53869=CARTESIAN_POINT ( 'NONE',  ( -20.64999999999999858, -8.999999999988844479, -191.5060308773475413 ) ) ;
#53874=CARTESIAN_POINT ( 'NONE',  ( -21.78635804494510708, 7.035661485164336426, -167.4009949344922745 ) ) ;
#53903=CARTESIAN_POINT ( 'NONE',  ( -21.05000000000000071, -12.41227409413852811, -198.0999999999999659 ) ) ;
#53908=LINE ( 'NONE', #124775, #47324 ) ;
#53919=AXIS2_PLACEMENT_3D ( 'NONE', #11490, #253919, #75329 ) ;
#53922=ORIENTED_EDGE ( 'NONE', *, *, #134453, .F. ) ;
#53937=ORIENTED_EDGE ( 'NONE', *, *, #26461, .F. ) ;
#53989=CARTESIAN_POINT ( 'NONE',  ( 20.94999999999999929, 5.900000000011162093, -190.7809002353436085 ) ) ;
#54003=ORIENTED_EDGE ( 'NONE', *, *, #146154, .T. ) ;
#54023=VERTEX_POINT ( 'NONE', #142908 ) ;
#54040=ADVANCED_FACE ( 'NONE', ( #7261 ), #64675, .F. ) ;
#54044=EDGE_CURVE ( 'NONE', #190824, #77502, #165066, .T. ) ;
#54055=DIRECTION ( 'NONE',  ( 0.000000000000000000, -1.776356839400308446E-15, -1.000000000000000000 ) ) ;
#54068=CARTESIAN_POINT ( 'NONE',  ( 21.13461538461538680, 8.885417037985613220, -179.7500000000000000 ) ) ;
#54095=CARTESIAN_POINT ( 'NONE',  ( 23.24999999999999289, 11.65000000001116298, -179.6499999999999773 ) ) ;
#54104=CARTESIAN_POINT ( 'NONE',  ( -20.64999999999999858, 7.150000000011155876, -188.7499999999999716 ) ) ;
#54110=EDGE_LOOP ( 'NONE', ( #182911, #135053, #168947, #252821 ) ) ;
#54123=EDGE_CURVE ( 'NONE', #17415, #235498, #21713, .T. ) ;
#54142=CARTESIAN_POINT ( 'NONE',  ( -20.94999999999999929, 1.115600667400684642E-11, -200.9999999999999432 ) ) ;
#54152=SPHERICAL_SURFACE ( 'NONE', #26099, 0.1000000000000000056 ) ;
#54218=FACE_OUTER_BOUND ( 'NONE', #4883, .T. ) ;
#54221=CARTESIAN_POINT ( 'NONE',  ( -21.37071067811865532, 8.070710678129811910, -188.7499999999999716 ) ) ;
#54229=AXIS2_PLACEMENT_3D ( 'NONE', #129018, #67750, #70351 ) ;
#54242=ORIENTED_EDGE ( 'NONE', *, *, #118507, .F. ) ;
#54250=EDGE_LOOP ( 'NONE', ( #121133, #439, #162908, #193570 ) ) ;
#54265=ORIENTED_EDGE ( 'NONE', *, *, #201465, .T. ) ;
#54268=ORIENTED_EDGE ( 'NONE', *, *, #208631, .T. ) ;
#54272=ORIENTED_EDGE ( 'NONE', *, *, #49033, .T. ) ;
#54306=VERTEX_POINT ( 'NONE', #88062 ) ;
#54318=ADVANCED_FACE ( 'NONE', ( #155801 ), #193618, .T. ) ;
#54340=ORIENTED_EDGE ( 'NONE', *, *, #200622, .F. ) ;
#54343=LINE ( 'NONE', #94757, #12877 ) ;
#54347=ORIENTED_EDGE ( 'NONE', *, *, #129594, .F. ) ;
#54380=CARTESIAN_POINT ( 'NONE',  ( -18.50000000000000000, 1.115600667400684642E-11, -200.9999999999999432 ) ) ;
#54397=ADVANCED_FACE ( 'NONE', ( #157072 ), #101147, .T. ) ;
#54400=CARTESIAN_POINT ( 'NONE',  ( 18.59999999999999432, -1.866714910046153308, -179.2526752462819672 ) ) ;
#54421=ORIENTED_EDGE ( 'NONE', *, *, #227737, .F. ) ;
#54429=ORIENTED_EDGE ( 'NONE', *, *, #2583, .T. ) ;
#54430=FACE_OUTER_BOUND ( 'NONE', #124824, .T. ) ;
#54432=CARTESIAN_POINT ( 'NONE',  ( -22.50000000000000000, 1.115600667400684642E-11, -167.4999999999999716 ) ) ;
#54443=CYLINDRICAL_SURFACE ( 'NONE', #53919, 0.1000000000000098310 ) ;
#54444=VECTOR ( 'NONE', #73706, 1000.000000000000000 ) ;
#54453=CARTESIAN_POINT ( 'NONE',  ( -18.50000000000000000, 11.65000000001115232, -179.6499999999999773 ) ) ;
#54466=ADVANCED_FACE ( 'NONE', ( #140036 ), #246946, .T. ) ;
#54479=ORIENTED_EDGE ( 'NONE', *, *, #252797, .T. ) ;
#54511=EDGE_LOOP ( 'NONE', ( #15335, #181333, #86687, #142882 ) ) ;
#54541=CARTESIAN_POINT ( 'NONE',  ( 19.99999999999998934, 11.65000000001115943, -188.7499999999999716 ) ) ;
#54632=ORIENTED_EDGE ( 'NONE', *, *, #213959, .F. ) ;
#54656=AXIS2_PLACEMENT_3D ( 'NONE', #147819, #48695, #244325 ) ;
#54663=VERTEX_POINT ( 'NONE', #210317 ) ;
#54666=CARTESIAN_POINT ( 'NONE',  ( -18.50000000000000000, 11.75000000001115197, -167.5999999999999659 ) ) ;
#54672=DIRECTION ( 'NONE',  ( -1.000000000000000000, 0.000000000000000000, 0.000000000000000000 ) ) ;
#54687=EDGE_CURVE ( 'NONE', #172274, #137741, #60677, .T. ) ;
#54688=AXIS2_PLACEMENT_3D ( 'NONE', #12895, #33762, #251468 ) ;
#54760=DIRECTION ( 'NONE',  ( 1.000000000000000000, 0.000000000000000000, -0.000000000000000000 ) ) ;
#54788=ORIENTED_EDGE ( 'NONE', *, *, #27012, .F. ) ;
#54790=LINE ( 'NONE', #249169, #221603 ) ;
#54793=CARTESIAN_POINT ( 'NONE',  ( -20.94999999999999929, 1.115600667400684642E-11, -189.2999999999999545 ) ) ;
#54806=CARTESIAN_POINT ( 'NONE',  ( -23.15000000000000213, -8.663551401858004652, -177.0241011180672785 ) ) ;
#54810=EDGE_CURVE ( 'NONE', #81259, #234897, #124058, .T. ) ;
#54819=DIRECTION ( 'NONE',  ( 7.304098846218134667E-16, 1.000000000000000000, -0.000000000000000000 ) ) ;
#54840=DIRECTION ( 'NONE',  ( 1.000000000000000000, 0.000000000000000000, 0.000000000000000000 ) ) ;
#54883=DIRECTION ( 'NONE',  ( 2.952720810173289112E-16, -1.000000000000000000, 0.000000000000000000 ) ) ;
#54895=EDGE_LOOP ( 'NONE', ( #199627, #34030, #141048, #149643 ) ) ;
#54918=ORIENTED_EDGE ( 'NONE', *, *, #200962, .F. ) ;
#54926=DIRECTION ( 'NONE',  ( -0.000000000000000000, -1.000000000000000000, 0.000000000000000000 ) ) ;
#54946=DIRECTION ( 'NONE',  ( -1.000000000000000000, -0.000000000000000000, -0.000000000000000000 ) ) ;
#54970=DIRECTION ( 'NONE',  ( -0.000000000000000000, 1.000000000000000000, 1.734723475976807292E-15 ) ) ;
#54976=ORIENTED_EDGE ( 'NONE', *, *, #48133, .F. ) ;
#54992=DIRECTION ( 'NONE',  ( 1.000000000000000000, 2.952720810173289112E-16, -0.000000000000000000 ) ) ;
#55017=VERTEX_POINT ( 'NONE', #27554 ) ;
#55020=DIRECTION ( 'NONE',  ( 0.000000000000000000, 1.776356839400188145E-15, 1.000000000000000000 ) ) ;
#55059=CARTESIAN_POINT ( 'NONE',  ( 20.85000000000000142, -1.835859311432481045, -212.5044391687984842 ) ) ;
#55063=DIRECTION ( 'NONE',  ( 2.952720810173289112E-16, -1.000000000000000000, 0.000000000000000000 ) ) ;
#55064=CARTESIAN_POINT ( 'NONE',  ( 19.81427058490544013, 11.66856398039208109, -192.2499999999999716 ) ) ;
#55092=CARTESIAN_POINT ( 'NONE',  ( -20.94999999999999929, 7.120270961708750512, -204.6595630418393057 ) ) ;
#55115=ORIENTED_EDGE ( 'NONE', *, *, #57073, .T. ) ;
#55204=AXIS2_PLACEMENT_3D ( 'NONE', #255665, #172377, #211455 ) ;
#55226=B_SPLINE_CURVE_WITH_KNOTS ( 'NONE', 3,
 ( #66772, #107167, #68047, #141482 ),
 .UNSPECIFIED., .F., .F.,
 ( 4, 4 ),
 ( 0.000000000000000000, 0.0002118541922231684618 ),
 .UNSPECIFIED. ) ;
#55240=ADVANCED_FACE ( 'NONE', ( #99007 ), #198136, .T. ) ;
#55305=ADVANCED_FACE ( 'NONE', ( #52849 ), #34606, .T. ) ;
#55325=CARTESIAN_POINT ( 'NONE',  ( 21.59780538579341780, 0.09897866960914131207, -160.6529094700567271 ) ) ;
#55338=CIRCLE ( 'NONE', #51261, 6.329289321881370611 ) ;
#55351=DIRECTION ( 'NONE',  ( -0.000000000000000000, 0.8660254037844502539, 0.4999999999999799050 ) ) ;
#55373=CARTESIAN_POINT ( 'NONE',  ( 20.94999999999999929, 1.115600667400684642E-11, -180.4749999999999659 ) ) ;
#55383=CARTESIAN_POINT ( 'NONE',  ( -18.49513951962167724, -9.437725026666544892, -207.7780725750291140 ) ) ;
#55422=EDGE_CURVE ( 'NONE', #80866, #33844, #214192, .T. ) ;
#55439=FACE_OUTER_BOUND ( 'NONE', #13465, .T. ) ;
#55447=CIRCLE ( 'NONE', #201226, 11.64999999999999325 ) ;
#55485=DIRECTION ( 'NONE',  ( 0.000000000000000000, 0.000000000000000000, 1.000000000000000000 ) ) ;
#55498=FACE_OUTER_BOUND ( 'NONE', #117881, .T. ) ;
#55527=ORIENTED_EDGE ( 'NONE', *, *, #14646, .T. ) ;
#55564=CARTESIAN_POINT ( 'NONE',  ( -20.96077737575314970, 11.62390063401601381, -194.1407919571067566 ) ) ;
#55572=AXIS2_PLACEMENT_3D ( 'NONE', #147483, #94880, #227011 ) ;
#55606=ORIENTED_EDGE ( 'NONE', *, *, #140249, .T. ) ;
#55622=EDGE_LOOP ( 'NONE', ( #252594, #225593, #112032, #161139 ) ) ;
#55654=DIRECTION ( 'NONE',  ( 0.000000000000000000, 0.000000000000000000, 1.000000000000000000 ) ) ;
#55659=CARTESIAN_POINT ( 'NONE',  ( 23.14999999999999858, 1.115600667400684642E-11, -167.4999999999999716 ) ) ;
#55673=CARTESIAN_POINT ( 'NONE',  ( -20.64999999999999858, 1.115623935689868526E-11, -199.0999999999999375 ) ) ;
#55690=FACE_OUTER_BOUND ( 'NONE', #237487, .T. ) ;
#55700=CARTESIAN_POINT ( 'NONE',  ( -21.64999999999999858, 7.350000000011155166, -179.8499999999999943 ) ) ;
#55701=DIRECTION ( 'NONE',  ( -0.000000000000000000, -0.000000000000000000, 1.000000000000000000 ) ) ;
#55703=EDGE_LOOP ( 'NONE', ( #219416, #237301, #257910, #126820 ) ) ;
#55740=DIRECTION ( 'NONE',  ( 1.000000000000000000, 0.000000000000000000, 0.000000000000000000 ) ) ;
#55750=DIRECTION ( 'NONE',  ( 2.952720810173289112E-16, -1.000000000000000000, -0.000000000000000000 ) ) ;
#55752=CARTESIAN_POINT ( 'NONE',  ( -18.59999999999999787, 7.070967871809997973, -204.7465642218682547 ) ) ;
#55794=DIRECTION ( 'NONE',  ( -0.7071067811865389130, 0.000000000000000000, 0.7071067811865561215 ) ) ;
#55801=CARTESIAN_POINT ( 'NONE',  ( 20.97438252431638972, 8.925423506087151182, -175.9723706890107735 ) ) ;
#55837=CIRCLE ( 'NONE', #243293, 0.5000000000000004441 ) ;
#55842=AXIS2_PLACEMENT_3D ( 'NONE', #137826, #38754, #120881 ) ;
#55859=CIRCLE ( 'NONE', #197528, 0.09999999999998898659 ) ;
#55872=DIRECTION ( 'NONE',  ( 0.000000000000000000, 0.000000000000000000, -1.000000000000000000 ) ) ;
#55909=CIRCLE ( 'NONE', #235015, 0.5999999999999894307 ) ;
#55910=ORIENTED_EDGE ( 'NONE', *, *, #241963, .F. ) ;
#55983=LINE ( 'NONE', #118572, #225810 ) ;
#55993=CARTESIAN_POINT ( 'NONE',  ( 20.94999999999999574, 8.926614585098251453, -175.9716830192230930 ) ) ;
#56002=CARTESIAN_POINT ( 'NONE',  ( 21.05000000000000071, 8.826429739528350638, -175.9140547129436527 ) ) ;
#56003=DIRECTION ( 'NONE',  ( 0.000000000000000000, 0.000000000000000000, -1.000000000000000000 ) ) ;
#56012=AXIS2_PLACEMENT_3D ( 'NONE', #42757, #23223, #225216 ) ;
#56037=ORIENTED_EDGE ( 'NONE', *, *, #135238, .T. ) ;
#56048=TOROIDAL_SURFACE ( 'NONE', #80998, 0.6000000000000013101, 0.1000000000000000056 ) ;
#56054=ORIENTED_EDGE ( 'NONE', *, *, #75390, .T. ) ;
#56058=CIRCLE ( 'NONE', #89210, 0.1000000000000089567 ) ;
#56086=ORIENTED_EDGE ( 'NONE', *, *, #211051, .T. ) ;
#56099=ADVANCED_FACE ( 'NONE', ( #211334 ), #227033, .T. ) ;
#56101=EDGE_CURVE ( 'NONE', #77358, #169886, #110307, .T. ) ;
#56121=EDGE_LOOP ( 'NONE', ( #68398, #188371, #205919, #235179 ) ) ;
#56153=DIRECTION ( 'NONE',  ( 0.000000000000000000, -3.122502256758250246E-14, -1.000000000000000000 ) ) ;
#56169=VERTEX_POINT ( 'NONE', #54806 ) ;
#56176=EDGE_LOOP ( 'NONE', ( #97926, #237340, #106250, #44564 ) ) ;
#56181=CARTESIAN_POINT ( 'NONE',  ( 21.05000000000000071, 5.000000000011153745, -179.9052660189130677 ) ) ;
#56185=CARTESIAN_POINT ( 'NONE',  ( 22.49544290803779489, 11.74987023786863283, -167.4346880407425147 ) ) ;
#56193=LINE ( 'NONE', #17113, #101604 ) ;
#56236=CARTESIAN_POINT ( 'NONE',  ( 21.07094088545370170, 0.09889370256337753906, -161.1798327780828117 ) ) ;
#56266=CARTESIAN_POINT ( 'NONE',  ( 20.94999999999999929, 1.115600667400684642E-11, -198.0999999999999659 ) ) ;
#56274=DIRECTION ( 'NONE',  ( -1.000000000000000000, 0.000000000000000000, 0.000000000000000000 ) ) ;
#56291=AXIS2_PLACEMENT_3D ( 'NONE', #229723, #51048, #31562 ) ;
#56295=ORIENTED_EDGE ( 'NONE', *, *, #35719, .T. ) ;
#56301=VECTOR ( 'NONE', #195867, 1000.000000000000000 ) ;
#56306=CARTESIAN_POINT ( 'NONE',  ( -20.64999999999999858, 2.400000000011155432, -187.7753780772378889 ) ) ;
#56307=CARTESIAN_POINT ( 'NONE',  ( 20.94999999999999929, -8.999999999988842703, -191.1060308773475072 ) ) ;
#56327=DIRECTION ( 'NONE',  ( -1.000000000000000000, 0.000000000000000000, 0.000000000000000000 ) ) ;
#56352=CARTESIAN_POINT ( 'NONE',  ( 20.01093837587850288, 11.75000000001116263, -192.2543974345975926 ) ) ;
#56358=EDGE_CURVE ( 'NONE', #4326, #157944, #34465, .T. ) ;
#56363=ORIENTED_EDGE ( 'NONE', *, *, #176340, .T. ) ;
#56370=CARTESIAN_POINT ( 'NONE',  ( 20.94999999999999574, -11.64999999998883595, -170.4999999999999716 ) ) ;
#56379=EDGE_CURVE ( 'NONE', #221674, #85751, #239508, .T. ) ;
#56387=VECTOR ( 'NONE', #183720, 1000.000000000000000 ) ;
#56421=VECTOR ( 'NONE', #50680, 1000.000000000000000 ) ;
#56426=DIRECTION ( 'NONE',  ( 1.000000000000000000, -0.000000000000000000, -0.000000000000000000 ) ) ;
#56449=ORIENTED_EDGE ( 'NONE', *, *, #61390, .F. ) ;
#56460=CARTESIAN_POINT ( 'NONE',  ( 20.94999999999999574, -11.64999999998883595, -170.3999999999999773 ) ) ;
#56532=CARTESIAN_POINT ( 'NONE',  ( -21.05000000000000071, 5.850000000011156942, -190.8675027757220448 ) ) ;
#56547=ORIENTED_EDGE ( 'NONE', *, *, #81364, .F. ) ;
#56564=DIRECTION ( 'NONE',  ( 0.000000000000000000, 0.9998779222360102414, 0.01562499999996356907 ) ) ;
#56590=CIRCLE ( 'NONE', #235688, 7.791421356237338003 ) ;
#56592=CARTESIAN_POINT ( 'NONE',  ( -18.50000000000000000, -1.835859311432484375, -212.5044391687984842 ) ) ;
#56595=AXIS2_PLACEMENT_3D ( 'NONE', #151351, #230888, #87484 ) ;
#56602=CARTESIAN_POINT ( 'NONE',  ( 23.15000000000000213, -11.48912529306489994, -197.8999999999999773 ) ) ;
#56625=B_SPLINE_CURVE_WITH_KNOTS ( 'NONE', 3,
 ( #135646, #218317, #117956, #77519, #154557, #194954, #155827 ),
 .UNSPECIFIED., .F., .F.,
 ( 4, 3, 4 ),
 ( 0.000000000000000000, 0.0007844235214594269838, 0.001767853679404345069 ),
 .UNSPECIFIED. ) ;
#56631=CARTESIAN_POINT ( 'NONE',  ( -18.59999999999999787, 7.021664781911246322, -204.8335654018972605 ) ) ;
#56635=FACE_OUTER_BOUND ( 'NONE', #158677, .T. ) ;
#56648=CIRCLE ( 'NONE', #148261, 0.09999999999998898659 ) ;
#56666=AXIS2_PLACEMENT_3D ( 'NONE', #161228, #144200, #3408 ) ;
#56679=CARTESIAN_POINT ( 'NONE',  ( 20.95595624212409547, 10.62389120310530366, -175.1296329141266312 ) ) ;
#56688=DIRECTION ( 'NONE',  ( 0.000000000000000000, 0.000000000000000000, -1.000000000000000000 ) ) ;
#56717=CYLINDRICAL_SURFACE ( 'NONE', #195576, 0.5000000000000004441 ) ;
#56729=VECTOR ( 'NONE', #229608, 1000.000000000000000 ) ;
#56731=AXIS2_PLACEMENT_3D ( 'NONE', #149430, #68596, #245951 ) ;
#56811=DIRECTION ( 'NONE',  ( 1.000000000000000000, -7.304098846218134667E-16, 0.000000000000000000 ) ) ;
#56849=CARTESIAN_POINT ( 'NONE',  ( -21.05315837717337857, 11.75000001535411798, -194.1583560218909099 ) ) ;
#56895=CARTESIAN_POINT ( 'NONE',  ( 21.05000000000000071, 1.115600667400684642E-11, -204.9999999999999716 ) ) ;
#56940=VERTEX_POINT ( 'NONE', #3647 ) ;
#56952=DIRECTION ( 'NONE',  ( 0.000000000000000000, 0.000000000000000000, -1.000000000000000000 ) ) ;
#56957=CARTESIAN_POINT ( 'NONE',  ( -18.59999999999999787, 11.75000000001115197, -155.7499999999999716 ) ) ;
#56961=DIRECTION ( 'NONE',  ( -0.000000000000000000, -0.8700118002898321601, 0.4930308989875230030 ) ) ;
#56968=AXIS2_PLACEMENT_3D ( 'NONE', #4310, #104672, #61734 ) ;
#56998=FACE_OUTER_BOUND ( 'NONE', #217008, .T. ) ;
#57006=EDGE_CURVE ( 'NONE', #12588, #133509, #257925, .T. ) ;
#57043=CARTESIAN_POINT ( 'NONE',  ( 18.55121869061587958, 10.32747123227773400, -206.5774032850248716 ) ) ;
#57047=CIRCLE ( 'NONE', #90387, 0.1000000000000089567 ) ;
#57058=ORIENTED_EDGE ( 'NONE', *, *, #101597, .F. ) ;
#57071=ORIENTED_EDGE ( 'NONE', *, *, #254640, .F. ) ;
#57072=DIRECTION ( 'NONE',  ( 0.000000000000000000, -0.4930308989874653269, -0.8700118002898649117 ) ) ;
#57073=EDGE_CURVE ( 'NONE', #87114, #13008, #123335, .T. ) ;
#57093=EDGE_LOOP ( 'NONE', ( #23402, #108347, #71005, #13399 ) ) ;
#57095=CARTESIAN_POINT ( 'NONE',  ( 20.97217846901851956, 8.875441724720829484, -176.0012276839371737 ) ) ;
#57096=DIRECTION ( 'NONE',  ( 0.000000000000000000, 1.000000000000000000, 0.000000000000000000 ) ) ;
#57125=DIRECTION ( 'NONE',  ( -1.000000000000000000, -1.040834085586090568E-13, 0.000000000000000000 ) ) ;
#57130=CIRCLE ( 'NONE', #252778, 0.6000000000000015321 ) ;
#57135=CARTESIAN_POINT ( 'NONE',  ( -21.30740335185486245, 0.09893452578700702438, -160.9433420779719768 ) ) ;
#57154=LINE ( 'NONE', #178444, #13478 ) ;
#57182=ORIENTED_EDGE ( 'NONE', *, *, #137398, .T. ) ;
#57200=VERTEX_POINT ( 'NONE', #90890 ) ;
#57203=DIRECTION ( 'NONE',  ( 2.952720810173289112E-16, -1.000000000000000000, -0.000000000000000000 ) ) ;
#57211=CARTESIAN_POINT ( 'NONE',  ( -18.59999999999999787, -1.835341550213255957, -179.0551512925629538 ) ) ;
#57238=PLANE ( 'NONE',  #65501 ) ;
#57250=CARTESIAN_POINT ( 'NONE',  ( -23.15000000000000213, 2.600000000011154278, -187.7753780772378889 ) ) ;
#57282=CARTESIAN_POINT ( 'NONE',  ( 20.94999999999999574, 10.47338541492405994, -175.0786544642485012 ) ) ;
#57283=EDGE_CURVE ( 'NONE', #11139, #209575, #85885, .T. ) ;
#57284=CIRCLE ( 'NONE', #207343, 0.5000000000000004441 ) ;
#57287=CARTESIAN_POINT ( 'NONE',  ( 22.59999954896768770, -0.008828232232978959135, -155.7494913259319844 ) ) ;
#57292=VERTEX_POINT ( 'NONE', #59428 ) ;
#57295=CARTESIAN_POINT ( 'NONE',  ( 20.85000000000000142, -1.835859311432481045, -212.5044391687984842 ) ) ;
#57312=AXIS2_PLACEMENT_3D ( 'NONE', #129795, #234027, #192346 ) ;
#57318=EDGE_LOOP ( 'NONE', ( #18609, #88398, #233558, #147293 ) ) ;
#57359=CARTESIAN_POINT ( 'NONE',  ( -20.00857864376270001, 9.150000000011157653, -179.7499999999999716 ) ) ;
#57378=VERTEX_POINT ( 'NONE', #39935 ) ;
#57417=ORIENTED_EDGE ( 'NONE', *, *, #112714, .T. ) ;
#57479=ORIENTED_EDGE ( 'NONE', *, *, #13001, .T. ) ;
#57491=VERTEX_POINT ( 'NONE', #86708 ) ;
#57499=DIRECTION ( 'NONE',  ( -0.000000000000000000, 1.000000000000000000, -1.224646799147352961E-16 ) ) ;
#57510=VECTOR ( 'NONE', #77993, 1000.000000000000000 ) ;
#57531=ORIENTED_EDGE ( 'NONE', *, *, #239703, .T. ) ;
#57533=EDGE_CURVE ( 'NONE', #196293, #175979, #127619, .T. ) ;
#57538=CARTESIAN_POINT ( 'NONE',  ( -23.25000000000000000, 6.933893972137497030, -204.7856458343735255 ) ) ;
#57553=FACE_OUTER_BOUND ( 'NONE', #58055, .T. ) ;
#57560=CARTESIAN_POINT ( 'NONE',  ( -18.59999999999999787, 11.75000000001115197, -174.5148057706539930 ) ) ;
#57570=CIRCLE ( 'NONE', #195163, 0.09999999999999062417 ) ;
#57599=CARTESIAN_POINT ( 'NONE',  ( -18.59999999999999787, 9.250000000011157297, -179.8499999999999943 ) ) ;
#57611=DIRECTION ( 'NONE',  ( -0.000000000000000000, 1.000000000000000000, 1.626303258728266709E-15 ) ) ;
#57614=AXIS2_PLACEMENT_3D ( 'NONE', #94224, #176361, #173826 ) ;
#57619=AXIS2_PLACEMENT_3D ( 'NONE', #116673, #157110, #138766 ) ;
#57640=CARTESIAN_POINT ( 'NONE',  ( 20.04142135623731136, 11.75000000001116263, -192.1499999999999488 ) ) ;
#57642=CARTESIAN_POINT ( 'NONE',  ( 23.25000000000000000, -8.596261682231828516, -191.5498724828496790 ) ) ;
#57647=DIRECTION ( 'NONE',  ( -1.000000000000000000, 0.000000000000000000, 0.000000000000000000 ) ) ;
#57672=AXIS2_PLACEMENT_3D ( 'NONE', #59323, #60628, #42371 ) ;
#57674=DIRECTION ( 'NONE',  ( 0.000000000000000000, 8.881784197002011602E-16, -1.000000000000000000 ) ) ;
#57684=ORIENTED_EDGE ( 'NONE', *, *, #237235, .T. ) ;
#57685=DIRECTION ( 'NONE',  ( -3.265361837132813093E-16, 1.000000000000000000, 0.000000000000000000 ) ) ;
#57705=( BOUNDED_CURVE ( )  B_SPLINE_CURVE ( 3, ( #140440, #200430, #126013, #202989 ),
 .UNSPECIFIED., .F., .F. ) 
 B_SPLINE_CURVE_WITH_KNOTS ( ( 4, 4 ),
 ( 3.141592653589793116, 4.712388980384689674 ),
 .UNSPECIFIED. ) 
 CURVE ( )  GEOMETRIC_REPRESENTATION_ITEM ( )  RATIONAL_B_SPLINE_CURVE ( ( 1.000000000000000000, 0.8047378541243649375, 0.8047378541243649375, 1.000000000000000000 ) ) 
 REPRESENTATION_ITEM ( '' )  );
#57719=CIRCLE ( 'NONE', #257576, 0.5000000000000004441 ) ;
#57735=ORIENTED_EDGE ( 'NONE', *, *, #34875, .F. ) ;
#57751=EDGE_CURVE ( 'NONE', #220457, #10283, #175299, .T. ) ;
#57770=CARTESIAN_POINT ( 'NONE',  ( 20.94999999999999929, 1.115600667400684642E-11, -205.0999999999999375 ) ) ;
#57848=CIRCLE ( 'NONE', #74485, 2.000000000000001776 ) ;
#57877=DIRECTION ( 'NONE',  ( -3.265361837132813093E-16, 1.000000000000000000, 0.000000000000000000 ) ) ;
#57879=ADVANCED_FACE ( 'NONE', ( #227223 ), #218795, .F. ) ;
#57881=ORIENTED_EDGE ( 'NONE', *, *, #22593, .T. ) ;
#57888=CARTESIAN_POINT ( 'NONE',  ( -18.50000324121759121, 10.29307482169070909, -206.4586421466939896 ) ) ;
#57898=AXIS2_PLACEMENT_3D ( 'NONE', #48033, #128874, #209684 ) ;
#57908=CARTESIAN_POINT ( 'NONE',  ( 22.57856590037848576, -0.004128330053175016841, -155.7499415373246165 ) ) ;
#57910=CARTESIAN_POINT ( 'NONE',  ( 21.12642695952774119, 0.09890328320052040045, -161.1243400779648027 ) ) ;
#57934=DIRECTION ( 'NONE',  ( 0.000000000000000000, -1.000000000000000000, 0.000000000000000000 ) ) ;
#57978=CARTESIAN_POINT ( 'NONE',  ( -21.05000000000000071, 1.162701749949165642, -175.5999999999999659 ) ) ;
#58002=DIRECTION ( 'NONE',  ( 1.000000000000000000, -0.000000000000000000, -0.000000000000000000 ) ) ;
#58019=CARTESIAN_POINT ( 'NONE',  ( -20.85000000000000142, -11.74999999998884448, -200.9999999999999432 ) ) ;
#58047=VECTOR ( 'NONE', #55750, 1000.000000000000000 ) ;
#58055=EDGE_LOOP ( 'NONE', ( #129352, #224284, #14573, #156041 ) ) ;
#58056=LINE ( 'NONE', #13820, #107382 ) ;
#58145=CARTESIAN_POINT ( 'NONE',  ( 23.14999999999999503, 14.10000000001115694, -195.3997023888606179 ) ) ;
#58163=CARTESIAN_POINT ( 'NONE',  ( 18.59999999999999076, 1.835341550235567887, -179.0551512925629538 ) ) ;
#58178=VERTEX_POINT ( 'NONE', #17192 ) ;
#58228=EDGE_CURVE ( 'NONE', #5557, #4296, #131503, .T. ) ;
#58251=CARTESIAN_POINT ( 'NONE',  ( 21.09107601085556638, 0.03930716472845496856, -161.1361220246400592 ) ) ;
#58254=DIRECTION ( 'NONE',  ( 1.000000000000000000, 0.000000000000000000, 0.000000000000000000 ) ) ;
#58276=EDGE_LOOP ( 'NONE', ( #13506, #118121, #141212, #79142 ) ) ;
#58282=AXIS2_PLACEMENT_3D ( 'NONE', #216390, #256753, #160305 ) ;
#58305=CARTESIAN_POINT ( 'NONE',  ( -21.05000000000000071, 11.65000000001115232, -174.2838656629781156 ) ) ;
#58307=DIRECTION ( 'NONE',  ( -1.000000000000000000, -0.000000000000000000, -0.000000000000000000 ) ) ;
#58308=ORIENTED_EDGE ( 'NONE', *, *, #45309, .T. ) ;
#58373=CARTESIAN_POINT ( 'NONE',  ( 23.14999999999999858, -2.099999999988846344, -200.9999999999999432 ) ) ;
#58374=CARTESIAN_POINT ( 'NONE',  ( 20.21494484322224849, 9.303170737879936425, -175.8402651917702428 ) ) ;
#58377=AXIS2_PLACEMENT_3D ( 'NONE', #22049, #63719, #181125 ) ;
#58385=DIRECTION ( 'NONE',  ( 0.000000000000000000, -0.000000000000000000, 1.000000000000000000 ) ) ;
#58394=DIRECTION ( 'NONE',  ( 1.000000000000000000, 0.000000000000000000, 0.000000000000000000 ) ) ;
#58402=CIRCLE ( 'NONE', #183344, 0.6000000000000015321 ) ;
#58423=ORIENTED_EDGE ( 'NONE', *, *, #4302, .F. ) ;
#58445=EDGE_CURVE ( 'NONE', #6262, #219222, #170869, .T. ) ;
#58446=CARTESIAN_POINT ( 'NONE',  ( 20.94999999999999929, -11.64999999998883595, -198.0999999999999659 ) ) ;
#58455=AXIS2_PLACEMENT_3D ( 'NONE', #184499, #185797, #123258 ) ;
#58475=CIRCLE ( 'NONE', #204242, 0.2000000000000000944 ) ;
#58514=ORIENTED_EDGE ( 'NONE', *, *, #240748, .T. ) ;
#58536=DIRECTION ( 'NONE',  ( -0.7070776581708965169, -0.7071359030027827286, -0.000000000000000000 ) ) ;
#58575=CIRCLE ( 'NONE', #179238, 0.1000000000000096922 ) ;
#58578=EDGE_CURVE ( 'NONE', #17335, #14833, #198325, .T. ) ;
#58588=DIRECTION ( 'NONE',  ( 1.000000000000000000, 1.836970198721029934E-16, 0.000000000000000000 ) ) ;
#58635=FACE_OUTER_BOUND ( 'NONE', #60171, .T. ) ;
#58645=ORIENTED_EDGE ( 'NONE', *, *, #36143, .F. ) ;
#58650=CARTESIAN_POINT ( 'NONE',  ( -21.14999999999999858, -11.74999999998884448, -167.4999999999999432 ) ) ;
#58719=VERTEX_POINT ( 'NONE', #12401 ) ;
#58727=EDGE_LOOP ( 'NONE', ( #180588, #141308, #83476, #106988 ) ) ;
#58786=CIRCLE ( 'NONE', #75412, 0.09999999999998898659 ) ;
#58828=DIRECTION ( 'NONE',  ( -1.000000000000000000, 0.000000000000000000, -0.000000000000000000 ) ) ;
#58831=DIRECTION ( 'NONE',  ( 0.000000000000000000, 0.000000000000000000, -1.000000000000000000 ) ) ;
#58879=DIRECTION ( 'NONE',  ( 1.000000000000000000, -0.000000000000000000, -0.000000000000000000 ) ) ;
#58883=CARTESIAN_POINT ( 'NONE',  ( -23.15000000000000213, 11.65000000001115588, -167.4999999999999716 ) ) ;
#58885=CARTESIAN_POINT ( 'NONE',  ( 18.49999999999999645, 1.115600667400684642E-11, -167.4999999999999716 ) ) ;
#58897=CARTESIAN_POINT ( 'NONE',  ( -18.41799967126724979, -9.499999999988851584, -174.5320698132565269 ) ) ;
#58898=LINE ( 'NONE', #38101, #12827 ) ;
#58899=VERTEX_POINT ( 'NONE', #83861 ) ;
#58902=CARTESIAN_POINT ( 'NONE',  ( 21.05000000000000071, 5.850000000011105428, -177.6324972242779268 ) ) ;
#58926=ORIENTED_EDGE ( 'NONE', *, *, #109214, .T. ) ;
#58930=CARTESIAN_POINT ( 'NONE',  ( -21.44999999999999929, 7.350000000011155166, -188.7499999999999716 ) ) ;
#58935=CARTESIAN_POINT ( 'NONE',  ( 20.94999999999999929, 1.115600667400684642E-11, -200.9999999999999432 ) ) ;
#58936=TOROIDAL_SURFACE ( 'NONE', #213086, 0.2000000000000000111, 0.1000000000000000056 ) ;
#58975=EDGE_CURVE ( 'NONE', #108203, #87151, #8236, .T. ) ;
#59008=ORIENTED_EDGE ( 'NONE', *, *, #26907, .F. ) ;
#59047=DIRECTION ( 'NONE',  ( 0.000000000000000000, 0.000000000000000000, -1.000000000000000000 ) ) ;
#59075=VERTEX_POINT ( 'NONE', #189440 ) ;
#59080=DIRECTION ( 'NONE',  ( -1.000000000000000000, 0.000000000000000000, 0.000000000000000000 ) ) ;
#59106=ORIENTED_EDGE ( 'NONE', *, *, #130936, .F. ) ;
#59108=CARTESIAN_POINT ( 'NONE',  ( 20.02499999999999858, 9.750000000011153745, -188.6499999999999488 ) ) ;
#59111=AXIS2_PLACEMENT_3D ( 'NONE', #160929, #222138, #22715 ) ;
#59140=AXIS2_PLACEMENT_3D ( 'NONE', #55673, #149711, #229234 ) ;
#59141=EDGE_CURVE ( 'NONE', #212963, #120605, #35533, .T. ) ;
#59151=AXIS2_PLACEMENT_3D ( 'NONE', #67568, #207089, #148398 ) ;
#59153=CARTESIAN_POINT ( 'NONE',  ( -18.54148534481894117, 10.32532329027886497, -206.5699343018359286 ) ) ;
#59160=ORIENTED_EDGE ( 'NONE', *, *, #91757, .T. ) ;
#59161=CARTESIAN_POINT ( 'NONE',  ( -22.49231231312463208, 11.64998490368843953, -167.4389471123986084 ) ) ;
#59167=DIRECTION ( 'NONE',  ( 5.421010862427554711E-16, -1.000000000000000000, -3.252606517456533024E-15 ) ) ;
#59187=ORIENTED_EDGE ( 'NONE', *, *, #146902, .F. ) ;
#59191=FACE_OUTER_BOUND ( 'NONE', #252490, .T. ) ;
#59199=FACE_OUTER_BOUND ( 'NONE', #214823, .T. ) ;
#59207=EDGE_LOOP ( 'NONE', ( #118183, #145339, #158865, #248056 ) ) ;
#59220=CARTESIAN_POINT ( 'NONE',  ( 21.13461538461538325, 8.885417037985616773, -179.8499999999999943 ) ) ;
#59222=AXIS2_PLACEMENT_3D ( 'NONE', #104805, #163537, #4447 ) ;
#59248=CARTESIAN_POINT ( 'NONE',  ( 21.14999999999998082, -11.74999999998884448, -167.4999999999999432 ) ) ;
#59252=CARTESIAN_POINT ( 'NONE',  ( -18.59999999999999787, 1.115600667400684642E-11, -200.9999999999999432 ) ) ;
#59262=CARTESIAN_POINT ( 'NONE',  ( 20.95035502843362707, 10.47763832678762164, -175.0762997087363431 ) ) ;
#59323=CARTESIAN_POINT ( 'NONE',  ( 21.14999999999999858, -0.09999999998884338825, -160.9593430482987344 ) ) ;
#59345=LINE ( 'NONE', #200188, #22123 ) ;
#59347=LINE ( 'NONE', #61964, #128244 ) ;
#59371=ADVANCED_FACE ( 'NONE', ( #130434 ), #212589, .T. ) ;
#59377=ORIENTED_EDGE ( 'NONE', *, *, #234440, .T. ) ;
#59411=AXIS2_PLACEMENT_3D ( 'NONE', #111791, #110492, #46654 ) ;
#59415=CARTESIAN_POINT ( 'NONE',  ( -21.05000000000000071, 11.60000000001115339, -194.0717967697244717 ) ) ;
#59428=CARTESIAN_POINT ( 'NONE',  ( -18.50000000000000000, 1.866714910068465239, -179.2526752462819672 ) ) ;
#59445=VERTEX_POINT ( 'NONE', #151308 ) ;
#59455=CIRCLE ( 'NONE', #5497, 0.09999999999998898659 ) ;
#59458=CARTESIAN_POINT ( 'NONE',  ( 21.05000000000000071, -11.29603075032412640, -197.9521008403361009 ) ) ;
#59469=CARTESIAN_POINT ( 'NONE',  ( -21.12230431290520016, 6.457566653304160909, -167.4947901483108978 ) ) ;
#59505=ORIENTED_EDGE ( 'NONE', *, *, #249325, .F. ) ;
#59512=CARTESIAN_POINT ( 'NONE',  ( -23.15000000000000213, 1.115600667400684642E-11, -167.4999999999999716 ) ) ;
#59518=DIRECTION ( 'NONE',  ( 0.000000000000000000, -1.224646799142185182E-16, 1.000000000000000000 ) ) ;
#59544=CYLINDRICAL_SURFACE ( 'NONE', #120757, 0.09999999999998898659 ) ;
#59547=ORIENTED_EDGE ( 'NONE', *, *, #218868, .F. ) ;
#59554=DIRECTION ( 'NONE',  ( 0.000000000000000000, 1.000000000000000000, 0.000000000000000000 ) ) ;
#59561=EDGE_CURVE ( 'NONE', #128403, #170879, #204173, .T. ) ;
#59598=CARTESIAN_POINT ( 'NONE',  ( 20.94999999999999929, 6.650000000011155876, -177.5170271704400022 ) ) ;
#59608=LINE ( 'NONE', #153669, #87289 ) ;
#59612=DIRECTION ( 'NONE',  ( 1.000000000000000000, -0.000000000000000000, -0.000000000000000000 ) ) ;
#59661=EDGE_CURVE ( 'NONE', #64710, #152450, #167007, .T. ) ;
#59679=AXIS2_PLACEMENT_3D ( 'NONE', #160186, #239700, #101411 ) ;
#59700=CARTESIAN_POINT ( 'NONE',  ( 21.05000000000000071, 5.400000000011154988, -179.9052660189130677 ) ) ;
#59704=AXIS2_PLACEMENT_3D ( 'NONE', #240939, #62293, #141819 ) ;
#59714=EDGE_CURVE ( 'NONE', #236598, #238413, #246235, .T. ) ;
#59716=VERTEX_POINT ( 'NONE', #224084 ) ;
#59748=CARTESIAN_POINT ( 'NONE',  ( -21.11101077989000530, 0.01528526892543718291, -161.0763152652738484 ) ) ;
#59760=ORIENTED_EDGE ( 'NONE', *, *, #67121, .T. ) ;
#59795=ORIENTED_EDGE ( 'NONE', *, *, #33126, .F. ) ;
#59810=CARTESIAN_POINT ( 'NONE',  ( 22.39999999999999503, 7.790779598384535376, -167.3999999999999773 ) ) ;
#59820=AXIS2_PLACEMENT_3D ( 'NONE', #202265, #96703, #198 ) ;
#59844=CARTESIAN_POINT ( 'NONE',  ( -18.59999999999999787, 1.162701749949165642, -175.5999999999999659 ) ) ;
#59856=DIRECTION ( 'NONE',  ( 0.000000000000000000, 0.000000000000000000, -1.000000000000000000 ) ) ;
#59873=AXIS2_PLACEMENT_3D ( 'NONE', #107721, #4744, #187285 ) ;
#59949=VECTOR ( 'NONE', #212710, 1000.000000000000000 ) ;
#59977=DIRECTION ( 'NONE',  ( 0.000000000000000000, -0.000000000000000000, -1.000000000000000000 ) ) ;
#59979=ADVANCED_FACE ( 'NONE', ( #163671 ), #250356, .T. ) ;
#59982=EDGE_CURVE ( 'NONE', #108203, #48993, #58786, .T. ) ;
#60015=DIRECTION ( 'NONE',  ( -3.265361837132813093E-16, 1.000000000000000000, 0.000000000000000000 ) ) ;
#60032=( BOUNDED_SURFACE ( )  B_SPLINE_SURFACE ( 3, 2, ( 
 ( #95154, #53462, #176000 ),
 ( #233407, #170895, #57287 ),
 ( #230837, #52159, #216375 ),
 ( #192982, #136838, #32658 ) ),
 .UNSPECIFIED., .F., .F., .F. ) 
 B_SPLINE_SURFACE_WITH_KNOTS ( ( 4, 4 ),
 ( 3, 3 ),
 ( -1.897353801849632760E-19, 0.0003124336600439506836 ),
 ( 0.000000000000000000, 1.000000000000000000 ),
 .UNSPECIFIED. ) 
 GEOMETRIC_REPRESENTATION_ITEM ( )  RATIONAL_B_SPLINE_SURFACE ( (
 ( 1.000000000000000000, 0.7071067811865475727, 1.000000000000000000),
 ( 1.000000000000000000, 0.7089187706049675519, 1.000000000000000000),
 ( 1.000000000000000000, 0.7039288185052250402, 1.000000000000000000),
 ( 1.000000000000000000, 0.7040654476015688612, 1.000000000000000000) ) ) 
 REPRESENTATION_ITEM ( '' )  SURFACE ( )  );
#60037=DIRECTION ( 'NONE',  ( 0.000000000000000000, 0.000000000000000000, -1.000000000000000000 ) ) ;
#60042=CIRCLE ( 'NONE', #80699, 0.1999999999999987899 ) ;
#60085=LINE ( 'NONE', #199637, #103892 ) ;
#60092=DIRECTION ( 'NONE',  ( 0.000000000000000000, 2.891205793294679805E-16, -1.000000000000000000 ) ) ;
#60126=ORIENTED_EDGE ( 'NONE', *, *, #27347, .T. ) ;
#60145=EDGE_LOOP ( 'NONE', ( #109109, #152905, #210735, #99904 ) ) ;
#60159=VECTOR ( 'NONE', #245691, 1000.000000000000000 ) ;
#60160=DIRECTION ( 'NONE',  ( 3.469446951953498700E-14, -0.7899159663865300551, -0.6132151058540831201 ) ) ;
#60171=EDGE_LOOP ( 'NONE', ( #152338, #107019, #130110, #235507 ) ) ;
#60181=DIRECTION ( 'NONE',  ( -1.000000000000000000, 0.000000000000000000, 0.000000000000000000 ) ) ;
#60195=CARTESIAN_POINT ( 'NONE',  ( -21.05000000000000071, 1.162701749949165642, -175.3999999999999773 ) ) ;
#60199=CARTESIAN_POINT ( 'NONE',  ( -18.59999996769639097, -9.363273769819180359, -174.6814939154657793 ) ) ;
#60251=VERTEX_POINT ( 'NONE', #55752 ) ;
#60252=AXIS2_PLACEMENT_3D ( 'NONE', #165829, #71858, #151395 ) ;
#60256=CARTESIAN_POINT ( 'NONE',  ( -20.85000000000000142, 7.021664781911246322, -204.7335654018972662 ) ) ;
#60267=DIRECTION ( 'NONE',  ( 1.000000000000000000, 0.000000000000000000, 0.000000000000000000 ) ) ;
#60283=DIRECTION ( 'NONE',  ( 0.000000000000000000, 0.000000000000000000, -1.000000000000000000 ) ) ;
#60311=AXIS2_PLACEMENT_3D ( 'NONE', #78280, #35359, #36638 ) ;
#60328=DIRECTION ( 'NONE',  ( 1.000000000000000000, -0.000000000000000000, -0.000000000000000000 ) ) ;
#60350=DIRECTION ( 'NONE',  ( 3.616040088954497272E-32, -1.224646799147352961E-16, 1.000000000000000000 ) ) ;
#60359=B_SPLINE_CURVE_WITH_KNOTS ( 'NONE', 3,
 ( #119363, #198887, #20266, #179350, #234156, #60642, #140177, #254947 ),
 .UNSPECIFIED., .F., .F.,
 ( 4, 2, 2, 4 ),
 ( 0.000000000000000000, 9.550056980123377442E-05, 0.0001910011396024675488, 0.0003820022792049778695 ),
 .UNSPECIFIED. ) ;
#60365=B_SPLINE_CURVE_WITH_KNOTS ( 'NONE', 3,
 ( #149722, #14052, #135248, #210958, #209669, #174446, #130121, #229244 ),
 .UNSPECIFIED., .F., .F.,
 ( 4, 2, 2, 4 ),
 ( 0.000000000000000000, 0.0001094981963948558640, 0.0002189963927897117281, 0.0004379927855794304493 ),
 .UNSPECIFIED. ) ;
#60381=CIRCLE ( 'NONE', #106162, 0.09999999999998898659 ) ;
#60395=ORIENTED_EDGE ( 'NONE', *, *, #13800, .T. ) ;
#60401=AXIS2_PLACEMENT_3D ( 'NONE', #159590, #21384, #216969 ) ;
#60407=VECTOR ( 'NONE', #205989, 1000.000000000000000 ) ;
#60433=EDGE_CURVE ( 'NONE', #47818, #59075, #142197, .T. ) ;
#60436=DIRECTION ( 'NONE',  ( -0.000000000000000000, -1.265107689135680095E-16, 1.000000000000000000 ) ) ;
#60474=EDGE_CURVE ( 'NONE', #236967, #66095, #66049, .T. ) ;
#60518=CIRCLE ( 'NONE', #135342, 0.09999999999999939493 ) ;
#60535=CARTESIAN_POINT ( 'NONE',  ( 21.05000000000000071, 1.115600667400684642E-11, -200.9999999999999432 ) ) ;
#60541=CARTESIAN_POINT ( 'NONE',  ( 23.15000000000000213, -8.596261682231833845, -176.9501275171502641 ) ) ;
#60549=ORIENTED_EDGE ( 'NONE', *, *, #101843, .T. ) ;
#60554=CARTESIAN_POINT ( 'NONE',  ( 21.04999999999997584, 10.47338541492403863, -175.0786544642485012 ) ) ;
#60566=DIRECTION ( 'NONE',  ( 1.000000000000000000, 0.000000000000000000, 0.000000000000000000 ) ) ;
#60578=ORIENTED_EDGE ( 'NONE', *, *, #136023, .T. ) ;
#60606=EDGE_CURVE ( 'NONE', #86456, #95048, #200651, .T. ) ;
#60628=DIRECTION ( 'NONE',  ( -0.000000000000000000, -0.000000000000000000, 1.000000000000000000 ) ) ;
#60642=CARTESIAN_POINT ( 'NONE',  ( -21.05000000000000426, 6.413759733821437159, -167.5856130608038939 ) ) ;
#60677=B_SPLINE_CURVE_WITH_KNOTS ( 'NONE', 3,
 ( #235012, #73395, #135878, #237578, #17255, #75936, #212881, #118925 ),
 .UNSPECIFIED., .F., .F.,
 ( 4, 2, 2, 4 ),
 ( 0.000000000000000000, 0.0001306511400391344700, 0.0001959767100587032906, 0.0002613022800782720842 ),
 .UNSPECIFIED. ) ;
#60683=CARTESIAN_POINT ( 'NONE',  ( 18.59999999999999432, 1.736257131608553550, -179.0686523290174819 ) ) ;
#60746=ORIENTED_EDGE ( 'NONE', *, *, #126864, .F. ) ;
#60779=ORIENTED_EDGE ( 'NONE', *, *, #100979, .F. ) ;
#60799=CARTESIAN_POINT ( 'NONE',  ( -23.25000000000000000, -1.249999999988843369, -208.8004807544150481 ) ) ;
#60820=CARTESIAN_POINT ( 'NONE',  ( -21.44999999999999929, 7.350000000011155166, -179.8499999999999943 ) ) ;
#60830=CARTESIAN_POINT ( 'NONE',  ( -21.05000000000000071, 14.05000000001115623, -173.0136950707609458 ) ) ;
#60852=CARTESIAN_POINT ( 'NONE',  ( -20.54999999999999716, 2.500000000011154633, -187.7753780772378889 ) ) ;
#60858=CIRCLE ( 'NONE', #239951, 0.09999999999999992228 ) ;
#60864=SPHERICAL_SURFACE ( 'NONE', #55842, 0.1000000000000000056 ) ;
#60881=ORIENTED_EDGE ( 'NONE', *, *, #9320, .F. ) ;
#60936=AXIS2_PLACEMENT_3D ( 'NONE', #254435, #155401, #234911 ) ;
#60961=EDGE_CURVE ( 'NONE', #138331, #182833, #42423, .T. ) ;
#60964=CARTESIAN_POINT ( 'NONE',  ( 23.24999999999999289, 11.65000000001116298, -167.5999999999999659 ) ) ;
#60983=DIRECTION ( 'NONE',  ( 1.000000000000000000, 0.000000000000000000, -0.000000000000000000 ) ) ;
#61004=CARTESIAN_POINT ( 'NONE',  ( -22.39999999999999858, 0.1000000000111554016, -159.7092204016265384 ) ) ;
#61007=VERTEX_POINT ( 'NONE', #112598 ) ;
#61023=LINE ( 'NONE', #136707, #177071 ) ;
#61055=CARTESIAN_POINT ( 'NONE',  ( -18.50000000000000000, 1.637172712981535883, -179.0821533654719815 ) ) ;
#61122=CARTESIAN_POINT ( 'NONE',  ( -21.05000000000000071, 1.360870587203197646, -175.5729979270909382 ) ) ;
#61129=AXIS2_PLACEMENT_3D ( 'NONE', #162833, #87107, #64986 ) ;
#61142=DIRECTION ( 'NONE',  ( 0.000000000000000000, 0.000000000000000000, -1.000000000000000000 ) ) ;
#61147=EDGE_LOOP ( 'NONE', ( #117426, #145101, #253071, #90877 ) ) ;
#61154=DIRECTION ( 'NONE',  ( 0.000000000000000000, 0.000000000000000000, 1.000000000000000000 ) ) ;
#61181=CIRCLE ( 'NONE', #106954, 0.09999999999999949207 ) ;
#61184=EDGE_CURVE ( 'NONE', #182355, #46904, #246788, .T. ) ;
#61223=DIRECTION ( 'NONE',  ( -1.000000000000000000, -0.000000000000000000, 0.000000000000000000 ) ) ;
#61225=DIRECTION ( 'NONE',  ( 0.000000000000000000, 0.000000000000000000, -1.000000000000000000 ) ) ;
#61268=FACE_OUTER_BOUND ( 'NONE', #37092, .T. ) ;
#61269=TOROIDAL_SURFACE ( 'NONE', #256842, 0.2000000000000000111, 0.1000000000000000056 ) ;
#61282=LINE ( 'NONE', #200795, #119162 ) ;
#61339=TOROIDAL_SURFACE ( 'NONE', #194639, 0.4000000000000005773, 0.1000000000000000056 ) ;
#61349=DIRECTION ( 'NONE',  ( 0.000000000000000000, 1.000000000000000000, 0.000000000000000000 ) ) ;
#61350=CARTESIAN_POINT ( 'NONE',  ( -21.05000000000000071, 0.09779029131994770863, -161.2421853895238542 ) ) ;
#61357=CIRCLE ( 'NONE', #94663, 0.09999999999999939493 ) ;
#61362=DIRECTION ( 'NONE',  ( 1.000000000000000000, 0.000000000000000000, 0.000000000000000000 ) ) ;
#61390=EDGE_CURVE ( 'NONE', #82222, #242287, #115805, .T. ) ;
#61394=ORIENTED_EDGE ( 'NONE', *, *, #104881, .F. ) ;
#61396=CARTESIAN_POINT ( 'NONE',  ( -21.05000000000000071, 0.09843750001115457449, -161.2007690899130807 ) ) ;
#61405=ORIENTED_EDGE ( 'NONE', *, *, #224312, .F. ) ;
#61449=ORIENTED_EDGE ( 'NONE', *, *, #248094, .F. ) ;
#61456=LINE ( 'NONE', #191036, #24710 ) ;
#61465=ORIENTED_EDGE ( 'NONE', *, *, #84433, .T. ) ;
#61467=CIRCLE ( 'NONE', #111352, 11.80000000000000426 ) ;
#61483=AXIS2_PLACEMENT_3D ( 'NONE', #224051, #89670, #105360 ) ;
#61505=AXIS2_PLACEMENT_3D ( 'NONE', #206583, #8397, #26685 ) ;
#61525=DIRECTION ( 'NONE',  ( -3.890533409366484652E-14, -0.1298341882520124002, -0.9915357197604841577 ) ) ;
#61529=CARTESIAN_POINT ( 'NONE',  ( -22.59999999999999787, 1.115600667400684642E-11, -167.4999999999999716 ) ) ;
#61543=AXIS2_PLACEMENT_3D ( 'NONE', #234381, #151017, #110591 ) ;
#61566=FACE_BOUND ( 'NONE', #78526, .T. ) ;
#61597=VERTEX_POINT ( 'NONE', #240890 ) ;
#61600=CARTESIAN_POINT ( 'NONE',  ( 18.49999999999999289, 6.846123162363745074, -204.7377262668498190 ) ) ;
#61635=DIRECTION ( 'NONE',  ( 1.000000000000000000, 0.000000000000000000, 0.000000000000000000 ) ) ;
#61637=EDGE_CURVE ( 'NONE', #208426, #251611, #64804, .T. ) ;
#61679=ORIENTED_EDGE ( 'NONE', *, *, #166301, .T. ) ;
#61702=CYLINDRICAL_SURFACE ( 'NONE', #103358, 0.09999999999998898659 ) ;
#61706=ORIENTED_EDGE ( 'NONE', *, *, #245953, .T. ) ;
#61729=EDGE_CURVE ( 'NONE', #215705, #95420, #146890, .T. ) ;
#61734=DIRECTION ( 'NONE',  ( 0.000000000000000000, -2.211772431870365684E-13, -1.000000000000000000 ) ) ;
#61761=CARTESIAN_POINT ( 'NONE',  ( -18.50000000000000000, 10.29270135741298375, -206.4573618871519045 ) ) ;
#61779=EDGE_CURVE ( 'NONE', #22594, #181739, #247285, .T. ) ;
#61793=EDGE_CURVE ( 'NONE', #78009, #190986, #253704, .T. ) ;
#61802=ORIENTED_EDGE ( 'NONE', *, *, #152705, .T. ) ;
#61837=ORIENTED_EDGE ( 'NONE', *, *, #237754, .T. ) ;
#61843=ORIENTED_EDGE ( 'NONE', *, *, #241883, .F. ) ;
#61853=AXIS2_PLACEMENT_3D ( 'NONE', #129121, #11763, #88676 ) ;
#61857=DIRECTION ( 'NONE',  ( -0.000000000000000000, 0.000000000000000000, 1.000000000000000000 ) ) ;
#61859=CARTESIAN_POINT ( 'NONE',  ( 21.05000000000000071, 6.257814610487280937, -167.4022097086911742 ) ) ;
#61866=DIRECTION ( 'NONE',  ( 0.000000000000000000, 1.000000000000000000, 0.000000000000000000 ) ) ;
#61925=VERTEX_POINT ( 'NONE', #252415 ) ;
#61964=CARTESIAN_POINT ( 'NONE',  ( 20.94999999999999929, -9.499999999988848032, -177.3939691226524076 ) ) ;
#61970=VECTOR ( 'NONE', #250387, 1000.000000000000000 ) ;
#61983=ORIENTED_EDGE ( 'NONE', *, *, #203192, .T. ) ;
#61988=ORIENTED_EDGE ( 'NONE', *, *, #114474, .F. ) ;
#61995=EDGE_CURVE ( 'NONE', #8860, #57378, #93042, .T. ) ;
#62000=DIRECTION ( 'NONE',  ( 0.000000000000000000, 0.000000000000000000, -1.000000000000000000 ) ) ;
#62075=VERTEX_POINT ( 'NONE', #47494 ) ;
#62134=DIRECTION ( 'NONE',  ( 0.000000000000000000, 0.9908441862701782288, 0.1350103645450542456 ) ) ;
#62156=PLANE ( 'NONE',  #241372 ) ;
#62157=CARTESIAN_POINT ( 'NONE',  ( 18.49999999999999289, 10.41716543472752399, -192.3499999994177472 ) ) ;
#62233=DIRECTION ( 'NONE',  ( 0.000000000000000000, 0.000000000000000000, -1.000000000000000000 ) ) ;
#62250=ORIENTED_EDGE ( 'NONE', *, *, #36675, .F. ) ;
#62293=DIRECTION ( 'NONE',  ( 1.000000000000000000, -0.000000000000000000, -0.000000000000000000 ) ) ;
#62319=DIRECTION ( 'NONE',  ( 0.000000000000000000, -0.000000000000000000, 1.000000000000000000 ) ) ;
#62379=ORIENTED_EDGE ( 'NONE', *, *, #4821, .F. ) ;
#62386=LINE ( 'NONE', #201893, #89281 ) ;
#62392=DIRECTION ( 'NONE',  ( 0.000000000000000000, 1.000000000000000000, 0.000000000000000000 ) ) ;
#62410=EDGE_CURVE ( 'NONE', #68443, #42929, #101569, .T. ) ;
#62424=AXIS2_PLACEMENT_3D ( 'NONE', #40260, #217560, #119791 ) ;
#62433=VERTEX_POINT ( 'NONE', #44652 ) ;
#62439=DIRECTION ( 'NONE',  ( 0.000000000000000000, 0.000000000000000000, -1.000000000000000000 ) ) ;
#62448=DIRECTION ( 'NONE',  ( 0.000000000000000000, 0.000000000000000000, -1.000000000000000000 ) ) ;
#62471=AXIS2_PLACEMENT_3D ( 'NONE', #189564, #33093, #168760 ) ;
#62476=EDGE_CURVE ( 'NONE', #215011, #6262, #128041, .T. ) ;
#62485=DIRECTION ( 'NONE',  ( 2.694716079187272946E-16, -1.000000000000000000, 0.000000000000000000 ) ) ;
#62496=ORIENTED_EDGE ( 'NONE', *, *, #191736, .F. ) ;
#62502=FACE_OUTER_BOUND ( 'NONE', #67566, .T. ) ;
#62512=EDGE_LOOP ( 'NONE', ( #60578, #40152, #136325, #256919 ) ) ;
#62523=CARTESIAN_POINT ( 'NONE',  ( 18.59999999999999076, 10.49142135624846439, -192.2499999999999716 ) ) ;
#62524=CARTESIAN_POINT ( 'NONE',  ( 22.44352723754029810, 0.009277095054436634847, -155.8502786546512482 ) ) ;
#62546=EDGE_LOOP ( 'NONE', ( #78553, #57735, #151724, #112281 ) ) ;
#62549=AXIS2_PLACEMENT_3D ( 'NONE', #215213, #39170, #200784 ) ;
#62552=AXIS2_PLACEMENT_3D ( 'NONE', #251667, #148734, #250386 ) ;
#62556=ORIENTED_EDGE ( 'NONE', *, *, #177913, .T. ) ;
#62600=CARTESIAN_POINT ( 'NONE',  ( 20.97468175916176847, 10.62526516438217605, -179.7547614354127745 ) ) ;
#62605=CIRCLE ( 'NONE', #208367, 0.09999999999998898659 ) ;
#62606=DIRECTION ( 'NONE',  ( -0.7071067811865475727, -0.7071067811865475727, 0.000000000000000000 ) ) ;
#62608=CARTESIAN_POINT ( 'NONE',  ( -23.25000000000000000, -1.835859311432481045, -212.6044391687984785 ) ) ;
#62615=CARTESIAN_POINT ( 'NONE',  ( -20.54999999999999716, 9.350000000011156942, -188.6499999999999488 ) ) ;
#62638=VERTEX_POINT ( 'NONE', #171063 ) ;
#62644=CARTESIAN_POINT ( 'NONE',  ( 22.39999999999999503, 11.65000000001116298, -167.4999999999999716 ) ) ;
#62648=AXIS2_PLACEMENT_3D ( 'NONE', #154023, #15777, #176125 ) ;
#62677=CARTESIAN_POINT ( 'NONE',  ( -21.29999999999995808, 1.115600667400684642E-11, -167.4999999999999716 ) ) ;
#62717=EDGE_LOOP ( 'NONE', ( #84340, #151630, #138347, #55910 ) ) ;
#62723=TOROIDAL_SURFACE ( 'NONE', #241774, 4.099999999999999645, 0.1000000000000000056 ) ;
#62734=AXIS2_PLACEMENT_3D ( 'NONE', #233770, #91679, #14738 ) ;
#62735=AXIS2_PLACEMENT_3D ( 'NONE', #139082, #161263, #4717 ) ;
#62741=CARTESIAN_POINT ( 'NONE',  ( 21.14999999999999858, 1.115600667400684642E-11, -179.6499999999999773 ) ) ;
#62750=CARTESIAN_POINT ( 'NONE',  ( 20.94999999999999574, -11.41227409413852989, -170.4999999999999716 ) ) ;
#62751=DIRECTION ( 'NONE',  ( 1.000000000000000000, 0.000000000000000000, 0.000000000000000000 ) ) ;
#62763=CARTESIAN_POINT ( 'NONE',  ( 23.24999999999999289, 11.75000000001116263, -179.6499999999999773 ) ) ;
#62764=FACE_OUTER_BOUND ( 'NONE', #151225, .T. ) ;
#62782=CIRCLE ( 'NONE', #208545, 0.5000000000000004441 ) ;
#62796=CYLINDRICAL_SURFACE ( 'NONE', #25636, 0.09999999999999939493 ) ;
#62797=EDGE_CURVE ( 'NONE', #41810, #178378, #219194, .T. ) ;
#62856=CARTESIAN_POINT ( 'NONE',  ( -20.00857864376270001, 9.150000000011157653, -179.8499999999999943 ) ) ;
#62870=LINE ( 'NONE', #142402, #135720 ) ;
#62945=AXIS2_PLACEMENT_3D ( 'NONE', #99923, #118237, #2120 ) ;
#62986=ORIENTED_EDGE ( 'NONE', *, *, #220763, .T. ) ;
#62995=ORIENTED_EDGE ( 'NONE', *, *, #161238, .T. ) ;
#62997=AXIS2_PLACEMENT_3D ( 'NONE', #128627, #205567, #49072 ) ;
#63061=AXIS2_PLACEMENT_3D ( 'NONE', #37184, #218344, #56688 ) ;
#63066=VERTEX_POINT ( 'NONE', #217180 ) ;
#63097=ORIENTED_EDGE ( 'NONE', *, *, #92283, .F. ) ;
#63126=ADVANCED_FACE ( 'NONE', ( #110727 ), #251224, .F. ) ;
#63130=FACE_OUTER_BOUND ( 'NONE', #143613, .T. ) ;
#63143=LINE ( 'NONE', #145251, #18541 ) ;
#63145=CARTESIAN_POINT ( 'NONE',  ( 20.95561247346651967, 10.59500736521470721, -175.0937827669816329 ) ) ;
#63178=AXIS2_PLACEMENT_3D ( 'NONE', #120570, #85235, #143951 ) ;
#63225=AXIS2_PLACEMENT_3D ( 'NONE', #174106, #55351, #191080 ) ;
#63249=VERTEX_POINT ( 'NONE', #48828 ) ;
#63270=EDGE_CURVE ( 'NONE', #85751, #176002, #150514, .T. ) ;
#63271=CARTESIAN_POINT ( 'NONE',  ( -20.64999999999999858, 7.150000000011155876, -179.8499999999999943 ) ) ;
#63282=ORIENTED_EDGE ( 'NONE', *, *, #176034, .T. ) ;
#63296=CARTESIAN_POINT ( 'NONE',  ( -21.06715728752538652, 11.75000000001115197, -174.5148057706539646 ) ) ;
#63312=DIRECTION ( 'NONE',  ( 0.000000000000000000, -0.8660254037844412611, -0.4999999999999956701 ) ) ;
#63351=ORIENTED_EDGE ( 'NONE', *, *, #44572, .F. ) ;
#63362=ORIENTED_EDGE ( 'NONE', *, *, #227193, .F. ) ;
#63370=CARTESIAN_POINT ( 'NONE',  ( 21.14999999999999858, 8.786607556611267356, -179.8499999999999943 ) ) ;
#63383=DIRECTION ( 'NONE',  ( -1.000000000000000000, -0.000000000000000000, -0.000000000000000000 ) ) ;
#63393=DIRECTION ( 'NONE',  ( 0.000000000000000000, -1.000000000000000000, 0.000000000000000000 ) ) ;
#63401=ADVANCED_FACE ( 'NONE', ( #34442 ), #76095, .F. ) ;
#63405=FACE_BOUND ( 'NONE', #98570, .T. ) ;
#63436=DIRECTION ( 'NONE',  ( 0.000000000000000000, 1.000000000000000000, -0.000000000000000000 ) ) ;
#63453=LINE ( 'NONE', #160023, #199624 ) ;
#63461=DIRECTION ( 'NONE',  ( 0.000000000000000000, 1.734723475976807292E-15, -1.000000000000000000 ) ) ;
#63483=DIRECTION ( 'NONE',  ( 0.000000000000000000, -1.000000000000000000, -0.000000000000000000 ) ) ;
#63534=CIRCLE ( 'NONE', #76025, 0.5999999999999894307 ) ;
#63537=CIRCLE ( 'NONE', #188441, 11.75000000000000000 ) ;
#63601=CARTESIAN_POINT ( 'NONE',  ( -21.00857864376268935, 11.60000000001115161, -174.4282032302755283 ) ) ;
#63605=LINE ( 'NONE', #8775, #89506 ) ;
#63638=CARTESIAN_POINT ( 'NONE',  ( 21.05000000000000071, 1.115600667400684642E-11, -180.3749999999999716 ) ) ;
#63653=ORIENTED_EDGE ( 'NONE', *, *, #15197, .F. ) ;
#63667=DIRECTION ( 'NONE',  ( 0.000000000000000000, 0.000000000000000000, -1.000000000000000000 ) ) ;
#63683=DIRECTION ( 'NONE',  ( -0.7071067811865475727, -0.7071067811865475727, 0.000000000000000000 ) ) ;
#63691=CARTESIAN_POINT ( 'NONE',  ( 18.31572054635732982, -9.548475435767892705, -207.8505701647481487 ) ) ;
#63695=VERTEX_POINT ( 'NONE', #31573 ) ;
#63719=DIRECTION ( 'NONE',  ( 0.000000000000000000, -0.1298341882520079038, -0.9915357197604846018 ) ) ;
#63740=DIRECTION ( 'NONE',  ( 0.000000000000000000, 1.000000000000000000, 0.000000000000000000 ) ) ;
#63752=CARTESIAN_POINT ( 'NONE',  ( 23.14999999999999858, 1.115600667400684642E-11, -200.9999999999999432 ) ) ;
#63756=LINE ( 'NONE', #224107, #56387 ) ;
#63785=EDGE_CURVE ( 'NONE', #175396, #86058, #143279, .T. ) ;
#63837=ORIENTED_EDGE ( 'NONE', *, *, #161923, .T. ) ;
#63844=DIRECTION ( 'NONE',  ( 0.000000000000000000, 0.000000000000000000, -1.000000000000000000 ) ) ;
#63852=ORIENTED_EDGE ( 'NONE', *, *, #176846, .T. ) ;
#63877=DIRECTION ( 'NONE',  ( 1.000000000000000000, 0.000000000000000000, 0.000000000000000000 ) ) ;
#63927=ADVANCED_FACE ( 'NONE', ( #174668 ), #238436, .T. ) ;
#63946=AXIS2_PLACEMENT_3D ( 'NONE', #137888, #196589, #76644 ) ;
#63969=CARTESIAN_POINT ( 'NONE',  ( -21.05000000000000071, -0.09999999998884474828, -160.9593430482987344 ) ) ;
#63994=DIRECTION ( 'NONE',  ( 0.000000000000000000, 1.000000000000000000, 0.000000000000000000 ) ) ;
#64062=CARTESIAN_POINT ( 'NONE',  ( 20.94999999999999574, 1.115600667400684642E-11, -167.4999999999999716 ) ) ;
#64078=EDGE_CURVE ( 'NONE', #252758, #163705, #31081, .T. ) ;
#64131=ADVANCED_FACE ( 'NONE', ( #12687 ), #51757, .T. ) ;
#64178=ORIENTED_EDGE ( 'NONE', *, *, #56379, .T. ) ;
#64219=CARTESIAN_POINT ( 'NONE',  ( -20.54999999999999716, 1.115600667400684642E-11, -200.9999999999999432 ) ) ;
#64248=ORIENTED_EDGE ( 'NONE', *, *, #180419, .T. ) ;
#64262=CYLINDRICAL_SURFACE ( 'NONE', #232482, 0.09999999999999939493 ) ;
#64282=VERTEX_POINT ( 'NONE', #96032 ) ;
#64290=VERTEX_POINT ( 'NONE', #215973 ) ;
#64348=CARTESIAN_POINT ( 'NONE',  ( -22.48970261584618058, 11.65000000001115588, -167.4446305117825773 ) ) ;
#64376=CIRCLE ( 'NONE', #147580, 4.049999999999998046 ) ;
#64418=LINE ( 'NONE', #143940, #51227 ) ;
#64422=CARTESIAN_POINT ( 'NONE',  ( 21.14999999999999858, 8.786607556611267356, -179.7499999999999716 ) ) ;
#64425=DIRECTION ( 'NONE',  ( 0.000000000000000000, 0.000000000000000000, 1.000000000000000000 ) ) ;
#64428=CARTESIAN_POINT ( 'NONE',  ( 21.05000000000000071, 6.477067021135912483, -167.5999999999999375 ) ) ;
#64434=CARTESIAN_POINT ( 'NONE',  ( 21.05563370358598263, 10.72423035585766549, -179.6830908159630269 ) ) ;
#64463=CARTESIAN_POINT ( 'NONE',  ( 18.49999999999998934, 10.29288807859941457, -206.4580020160121308 ) ) ;
#64478=CARTESIAN_POINT ( 'NONE',  ( 20.85000000000000142, 6.982009704867603972, -204.6961521182562649 ) ) ;
#64480=ORIENTED_EDGE ( 'NONE', *, *, #43396, .F. ) ;
#64487=VERTEX_POINT ( 'NONE', #219835 ) ;
#64490=DIRECTION ( 'NONE',  ( 0.000000000000000000, 0.000000000000000000, 1.000000000000000000 ) ) ;
#64503=DIRECTION ( 'NONE',  ( 1.000000000000000000, 0.000000000000000000, 0.000000000000000000 ) ) ;
#64544=LINE ( 'NONE', #144064, #230614 ) ;
#64575=EDGE_LOOP ( 'NONE', ( #147673, #236354, #243270, #20232 ) ) ;
#64577=DIRECTION ( 'NONE',  ( 0.000000000000000000, 0.9908441862701782288, 0.1350103645450542456 ) ) ;
#64590=DIRECTION ( 'NONE',  ( -4.391705002472929091E-16, 1.000000000000000000, 0.000000000000000000 ) ) ;
#64623=ORIENTED_EDGE ( 'NONE', *, *, #10872, .F. ) ;
#64627=DIRECTION ( 'NONE',  ( 0.000000000000000000, 0.000000000000000000, -1.000000000000000000 ) ) ;
#64635=ORIENTED_EDGE ( 'NONE', *, *, #43834, .F. ) ;
#64649=DIRECTION ( 'NONE',  ( -1.000000000000000000, 0.000000000000000000, 0.000000000000000000 ) ) ;
#64657=EDGE_CURVE ( 'NONE', #163705, #185332, #97824, .T. ) ;
#64666=ORIENTED_EDGE ( 'NONE', *, *, #111611, .F. ) ;
#64675=PLANE ( 'NONE',  #13548 ) ;
#64710=VERTEX_POINT ( 'NONE', #236210 ) ;
#64714=CARTESIAN_POINT ( 'NONE',  ( 18.50000000000000711, 10.28015861706802880, -192.2245720712021182 ) ) ;
#64749=DIRECTION ( 'NONE',  ( 1.000000000000000000, 2.952720810173289112E-16, -0.000000000000000000 ) ) ;
#64790=AXIS2_PLACEMENT_3D ( 'NONE', #170734, #9037, #188961 ) ;
#64804=LINE ( 'NONE', #144317, #151146 ) ;
#64806=CARTESIAN_POINT ( 'NONE',  ( -20.94999999999999929, -1.835341550213255957, -179.0551512925629538 ) ) ;
#64820=CARTESIAN_POINT ( 'NONE',  ( -20.85000000000000142, 11.75000000001115197, -194.2161343370218560 ) ) ;
#64828=VERTEX_POINT ( 'NONE', #86095 ) ;
#64845=AXIS2_PLACEMENT_3D ( 'NONE', #242197, #2288, #180956 ) ;
#64860=EDGE_CURVE ( 'NONE', #69117, #177551, #185525, .T. ) ;
#64889=VECTOR ( 'NONE', #179519, 999.9999999999998863 ) ;
#64907=VECTOR ( 'NONE', #203840, 1000.000000000000000 ) ;
#64913=EDGE_LOOP ( 'NONE', ( #240799, #229649, #129967, #117821 ) ) ;
#64917=ORIENTED_EDGE ( 'NONE', *, *, #144488, .F. ) ;
#64925=ORIENTED_EDGE ( 'NONE', *, *, #203835, .T. ) ;
#64927=CARTESIAN_POINT ( 'NONE',  ( 21.05000000000000071, 1.162701749949165642, -175.3999999999999773 ) ) ;
#64930=ORIENTED_EDGE ( 'NONE', *, *, #18038, .T. ) ;
#64936=CARTESIAN_POINT ( 'NONE',  ( -20.54999999999999716, 1.115600667400684642E-11, -200.9999999999999432 ) ) ;
#64946=CARTESIAN_POINT ( 'NONE',  ( 20.94999999999999929, 1.835341550235569663, -179.0551512925629538 ) ) ;
#64965=DIRECTION ( 'NONE',  ( 0.000000000000000000, 0.000000000000000000, 1.000000000000000000 ) ) ;
#64973=EDGE_CURVE ( 'NONE', #141186, #143156, #48147, .T. ) ;
#64974=CARTESIAN_POINT ( 'NONE',  ( 18.33996824403518389, -9.569639859420076888, -207.8190656375170704 ) ) ;
#64976=AXIS2_PLACEMENT_3D ( 'NONE', #245351, #242758, #48415 ) ;
#64986=DIRECTION ( 'NONE',  ( 0.000000000000000000, 0.000000000000000000, -1.000000000000000000 ) ) ;
#65045=EDGE_CURVE ( 'NONE', #176002, #7516, #14855, .T. ) ;
#65067=ADVANCED_FACE ( 'NONE', ( #174709 ), #189627, .F. ) ;
#65089=AXIS2_PLACEMENT_3D ( 'NONE', #123846, #78272, #241231 ) ;
#65132=AXIS2_PLACEMENT_3D ( 'NONE', #27862, #68240, #44823 ) ;
#65166=DIRECTION ( 'NONE',  ( 0.000000000000000000, 0.000000000000000000, -1.000000000000000000 ) ) ;
#65172=FACE_OUTER_BOUND ( 'NONE', #90194, .T. ) ;
#65180=CIRCLE ( 'NONE', #110974, 0.2000000000000057288 ) ;
#65230=CYLINDRICAL_SURFACE ( 'NONE', #227083, 0.09999999999999939493 ) ;
#65231=ORIENTED_EDGE ( 'NONE', *, *, #178298, .F. ) ;
#65243=CARTESIAN_POINT ( 'NONE',  ( -21.52071067811865746, 7.779289321892505882, -179.8499999999999943 ) ) ;
#65246=ORIENTED_EDGE ( 'NONE', *, *, #138333, .T. ) ;
#65326=CARTESIAN_POINT ( 'NONE',  ( -23.15000000000000213, -11.74999999998884448, -197.8999999999999773 ) ) ;
#65341=DIRECTION ( 'NONE',  ( -1.000000000000000000, -2.952720810173289112E-16, 0.000000000000000000 ) ) ;
#65368=CARTESIAN_POINT ( 'NONE',  ( 20.97239005616515684, 8.874843841361279573, -179.7501528021531954 ) ) ;
#65372=AXIS2_PLACEMENT_3D ( 'NONE', #221760, #139659, #104384 ) ;
#65376=ORIENTED_EDGE ( 'NONE', *, *, #44090, .F. ) ;
#65442=CARTESIAN_POINT ( 'NONE',  ( 23.14999999999999503, 11.65000000001116298, -193.9851942293460070 ) ) ;
#65449=ORIENTED_EDGE ( 'NONE', *, *, #210907, .F. ) ;
#65461=EDGE_CURVE ( 'NONE', #255780, #95676, #15032, .T. ) ;
#65484=CARTESIAN_POINT ( 'NONE',  ( -21.55000000000000071, 7.350000000011155166, -188.6499999999999488 ) ) ;
#65485=ORIENTED_EDGE ( 'NONE', *, *, #45309, .F. ) ;
#65501=AXIS2_PLACEMENT_3D ( 'NONE', #257978, #117243, #196760 ) ;
#65531=CARTESIAN_POINT ( 'NONE',  ( -23.25000000000000000, 1.115600667400684642E-11, -200.9999999999999432 ) ) ;
#65601=ORIENTED_EDGE ( 'NONE', *, *, #99646, .T. ) ;
#65648=CARTESIAN_POINT ( 'NONE',  ( 18.49999999999999645, -1.637172712959225507, -179.0821533654719815 ) ) ;
#65662=ORIENTED_EDGE ( 'NONE', *, *, #114300, .T. ) ;
#65685=DIRECTION ( 'NONE',  ( 1.000000000000000000, -0.000000000000000000, -0.000000000000000000 ) ) ;
#65689=CARTESIAN_POINT ( 'NONE',  ( 21.13498764882293557, 6.495618143485025975, -167.4983436052686443 ) ) ;
#65708=CARTESIAN_POINT ( 'NONE',  ( 21.08750232978087524, 10.72486338602132250, -179.7288581729995371 ) ) ;
#65717=CARTESIAN_POINT ( 'NONE',  ( -20.94999999999999929, 11.75000000001115552, -174.5148057706539930 ) ) ;
#65721=CIRCLE ( 'NONE', #107413, 0.1999999999999996503 ) ;
#65727=AXIS2_PLACEMENT_3D ( 'NONE', #59700, #117141, #180965 ) ;
#65730=CARTESIAN_POINT ( 'NONE',  ( 18.43565242384934066, -9.519327731081283162, -174.4729763765593020 ) ) ;
#65741=CARTESIAN_POINT ( 'NONE',  ( -22.00356870140456422, 7.254242362510445297, -167.4999999999999432 ) ) ;
#65765=CARTESIAN_POINT ( 'NONE',  ( -21.64999999999999858, 7.350000000011155166, -188.6499999999999488 ) ) ;
#65783=DIRECTION ( 'NONE',  ( 0.000000000000000000, -1.000000000000000000, 0.000000000000000000 ) ) ;
#65792=CARTESIAN_POINT ( 'NONE',  ( -18.59999999999999787, 7.021664781911246322, -204.6335654018972434 ) ) ;
#65808=B_SPLINE_CURVE_WITH_KNOTS ( 'NONE', 3,
 ( #243726, #85898, #140776, #205872, #41691, #62524, #121255, #200750, #181204, #2528, #247574, #248865, #168086, #68963, #131479, #31137 ),
 .UNSPECIFIED., .F., .F.,
 ( 4, 3, 3, 3, 3, 4 ),
 ( 0.000000000000000000, 2.209833635978080524E-05, 5.595056164119276626E-05, 8.979992002655378693E-05, 0.0001236482757198913282, 0.0001574984039362987726 ),
 .UNSPECIFIED. ) ;
#65868=CARTESIAN_POINT ( 'NONE',  ( -20.94999999999999929, 0.2561057921033771945, -167.4651035583276553 ) ) ;
#65878=CIRCLE ( 'NONE', #186708, 0.09999999999999939493 ) ;
#65881=SPHERICAL_SURFACE ( 'NONE', #68272, 0.1000000000000000056 ) ;
#65898=DIRECTION ( 'NONE',  ( 1.000000000000000000, 0.000000000000000000, 0.000000000000000000 ) ) ;
#65900=EDGE_LOOP ( 'NONE', ( #90990, #115809, #18892, #21333 ) ) ;
#65903=AXIS2_PLACEMENT_3D ( 'NONE', #51681, #172987, #253748 ) ;
#65919=CIRCLE ( 'NONE', #32655, 0.09999999999998898659 ) ;
#65932=ORIENTED_EDGE ( 'NONE', *, *, #85034, .F. ) ;
#65933=TOROIDAL_SURFACE ( 'NONE', #157560, 11.90000000000000213, 0.1000000000000000056 ) ;
#65966=CARTESIAN_POINT ( 'NONE',  ( 23.24999999999999289, 11.75000000001116263, -155.7499999999999716 ) ) ;
#65984=CARTESIAN_POINT ( 'NONE',  ( 20.94999999999999574, -11.64999999998883595, -170.3999999999999773 ) ) ;
#65989=ORIENTED_EDGE ( 'NONE', *, *, #69778, .T. ) ;
#66009=DIRECTION ( 'NONE',  ( -0.000000000000000000, 0.000000000000000000, 1.000000000000000000 ) ) ;
#66024=CIRCLE ( 'NONE', #224240, 4.149999999999987033 ) ;
#66049=LINE ( 'NONE', #148156, #192284 ) ;
#66056=CARTESIAN_POINT ( 'NONE',  ( 21.05000000000000071, 8.926614585098256782, -175.9716830192231214 ) ) ;
#66059=ORIENTED_EDGE ( 'NONE', *, *, #98520, .F. ) ;
#66066=CIRCLE ( 'NONE', #232683, 0.09999999999998898659 ) ;
#66071=EDGE_CURVE ( 'NONE', #99579, #80509, #149170, .T. ) ;
#66091=CARTESIAN_POINT ( 'NONE',  ( -20.99142135623731065, 11.60000000001115161, -194.0717967697245001 ) ) ;
#66095=VERTEX_POINT ( 'NONE', #211585 ) ;
#66104=CIRCLE ( 'NONE', #136837, 0.09999999999999971412 ) ;
#66105=CARTESIAN_POINT ( 'NONE',  ( 20.96937028524355640, 10.62446937163783289, -174.9914261011695373 ) ) ;
#66108=EDGE_CURVE ( 'NONE', #16613, #154602, #15405, .T. ) ;
#66109=DIRECTION ( 'NONE',  ( 1.000000000000000000, 0.000000000000000000, -0.000000000000000000 ) ) ;
#66110=ADVANCED_FACE ( 'NONE', ( #6948 ), #235001, .F. ) ;
#66182=ORIENTED_EDGE ( 'NONE', *, *, #257148, .F. ) ;
#66236=CARTESIAN_POINT ( 'NONE',  ( -20.94999999999999929, -1.835341550213257733, -179.0551512925629538 ) ) ;
#66238=EDGE_LOOP ( 'NONE', ( #166191, #80348, #224888, #32992, #180896 ) ) ;
#66241=CARTESIAN_POINT ( 'NONE',  ( 18.59999999999999076, -1.851617760457748618, -212.6031897196036198 ) ) ;
#66244=CARTESIAN_POINT ( 'NONE',  ( 18.60000000000000142, -9.399999999988782662, -174.7972597596632625 ) ) ;
#66264=DIRECTION ( 'NONE',  ( 1.000000000000000000, 0.000000000000000000, 0.000000000000000000 ) ) ;
#66274=CARTESIAN_POINT ( 'NONE',  ( 18.39999999999999858, -9.682403433465237796, -207.6568433774127698 ) ) ;
#66300=DIRECTION ( 'NONE',  ( 0.000000000000000000, 0.000000000000000000, -1.000000000000000000 ) ) ;
#66336=CIRCLE ( 'NONE', #53866, 11.89999999999999325 ) ;
#66360=DIRECTION ( 'NONE',  ( -1.000000000000000000, 0.000000000000000000, 0.000000000000000000 ) ) ;
#66364=EDGE_CURVE ( 'NONE', #66550, #14558, #224079, .T. ) ;
#66373=CARTESIAN_POINT ( 'NONE',  ( -23.25000000000000000, -1.851617760457748618, -212.6031897196036198 ) ) ;
#66388=DIRECTION ( 'NONE',  ( -0.000000000000000000, -0.000000000000000000, -1.000000000000000000 ) ) ;
#66498=AXIS2_PLACEMENT_3D ( 'NONE', #238837, #57611, #100571 ) ;
#66507=CARTESIAN_POINT ( 'NONE',  ( -22.39999999999999858, -0.1008583690875575894, -155.7504328765105868 ) ) ;
#66550=VERTEX_POINT ( 'NONE', #32345 ) ;
#66560=FACE_OUTER_BOUND ( 'NONE', #116197, .T. ) ;
#66566=ORIENTED_EDGE ( 'NONE', *, *, #187938, .F. ) ;
#66576=CARTESIAN_POINT ( 'NONE',  ( -21.10257677756356642, 6.398381742543883810, -167.4750492504319936 ) ) ;
#66612=DIRECTION ( 'NONE',  ( -0.000000000000000000, 0.1298341882520022694, 0.9915357197604853789 ) ) ;
#66655=DIRECTION ( 'NONE',  ( -0.000000000000000000, 1.000000000000000000, 0.000000000000000000 ) ) ;
#66669=DIRECTION ( 'NONE',  ( -4.801466763864313332E-15, -0.2605042016806672911, -0.9654727137038716656 ) ) ;
#66690=DIRECTION ( 'NONE',  ( 1.000000000000000000, 0.000000000000000000, 0.000000000000000000 ) ) ;
#66703=AXIS2_PLACEMENT_3D ( 'NONE', #213408, #135147, #34817 ) ;
#66743=B_SPLINE_CURVE_WITH_KNOTS ( 'NONE', 3,
 ( #159673, #140078, #219623, #41024, #21460, #180520, #1846, #201354, #160964, #22747, #102214, #108681, #224757, #25311, #243044, #64422 ),
 .UNSPECIFIED., .F., .F.,
 ( 4, 3, 3, 3, 3, 4 ),
 ( 0.000000000000000000, 2.372700795694929657E-05, 5.739057815869540267E-05, 9.073899019181866019E-05, 0.0001243544287365906317, 0.0001585386695601349893 ),
 .UNSPECIFIED. ) ;
#66772=CARTESIAN_POINT ( 'NONE',  ( 21.05000000000000071, 8.776282895303632259, -176.0586289951409071 ) ) ;
#66784=CARTESIAN_POINT ( 'NONE',  ( 22.50014994444007499, 11.74971973190327468, -167.4169198432807093 ) ) ;
#66787=DIRECTION ( 'NONE',  ( 1.000000000000000000, 0.000000000000000000, 0.000000000000000000 ) ) ;
#66806=VERTEX_POINT ( 'NONE', #30745 ) ;
#66826=AXIS2_PLACEMENT_3D ( 'NONE', #239828, #45464, #24653 ) ;
#66923=AXIS2_PLACEMENT_3D ( 'NONE', #1850, #39752, #237914 ) ;
#66930=EDGE_CURVE ( 'NONE', #136769, #58719, #254835, .T. ) ;
#66952=DIRECTION ( 'NONE',  ( 0.000000000000000000, 1.000000000000000000, 0.000000000000000000 ) ) ;
#66975=AXIS2_PLACEMENT_3D ( 'NONE', #92042, #170354, #28263 ) ;
#66981=CIRCLE ( 'NONE', #87804, 0.09999999999999939493 ) ;
#67013=DIRECTION ( 'NONE',  ( 1.000000000000000000, 0.000000000000000000, 0.000000000000000000 ) ) ;
#67014=CARTESIAN_POINT ( 'NONE',  ( 18.39999999999999858, -9.519327731081283162, -174.4729763765593020 ) ) ;
#67026=EDGE_CURVE ( 'NONE', #213186, #190383, #140641, .T. ) ;
#67028=ORIENTED_EDGE ( 'NONE', *, *, #230815, .T. ) ;
#67051=EDGE_CURVE ( 'NONE', #72236, #54023, #203185, .T. ) ;
#67058=DIRECTION ( 'NONE',  ( 0.000000000000000000, -1.000000000000000000, -0.000000000000000000 ) ) ;
#67066=AXIS2_PLACEMENT_3D ( 'NONE', #157353, #80309, #239429 ) ;
#67080=CARTESIAN_POINT ( 'NONE',  ( -20.64999999999999858, 1.115600667400684642E-11, -200.9999999999999432 ) ) ;
#67120=EDGE_LOOP ( 'NONE', ( #225179, #173745, #199436, #218808 ) ) ;
#67121=EDGE_CURVE ( 'NONE', #135643, #68978, #40908, .T. ) ;
#67178=EDGE_CURVE ( 'NONE', #116285, #128410, #206480, .T. ) ;
#67183=FACE_OUTER_BOUND ( 'NONE', #62546, .T. ) ;
#67211=DIRECTION ( 'NONE',  ( 1.000000000000000000, 0.000000000000000000, 0.000000000000000000 ) ) ;
#67213=LINE ( 'NONE', #132006, #222240 ) ;
#67244=DIRECTION ( 'NONE',  ( 1.000000000000000000, 3.265361837132813093E-16, -0.000000000000000000 ) ) ;
#67250=CARTESIAN_POINT ( 'NONE',  ( 20.84999999999999787, 11.75000000001116085, -194.0808527540412172 ) ) ;
#67265=CARTESIAN_POINT ( 'NONE',  ( -20.85000000000000142, 1.115600667400684642E-11, -200.9999999999999432 ) ) ;
#67271=ORIENTED_EDGE ( 'NONE', *, *, #99450, .T. ) ;
#67282=EDGE_CURVE ( 'NONE', #102805, #46904, #219942, .T. ) ;
#67305=VERTEX_POINT ( 'NONE', #56370 ) ;
#67318=LINE ( 'NONE', #85556, #159093 ) ;
#67349=CARTESIAN_POINT ( 'NONE',  ( 21.05000000000000071, 8.776282895303630482, -176.0586289951409071 ) ) ;
#67359=EDGE_CURVE ( 'NONE', #222817, #64290, #201037, .T. ) ;
#67421=DIRECTION ( 'NONE',  ( 1.000000000000000000, 0.000000000000000000, 0.000000000000000000 ) ) ;
#67428=VERTEX_POINT ( 'NONE', #248871 ) ;
#67524=EDGE_LOOP ( 'NONE', ( #125805, #250483, #37983, #131130 ) ) ;
#67534=FACE_OUTER_BOUND ( 'NONE', #187959, .T. ) ;
#67566=EDGE_LOOP ( 'NONE', ( #164958, #246323, #238388, #155127 ) ) ;
#67568=CARTESIAN_POINT ( 'NONE',  ( 21.05000000000000071, -9.399999999988844834, -191.1060308773475072 ) ) ;
#67574=CARTESIAN_POINT ( 'NONE',  ( 20.94999999999999574, -11.48912529306490349, -170.5999999999999659 ) ) ;
#67601=LINE ( 'NONE', #241133, #231314 ) ;
#67609=DIRECTION ( 'NONE',  ( -6.938893903907222067E-15, 1.000000000000000000, 0.000000000000000000 ) ) ;
#67612=AXIS2_PLACEMENT_3D ( 'NONE', #80825, #46835, #24759 ) ;
#67639=DIRECTION ( 'NONE',  ( -1.000000000000000000, -7.304098846218135653E-16, 4.607487905232624742E-31 ) ) ;
#67682=CARTESIAN_POINT ( 'NONE',  ( -22.50000000000000000, 1.115600667400684642E-11, -161.2499999999999716 ) ) ;
#67692=AXIS2_PLACEMENT_3D ( 'NONE', #136771, #33882, #32591 ) ;
#67711=CIRCLE ( 'NONE', #42582, 3.999999999999999112 ) ;
#67713=AXIS2_PLACEMENT_3D ( 'NONE', #256225, #157230, #217148 ) ;
#67747=CARTESIAN_POINT ( 'NONE',  ( 18.59999999999999076, 6.400000000011158541, -177.4304246300615375 ) ) ;
#67750=DIRECTION ( 'NONE',  ( 0.000000000000000000, -1.000000000000000000, 0.000000000000000000 ) ) ;
#67765=CIRCLE ( 'NONE', #155289, 0.5000000000000004441 ) ;
#67799=DIRECTION ( 'NONE',  ( 1.000000000000000000, -0.000000000000000000, -0.000000000000000000 ) ) ;
#67807=DIRECTION ( 'NONE',  ( 0.000000000000000000, 0.000000000000000000, -1.000000000000000000 ) ) ;
#67816=DIRECTION ( 'NONE',  ( -2.578261006436900068E-14, 0.1350103645451904977, -0.9908441862701597991 ) ) ;
#67852=DIRECTION ( 'NONE',  ( 0.000000000000000000, 1.000000000000000000, 0.000000000000000000 ) ) ;
#67853=CARTESIAN_POINT ( 'NONE',  ( -23.24999999999999645, -9.599999999988845900, -207.6001893912220169 ) ) ;
#67866=DIRECTION ( 'NONE',  ( -1.000000000000000000, 0.000000000000000000, 0.000000000000000000 ) ) ;
#67867=CARTESIAN_POINT ( 'NONE',  ( 20.94999999999999574, 11.62071067812981795, -194.1315833476589887 ) ) ;
#67878=CIRCLE ( 'NONE', #101130, 7.720710678118692272 ) ;
#67935=CARTESIAN_POINT ( 'NONE',  ( -23.15000000000000213, -8.999999999988844479, -191.1060308773475356 ) ) ;
#67949=FACE_OUTER_BOUND ( 'NONE', #129049, .T. ) ;
#67950=DIRECTION ( 'NONE',  ( 0.000000000000000000, 0.000000000000000000, -1.000000000000000000 ) ) ;
#67959=DIRECTION ( 'NONE',  ( 0.000000000000000000, 0.000000000000000000, -1.000000000000000000 ) ) ;
#67961=VECTOR ( 'NONE', #30163, 1000.000000000000000 ) ;
#67974=DIRECTION ( 'NONE',  ( -0.000000000000000000, -1.000000000000000000, -0.000000000000000000 ) ) ;
#67975=DIRECTION ( 'NONE',  ( 0.000000000000000000, 0.000000000000000000, -1.000000000000000000 ) ) ;
#67984=DIRECTION ( 'NONE',  ( -1.000000000000000000, 0.000000000000000000, 0.000000000000000000 ) ) ;
#67993=CARTESIAN_POINT ( 'NONE',  ( -21.05000000000000071, -0.09999999998884338825, -160.9593430482987344 ) ) ;
#68018=EDGE_LOOP ( 'NONE', ( #139301, #111534, #54242, #196431 ) ) ;
#68047=CARTESIAN_POINT ( 'NONE',  ( 21.05000000000000071, 8.815452279208711772, -175.9203925526142314 ) ) ;
#68075=DIRECTION ( 'NONE',  ( -0.000000000000000000, -1.000000000000000000, -0.000000000000000000 ) ) ;
#68099=ORIENTED_EDGE ( 'NONE', *, *, #173235, .T. ) ;
#68113=CARTESIAN_POINT ( 'NONE',  ( 23.14999999999999858, 1.115600667400684642E-11, -180.3749999999999716 ) ) ;
#68114=PLANE ( 'NONE',  #203234 ) ;
#68115=ORIENTED_EDGE ( 'NONE', *, *, #105555, .T. ) ;
#68149=CARTESIAN_POINT ( 'NONE',  ( -20.54999999999999716, 1.115624548013267999E-11, -199.0999999999999375 ) ) ;
#68186=DIRECTION ( 'NONE',  ( 6.938893903907222067E-15, -1.000000000000000000, -0.000000000000000000 ) ) ;
#68213=ORIENTED_EDGE ( 'NONE', *, *, #43838, .F. ) ;
#68220=ORIENTED_EDGE ( 'NONE', *, *, #30889, .F. ) ;
#68230=FACE_OUTER_BOUND ( 'NONE', #211456, .T. ) ;
#68233=CIRCLE ( 'NONE', #234835, 0.09999999999999967248 ) ;
#68240=DIRECTION ( 'NONE',  ( -1.000000000000000000, -0.000000000000000000, -0.000000000000000000 ) ) ;
#68252=DIRECTION ( 'NONE',  ( 1.000000000000000000, 0.000000000000000000, 0.000000000000000000 ) ) ;
#68263=CARTESIAN_POINT ( 'NONE',  ( 21.05000000000000071, 11.65000000001116298, -193.9851942293460070 ) ) ;
#68272=AXIS2_PLACEMENT_3D ( 'NONE', #124585, #9753, #205371 ) ;
#68308=CARTESIAN_POINT ( 'NONE',  ( 18.58685178364168777, -9.406733083793099581, -174.6244204690876813 ) ) ;
#68389=EDGE_CURVE ( 'NONE', #175979, #42715, #100381, .T. ) ;
#68398=ORIENTED_EDGE ( 'NONE', *, *, #20605, .F. ) ;
#68415=LINE ( 'NONE', #111396, #41045 ) ;
#68419=TOROIDAL_SURFACE ( 'NONE', #155924, 11.89999999999999858, 0.1000000000000000056 ) ;
#68443=VERTEX_POINT ( 'NONE', #207229 ) ;
#68454=CARTESIAN_POINT ( 'NONE',  ( -23.15000000000000213, 11.75000000001115552, -188.8499999999999659 ) ) ;
#68525=PLANE ( 'NONE',  #239477 ) ;
#68596=DIRECTION ( 'NONE',  ( -1.000000000000000000, -0.000000000000000000, -0.000000000000000000 ) ) ;
#68616=CIRCLE ( 'NONE', #197594, 0.1999999999999987899 ) ;
#68646=ORIENTED_EDGE ( 'NONE', *, *, #6977, .F. ) ;
#68659=AXIS2_PLACEMENT_3D ( 'NONE', #170966, #250443, #151370 ) ;
#68686=CARTESIAN_POINT ( 'NONE',  ( -23.25000000000000000, 4.350000000011156054, -179.7499999999999716 ) ) ;
#68707=EDGE_CURVE ( 'NONE', #179090, #76578, #91586, .T. ) ;
#68728=AXIS2_PLACEMENT_3D ( 'NONE', #16085, #95584, #21222 ) ;
#68732=AXIS2_PLACEMENT_3D ( 'NONE', #158207, #137300, #197284 ) ;
#68739=ORIENTED_EDGE ( 'NONE', *, *, #179587, .T. ) ;
#68758=ORIENTED_EDGE ( 'NONE', *, *, #48281, .F. ) ;
#68762=DIRECTION ( 'NONE',  ( 2.952720810173288619E-16, -1.000000000000000000, 0.000000000000000000 ) ) ;
#68811=DIRECTION ( 'NONE',  ( 0.000000000000000000, 1.000000000000000000, 0.000000000000000000 ) ) ;
#68815=VECTOR ( 'NONE', #93108, 1000.000000000000000 ) ;
#68828=ORIENTED_EDGE ( 'NONE', *, *, #116386, .T. ) ;
#68868=CARTESIAN_POINT ( 'NONE',  ( -21.46681500597178882, 1.115541036281197940E-11, -160.6424888405653633 ) ) ;
#68870=ORIENTED_EDGE ( 'NONE', *, *, #179466, .F. ) ;
#68874=VERTEX_POINT ( 'NONE', #143057 ) ;
#68890=VERTEX_POINT ( 'NONE', #45258 ) ;
#68901=CARTESIAN_POINT ( 'NONE',  ( 21.05000000000000071, 1.115600667400684642E-11, -200.9999999999999432 ) ) ;
#68952=DIRECTION ( 'NONE',  ( 1.000000000000000000, 7.304098846218134667E-16, -4.607487905232622991E-31 ) ) ;
#68963=CARTESIAN_POINT ( 'NONE',  ( 22.49806830649814060, 0.07746431633666325811, -155.8501103451608856 ) ) ;
#68965=EDGE_LOOP ( 'NONE', ( #126434, #32227, #133185 ) ) ;
#68978=VERTEX_POINT ( 'NONE', #133776 ) ;
#68991=ORIENTED_EDGE ( 'NONE', *, *, #150787, .T. ) ;
#68994=DIRECTION ( 'NONE',  ( 1.000000000000000000, 2.952720810173289112E-16, -0.000000000000000000 ) ) ;
#69003=ORIENTED_EDGE ( 'NONE', *, *, #114407, .T. ) ;
#69026=VERTEX_POINT ( 'NONE', #191220 ) ;
#69044=LINE ( 'NONE', #28667, #235716 ) ;
#69071=DIRECTION ( 'NONE',  ( -1.000000000000000000, -3.265361837132813093E-16, 0.000000000000000000 ) ) ;
#69117=VERTEX_POINT ( 'NONE', #18957 ) ;
#69124=ORIENTED_EDGE ( 'NONE', *, *, #43435, .F. ) ;
#69135=EDGE_CURVE ( 'NONE', #237038, #118040, #60359, .T. ) ;
#69138=CYLINDRICAL_SURFACE ( 'NONE', #148327, 0.09999999999999939493 ) ;
#69192=CARTESIAN_POINT ( 'NONE',  ( -20.94999999999999929, 1.115600667400684642E-11, -167.4999999999999716 ) ) ;
#69193=AXIS2_PLACEMENT_3D ( 'NONE', #192077, #13432, #154263 ) ;
#69206=DIRECTION ( 'NONE',  ( 1.000000000000000000, 0.000000000000000000, 0.000000000000000000 ) ) ;
#69229=AXIS2_PLACEMENT_3D ( 'NONE', #122753, #104422, #242668 ) ;
#69253=FACE_OUTER_BOUND ( 'NONE', #68018, .T. ) ;
#69267=DIRECTION ( 'NONE',  ( 0.000000000000000000, -1.000000000000000000, 0.000000000000000000 ) ) ;
#69341=CARTESIAN_POINT ( 'NONE',  ( -21.05000000000000071, 1.115600667400684642E-11, -175.3999999999999773 ) ) ;
#69367=DIRECTION ( 'NONE',  ( -0.000000000000000000, -0.000000000000000000, 1.000000000000000000 ) ) ;
#69377=ADVANCED_FACE ( 'NONE', ( #112326 ), #250530, .F. ) ;
#69413=DIRECTION ( 'NONE',  ( 0.000000000000000000, 0.000000000000000000, -1.000000000000000000 ) ) ;
#69487=EDGE_LOOP ( 'NONE', ( #193440, #106287, #177909, #171319 ) ) ;
#69521=CARTESIAN_POINT ( 'NONE',  ( -18.50000000000000000, 5.341242990002803559, -157.6933497935119419 ) ) ;
#69523=CIRCLE ( 'NONE', #215251, 0.09999999999998715472 ) ;
#69538=DIRECTION ( 'NONE',  ( -1.000000000000000000, -2.952720810173289112E-16, 0.000000000000000000 ) ) ;
#69705=VERTEX_POINT ( 'NONE', #67747 ) ;
#69726=EDGE_CURVE ( 'NONE', #130308, #82909, #168176, .T. ) ;
#69732=ORIENTED_EDGE ( 'NONE', *, *, #66364, .F. ) ;
#69738=ADVANCED_FACE ( 'NONE', ( #45620 ), #1924, .T. ) ;
#69778=EDGE_CURVE ( 'NONE', #103174, #66550, #60381, .T. ) ;
#69785=CARTESIAN_POINT ( 'NONE',  ( 20.89878130938411616, 10.32747123227773045, -206.5774032850248716 ) ) ;
#69815=AXIS2_PLACEMENT_3D ( 'NONE', #247604, #68994, #169398 ) ;
#69821=CARTESIAN_POINT ( 'NONE',  ( -18.50000000000000000, 9.250000000011157297, -188.7499999999999716 ) ) ;
#69824=VECTOR ( 'NONE', #136503, 1000.000000000000000 ) ;
#69835=AXIS2_PLACEMENT_3D ( 'NONE', #177547, #216627, #135 ) ;
#69847=ORIENTED_EDGE ( 'NONE', *, *, #88043, .T. ) ;
#69895=CARTESIAN_POINT ( 'NONE',  ( 21.05000000000000071, 1.115600667400684642E-11, -167.4999999999999716 ) ) ;
#69901=CARTESIAN_POINT ( 'NONE',  ( 20.94999999999999574, 1.261786168576181755, -175.5864989635454378 ) ) ;
#69911=ADVANCED_FACE ( 'NONE', ( #161416 ), #257878, .F. ) ;
#69918=DIRECTION ( 'NONE',  ( 0.000000000000000000, 0.000000000000000000, -1.000000000000000000 ) ) ;
#69926=EDGE_CURVE ( 'NONE', #169929, #97822, #168927, .T. ) ;
#69939=CARTESIAN_POINT ( 'NONE',  ( -22.57320508075686405, 11.75000000001115552, -167.5000000000000000 ) ) ;
#69980=ORIENTED_EDGE ( 'NONE', *, *, #50722, .F. ) ;
#70009=EDGE_CURVE ( 'NONE', #62433, #22716, #6209, .T. ) ;
#70017=AXIS2_PLACEMENT_3D ( 'NONE', #21202, #56426, #116430 ) ;
#70046=CARTESIAN_POINT ( 'NONE',  ( 20.94999999999997442, -1.263275465206102233, -208.9018646667463770 ) ) ;
#70081=DIRECTION ( 'NONE',  ( -1.000000000000000000, -2.952720810173289112E-16, 0.000000000000000000 ) ) ;
#70092=CARTESIAN_POINT ( 'NONE',  ( 21.05000000000000071, 10.48443348965288635, -174.9568058014918961 ) ) ;
#70106=ORIENTED_EDGE ( 'NONE', *, *, #180508, .F. ) ;
#70132=DIRECTION ( 'NONE',  ( -4.448008912761043807E-16, 1.000000000000000000, 0.000000000000000000 ) ) ;
#70138=DIRECTION ( 'NONE',  ( 0.000000000000000000, -1.000000000000000000, -0.000000000000000000 ) ) ;
#70268=LINE ( 'NONE', #245018, #148214 ) ;
#70310=CARTESIAN_POINT ( 'NONE',  ( 18.39999999999999858, -9.682403433465241349, -207.6568433774127413 ) ) ;
#70323=LINE ( 'NONE', #149843, #146555 ) ;
#70327=VECTOR ( 'NONE', #6967, 1000.000000000000000 ) ;
#70351=DIRECTION ( 'NONE',  ( 0.000000000000000000, 0.000000000000000000, -1.000000000000000000 ) ) ;
#70364=DIRECTION ( 'NONE',  ( 0.000000000000000000, 0.000000000000000000, 1.000000000000000000 ) ) ;
#70413=ORIENTED_EDGE ( 'NONE', *, *, #95887, .T. ) ;
#70446=CARTESIAN_POINT ( 'NONE',  ( -20.94999999999999929, -11.64999999998884483, -170.3999999999999773 ) ) ;
#70505=DIRECTION ( 'NONE',  ( 0.000000000000000000, 0.000000000000000000, -1.000000000000000000 ) ) ;
#70506=CARTESIAN_POINT ( 'NONE',  ( -20.94684162708999864, 11.74999999080544022, -174.3416440060701973 ) ) ;
#70508=DIRECTION ( 'NONE',  ( 0.000000000000000000, -1.000000000000000000, 0.000000000000000000 ) ) ;
#70546=CARTESIAN_POINT ( 'NONE',  ( 20.95083306685154056, 8.916842641901356004, -175.9773248532583239 ) ) ;
#70560=TOROIDAL_SURFACE ( 'NONE', #249599, 0.2000000000000000111, 0.1000000000000000056 ) ;
#70591=CYLINDRICAL_SURFACE ( 'NONE', #63946, 0.5000000000000004441 ) ;
#70620=VERTEX_POINT ( 'NONE', #175255 ) ;
#70636=DIRECTION ( 'NONE',  ( -3.265361837132813093E-16, 1.000000000000000000, -0.000000000000000000 ) ) ;
#70657=DIRECTION ( 'NONE',  ( 1.000000000000000000, 0.000000000000000000, -0.000000000000000000 ) ) ;
#70663=EDGE_LOOP ( 'NONE', ( #218608, #247151, #251992, #4193, #99139, #120905, #107335, #164417, #151501, #217158, #81588, #36603, #194518, #221195, #248378, #59505 ) ) ;
#70679=AXIS2_PLACEMENT_3D ( 'NONE', #177278, #16902, #199400 ) ;
#70709=FACE_BOUND ( 'NONE', #212064, .T. ) ;
#70730=VECTOR ( 'NONE', #89013, 1000.000000000000000 ) ;
#70738=CYLINDRICAL_SURFACE ( 'NONE', #121379, 0.09999999999998898659 ) ;
#70782=ORIENTED_EDGE ( 'NONE', *, *, #53689, .F. ) ;
#70818=ORIENTED_EDGE ( 'NONE', *, *, #255539, .F. ) ;
#70822=ORIENTED_EDGE ( 'NONE', *, *, #4982, .F. ) ;
#70829=DIRECTION ( 'NONE',  ( 0.000000000000000000, 0.000000000000000000, -1.000000000000000000 ) ) ;
#70841=EDGE_CURVE ( 'NONE', #133882, #13363, #223073, .T. ) ;
#70866=CARTESIAN_POINT ( 'NONE',  ( 21.07933241753356768, 6.328645948390904330, -167.4066204095806540 ) ) ;
#70877=DIRECTION ( 'NONE',  ( -1.000000000000000000, -0.000000000000000000, -0.000000000000000000 ) ) ;
#70878=CARTESIAN_POINT ( 'NONE',  ( 20.87155475150661132, 11.75000000001115907, -194.0955865291576004 ) ) ;
#70888=VERTEX_POINT ( 'NONE', #31579 ) ;
#70908=ORIENTED_EDGE ( 'NONE', *, *, #14700, .T. ) ;
#70950=AXIS2_PLACEMENT_3D ( 'NONE', #236055, #155275, #139512 ) ;
#70965=DIRECTION ( 'NONE',  ( 0.000000000000000000, 0.000000000000000000, -1.000000000000000000 ) ) ;
#71005=ORIENTED_EDGE ( 'NONE', *, *, #52470, .F. ) ;
#71052=DIRECTION ( 'NONE',  ( 0.000000000000000000, 1.000000000000000000, 0.000000000000000000 ) ) ;
#71055=CARTESIAN_POINT ( 'NONE',  ( -18.50000000000000711, 11.65000000001115232, -174.5148057706539930 ) ) ;
#71090=CARTESIAN_POINT ( 'NONE',  ( 21.09546886439552438, 8.878553113026056209, -179.7370938505546007 ) ) ;
#71097=ORIENTED_EDGE ( 'NONE', *, *, #48281, .T. ) ;
#71106=CARTESIAN_POINT ( 'NONE',  ( 20.94999999999999929, 5.000000000011153745, -188.5947339810868755 ) ) ;
#71176=CARTESIAN_POINT ( 'NONE',  ( 21.14999999999999858, 11.65000000001116298, -155.7499999999999716 ) ) ;
#71180=CARTESIAN_POINT ( 'NONE',  ( 21.05000000000000071, 6.540656951712402467, -167.4999999999999716 ) ) ;
#71184=VERTEX_POINT ( 'NONE', #105241 ) ;
#71193=CARTESIAN_POINT ( 'NONE',  ( -23.15000000000000213, 2.000000000011154189, -187.7753780772378889 ) ) ;
#71202=ORIENTED_EDGE ( 'NONE', *, *, #226340, .T. ) ;
#71208=FACE_OUTER_BOUND ( 'NONE', #135780, .T. ) ;
#71218=CARTESIAN_POINT ( 'NONE',  ( -22.49999999999999645, 11.74956712350054744, -167.3991416309012550 ) ) ;
#71223=FACE_OUTER_BOUND ( 'NONE', #56176, .T. ) ;
#71235=EDGE_CURVE ( 'NONE', #59075, #16193, #88260, .T. ) ;
#71249=PLANE ( 'NONE',  #116872 ) ;
#71253=CIRCLE ( 'NONE', #54656, 0.5000000000000004441 ) ;
#71262=ORIENTED_EDGE ( 'NONE', *, *, #91537, .F. ) ;
#71353=CARTESIAN_POINT ( 'NONE',  ( 20.94999999999999929, 1.115600667400684642E-11, -167.4999999999999716 ) ) ;
#71391=CARTESIAN_POINT ( 'NONE',  ( -20.54999999999999716, -9.499999999988846255, -191.1060308773475356 ) ) ;
#71409=CARTESIAN_POINT ( 'NONE',  ( -20.54999999999999716, 1.115600667400684642E-11, -200.9999999999999432 ) ) ;
#71445=CARTESIAN_POINT ( 'NONE',  ( 20.94999999999999929, 1.115624548013267999E-11, -199.0999999999999375 ) ) ;
#71469=VECTOR ( 'NONE', #184272, 1000.000000000000000 ) ;
#71490=DIRECTION ( 'NONE',  ( 2.952720810173289112E-16, -1.000000000000000000, 0.000000000000000000 ) ) ;
#71513=AXIS2_PLACEMENT_3D ( 'NONE', #96692, #116310, #234966 ) ;
#71560=ORIENTED_EDGE ( 'NONE', *, *, #205901, .T. ) ;
#71570=DIRECTION ( 'NONE',  ( 1.000000000000000000, -0.000000000000000000, -0.000000000000000000 ) ) ;
#71584=DIRECTION ( 'NONE',  ( 1.000000000000000000, 3.265361837132813093E-16, -0.000000000000000000 ) ) ;
#71626=AXIS2_PLACEMENT_3D ( 'NONE', #29787, #28513, #49307 ) ;
#71634=AXIS2_PLACEMENT_3D ( 'NONE', #91031, #131435, #187589 ) ;
#71637=EDGE_LOOP ( 'NONE', ( #115351, #83252, #25941, #198606 ) ) ;
#71659=LINE ( 'NONE', #151186, #172024 ) ;
#71692=EDGE_LOOP ( 'NONE', ( #216607, #237355, #81471, #28460 ) ) ;
#71696=ORIENTED_EDGE ( 'NONE', *, *, #99475, .F. ) ;
#71699=ORIENTED_EDGE ( 'NONE', *, *, #141792, .T. ) ;
#71702=CARTESIAN_POINT ( 'NONE',  ( -20.85000000000000142, 11.65000000001115232, -200.9999999999999432 ) ) ;
#71705=ORIENTED_EDGE ( 'NONE', *, *, #4415, .F. ) ;
#71713=CARTESIAN_POINT ( 'NONE',  ( 21.05000000000000071, 0.09779029131994770863, -161.2421853895238542 ) ) ;
#71717=DIRECTION ( 'NONE',  ( 1.000000000000000000, 0.000000000000000000, 0.000000000000000000 ) ) ;
#71719=ORIENTED_EDGE ( 'NONE', *, *, #44960, .T. ) ;
#71738=EDGE_CURVE ( 'NONE', #142512, #87114, #19628, .T. ) ;
#71745=DIRECTION ( 'NONE',  ( -0.000000000000000000, 0.000000000000000000, 1.000000000000000000 ) ) ;
#71754=CIRCLE ( 'NONE', #217445, 0.09999999999998898659 ) ;
#71759=FACE_OUTER_BOUND ( 'NONE', #102750, .T. ) ;
#71766=CARTESIAN_POINT ( 'NONE',  ( -21.05000000000000071, -1.162701749926853712, -175.5999999999999659 ) ) ;
#71770=ORIENTED_EDGE ( 'NONE', *, *, #61184, .T. ) ;
#71771=CARTESIAN_POINT ( 'NONE',  ( -20.54999999999999716, -9.399999999988848387, -177.3939691226524076 ) ) ;
#71781=DIRECTION ( 'NONE',  ( -1.000000000000000000, 0.000000000000000000, 0.000000000000000000 ) ) ;
#71842=FACE_OUTER_BOUND ( 'NONE', #54110, .T. ) ;
#71855=EDGE_LOOP ( 'NONE', ( #36950, #41885, #247020, #222584 ) ) ;
#71858=DIRECTION ( 'NONE',  ( 0.000000000000000000, 0.000000000000000000, 1.000000000000000000 ) ) ;
#71876=LINE ( 'NONE', #73175, #252401 ) ;
#71904=EDGE_CURVE ( 'NONE', #14880, #252820, #11443, .T. ) ;
#71907=CARTESIAN_POINT ( 'NONE',  ( 18.59999999999999432, -1.835859311432484375, -212.5044391687984842 ) ) ;
#71918=AXIS2_PLACEMENT_3D ( 'NONE', #186234, #6289, #25885 ) ;
#71947=ORIENTED_EDGE ( 'NONE', *, *, #215185, .F. ) ;
#71972=AXIS2_PLACEMENT_3D ( 'NONE', #4307, #102108, #162135 ) ;
#71988=DIRECTION ( 'NONE',  ( 0.000000000000000000, 6.938893903907270030E-14, 1.000000000000000000 ) ) ;
#71995=VERTEX_POINT ( 'NONE', #108528 ) ;
#72053=ADVANCED_FACE ( 'NONE', ( #91539 ), #109798, .T. ) ;
#72072=DIRECTION ( 'NONE',  ( 1.000000000000000000, -7.304098846218134667E-16, -0.000000000000000000 ) ) ;
#72077=EDGE_CURVE ( 'NONE', #172330, #69117, #190522, .T. ) ;
#72109=VERTEX_POINT ( 'NONE', #96631 ) ;
#72147=ADVANCED_FACE ( 'NONE', ( #193216 ), #137760, .F. ) ;
#72149=CARTESIAN_POINT ( 'NONE',  ( 20.85000000106584750, 11.75000000001115907, -194.1555046564733971 ) ) ;
#72150=DIRECTION ( 'NONE',  ( -0.000000000000000000, -0.000000000000000000, 1.000000000000000000 ) ) ;
#72169=ORIENTED_EDGE ( 'NONE', *, *, #169041, .T. ) ;
#72177=DIRECTION ( 'NONE',  ( 1.000000000000000000, -0.000000000000000000, -0.000000000000000000 ) ) ;
#72189=LINE ( 'NONE', #167445, #197551 ) ;
#72191=EDGE_LOOP ( 'NONE', ( #201449, #245682, #53417, #203860 ) ) ;
#72206=FACE_OUTER_BOUND ( 'NONE', #138059, .T. ) ;
#72213=ADVANCED_FACE ( 'NONE', ( #80935 ), #206674, .F. ) ;
#72222=CARTESIAN_POINT ( 'NONE',  ( -18.43569575749026512, -9.519327731081288491, -174.4729763765592736 ) ) ;
#72227=ORIENTED_EDGE ( 'NONE', *, *, #78351, .T. ) ;
#72236=VERTEX_POINT ( 'NONE', #166620 ) ;
#72244=DIRECTION ( 'NONE',  ( 0.000000000000000000, -1.000000000000000000, 0.000000000000000000 ) ) ;
#72306=DIRECTION ( 'NONE',  ( 6.938893903907224433E-15, -1.000000000000000000, -2.891205793294679805E-16 ) ) ;
#72321=CARTESIAN_POINT ( 'NONE',  ( 18.59999999999999787, -1.835341550213255957, -179.1551512925629197 ) ) ;
#72336=DIRECTION ( 'NONE',  ( 0.000000000000000000, 0.000000000000000000, -1.000000000000000000 ) ) ;
#72376=CARTESIAN_POINT ( 'NONE',  ( 21.05000000000000071, 8.776282895303626930, -179.6499999999999773 ) ) ;
#72388=CARTESIAN_POINT ( 'NONE',  ( 22.39999999999999858, 7.790779598384538929, -167.3999999999999773 ) ) ;
#72398=VECTOR ( 'NONE', #168494, 1000.000000000000000 ) ;
#72418=ORIENTED_EDGE ( 'NONE', *, *, #160584, .T. ) ;
#72427=ORIENTED_EDGE ( 'NONE', *, *, #178239, .T. ) ;
#72468=CARTESIAN_POINT ( 'NONE',  ( 23.24999999999999645, 1.115600667400684642E-11, -167.4999999999999716 ) ) ;
#72488=AXIS2_PLACEMENT_3D ( 'NONE', #248975, #46889, #187724 ) ;
#72517=ORIENTED_EDGE ( 'NONE', *, *, #26394, .T. ) ;
#72529=DIRECTION ( 'NONE',  ( 0.000000000000000000, 0.000000000000000000, 1.000000000000000000 ) ) ;
#72538=ORIENTED_EDGE ( 'NONE', *, *, #132290, .F. ) ;
#72564=EDGE_CURVE ( 'NONE', #103201, #224509, #20374, .T. ) ;
#72568=ORIENTED_EDGE ( 'NONE', *, *, #119656, .T. ) ;
#72592=EDGE_CURVE ( 'NONE', #11610, #147404, #19426, .T. ) ;
#72612=EDGE_CURVE ( 'NONE', #251611, #5997, #111002, .T. ) ;
#72662=ORIENTED_EDGE ( 'NONE', *, *, #22304, .F. ) ;
#72692=DIRECTION ( 'NONE',  ( 0.000000000000000000, -8.881784197000685330E-16, -1.000000000000000000 ) ) ;
#72732=EDGE_CURVE ( 'NONE', #158852, #252820, #186200, .T. ) ;
#72743=AXIS2_PLACEMENT_3D ( 'NONE', #21672, #221129, #101144 ) ;
#72776=ORIENTED_EDGE ( 'NONE', *, *, #13214, .T. ) ;
#72781=PLANE ( 'NONE',  #153038 ) ;
#72797=EDGE_LOOP ( 'NONE', ( #97019, #256956, #43378, #88594 ) ) ;
#72806=DIRECTION ( 'NONE',  ( -1.000000000000000000, 0.000000000000000000, 0.000000000000000000 ) ) ;
#72811=DIRECTION ( 'NONE',  ( 1.000000000000000000, 0.000000000000000000, 0.000000000000000000 ) ) ;
#72839=ORIENTED_EDGE ( 'NONE', *, *, #196100, .T. ) ;
#72863=CARTESIAN_POINT ( 'NONE',  ( -20.64999999999999858, 1.115600667400684642E-11, -200.9999999999999432 ) ) ;
#72892=ADVANCED_FACE ( 'NONE', ( #30646 ), #133571, .T. ) ;
#72964=CARTESIAN_POINT ( 'NONE',  ( -22.50000000000000000, 11.75000000001115552, -167.4999999999999716 ) ) ;
#72975=CARTESIAN_POINT ( 'NONE',  ( -20.85000000000000142, 1.115600667400684642E-11, -208.8999999999999488 ) ) ;
#73051=EDGE_LOOP ( 'NONE', ( #24524, #16438, #73245, #171886, #19536 ) ) ;
#73130=CARTESIAN_POINT ( 'NONE',  ( -21.05000000000000071, -0.09999999998884338825, -160.9593430482987344 ) ) ;
#73175=CARTESIAN_POINT ( 'NONE',  ( 18.50000000000000000, -9.399999999988843058, -174.4992856778388273 ) ) ;
#73176=EDGE_LOOP ( 'NONE', ( #257847, #175698, #107217, #180344 ) ) ;
#73204=DIRECTION ( 'NONE',  ( -0.000000000000000000, -0.000000000000000000, 1.000000000000000000 ) ) ;
#73245=ORIENTED_EDGE ( 'NONE', *, *, #38502, .F. ) ;
#73250=CIRCLE ( 'NONE', #56595, 0.09999999999999158173 ) ;
#73261=CARTESIAN_POINT ( 'NONE',  ( 19.97071067811864609, 11.72071067812981404, -188.8499999999999659 ) ) ;
#73266=AXIS2_PLACEMENT_3D ( 'NONE', #187707, #152442, #231970 ) ;
#73281=CARTESIAN_POINT ( 'NONE',  ( 22.47071067811865319, 7.720074744509199505, -167.4009075452973434 ) ) ;
#73289=DIRECTION ( 'NONE',  ( -0.000000000000000000, -0.9887567792719339499, -0.1495327102803676589 ) ) ;
#73358=CARTESIAN_POINT ( 'NONE',  ( -20.54999999999999716, 1.115600667400684642E-11, -180.4749999999999659 ) ) ;
#73387=ADVANCED_FACE ( 'NONE', ( #26178 ), #211324, .T. ) ;
#73390=EDGE_CURVE ( 'NONE', #16272, #152584, #159274, .T. ) ;
#73395=CARTESIAN_POINT ( 'NONE',  ( 21.13614978966381841, 1.115648815929779806E-11, -161.0008952981661707 ) ) ;
#73428=ADVANCED_FACE ( 'NONE', ( #49584 ), #245226, .T. ) ;
#73463=VERTEX_POINT ( 'NONE', #169576 ) ;
#73469=ORIENTED_EDGE ( 'NONE', *, *, #241848, .T. ) ;
#73497=DIRECTION ( 'NONE',  ( 0.000000000000000000, 0.000000000000000000, -1.000000000000000000 ) ) ;
#73520=EDGE_CURVE ( 'NONE', #204695, #46891, #6046, .T. ) ;
#73579=ORIENTED_EDGE ( 'NONE', *, *, #152964, .T. ) ;
#73598=ORIENTED_EDGE ( 'NONE', *, *, #179678, .T. ) ;
#73604=ORIENTED_EDGE ( 'NONE', *, *, #52839, .F. ) ;
#73629=DIRECTION ( 'NONE',  ( 0.000000000000000000, 0.000000000000000000, -1.000000000000000000 ) ) ;
#73632=DIRECTION ( 'NONE',  ( -1.000000000000000000, -2.952720810173289112E-16, 0.000000000000000000 ) ) ;
#73698=CARTESIAN_POINT ( 'NONE',  ( -21.05000000000000071, 1.115600667400684642E-11, -167.4999999999999716 ) ) ;
#73706=DIRECTION ( 'NONE',  ( -1.000000000000000000, 0.000000000000000000, 0.000000000000000000 ) ) ;
#73709=CARTESIAN_POINT ( 'NONE',  ( -18.46093223321767596, -9.480682968263407062, -174.5845505139266436 ) ) ;
#73711=FACE_OUTER_BOUND ( 'NONE', #108888, .T. ) ;
#73725=CARTESIAN_POINT ( 'NONE',  ( 20.94999999999999574, -1.851028230129704522, -179.1539132694224463 ) ) ;
#73730=CARTESIAN_POINT ( 'NONE',  ( -23.25000000000000000, 2.000000000011154189, -180.7246219227620543 ) ) ;
#73755=CARTESIAN_POINT ( 'NONE',  ( -23.25000000000000000, 1.115600667400684642E-11, -203.0999999999999375 ) ) ;
#73772=DIRECTION ( 'NONE',  ( 1.000000000000000000, 0.000000000000000000, -0.000000000000000000 ) ) ;
#73788=CARTESIAN_POINT ( 'NONE',  ( -20.94999999999999929, -11.48912529306490349, -170.5999999999999659 ) ) ;
#73817=DIRECTION ( 'NONE',  ( -0.000000000000000000, 1.000000000000000000, 0.000000000000000000 ) ) ;
#73845=EDGE_CURVE ( 'NONE', #26557, #138331, #88366, .T. ) ;
#73864=EDGE_CURVE ( 'NONE', #34141, #26557, #161240, .T. ) ;
#73918=CARTESIAN_POINT ( 'NONE',  ( -20.87155475150660777, 11.75000000001115197, -194.0955865291576004 ) ) ;
#73931=CARTESIAN_POINT ( 'NONE',  ( -22.48479450179659977, 0.04699158119804078271, -155.8500015537483421 ) ) ;
#73954=ORIENTED_EDGE ( 'NONE', *, *, #9995, .F. ) ;
#73964=EDGE_LOOP ( 'NONE', ( #181787, #230052, #222693, #159838, #86336 ) ) ;
#73966=CARTESIAN_POINT ( 'NONE',  ( -23.15000000000000213, 11.65000000001115588, -188.8499999999999659 ) ) ;
#73970=CARTESIAN_POINT ( 'NONE',  ( 21.53752568617682428, 6.786807874514932060, -167.4010255387155155 ) ) ;
#73984=EDGE_LOOP ( 'NONE', ( #18187, #228850, #171916, #97868 ) ) ;
#73992=ORIENTED_EDGE ( 'NONE', *, *, #222061, .F. ) ;
#74013=ORIENTED_EDGE ( 'NONE', *, *, #146156, .T. ) ;
#74015=DIRECTION ( 'NONE',  ( 0.000000000000000000, -0.000000000000000000, 1.000000000000000000 ) ) ;
#74084=ADVANCED_FACE ( 'NONE', ( #203853 ), #181734, .T. ) ;
#74098=CARTESIAN_POINT ( 'NONE',  ( -18.59999999999999787, 11.65000000001115232, -174.5148057706539930 ) ) ;
#74116=AXIS2_PLACEMENT_3D ( 'NONE', #8210, #86412, #147711 ) ;
#74155=CIRCLE ( 'NONE', #174119, 0.09999999999999939493 ) ;
#74196=ADVANCED_FACE ( 'NONE', ( #163031 ), #83439, .F. ) ;
#74199=DIRECTION ( 'NONE',  ( 0.000000000000000000, -0.1350103645451876666, -0.9908441862701600211 ) ) ;
#74213=DIRECTION ( 'NONE',  ( 1.000000000000000000, -0.000000000000000000, -0.000000000000000000 ) ) ;
#74232=DIRECTION ( 'NONE',  ( 0.000000000000000000, -1.000000000000000000, 0.000000000000000000 ) ) ;
#74236=ORIENTED_EDGE ( 'NONE', *, *, #170429, .F. ) ;
#74245=EDGE_LOOP ( 'NONE', ( #141423, #213071, #107675, #46974 ) ) ;
#74288=ORIENTED_EDGE ( 'NONE', *, *, #98920, .T. ) ;
#74307=CARTESIAN_POINT ( 'NONE',  ( -18.50000000000000000, -9.399999999988850163, -174.7972597596632625 ) ) ;
#74314=CIRCLE ( 'NONE', #253333, 0.2000000000000057288 ) ;
#74323=ORIENTED_EDGE ( 'NONE', *, *, #185009, .T. ) ;
#74335=CARTESIAN_POINT ( 'NONE',  ( 21.14999999999999858, 11.75000000001116263, -155.7499999999999716 ) ) ;
#74342=CARTESIAN_POINT ( 'NONE',  ( 19.58285714285715073, 9.015001489659738354, -175.9206528160816845 ) ) ;
#74371=DIRECTION ( 'NONE',  ( 0.000000000000000000, -0.000000000000000000, 1.000000000000000000 ) ) ;
#74389=ORIENTED_EDGE ( 'NONE', *, *, #215703, .T. ) ;
#74445=AXIS2_PLACEMENT_3D ( 'NONE', #155763, #179177, #54055 ) ;
#74467=TOROIDAL_SURFACE ( 'NONE', #90987, 0.2000000000000000111, 0.1000000000000000056 ) ;
#74477=EDGE_CURVE ( 'NONE', #60251, #33844, #157607, .T. ) ;
#74485=AXIS2_PLACEMENT_3D ( 'NONE', #139404, #218954, #40369 ) ;
#74501=DIRECTION ( 'NONE',  ( -1.000000000000000000, -0.000000000000000000, -0.000000000000000000 ) ) ;
#74516=CIRCLE ( 'NONE', #241080, 4.099999999999992539 ) ;
#74521=( BOUNDED_CURVE ( )  B_SPLINE_CURVE ( 3, ( #182075, #67250, #204182, #26873 ),
 .UNSPECIFIED., .F., .F. ) 
 B_SPLINE_CURVE_WITH_KNOTS ( ( 4, 4 ),
 ( 4.712388980384690562, 6.283185307179586232 ),
 .UNSPECIFIED. ) 
 CURVE ( )  GEOMETRIC_REPRESENTATION_ITEM ( )  RATIONAL_B_SPLINE_CURVE ( ( 1.000000000000000000, 0.8047378541243652705, 0.8047378541243652705, 1.000000000000000000 ) ) 
 REPRESENTATION_ITEM ( '' )  );
#74575=DIRECTION ( 'NONE',  ( 1.000000000000000000, -7.304098846218133681E-16, 4.217023435051677994E-16 ) ) ;
#74576=ORIENTED_EDGE ( 'NONE', *, *, #228139, .F. ) ;
#74591=ORIENTED_EDGE ( 'NONE', *, *, #57533, .F. ) ;
#74627=DIRECTION ( 'NONE',  ( 2.978066053179067751E-16, -1.000000000000000000, -2.382452842543254201E-15 ) ) ;
#74631=AXIS2_PLACEMENT_3D ( 'NONE', #21089, #161880, #19793 ) ;
#74692=DIRECTION ( 'NONE',  ( 1.000000000000000000, -7.304098846218134667E-16, -4.217023435051626718E-16 ) ) ;
#74694=FACE_OUTER_BOUND ( 'NONE', #228907, .T. ) ;
#74705=CARTESIAN_POINT ( 'NONE',  ( -23.25000000000000000, -1.835859311432481045, -212.5044391687984842 ) ) ;
#74718=LINE ( 'NONE', #29172, #28366 ) ;
#74725=CIRCLE ( 'NONE', #20537, 3.899999999999987033 ) ;
#74733=AXIS2_PLACEMENT_3D ( 'NONE', #130742, #173782, #189444 ) ;
#74741=DIRECTION ( 'NONE',  ( 0.000000000000000000, 0.000000000000000000, -1.000000000000000000 ) ) ;
#74782=ORIENTED_EDGE ( 'NONE', *, *, #22685, .F. ) ;
#74809=CIRCLE ( 'NONE', #74631, 4.099999999999992539 ) ;
#74846=CIRCLE ( 'NONE', #175361, 0.09999999999998898659 ) ;
#74885=MECHANICAL_DESIGN_GEOMETRIC_PRESENTATION_REPRESENTATION('',(#178941),#20700);
#74898=ADVANCED_FACE ( 'NONE', ( #245080 ), #156095, .F. ) ;
#74909=CARTESIAN_POINT ( 'NONE',  ( -18.39999999999999858, -9.499999999988849808, -174.5320693966996259 ) ) ;
#74913=CARTESIAN_POINT ( 'NONE',  ( 21.05000000000000071, 1.115623935689868526E-11, -199.0999999999999375 ) ) ;
#74970=ORIENTED_EDGE ( 'NONE', *, *, #176940, .T. ) ;
#74989=CARTESIAN_POINT ( 'NONE',  ( 20.94999999999999929, -11.39257802169451317, -197.9260504201680249 ) ) ;
#75008=TOROIDAL_SURFACE ( 'NONE', #124865, 11.70000000000000462, 0.1000000000000000056 ) ;
#75020=CIRCLE ( 'NONE', #104201, 0.1000000000000106914 ) ;
#75036=VECTOR ( 'NONE', #145198, 1000.000000000000000 ) ;
#75101=AXIS2_PLACEMENT_3D ( 'NONE', #161447, #18059, #42765 ) ;
#75137=AXIS2_PLACEMENT_3D ( 'NONE', #197120, #257052, #253240 ) ;
#75147=ORIENTED_EDGE ( 'NONE', *, *, #219693, .F. ) ;
#75160=DIRECTION ( 'NONE',  ( -7.304098846218134667E-16, -1.000000000000000000, 0.000000000000000000 ) ) ;
#75167=DIRECTION ( 'NONE',  ( 0.000000000000000000, 0.8660254037844482555, 0.4999999999999837907 ) ) ;
#75192=CARTESIAN_POINT ( 'NONE',  ( -21.05000000000000071, 1.835341550235567887, -179.1551512925629197 ) ) ;
#75209=CARTESIAN_POINT ( 'NONE',  ( -22.39999999999999858, 1.115600667400684642E-11, -155.8504291924551808 ) ) ;
#75238=VERTEX_POINT ( 'NONE', #257861 ) ;
#75252=DIRECTION ( 'NONE',  ( -5.603264701231743991E-32, 1.897661533703519897E-16, -1.000000000000000000 ) ) ;
#75281=DIRECTION ( 'NONE',  ( 0.000000000000000000, 0.9876197685951252359, -0.1568667991644863424 ) ) ;
#75293=CARTESIAN_POINT ( 'NONE',  ( 20.85000000000000142, -1.149570369564537842, -208.8159124845019221 ) ) ;
#75295=CARTESIAN_POINT ( 'NONE',  ( 21.11825140030092740, 0.007203620643933773479, -161.0545924345799165 ) ) ;
#75296=LINE ( 'NONE', #176965, #215673 ) ;
#75302=ADVANCED_FACE ( 'NONE', ( #203066 ), #183514, .F. ) ;
#75329=DIRECTION ( 'NONE',  ( 0.000000000000000000, 0.4999999999999478195, -0.8660254037844686836 ) ) ;
#75334=ORIENTED_EDGE ( 'NONE', *, *, #26394, .F. ) ;
#75355=VERTEX_POINT ( 'NONE', #107820 ) ;
#75390=EDGE_CURVE ( 'NONE', #97822, #196712, #83201, .T. ) ;
#75406=ORIENTED_EDGE ( 'NONE', *, *, #51725, .T. ) ;
#75408=DIRECTION ( 'NONE',  ( -1.000000000000000000, 0.000000000000000000, 0.000000000000000000 ) ) ;
#75412=AXIS2_PLACEMENT_3D ( 'NONE', #63271, #24171, #121973 ) ;
#75418=DIRECTION ( 'NONE',  ( 0.000000000000000000, 0.000000000000000000, 1.000000000000000000 ) ) ;
#75457=CARTESIAN_POINT ( 'NONE',  ( 18.58719872626880942, -9.566644397587477755, -207.8224781963969860 ) ) ;
#75463=CARTESIAN_POINT ( 'NONE',  ( -18.47130263965431496, -9.471155585952907074, -207.6834047654772348 ) ) ;
#75493=ORIENTED_EDGE ( 'NONE', *, *, #27347, .F. ) ;
#75497=ORIENTED_EDGE ( 'NONE', *, *, #179678, .F. ) ;
#75510=ORIENTED_EDGE ( 'NONE', *, *, #129265, .F. ) ;
#75537=EDGE_CURVE ( 'NONE', #156856, #86816, #145761, .T. ) ;
#75550=ADVANCED_FACE ( 'NONE', ( #100735 ), #26, .F. ) ;
#75558=DIRECTION ( 'NONE',  ( -1.000000000000000000, -3.265361837132813093E-16, 0.000000000000000000 ) ) ;
#75581=VERTEX_POINT ( 'NONE', #156930 ) ;
#75614=DIRECTION ( 'NONE',  ( 0.000000000000000000, 0.000000000000000000, -1.000000000000000000 ) ) ;
#75627=DIRECTION ( 'NONE',  ( 0.000000000000000000, -1.000000000000000000, 0.000000000000000000 ) ) ;
#75632=DIRECTION ( 'NONE',  ( -3.265361837132813093E-16, 1.000000000000000000, 0.000000000000000000 ) ) ;
#75668=AXIS2_PLACEMENT_3D ( 'NONE', #74098, #149774, #213561 ) ;
#75698=ORIENTED_EDGE ( 'NONE', *, *, #30563, .F. ) ;
#75721=VERTEX_POINT ( 'NONE', #168508 ) ;
#75733=ORIENTED_EDGE ( 'NONE', *, *, #198383, .T. ) ;
#75734=CIRCLE ( 'NONE', #38313, 0.1000000000000002554 ) ;
#75736=EDGE_CURVE ( 'NONE', #54663, #20774, #204029, .T. ) ;
#75743=DIRECTION ( 'NONE',  ( -0.000000000000000000, 0.000000000000000000, 1.000000000000000000 ) ) ;
#75817=ORIENTED_EDGE ( 'NONE', *, *, #84433, .F. ) ;
#75832=ORIENTED_EDGE ( 'NONE', *, *, #106192, .F. ) ;
#75849=ORIENTED_EDGE ( 'NONE', *, *, #138555, .F. ) ;
#75931=ADVANCED_FACE ( 'NONE', ( #159197 ), #177488, .F. ) ;
#75936=CARTESIAN_POINT ( 'NONE',  ( 21.08479644141222664, 0.05855444257529676677, -161.1549613422680522 ) ) ;
#75940=CARTESIAN_POINT ( 'NONE',  ( 18.49999999999999289, 10.20857864377385127, -192.1499999999999488 ) ) ;
#75947=DIRECTION ( 'NONE',  ( 0.000000000000000000, -1.000000000000000000, -2.891205793294679805E-16 ) ) ;
#75949=DIRECTION ( 'NONE',  ( 0.000000000000000000, 0.000000000000000000, -1.000000000000000000 ) ) ;
#75975=AXIS2_PLACEMENT_3D ( 'NONE', #108989, #129838, #208127 ) ;
#75986=FACE_BOUND ( 'NONE', #245485, .T. ) ;
#75989=CARTESIAN_POINT ( 'NONE',  ( 20.95000000000000284, 11.60000000001116227, -194.0717967697244717 ) ) ;
#75991=ORIENTED_EDGE ( 'NONE', *, *, #240963, .F. ) ;
#76001=CARTESIAN_POINT ( 'NONE',  ( -22.47071067811865319, 7.720074744509219933, -167.4009075452973434 ) ) ;
#76005=DIRECTION ( 'NONE',  ( 0.000000000000000000, -0.8660254037844459241, -0.4999999999999873990 ) ) ;
#76010=AXIS2_PLACEMENT_3D ( 'NONE', #156320, #158875, #1020 ) ;
#76023=DIRECTION ( 'NONE',  ( 1.000000000000000000, 0.000000000000000000, 0.000000000000000000 ) ) ;
#76025=AXIS2_PLACEMENT_3D ( 'NONE', #73730, #155831, #112833 ) ;
#76044=EDGE_CURVE ( 'NONE', #184791, #152584, #125132, .T. ) ;
#76060=CYLINDRICAL_SURFACE ( 'NONE', #225546, 0.09999999999999817368 ) ;
#76095=PLANE ( 'NONE',  #214021 ) ;
#76107=AXIS2_PLACEMENT_3D ( 'NONE', #225034, #25588, #86812 ) ;
#76115=CARTESIAN_POINT ( 'NONE',  ( 18.59999999999999432, 1.162701749949165642, -175.5999999999999659 ) ) ;
#76171=EDGE_CURVE ( 'NONE', #170879, #185463, #134147, .T. ) ;
#76185=ADVANCED_FACE ( 'NONE', ( #129036 ), #229419, .T. ) ;
#76201=EDGE_CURVE ( 'NONE', #232936, #191282, #129589, .T. ) ;
#76230=ORIENTED_EDGE ( 'NONE', *, *, #95931, .F. ) ;
#76234=EDGE_LOOP ( 'NONE', ( #74782, #100184, #189401, #68991 ) ) ;
#76250=EDGE_CURVE ( 'NONE', #3673, #67428, #160170, .T. ) ;
#76254=CIRCLE ( 'NONE', #221980, 11.80000000000000249 ) ;
#76271=DIRECTION ( 'NONE',  ( 0.000000000000000000, 0.000000000000000000, -1.000000000000000000 ) ) ;
#76276=DIRECTION ( 'NONE',  ( -0.000000000000000000, 0.000000000000000000, 1.000000000000000000 ) ) ;
#76282=DIRECTION ( 'NONE',  ( 0.000000000000000000, 0.000000000000000000, 1.000000000000000000 ) ) ;
#76299=VERTEX_POINT ( 'NONE', #58446 ) ;
#76328=AXIS2_PLACEMENT_3D ( 'NONE', #93749, #12957, #233290 ) ;
#76329=EDGE_CURVE ( 'NONE', #160190, #245420, #146153, .T. ) ;
#76373=ORIENTED_EDGE ( 'NONE', *, *, #216243, .T. ) ;
#76374=DIRECTION ( 'NONE',  ( -1.000000000000000000, -0.000000000000000000, 0.000000000000000000 ) ) ;
#76439=FACE_OUTER_BOUND ( 'NONE', #134592, .T. ) ;
#76488=DIRECTION ( 'NONE',  ( 0.000000000000000000, 0.000000000000000000, -1.000000000000000000 ) ) ;
#76511=ORIENTED_EDGE ( 'NONE', *, *, #25094, .T. ) ;
#76516=EDGE_LOOP ( 'NONE', ( #3144, #113466, #113388, #408 ) ) ;
#76538=CARTESIAN_POINT ( 'NONE',  ( 21.05000000000000071, 0.09779029132037916905, -161.2421853895184540 ) ) ;
#76543=ORIENTED_EDGE ( 'NONE', *, *, #164813, .F. ) ;
#76545=ORIENTED_EDGE ( 'NONE', *, *, #215128, .T. ) ;
#76547=LINE ( 'NONE', #176974, #104448 ) ;
#76555=VECTOR ( 'NONE', #142099, 1000.000000000000000 ) ;
#76569=EDGE_LOOP ( 'NONE', ( #34674, #166519, #225584, #215400 ) ) ;
#76578=VERTEX_POINT ( 'NONE', #153464 ) ;
#76617=DIRECTION ( 'NONE',  ( 1.000000000000000000, 2.952720810173289112E-16, -0.000000000000000000 ) ) ;
#76633=CARTESIAN_POINT ( 'NONE',  ( 18.50211644919734866, 10.30207779525984968, -206.4895520716782187 ) ) ;
#76637=AXIS2_PLACEMENT_3D ( 'NONE', #113640, #54926, #92781 ) ;
#76644=DIRECTION ( 'NONE',  ( 0.000000000000000000, 0.000000000000000000, -1.000000000000000000 ) ) ;
#76655=CARTESIAN_POINT ( 'NONE',  ( -20.85000000000000142, 7.120270961708750512, -204.6595630418393057 ) ) ;
#76717=ORIENTED_EDGE ( 'NONE', *, *, #136879, .T. ) ;
#76736=CARTESIAN_POINT ( 'NONE',  ( 21.05000000000000071, -11.64999999998883595, -198.0999999999999659 ) ) ;
#76746=VECTOR ( 'NONE', #2312, 1000.000000000000227 ) ;
#76749=TOROIDAL_SURFACE ( 'NONE', #151620, 0.2000000000000000111, 0.1000000000000000056 ) ;
#76767=CARTESIAN_POINT ( 'NONE',  ( -21.08198257630413508, 0.07264332379574613141, -161.1634032659849254 ) ) ;
#76781=CYLINDRICAL_SURFACE ( 'NONE', #62424, 4.049999999999998046 ) ;
#76788=ORIENTED_EDGE ( 'NONE', *, *, #218231, .T. ) ;
#76804=ORIENTED_EDGE ( 'NONE', *, *, #234843, .F. ) ;
#76805=AXIS2_PLACEMENT_3D ( 'NONE', #244963, #211953, #87163 ) ;
#76809=CARTESIAN_POINT ( 'NONE',  ( -18.59999999999999787, 11.60000000001115872, -174.4282032302755283 ) ) ;
#76814=CIRCLE ( 'NONE', #35170, 4.049999999999998934 ) ;
#76882=ORIENTED_EDGE ( 'NONE', *, *, #88255, .F. ) ;
#76935=DIRECTION ( 'NONE',  ( 0.000000000000000000, 0.000000000000000000, -1.000000000000000000 ) ) ;
#76952=EDGE_CURVE ( 'NONE', #17335, #75581, #175222, .T. ) ;
#76958=AXIS2_PLACEMENT_3D ( 'NONE', #225194, #127410, #7447 ) ;
#76985=FACE_OUTER_BOUND ( 'NONE', #118608, .T. ) ;
#76993=EDGE_CURVE ( 'NONE', #13008, #85372, #130980, .T. ) ;
#77043=CARTESIAN_POINT ( 'NONE',  ( 22.59066674512285999, 11.75000000001115552, -167.4694958763696206 ) ) ;
#77050=CARTESIAN_POINT ( 'NONE',  ( -23.25000000000000000, 11.75000000001115552, -155.7499999999999716 ) ) ;
#77066=ORIENTED_EDGE ( 'NONE', *, *, #78522, .F. ) ;
#77095=ADVANCED_FACE ( 'NONE', ( #147344 ), #8582, .F. ) ;
#77106=DIRECTION ( 'NONE',  ( 0.000000000000000000, -3.552713678800483969E-15, 1.000000000000000000 ) ) ;
#77108=ORIENTED_EDGE ( 'NONE', *, *, #30580, .T. ) ;
#77122=ORIENTED_EDGE ( 'NONE', *, *, #100045, .T. ) ;
#77139=CIRCLE ( 'NONE', #93709, 0.09999999999998898659 ) ;
#77187=DIRECTION ( 'NONE',  ( 2.952720810173289112E-16, -1.000000000000000000, 0.000000000000000000 ) ) ;
#77188=AXIS2_PLACEMENT_3D ( 'NONE', #57250, #135509, #118557 ) ;
#77223=DIRECTION ( 'NONE',  ( -1.000000000000000000, 0.000000000000000000, 0.000000000000000000 ) ) ;
#77229=CARTESIAN_POINT ( 'NONE',  ( 23.14999999999999503, 11.75000000001116263, -155.7499999999999716 ) ) ;
#77269=CIRCLE ( 'NONE', #64790, 0.09999999999999939493 ) ;
#77299=VECTOR ( 'NONE', #40116, 999.9999999999998863 ) ;
#77349=DIRECTION ( 'NONE',  ( -0.000000000000000000, -0.000000000000000000, 1.000000000000000000 ) ) ;
#77358=VERTEX_POINT ( 'NONE', #100177 ) ;
#77370=ORIENTED_EDGE ( 'NONE', *, *, #204028, .F. ) ;
#77400=VERTEX_POINT ( 'NONE', #1079 ) ;
#77401=CARTESIAN_POINT ( 'NONE',  ( -21.05000000000000071, -11.48912529306489994, -197.8999999999999773 ) ) ;
#77420=CYLINDRICAL_SURFACE ( 'NONE', #256667, 12.87499999999999822 ) ;
#77440=CARTESIAN_POINT ( 'NONE',  ( 20.94999999999999929, 10.29270135741298731, -206.4573618871519045 ) ) ;
#77444=CARTESIAN_POINT ( 'NONE',  ( -18.55807992284871943, 10.32898536001801126, -206.5826683222764188 ) ) ;
#77482=ORIENTED_EDGE ( 'NONE', *, *, #236912, .F. ) ;
#77492=CARTESIAN_POINT ( 'NONE',  ( -23.25000000000000000, 11.65000000001115588, -188.8499999999999659 ) ) ;
#77494=CARTESIAN_POINT ( 'NONE',  ( -21.14999999999999858, 11.65000000001115588, -167.4999999999999716 ) ) ;
#77496=ADVANCED_FACE ( 'NONE', ( #256659 ), #161488, .F. ) ;
#77502=VERTEX_POINT ( 'NONE', #2372 ) ;
#77519=CARTESIAN_POINT ( 'NONE',  ( 21.70464131381650219, 7.095358018979006864, -167.4999999999999716 ) ) ;
#77559=EDGE_LOOP ( 'NONE', ( #249473, #42818, #200377, #183988 ) ) ;
#77571=ORIENTED_EDGE ( 'NONE', *, *, #119420, .T. ) ;
#77638=EDGE_CURVE ( 'NONE', #159944, #41810, #54343, .T. ) ;
#77654=ADVANCED_FACE ( 'NONE', ( #33559 ), #13959, .F. ) ;
#77690=ORIENTED_EDGE ( 'NONE', *, *, #203192, .F. ) ;
#77714=ORIENTED_EDGE ( 'NONE', *, *, #252726, .T. ) ;
#77719=VERTEX_POINT ( 'NONE', #38647 ) ;
#77732=CARTESIAN_POINT ( 'NONE',  ( -20.94999999999999929, 1.115649653272650466E-11, -204.9999999999999716 ) ) ;
#77805=ADVANCED_FACE ( 'NONE', ( #171349 ), #95606, .T. ) ;
#77818=ORIENTED_EDGE ( 'NONE', *, *, #112714, .F. ) ;
#77825=ORIENTED_EDGE ( 'NONE', *, *, #134465, .T. ) ;
#77839=CARTESIAN_POINT ( 'NONE',  ( -20.64999999999999858, -8.999999999988846255, -177.3939691226524076 ) ) ;
#77849=FACE_OUTER_BOUND ( 'NONE', #35838, .T. ) ;
#77872=EDGE_CURVE ( 'NONE', #154991, #67305, #213400, .T. ) ;
#77909=CARTESIAN_POINT ( 'NONE',  ( 18.57399277249656322, 10.33112638556969820, -206.5901228926974227 ) ) ;
#77912=TOROIDAL_SURFACE ( 'NONE', #186276, 0.4000000000000010214, 0.1000000000000000056 ) ;
#77946=ORIENTED_EDGE ( 'NONE', *, *, #202893, .F. ) ;
#77947=VERTEX_POINT ( 'NONE', #158199 ) ;
#77981=ORIENTED_EDGE ( 'NONE', *, *, #250232, .T. ) ;
#77986=DIRECTION ( 'NONE',  ( 0.000000000000000000, 0.000000000000000000, 1.000000000000000000 ) ) ;
#77991=AXIS2_PLACEMENT_3D ( 'NONE', #230902, #130483, #67950 ) ;
#77993=DIRECTION ( 'NONE',  ( 1.000000000000000000, -0.000000000000000000, -0.000000000000000000 ) ) ;
#78008=DIRECTION ( 'NONE',  ( 0.000000000000000000, 1.953992523340277404E-14, 1.000000000000000000 ) ) ;
#78009=VERTEX_POINT ( 'NONE', #138556 ) ;
#78022=CARTESIAN_POINT ( 'NONE',  ( 18.59999999999999076, 10.20857864377385127, -188.8499999999999659 ) ) ;
#78024=ORIENTED_EDGE ( 'NONE', *, *, #203262, .F. ) ;
#78038=EDGE_LOOP ( 'NONE', ( #142468, #241221, #95005, #67271 ) ) ;
#78068=DIRECTION ( 'NONE',  ( 1.000000000000000000, 0.000000000000000000, 0.000000000000000000 ) ) ;
#78071=DIRECTION ( 'NONE',  ( 0.000000000000000000, 0.000000000000000000, 1.000000000000000000 ) ) ;
#78081=FACE_OUTER_BOUND ( 'NONE', #253091, .T. ) ;
#78089=CARTESIAN_POINT ( 'NONE',  ( 21.05000000000000071, -11.48912529306489994, -198.0999999999999659 ) ) ;
#78111=CARTESIAN_POINT ( 'NONE',  ( 23.14999999999999858, 5.600000000011153389, -188.5947339810868755 ) ) ;
#78127=FACE_OUTER_BOUND ( 'NONE', #55622, .T. ) ;
#78140=ORIENTED_EDGE ( 'NONE', *, *, #159460, .T. ) ;
#78183=ORIENTED_EDGE ( 'NONE', *, *, #102262, .T. ) ;
#78200=DIRECTION ( 'NONE',  ( -1.000000000000000000, 0.000000000000000000, 0.000000000000000000 ) ) ;
#78206=AXIS2_PLACEMENT_3D ( 'NONE', #249767, #188505, #51526 ) ;
#78272=DIRECTION ( 'NONE',  ( -1.000000000000000000, -0.000000000000000000, -0.000000000000000000 ) ) ;
#78280=CARTESIAN_POINT ( 'NONE',  ( -20.54999999999999716, 4.250000000011156409, -179.7499999999999716 ) ) ;
#78282=ORIENTED_EDGE ( 'NONE', *, *, #213467, .T. ) ;
#78325=ORIENTED_EDGE ( 'NONE', *, *, #209506, .F. ) ;
#78351=EDGE_CURVE ( 'NONE', #223496, #137741, #55338, .T. ) ;
#78405=ORIENTED_EDGE ( 'NONE', *, *, #240963, .T. ) ;
#78469=EDGE_LOOP ( 'NONE', ( #51719, #75510, #173395, #256906 ) ) ;
#78472=ORIENTED_EDGE ( 'NONE', *, *, #149518, .T. ) ;
#78494=ADVANCED_FACE ( 'NONE', ( #151607 ), #251382, .T. ) ;
#78522=EDGE_CURVE ( 'NONE', #152450, #67428, #172325, .T. ) ;
#78526=EDGE_LOOP ( 'NONE', ( #232791, #126836 ) ) ;
#78553=ORIENTED_EDGE ( 'NONE', *, *, #76952, .T. ) ;
#78582=ORIENTED_EDGE ( 'NONE', *, *, #126822, .F. ) ;
#78584=CARTESIAN_POINT ( 'NONE',  ( 21.00000000000000000, 9.750000000011153745, -188.6499999999999488 ) ) ;
#78599=ADVANCED_FACE ( 'NONE', ( #138403 ), #205569, .F. ) ;
#78611=CARTESIAN_POINT ( 'NONE',  ( 20.94999999999999574, 6.350000000011161383, -177.3438220896831012 ) ) ;
#78633=DIRECTION ( 'NONE',  ( -1.000000000000000000, 0.000000000000000000, 0.000000000000000000 ) ) ;
#78667=CARTESIAN_POINT ( 'NONE',  ( -18.50000000000000000, 11.65000000001115232, -167.5999999999999659 ) ) ;
#78669=CARTESIAN_POINT ( 'NONE',  ( 21.14999999999999858, 6.540656951712400691, -167.4999999999999716 ) ) ;
#78670=ORIENTED_EDGE ( 'NONE', *, *, #175416, .F. ) ;
#78736=CARTESIAN_POINT ( 'NONE',  ( -18.50000000000000000, 10.29288807859935950, -206.4580020160121592 ) ) ;
#78739=EDGE_CURVE ( 'NONE', #236886, #238413, #122209, .T. ) ;
#78746=ORIENTED_EDGE ( 'NONE', *, *, #161785, .T. ) ;
#78767=CIRCLE ( 'NONE', #103890, 0.5000000000000004441 ) ;
#78771=( NAMED_UNIT ( * ) PLANE_ANGLE_UNIT ( ) SI_UNIT ( $, .RADIAN. ) );
#78773=AXIS2_PLACEMENT_3D ( 'NONE', #105868, #70657, #48483 ) ;
#78792=ORIENTED_EDGE ( 'NONE', *, *, #31028, .F. ) ;
#78798=EDGE_CURVE ( 'NONE', #253024, #159614, #198176, .T. ) ;
#78821=FACE_OUTER_BOUND ( 'NONE', #254681, .T. ) ;
#78824=CARTESIAN_POINT ( 'NONE',  ( 21.05000000000000071, 10.42338541492404680, -174.9920519238700649 ) ) ;
#78850=ADVANCED_FACE ( 'NONE', ( #113432 ), #14362, .T. ) ;
#78858=LINE ( 'NONE', #256166, #48616 ) ;
#78878=EDGE_LOOP ( 'NONE', ( #238639, #250538, #226544, #75147 ) ) ;
#78888=EDGE_CURVE ( 'NONE', #196430, #245420, #240765, .T. ) ;
#78898=ORIENTED_EDGE ( 'NONE', *, *, #115659, .T. ) ;
#78899=DIRECTION ( 'NONE',  ( 0.7071067811865475727, 0.7071067811865475727, -0.000000000000000000 ) ) ;
#78927=DIRECTION ( 'NONE',  ( -0.000000000000000000, 1.265107689135680095E-16, -1.000000000000000000 ) ) ;
#78932=EDGE_CURVE ( 'NONE', #209575, #8977, #235762, .T. ) ;
#78939=VECTOR ( 'NONE', #39777, 1000.000000000000000 ) ;
#78954=DIRECTION ( 'NONE',  ( -2.840903330521631775E-16, 0.8700118002898321601, -0.4930308989875230030 ) ) ;
#78955=EDGE_CURVE ( 'NONE', #12339, #6622, #248254, .T. ) ;
#78960=ORIENTED_EDGE ( 'NONE', *, *, #202258, .T. ) ;
#79002=CIRCLE ( 'NONE', #120760, 0.09999999999999939493 ) ;
#79003=DIRECTION ( 'NONE',  ( -3.265361837132813093E-16, 1.000000000000000000, 0.000000000000000000 ) ) ;
#79013=ORIENTED_EDGE ( 'NONE', *, *, #182, .T. ) ;
#79028=ORIENTED_EDGE ( 'NONE', *, *, #200889, .T. ) ;
#79053=CIRCLE ( 'NONE', #112243, 0.1000000000000013933 ) ;
#79139=DIRECTION ( 'NONE',  ( -0.000000000000000000, -1.000000000000000000, -0.000000000000000000 ) ) ;
#79142=ORIENTED_EDGE ( 'NONE', *, *, #24410, .T. ) ;
#79151=TOROIDAL_SURFACE ( 'NONE', #170989, 0.6000000000000009770, 0.1000000000000000056 ) ;
#79173=CARTESIAN_POINT ( 'NONE',  ( 20.94999999999999574, -1.162701749926853712, -175.5999999999999659 ) ) ;
#79204=CARTESIAN_POINT ( 'NONE',  ( -23.15000000000000213, -11.64999999998884483, -197.8999999999999773 ) ) ;
#79205=DIRECTION ( 'NONE',  ( 0.000000000000000000, 0.000000000000000000, 1.000000000000000000 ) ) ;
#79230=CARTESIAN_POINT ( 'NONE',  ( 20.52683494730037239, 8.980530818312608687, -176.0052527225371648 ) ) ;
#79258=CARTESIAN_POINT ( 'NONE',  ( -20.64999999999999858, 4.350000000011156054, -179.8499999999999943 ) ) ;
#79283=CARTESIAN_POINT ( 'NONE',  ( 20.84999999999999432, 7.021664781911246322, -204.8335654018972605 ) ) ;
#79300=DIRECTION ( 'NONE',  ( 1.000000000000000000, 0.000000000000000000, 0.000000000000000000 ) ) ;
#79311=CARTESIAN_POINT ( 'NONE',  ( 21.05000000000000071, 1.115600667400684642E-11, -167.4999999999999716 ) ) ;
#79320=CARTESIAN_POINT ( 'NONE',  ( -21.08078803292166725, 0.07918598716886542099, -161.1669870355628120 ) ) ;
#79357=CARTESIAN_POINT ( 'NONE',  ( -21.14999999999999858, 11.65000000001115588, -167.5999999999999659 ) ) ;
#79363=CARTESIAN_POINT ( 'NONE',  ( 20.94999999999999929, -1.135018845899022466, -208.7169768834322952 ) ) ;
#79370=CARTESIAN_POINT ( 'NONE',  ( 20.94999999999999929, 5.400000000011154988, -191.1060308773475072 ) ) ;
#79387=DIRECTION ( 'NONE',  ( 0.000000000000000000, -2.220446049250311819E-14, -1.000000000000000000 ) ) ;
#79473=CARTESIAN_POINT ( 'NONE',  ( -18.50000000000000000, 9.350000000011156942, -188.6499999999999488 ) ) ;
#79499=ORIENTED_EDGE ( 'NONE', *, *, #40110, .T. ) ;
#79527=B_SPLINE_CURVE_WITH_KNOTS ( 'NONE', 3,
 ( #253845, #45716, #125261, #204775, #66576, #59469, #19093, #139005 ),
 .UNSPECIFIED., .F., .F.,
 ( 4, 2, 2, 4 ),
 ( 0.000000000000000000, 6.534141206311429892E-05, 0.0001306828241262285978, 0.0002613656482524603399 ),
 .UNSPECIFIED. ) ;
#79528=SPHERICAL_SURFACE ( 'NONE', #41510, 0.1000000000000000056 ) ;
#79538=ORIENTED_EDGE ( 'NONE', *, *, #220741, .F. ) ;
#79541=CARTESIAN_POINT ( 'NONE',  ( 23.15000000000000213, -11.64999999998884483, -167.4999999999999432 ) ) ;
#79573=CYLINDRICAL_SURFACE ( 'NONE', #154107, 0.09999999999999939493 ) ;
#79576=DIRECTION ( 'NONE',  ( -0.000000000000000000, -0.000000000000000000, 1.000000000000000000 ) ) ;
#79596=EDGE_CURVE ( 'NONE', #249596, #130308, #235014, .T. ) ;
#79609=DIRECTION ( 'NONE',  ( -1.000000000000000000, 7.304098846218135653E-16, 0.000000000000000000 ) ) ;
#79619=AXIS2_PLACEMENT_3D ( 'NONE', #252983, #172222, #116063 ) ;
#79639=EDGE_CURVE ( 'NONE', #130077, #77719, #90382, .T. ) ;
#79668=CARTESIAN_POINT ( 'NONE',  ( 23.25000000000000000, -9.599999999988842347, -191.1060308773475072 ) ) ;
#79676=ADVANCED_FACE ( 'NONE', ( #138442 ), #121506, .T. ) ;
#79726=VERTEX_POINT ( 'NONE', #58902 ) ;
#79728=DIRECTION ( 'NONE',  ( 0.000000000000000000, 0.000000000000000000, -1.000000000000000000 ) ) ;
#79737=DIRECTION ( 'NONE',  ( 1.000000000000000000, 0.000000000000000000, 0.000000000000000000 ) ) ;
#79740=ORIENTED_EDGE ( 'NONE', *, *, #39156, .F. ) ;
#79741=EDGE_LOOP ( 'NONE', ( #192516, #131953, #41367 ) ) ;
#79791=ADVANCED_FACE ( 'NONE', ( #228295 ), #26246, .F. ) ;
#79793=CARTESIAN_POINT ( 'NONE',  ( 23.14999999999999858, 11.60000000001116227, -194.0717967697244717 ) ) ;
#79796=DIRECTION ( 'NONE',  ( -1.000000000000000000, -0.000000000000000000, -0.000000000000000000 ) ) ;
#79814=PLANE ( 'NONE',  #188774 ) ;
#79824=CARTESIAN_POINT ( 'NONE',  ( -21.40925344232282512, 6.658518859401606704, -167.4010498113803180 ) ) ;
#79850=DIRECTION ( 'NONE',  ( 0.000000000000000000, -0.000000000000000000, 1.000000000000000000 ) ) ;
#79859=CIRCLE ( 'NONE', #225599, 0.09999999999999939493 ) ;
#79963=CIRCLE ( 'NONE', #229841, 0.09999999999999939493 ) ;
#80003=CIRCLE ( 'NONE', #225770, 11.75000000000001066 ) ;
#80036=FILL_AREA_STYLE ('',( #523 ) ) ;
#80047=AXIS2_PLACEMENT_3D ( 'NONE', #122409, #7588, #3733 ) ;
#80088=CARTESIAN_POINT ( 'NONE',  ( 20.95512820512820085, 10.62384868372303615, -175.1649135690875880 ) ) ;
#80100=AXIS2_PLACEMENT_3D ( 'NONE', #208315, #252540, #153510 ) ;
#80112=CARTESIAN_POINT ( 'NONE',  ( 20.95556889135987788, 10.62194358774625513, -175.1423942218574723 ) ) ;
#80138=AXIS2_PLACEMENT_3D ( 'NONE', #220589, #2799, #41966 ) ;
#80203=ORIENTED_EDGE ( 'NONE', *, *, #104002, .T. ) ;
#80230=CARTESIAN_POINT ( 'NONE',  ( 20.94999999999999929, 5.850000000011160495, -190.8675027757220448 ) ) ;
#80246=EDGE_CURVE ( 'NONE', #66550, #153829, #3072, .T. ) ;
#80269=EDGE_CURVE ( 'NONE', #207515, #36105, #215644, .T. ) ;
#80309=DIRECTION ( 'NONE',  ( 0.000000000000000000, 0.000000000000000000, -1.000000000000000000 ) ) ;
#80348=ORIENTED_EDGE ( 'NONE', *, *, #163597, .T. ) ;
#80370=EDGE_LOOP ( 'NONE', ( #59795, #53583, #53706, #144296 ) ) ;
#80383=CARTESIAN_POINT ( 'NONE',  ( -1.820710678118658388, -9.929289321870186313, -192.1499999999999488 ) ) ;
#80390=DIRECTION ( 'NONE',  ( 0.000000000000000000, -1.000000000000000000, 0.000000000000000000 ) ) ;
#80400=SPHERICAL_SURFACE ( 'NONE', #175459, 0.1000000000000000056 ) ;
#80427=DIRECTION ( 'NONE',  ( 0.000000000000000000, 1.000000000000000000, 1.734723475976807292E-15 ) ) ;
#80438=DIRECTION ( 'NONE',  ( 1.000000000000000000, -0.000000000000000000, 0.000000000000000000 ) ) ;
#80439=CIRCLE ( 'NONE', #188623, 0.09999999999998898659 ) ;
#80454=DIRECTION ( 'NONE',  ( -1.000000000000000000, -2.952720810173289112E-16, 0.000000000000000000 ) ) ;
#80475=CARTESIAN_POINT ( 'NONE',  ( -21.05000000000000071, -11.64999999998884483, -170.4999999999999716 ) ) ;
#80477=VECTOR ( 'NONE', #105431, 1000.000000000000000 ) ;
#80480=CARTESIAN_POINT ( 'NONE',  ( -20.54999999999999716, 9.350000000011156942, -179.7499999999999716 ) ) ;
#80499=DIRECTION ( 'NONE',  ( 0.000000000000000000, 0.000000000000000000, -1.000000000000000000 ) ) ;
#80509=VERTEX_POINT ( 'NONE', #127285 ) ;
#80517=CIRCLE ( 'NONE', #26404, 11.69999999999998863 ) ;
#80530=DIRECTION ( 'NONE',  ( 1.000000000000000000, 0.000000000000000000, 0.000000000000000000 ) ) ;
#80543=CARTESIAN_POINT ( 'NONE',  ( -22.14074124539699540, 0.09905289585522827900, -160.1099221489562012 ) ) ;
#80589=CYLINDRICAL_SURFACE ( 'NONE', #59679, 7.899999999999990585 ) ;
#80592=CARTESIAN_POINT ( 'NONE',  ( 20.94999999999999929, 5.400000000011154988, -188.5947339810868755 ) ) ;
#80596=CARTESIAN_POINT ( 'NONE',  ( -21.07971444708686093, 0.08782343632898226282, -161.1702079183734213 ) ) ;
#80607=ORIENTED_EDGE ( 'NONE', *, *, #107506, .T. ) ;
#80623=ORIENTED_EDGE ( 'NONE', *, *, #249823, .T. ) ;
#80625=CARTESIAN_POINT ( 'NONE',  ( -20.94999999999999929, 1.115600667400684642E-11, -167.4999999999999716 ) ) ;
#80649=AXIS2_PLACEMENT_3D ( 'NONE', #49994, #70877, #150399 ) ;
#80689=CARTESIAN_POINT ( 'NONE',  ( -21.05000000000000071, 6.258842723548988296, -167.4679863068125769 ) ) ;
#80699=AXIS2_PLACEMENT_3D ( 'NONE', #5072, #84594, #243720 ) ;
#80706=DIRECTION ( 'NONE',  ( 0.000000000000000000, 0.000000000000000000, -1.000000000000000000 ) ) ;
#80735=DIRECTION ( 'NONE',  ( 0.000000000000000000, 0.000000000000000000, -1.000000000000000000 ) ) ;
#80769=DIRECTION ( 'NONE',  ( 0.000000000000000000, 0.000000000000000000, 1.000000000000000000 ) ) ;
#80776=EDGE_LOOP ( 'NONE', ( #218010, #169869, #57479 ) ) ;
#80786=ORIENTED_EDGE ( 'NONE', *, *, #39770, .T. ) ;
#80791=CIRCLE ( 'NONE', #218346, 0.09999999999998898659 ) ;
#80824=CARTESIAN_POINT ( 'NONE',  ( 18.49999999999999645, -1.299733671219632791, -157.5281295228693637 ) ) ;
#80825=CARTESIAN_POINT ( 'NONE',  ( -18.59999999999999787, -1.835859311432481045, -212.5044391687984842 ) ) ;
#80838=ORIENTED_EDGE ( 'NONE', *, *, #193323, .T. ) ;
#80847=DIRECTION ( 'NONE',  ( 0.000000000000000000, 0.4999999999999956701, -0.8660254037844411501 ) ) ;
#80866=VERTEX_POINT ( 'NONE', #60256 ) ;
#80884=ORIENTED_EDGE ( 'NONE', *, *, #189302, .T. ) ;
#80896=DIRECTION ( 'NONE',  ( 0.000000000000000000, 0.000000000000000000, 1.000000000000000000 ) ) ;
#80912=ORIENTED_EDGE ( 'NONE', *, *, #175922, .F. ) ;
#80921=ADVANCED_FACE ( 'NONE', ( #126658 ), #32727, .T. ) ;
#80935=FACE_OUTER_BOUND ( 'NONE', #219038, .T. ) ;
#80971=ORIENTED_EDGE ( 'NONE', *, *, #19807, .T. ) ;
#80988=ORIENTED_EDGE ( 'NONE', *, *, #63785, .T. ) ;
#80998=AXIS2_PLACEMENT_3D ( 'NONE', #118909, #215418, #77187 ) ;
#81069=DIRECTION ( 'NONE',  ( 1.000000000000000000, 0.000000000000000000, 0.000000000000000000 ) ) ;
#81074=ADVANCED_FACE ( 'NONE', ( #71842 ), #236025, .T. ) ;
#81076=LINE ( 'NONE', #77229, #115138 ) ;
#81087=DIRECTION ( 'NONE',  ( -1.000000000000000000, 0.000000000000000000, 0.000000000000000000 ) ) ;
#81111=CIRCLE ( 'NONE', #226864, 12.87499999999999822 ) ;
#81113=EDGE_CURVE ( 'NONE', #90327, #105545, #82716, .T. ) ;
#81114=FACE_OUTER_BOUND ( 'NONE', #245372, .T. ) ;
#81116=LINE ( 'NONE', #121585, #138724 ) ;
#81129=DIRECTION ( 'NONE',  ( -0.000000000000000000, -0.000000000000000000, 1.000000000000000000 ) ) ;
#81164=VECTOR ( 'NONE', #26084, 1000.000000000000000 ) ;
#81197=ORIENTED_EDGE ( 'NONE', *, *, #44584, .F. ) ;
#81200=EDGE_CURVE ( 'NONE', #131341, #133509, #220331, .T. ) ;
#81206=DIRECTION ( 'NONE',  ( 0.000000000000000000, -0.1455152366551721865, -0.9893560106964475187 ) ) ;
#81242=EDGE_CURVE ( 'NONE', #156141, #234175, #222875, .T. ) ;
#81259=VERTEX_POINT ( 'NONE', #145901 ) ;
#81364=EDGE_CURVE ( 'NONE', #69117, #207515, #231894, .T. ) ;
#81378=CARTESIAN_POINT ( 'NONE',  ( 21.05000000000000071, 1.115600667400684642E-11, -180.4749999999999659 ) ) ;
#81387=EDGE_CURVE ( 'NONE', #134756, #47818, #36263, .T. ) ;
#81402=ORIENTED_EDGE ( 'NONE', *, *, #29314, .F. ) ;
#81420=ORIENTED_EDGE ( 'NONE', *, *, #97023, .F. ) ;
#81437=EDGE_CURVE ( 'NONE', #152124, #41100, #207869, .T. ) ;
#81440=CIRCLE ( 'NONE', #169000, 12.87499999999999822 ) ;
#81446=ORIENTED_EDGE ( 'NONE', *, *, #240222, .F. ) ;
#81471=ORIENTED_EDGE ( 'NONE', *, *, #211565, .T. ) ;
#81488=CIRCLE ( 'NONE', #127320, 0.09999999999998898659 ) ;
#81510=CIRCLE ( 'NONE', #14930, 4.149999999999987033 ) ;
#81523=VECTOR ( 'NONE', #117530, 1000.000000000000000 ) ;
#81528=CARTESIAN_POINT ( 'NONE',  ( -20.64999999999999858, 1.115600667400684642E-11, -180.4749999999999659 ) ) ;
#81554=DIRECTION ( 'NONE',  ( 1.000000000000000000, 0.000000000000000000, 0.000000000000000000 ) ) ;
#81588=ORIENTED_EDGE ( 'NONE', *, *, #195970, .T. ) ;
#81608=CYLINDRICAL_SURFACE ( 'NONE', #49389, 0.1000000000000098310 ) ;
#81624=ADVANCED_FACE ( 'NONE', ( #25661 ), #127892, .F. ) ;
#81630=CYLINDRICAL_SURFACE ( 'NONE', #256761, 0.09999999999998898659 ) ;
#81661=ADVANCED_FACE ( 'NONE', ( #88160 ), #83022, .T. ) ;
#81670=FACE_OUTER_BOUND ( 'NONE', #88181, .T. ) ;
#81704=ORIENTED_EDGE ( 'NONE', *, *, #1548, .F. ) ;
#81711=LINE ( 'NONE', #158753, #41275 ) ;
#81723=AXIS2_PLACEMENT_3D ( 'NONE', #2022, #41197, #118140 ) ;
#81746=AXIS2_PLACEMENT_3D ( 'NONE', #107832, #247335, #67421 ) ;
#81826=CARTESIAN_POINT ( 'NONE',  ( 21.05000000000000071, -1.736257131586239844, -179.0686523290174819 ) ) ;
#81841=FACE_OUTER_BOUND ( 'NONE', #131277, .T. ) ;
#81870=CARTESIAN_POINT ( 'NONE',  ( -21.07928932188134041, 0.09889514566555068775, -161.1714833436066669 ) ) ;
#81899=VECTOR ( 'NONE', #129480, 1000.000000000000114 ) ;
#81956=ORIENTED_EDGE ( 'NONE', *, *, #59661, .T. ) ;
#81957=FACE_OUTER_BOUND ( 'NONE', #184185, .T. ) ;
#81981=DIRECTION ( 'NONE',  ( 1.000000000000000000, 0.000000000000000000, 0.000000000000000000 ) ) ;
#81986=FACE_OUTER_BOUND ( 'NONE', #229020, .T. ) ;
#82010=CIRCLE ( 'NONE', #215315, 0.09999999999998898659 ) ;
#82024=ORIENTED_EDGE ( 'NONE', *, *, #103176, .F. ) ;
#82029=ADVANCED_FACE ( 'NONE', ( #118012 ), #56717, .F. ) ;
#82062=DIRECTION ( 'NONE',  ( 2.952720810173289112E-16, -1.000000000000000000, 0.000000000000000000 ) ) ;
#82086=FACE_OUTER_BOUND ( 'NONE', #42128, .T. ) ;
#82096=DIRECTION ( 'NONE',  ( -0.000000000000000000, -0.000000000000000000, 1.000000000000000000 ) ) ;
#82103=CARTESIAN_POINT ( 'NONE',  ( -21.05000000000000071, -1.835341550213255957, -179.0551512925629538 ) ) ;
#82148=CARTESIAN_POINT ( 'NONE',  ( -21.14999999999999858, 6.540656951712397138, -167.4999999999999716 ) ) ;
#82164=FACE_OUTER_BOUND ( 'NONE', #28345, .T. ) ;
#82222=VERTEX_POINT ( 'NONE', #93014 ) ;
#82251=EDGE_CURVE ( 'NONE', #41250, #165976, #112530, .T. ) ;
#82255=CIRCLE ( 'NONE', #165511, 0.1999999999999999833 ) ;
#82260=CYLINDRICAL_SURFACE ( 'NONE', #182105, 0.09999999999998898659 ) ;
#82263=AXIS2_PLACEMENT_3D ( 'NONE', #1004, #44022, #201805 ) ;
#82264=CARTESIAN_POINT ( 'NONE',  ( 21.14999999999999858, 11.65000000001115943, -167.5999999999999659 ) ) ;
#82286=DIRECTION ( 'NONE',  ( 0.000000000000000000, 0.000000000000000000, -1.000000000000000000 ) ) ;
#82362=SPHERICAL_SURFACE ( 'NONE', #236612, 0.1000000000000000056 ) ;
#82394=CARTESIAN_POINT ( 'NONE',  ( -23.15000000000000213, 1.115600667400684642E-11, -167.4999999999999716 ) ) ;
#82400=AXIS2_PLACEMENT_3D ( 'NONE', #164654, #104629, #227175 ) ;
#82401=ORIENTED_EDGE ( 'NONE', *, *, #117789, .F. ) ;
#82412=CARTESIAN_POINT ( 'NONE',  ( -20.94999999999999929, -1.851028230129704522, -179.1539132694224463 ) ) ;
#82418=FACE_OUTER_BOUND ( 'NONE', #244571, .T. ) ;
#82445=CARTESIAN_POINT ( 'NONE',  ( -18.50000000000000000, 9.350000000011156942, -179.6499999999999773 ) ) ;
#82457=CIRCLE ( 'NONE', #228254, 0.4000000000000114575 ) ;
#82475=ORIENTED_EDGE ( 'NONE', *, *, #176340, .F. ) ;
#82480=DIRECTION ( 'NONE',  ( 0.000000000000000000, -0.9893560106964500722, 0.1455152366551550613 ) ) ;
#82503=CARTESIAN_POINT ( 'NONE',  ( -23.15000000000000213, 1.115600667400684642E-11, -189.1999999999999602 ) ) ;
#82538=EDGE_LOOP ( 'NONE', ( #149313, #8815, #70782, #121577 ) ) ;
#82550=CIRCLE ( 'NONE', #145112, 12.87499999999999822 ) ;
#82557=ORIENTED_EDGE ( 'NONE', *, *, #193323, .F. ) ;
#82604=AXIS2_PLACEMENT_3D ( 'NONE', #19858, #161941, #47084 ) ;
#82616=LINE ( 'NONE', #223434, #219890 ) ;
#82647=AXIS2_PLACEMENT_3D ( 'NONE', #242538, #46892, #125177 ) ;
#82652=AXIS2_PLACEMENT_3D ( 'NONE', #125081, #104202, #41697 ) ;
#82667=CARTESIAN_POINT ( 'NONE',  ( -20.85000000000000142, -1.835859311432481045, -212.5044391687984842 ) ) ;
#82670=FACE_OUTER_BOUND ( 'NONE', #218097, .T. ) ;
#82695=CARTESIAN_POINT ( 'NONE',  ( 18.50000324121758055, 10.29307482169092403, -206.4586421466939328 ) ) ;
#82699=EDGE_LOOP ( 'NONE', ( #81956, #100870, #49808, #198805 ) ) ;
#82701=VERTEX_POINT ( 'NONE', #138233 ) ;
#82716=CIRCLE ( 'NONE', #174382, 0.09999999999998898659 ) ;
#82717=AXIS2_PLACEMENT_3D ( 'NONE', #25196, #160852, #1740 ) ;
#82745=DIRECTION ( 'NONE',  ( 0.000000000000000000, 0.000000000000000000, -1.000000000000000000 ) ) ;
#82757=CIRCLE ( 'NONE', #49491, 0.09999999999998898659 ) ;
#82793=ADVANCED_FACE ( 'NONE', ( #173591 ), #253060, .F. ) ;
#82821=VERTEX_POINT ( 'NONE', #187335 ) ;
#82851=ORIENTED_EDGE ( 'NONE', *, *, #19743, .F. ) ;
#82856=VERTEX_POINT ( 'NONE', #186035 ) ;
#82862=EDGE_CURVE ( 'NONE', #8158, #20774, #148186, .T. ) ;
#82909=VERTEX_POINT ( 'NONE', #107778 ) ;
#82926=CARTESIAN_POINT ( 'NONE',  ( -23.25000000000000000, 1.115650265596050101E-11, -163.4499999999999886 ) ) ;
#82955=EDGE_CURVE ( 'NONE', #135869, #54023, #37904, .T. ) ;
#82982=ADVANCED_FACE ( 'NONE', ( #251118 ), #33419, .T. ) ;
#83022=SPHERICAL_SURFACE ( 'NONE', #28829, 0.1000000000000000056 ) ;
#83023=CIRCLE ( 'NONE', #66498, 0.09999999999998898659 ) ;
#83033=AXIS2_PLACEMENT_3D ( 'NONE', #126798, #147645, #227173 ) ;
#83060=CARTESIAN_POINT ( 'NONE',  ( 20.97565083910961548, 10.47461740128996510, -175.0779431765885192 ) ) ;
#83071=AXIS2_PLACEMENT_3D ( 'NONE', #192128, #249524, #9605 ) ;
#83088=ADVANCED_FACE ( 'NONE', ( #34684 ), #183631, .T. ) ;
#83102=CARTESIAN_POINT ( 'NONE',  ( -20.64999999999999858, 7.150000000011155876, -188.6499999999999488 ) ) ;
#83146=ORIENTED_EDGE ( 'NONE', *, *, #185154, .T. ) ;
#83149=CARTESIAN_POINT ( 'NONE',  ( 20.85000000000000142, 1.115600667400684642E-11, -200.9999999999999432 ) ) ;
#83201=CIRCLE ( 'NONE', #178951, 6.329289321881370611 ) ;
#83210=ADVANCED_FACE ( 'NONE', ( #25394 ), #146577, .T. ) ;
#83250=VERTEX_POINT ( 'NONE', #104864 ) ;
#83252=ORIENTED_EDGE ( 'NONE', *, *, #146864, .F. ) ;
#83302=CARTESIAN_POINT ( 'NONE',  ( 22.48970261584622321, 11.65000000001115588, -167.4446305117825773 ) ) ;
#83319=LINE ( 'NONE', #5065, #189009 ) ;
#83326=ADVANCED_FACE ( 'NONE', ( #149198 ), #10957, .F. ) ;
#83345=DIRECTION ( 'NONE',  ( 0.000000000000000000, 0.000000000000000000, -1.000000000000000000 ) ) ;
#83372=DIRECTION ( 'NONE',  ( 0.000000000000000000, -0.4999999999999673039, -0.8660254037844573594 ) ) ;
#83374=ORIENTED_EDGE ( 'NONE', *, *, #238012, .F. ) ;
#83403=DIRECTION ( 'NONE',  ( 0.000000000000000000, 0.8660254037844411501, 0.4999999999999956701 ) ) ;
#83415=CIRCLE ( 'NONE', #241838, 0.1000000000000033223 ) ;
#83439=CYLINDRICAL_SURFACE ( 'NONE', #82647, 11.80000000000000426 ) ;
#83448=EDGE_CURVE ( 'NONE', #75238, #71995, #229040, .T. ) ;
#83466=ORIENTED_EDGE ( 'NONE', *, *, #95193, .T. ) ;
#83474=CARTESIAN_POINT ( 'NONE',  ( -18.50000000000000000, 9.350000000011156942, -179.8499999999999943 ) ) ;
#83476=ORIENTED_EDGE ( 'NONE', *, *, #18720, .F. ) ;
#83481=DIRECTION ( 'NONE',  ( -1.000000000000000000, -2.952720810173289112E-16, 0.000000000000000000 ) ) ;
#83547=ORIENTED_EDGE ( 'NONE', *, *, #53225, .T. ) ;
#83565=CARTESIAN_POINT ( 'NONE',  ( 23.14999999999999858, 5.900000000011162093, -190.7809002353436085 ) ) ;
#83579=CARTESIAN_POINT ( 'NONE',  ( 23.14999999999999858, 1.115600667400684642E-11, -200.9999999999999432 ) ) ;
#83581=CIRCLE ( 'NONE', #229373, 11.64999999999999325 ) ;
#83586=AXIS2_PLACEMENT_3D ( 'NONE', #14619, #32921, #92836 ) ;
#83609=AXIS2_PLACEMENT_3D ( 'NONE', #88575, #148576, #38904 ) ;
#83617=DIRECTION ( 'NONE',  ( -0.000000000000000000, -0.4791956752371546724, -0.8777080977375153470 ) ) ;
#83641=ORIENTED_EDGE ( 'NONE', *, *, #199590, .T. ) ;
#83655=VERTEX_POINT ( 'NONE', #82445 ) ;
#83656=CARTESIAN_POINT ( 'NONE',  ( -20.94999999999999929, 1.115600667400684642E-11, -200.9999999999999432 ) ) ;
#83677=ORIENTED_EDGE ( 'NONE', *, *, #162200, .F. ) ;
#83750=ORIENTED_EDGE ( 'NONE', *, *, #256461, .T. ) ;
#83772=ORIENTED_EDGE ( 'NONE', *, *, #37540, .T. ) ;
#83785=AXIS2_PLACEMENT_3D ( 'NONE', #36997, #201175, #236446 ) ;
#83818=VECTOR ( 'NONE', #230571, 1000.000000000000000 ) ;
#83855=ORIENTED_EDGE ( 'NONE', *, *, #201434, .T. ) ;
#83861=CARTESIAN_POINT ( 'NONE',  ( -23.25000000000000000, -9.599999999988847676, -177.3939691226524076 ) ) ;
#83889=DIRECTION ( 'NONE',  ( -1.000000000000000000, 0.000000000000000000, 0.000000000000000000 ) ) ;
#83908=ORIENTED_EDGE ( 'NONE', *, *, #92891, .T. ) ;
#83927=CARTESIAN_POINT ( 'NONE',  ( -20.54999999999999716, -8.663551401858001100, -191.4758988819326646 ) ) ;
#83944=CARTESIAN_POINT ( 'NONE',  ( 22.59999999999999432, 11.74987124438766273, -167.4345704089863034 ) ) ;
#83956=CARTESIAN_POINT ( 'NONE',  ( 18.49999999999999645, -1.866714910046153308, -179.2526752462819672 ) ) ;
#83961=CARTESIAN_POINT ( 'NONE',  ( 18.59999999999999787, -1.835859311432481045, -212.5044391687984842 ) ) ;
#83964=CARTESIAN_POINT ( 'NONE',  ( 20.94999999999999929, -9.499999999988844479, -191.1060308773475072 ) ) ;
#84032=CIRCLE ( 'NONE', #250673, 7.899999999999990585 ) ;
#84060=CIRCLE ( 'NONE', #883, 0.09999999999999939493 ) ;
#84068=LINE ( 'NONE', #244472, #216076 ) ;
#84071=ORIENTED_EDGE ( 'NONE', *, *, #117975, .F. ) ;
#84077=ORIENTED_EDGE ( 'NONE', *, *, #227965, .F. ) ;
#84085=ORIENTED_EDGE ( 'NONE', *, *, #84544, .T. ) ;
#84092=ADVANCED_FACE ( 'NONE', ( #228119 ), #33800, .T. ) ;
#84093=DIRECTION ( 'NONE',  ( 0.000000000000000000, 0.1350103645451876666, -0.9908441862701600211 ) ) ;
#84095=DIRECTION ( 'NONE',  ( 1.000000000000000000, -0.000000000000000000, -0.000000000000000000 ) ) ;
#84116=CARTESIAN_POINT ( 'NONE',  ( 21.05000000000000071, 5.000000000011153745, -188.5947339810868755 ) ) ;
#84119=TOROIDAL_SURFACE ( 'NONE', #146524, 0.2000000000000000111, 0.1000000000000000056 ) ;
#84126=ADVANCED_FACE ( 'NONE', ( #12939 ), #200180, .F. ) ;
#84140=EDGE_CURVE ( 'NONE', #54663, #75721, #245969, .T. ) ;
#84153=AXIS2_PLACEMENT_3D ( 'NONE', #16039, #155557, #235068 ) ;
#84171=EDGE_LOOP ( 'NONE', ( #182192, #57684, #201702 ) ) ;
#84221=AXIS2_PLACEMENT_3D ( 'NONE', #153859, #71717, #251621 ) ;
#84223=ORIENTED_EDGE ( 'NONE', *, *, #7245, .F. ) ;
#84225=AXIS2_PLACEMENT_3D ( 'NONE', #8616, #32054, #208116 ) ;
#84227=ORIENTED_EDGE ( 'NONE', *, *, #104881, .T. ) ;
#84255=DIRECTION ( 'NONE',  ( 2.952720810173289112E-16, -1.000000000000000000, -0.000000000000000000 ) ) ;
#84282=ORIENTED_EDGE ( 'NONE', *, *, #41744, .T. ) ;
#84311=AXIS2_PLACEMENT_3D ( 'NONE', #84116, #65898, #48898 ) ;
#84314=CIRCLE ( 'NONE', #76010, 7.899999999999990585 ) ;
#84340=ORIENTED_EDGE ( 'NONE', *, *, #89081, .T. ) ;
#84382=AXIS2_PLACEMENT_3D ( 'NONE', #216308, #117225, #13013 ) ;
#84433=EDGE_CURVE ( 'NONE', #185664, #43467, #251, .T. ) ;
#84437=ORIENTED_EDGE ( 'NONE', *, *, #245045, .F. ) ;
#84442=DIRECTION ( 'NONE',  ( 0.000000000000000000, -0.1455152366551721865, -0.9893560106964475187 ) ) ;
#84468=SPHERICAL_SURFACE ( 'NONE', #220180, 0.1000000000000000056 ) ;
#84513=CARTESIAN_POINT ( 'NONE',  ( -22.50000000000000000, 1.115600667400684642E-11, -155.8504291924551808 ) ) ;
#84541=CIRCLE ( 'NONE', #5454, 0.09999999999999939493 ) ;
#84544=EDGE_CURVE ( 'NONE', #112231, #90455, #106535, .T. ) ;
#84551=DIRECTION ( 'NONE',  ( 0.000000000000000000, 0.000000000000000000, 1.000000000000000000 ) ) ;
#84588=LINE ( 'NONE', #145883, #171535 ) ;
#84594=DIRECTION ( 'NONE',  ( 1.836970198721029934E-16, -1.000000000000000000, -0.000000000000000000 ) ) ;
#84614=FACE_OUTER_BOUND ( 'NONE', #31521, .T. ) ;
#84620=VERTEX_POINT ( 'NONE', #11312 ) ;
#84670=EDGE_CURVE ( 'NONE', #255780, #6055, #146184, .T. ) ;
#84682=ADVANCED_FACE ( 'NONE', ( #120398 ), #154596, .F. ) ;
#84699=TOROIDAL_SURFACE ( 'NONE', #76328, 7.791421356237335338, 0.1000000000000000056 ) ;
#84748=VECTOR ( 'NONE', #140812, 1000.000000000000000 ) ;
#84770=ORIENTED_EDGE ( 'NONE', *, *, #150787, .F. ) ;
#84771=AXIS2_PLACEMENT_3D ( 'NONE', #189398, #171166, #150284 ) ;
#84776=ORIENTED_EDGE ( 'NONE', *, *, #86466, .T. ) ;
#84848=CARTESIAN_POINT ( 'NONE',  ( -22.50000000000000000, 0.1000000000111554016, -159.7092204016265384 ) ) ;
#84883=CARTESIAN_POINT ( 'NONE',  ( -21.55000000000000071, 7.250000000011155521, -179.8499999999999943 ) ) ;
#84934=ORIENTED_EDGE ( 'NONE', *, *, #189210, .F. ) ;
#84960=AXIS2_PLACEMENT_3D ( 'NONE', #29725, #130058, #70132 ) ;
#85032=ORIENTED_EDGE ( 'NONE', *, *, #11828, .F. ) ;
#85034=EDGE_CURVE ( 'NONE', #34375, #196293, #84588, .T. ) ;
#85056=AXIS2_PLACEMENT_3D ( 'NONE', #3902, #80847, #83403 ) ;
#85064=CIRCLE ( 'NONE', #89188, 4.049999999999998046 ) ;
#85068=DIRECTION ( 'NONE',  ( 1.000000000000000000, 0.000000000000000000, 0.000000000000000000 ) ) ;
#85098=ORIENTED_EDGE ( 'NONE', *, *, #218868, .T. ) ;
#85110=CIRCLE ( 'NONE', #35123, 0.09999999999999363565 ) ;
#85118=CARTESIAN_POINT ( 'NONE',  ( 20.94999999999999929, -11.29603075032412640, -197.9521008403361009 ) ) ;
#85156=CARTESIAN_POINT ( 'NONE',  ( -23.15000000000000213, -11.64999999998884483, -155.7499999999999716 ) ) ;
#85163=AXIS2_PLACEMENT_3D ( 'NONE', #138507, #14774, #159401 ) ;
#85171=ADVANCED_FACE ( 'NONE', ( #131468 ), #252681, .T. ) ;
#85172=( NAMED_UNIT ( * ) PLANE_ANGLE_UNIT ( ) SI_UNIT ( $, .RADIAN. ) );
#85184=CARTESIAN_POINT ( 'NONE',  ( 21.05000000000000071, 10.72371710471867701, -175.1649135690875880 ) ) ;
#85197=VERTEX_POINT ( 'NONE', #151041 ) ;
#85235=DIRECTION ( 'NONE',  ( 0.000000000000000000, 1.265107689135680095E-16, -1.000000000000000000 ) ) ;
#85239=ORIENTED_EDGE ( 'NONE', *, *, #82251, .T. ) ;
#85254=FILL_AREA_STYLE_COLOUR ( '', #99763 ) ;
#85302=FACE_OUTER_BOUND ( 'NONE', #210605, .T. ) ;
#85335=CARTESIAN_POINT ( 'NONE',  ( -18.59999999999999787, -1.835859311432481045, -212.5044391687984842 ) ) ;
#85348=ORIENTED_EDGE ( 'NONE', *, *, #231016, .T. ) ;
#85352=CARTESIAN_POINT ( 'NONE',  ( -21.55000000000000426, 7.708578643773852157, -188.6499999999999488 ) ) ;
#85357=CARTESIAN_POINT ( 'NONE',  ( 18.59999999999999076, 7.120270961708750512, -204.6595630418393057 ) ) ;
#85372=VERTEX_POINT ( 'NONE', #104018 ) ;
#85375=LINE ( 'NONE', #204067, #211863 ) ;
#85405=EDGE_CURVE ( 'NONE', #68443, #246745, #134067, .T. ) ;
#85418=CARTESIAN_POINT ( 'NONE',  ( -23.15000000000000213, 2.500000000011156409, -180.7246219227620543 ) ) ;
#85452=VERTEX_POINT ( 'NONE', #87024 ) ;
#85460=CARTESIAN_POINT ( 'NONE',  ( -18.59999999999999787, 11.65000000001115232, -155.7499999999999716 ) ) ;
#85475=VERTEX_POINT ( 'NONE', #49206 ) ;
#85485=DIRECTION ( 'NONE',  ( 1.000000000000000000, -0.000000000000000000, -0.000000000000000000 ) ) ;
#85487=CARTESIAN_POINT ( 'NONE',  ( -21.05000000000000071, 5.850000000011108092, -177.6324972242779268 ) ) ;
#85532=CARTESIAN_POINT ( 'NONE',  ( 21.05000000000000071, 6.650000000011155876, -177.3438220896830728 ) ) ;
#85540=LINE ( 'NONE', #28212, #117851 ) ;
#85554=DIRECTION ( 'NONE',  ( -0.000000000000000000, -0.000000000000000000, -1.000000000000000000 ) ) ;
#85556=CARTESIAN_POINT ( 'NONE',  ( -21.05000000000000071, -1.851028230129704522, -179.1539132694224463 ) ) ;
#85559=CIRCLE ( 'NONE', #152275, 0.09999999999998898659 ) ;
#85619=DIRECTION ( 'NONE',  ( 0.000000000000000000, -0.000000000000000000, 1.000000000000000000 ) ) ;
#85630=AXIS2_PLACEMENT_3D ( 'NONE', #2833, #122819, #23736 ) ;
#85663=CARTESIAN_POINT ( 'NONE',  ( 21.30000000000002558, 1.115650265596050101E-11, -163.4499999999999886 ) ) ;
#85679=AXIS2_PLACEMENT_3D ( 'NONE', #102496, #238175, #59518 ) ;
#85716=FACE_OUTER_BOUND ( 'NONE', #39627, .T. ) ;
#85728=ORIENTED_EDGE ( 'NONE', *, *, #30030, .F. ) ;
#85751=VERTEX_POINT ( 'NONE', #85418 ) ;
#85798=CARTESIAN_POINT ( 'NONE',  ( 23.14999999999999858, 6.650000000011155876, -179.8499999999999943 ) ) ;
#85821=CIRCLE ( 'NONE', #6750, 12.87500000000000000 ) ;
#85836=DIRECTION ( 'NONE',  ( 0.000000000000000000, -1.000000000000000000, 0.000000000000000000 ) ) ;
#85849=ADVANCED_FACE ( 'NONE', ( #204112 ), #200902, .F. ) ;
#85856=FACE_OUTER_BOUND ( 'NONE', #82538, .T. ) ;
#85858=CIRCLE ( 'NONE', #48467, 0.09999999999998898659 ) ;
#85865=VECTOR ( 'NONE', #235824, 1000.000000000000000 ) ;
#85871=CYLINDRICAL_SURFACE ( 'NONE', #217335, 0.09999999999999939493 ) ;
#85885=CIRCLE ( 'NONE', #40162, 12.97499999999998721 ) ;
#85889=CYLINDRICAL_SURFACE ( 'NONE', #124149, 0.09999999999999939493 ) ;
#85892=ADVANCED_FACE ( 'NONE', ( #125855 ), #148007, .T. ) ;
#85898=CARTESIAN_POINT ( 'NONE',  ( 22.40736611211992368, 1.115600667400684642E-11, -155.8504291924551808 ) ) ;
#85907=CARTESIAN_POINT ( 'NONE',  ( 20.94999999999999574, 1.162701749949165642, -175.4999999999999716 ) ) ;
#85912=CARTESIAN_POINT ( 'NONE',  ( -20.94999999999999929, 1.835341550235569663, -179.0551512925629538 ) ) ;
#85917=VECTOR ( 'NONE', #97054, 1000.000000000000000 ) ;
#85971=FACE_OUTER_BOUND ( 'NONE', #217343, .T. ) ;
#85975=ORIENTED_EDGE ( 'NONE', *, *, #229152, .F. ) ;
#85990=VECTOR ( 'NONE', #257540, 1000.000000000000000 ) ;
#85997=AXIS2_PLACEMENT_3D ( 'NONE', #244729, #66109, #145631 ) ;
#86015=CARTESIAN_POINT ( 'NONE',  ( 23.14999999999998437, 1.115600667400684642E-11, -167.4999999999999716 ) ) ;
#86023=FACE_OUTER_BOUND ( 'NONE', #29776, .T. ) ;
#86032=ORIENTED_EDGE ( 'NONE', *, *, #95944, .T. ) ;
#86041=ORIENTED_EDGE ( 'NONE', *, *, #199622, .F. ) ;
#86049=CARTESIAN_POINT ( 'NONE',  ( 20.94999999999999929, -8.663551401857999323, -191.4758988819326646 ) ) ;
#86050=VERTEX_POINT ( 'NONE', #121737 ) ;
#86058=VERTEX_POINT ( 'NONE', #254756 ) ;
#86070=CARTESIAN_POINT ( 'NONE',  ( 23.14999999999999858, 4.813084112160684214, -189.0584822434761634 ) ) ;
#86095=CARTESIAN_POINT ( 'NONE',  ( -21.05000000000000071, -1.360870587180885716, -175.5729979270909382 ) ) ;
#86132=VERTEX_POINT ( 'NONE', #71713 ) ;
#86134=DIRECTION ( 'NONE',  ( -0.000000000000000000, 0.000000000000000000, -1.000000000000000000 ) ) ;
#86211=DIRECTION ( 'NONE',  ( 1.000000000000000000, 0.000000000000000000, -0.000000000000000000 ) ) ;
#86215=DIRECTION ( 'NONE',  ( 0.000000000000000000, 1.000000000000000000, 0.000000000000000000 ) ) ;
#86232=CIRCLE ( 'NONE', #148629, 0.09999999999999817368 ) ;
#86234=ORIENTED_EDGE ( 'NONE', *, *, #189237, .F. ) ;
#86243=VERTEX_POINT ( 'NONE', #85118 ) ;
#86259=EDGE_LOOP ( 'NONE', ( #219171, #230186, #228156, #214305 ) ) ;
#86264=FACE_OUTER_BOUND ( 'NONE', #234045, .T. ) ;
#86272=CARTESIAN_POINT ( 'NONE',  ( 18.40000000000000213, -9.499999999988844479, -174.4993620971800965 ) ) ;
#86298=CARTESIAN_POINT ( 'NONE',  ( -21.52071067811865746, 7.779289321892505882, -188.7499999999999716 ) ) ;
#86310=CARTESIAN_POINT ( 'NONE',  ( 22.49999999999999645, 11.74956712350054744, -167.3991416309012550 ) ) ;
#86313=DIRECTION ( 'NONE',  ( 0.000000000000000000, 1.000000000000000000, 0.000000000000000000 ) ) ;
#86336=ORIENTED_EDGE ( 'NONE', *, *, #218430, .F. ) ;
#86387=B_SPLINE_CURVE_WITH_KNOTS ( 'NONE', 3,
 ( #246621, #127977, #227059, #167130, #190537, #67993 ),
 .UNSPECIFIED., .F., .F.,
 ( 4, 2, 4 ),
 ( 0.000000000000000000, 0.0001891491689349436448, 0.0003782983378698872895 ),
 .UNSPECIFIED. ) ;
#86401=DIRECTION ( 'NONE',  ( 0.000000000000000000, 0.000000000000000000, -1.000000000000000000 ) ) ;
#86412=DIRECTION ( 'NONE',  ( -1.000000000000000000, 0.000000000000000000, 0.000000000000000000 ) ) ;
#86420=DIRECTION ( 'NONE',  ( 1.000000000000000000, 0.000000000000000000, 0.000000000000000000 ) ) ;
#86421=ORIENTED_EDGE ( 'NONE', *, *, #76329, .F. ) ;
#86425=EDGE_CURVE ( 'NONE', #242287, #183962, #139345, .T. ) ;
#86456=VERTEX_POINT ( 'NONE', #143205 ) ;
#86466=EDGE_CURVE ( 'NONE', #142512, #132861, #39003, .T. ) ;
#86482=ADVANCED_FACE ( 'NONE', ( #198053 ), #98925, .F. ) ;
#86490=DIRECTION ( 'NONE',  ( 1.000000000000000000, 0.000000000000000000, 0.000000000000000000 ) ) ;
#86496=DIRECTION ( 'NONE',  ( 0.000000000000000000, 1.000000000000000000, 0.000000000000000000 ) ) ;
#86501=DIRECTION ( 'NONE',  ( 0.000000000000000000, 1.084202172485623868E-14, 1.000000000000000000 ) ) ;
#86558=CARTESIAN_POINT ( 'NONE',  ( -21.93340585971692391, 7.324147022868191748, -167.4999999999999432 ) ) ;
#86587=ADVANCED_FACE ( 'NONE', ( #106634 ), #188759, .T. ) ;
#86676=VECTOR ( 'NONE', #68952, 1000.000000000000000 ) ;
#86687=ORIENTED_EDGE ( 'NONE', *, *, #213467, .F. ) ;
#86693=FACE_OUTER_BOUND ( 'NONE', #33108, .T. ) ;
#86708=CARTESIAN_POINT ( 'NONE',  ( 20.94999999999999929, 4.850467289730772791, -179.5342674090016430 ) ) ;
#86720=TOROIDAL_SURFACE ( 'NONE', #165886, 0.2000000000000000111, 0.1000000000000000056 ) ;
#86732=LINE ( 'NONE', #139336, #133157 ) ;
#86744=ORIENTED_EDGE ( 'NONE', *, *, #78888, .T. ) ;
#86753=TOROIDAL_SURFACE ( 'NONE', #24258, 0.4000000000000009104, 0.1000000000000000056 ) ;
#86757=DIRECTION ( 'NONE',  ( -1.000000000000000000, 0.000000000000000000, 0.000000000000000000 ) ) ;
#86770=DIRECTION ( 'NONE',  ( 0.000000000000000000, 0.4999999999999348299, -0.8660254037844762331 ) ) ;
#86812=DIRECTION ( 'NONE',  ( 0.000000000000000000, -0.9908441862701782288, 0.1350103645450542456 ) ) ;
#86816=VERTEX_POINT ( 'NONE', #42517 ) ;
#86823=CARTESIAN_POINT ( 'NONE',  ( 18.52928932188133970, 10.27928932189250055, -192.1499999999999488 ) ) ;
#86868=VECTOR ( 'NONE', #12713, 999.9999999999998863 ) ;
#86979=ORIENTED_EDGE ( 'NONE', *, *, #218430, .T. ) ;
#86986=B_SPLINE_CURVE_WITH_KNOTS ( 'NONE', 3,
 ( #235084, #175152, #193402, #197225, #79824, #301, #53874, #218052, #39478, #76001 ),
 .UNSPECIFIED., .F., .F.,
 ( 4, 3, 3, 4 ),
 ( 0.000000000000000000, 0.0002000000000008585893, 0.001000000000082977483, 0.001967863649483336721 ),
 .UNSPECIFIED. ) ;
#87009=FACE_OUTER_BOUND ( 'NONE', #102631, .T. ) ;
#87010=ORIENTED_EDGE ( 'NONE', *, *, #224557, .T. ) ;
#87014=AXIS2_PLACEMENT_3D ( 'NONE', #91330, #230855, #71781 ) ;
#87024=CARTESIAN_POINT ( 'NONE',  ( 21.05000000000000071, 1.115649653272650466E-11, -196.9999999999999432 ) ) ;
#87052=LINE ( 'NONE', #190033, #220824 ) ;
#87063=DIRECTION ( 'NONE',  ( 1.000000000000000000, 0.000000000000000000, 0.000000000000000000 ) ) ;
#87079=DIRECTION ( 'NONE',  ( 0.000000000000000000, 0.000000000000000000, -1.000000000000000000 ) ) ;
#87080=VERTEX_POINT ( 'NONE', #165040 ) ;
#87085=ORIENTED_EDGE ( 'NONE', *, *, #161719, .F. ) ;
#87089=CARTESIAN_POINT ( 'NONE',  ( -23.25000000000000000, -0.1008583690875562017, -155.7504328765105868 ) ) ;
#87092=CARTESIAN_POINT ( 'NONE',  ( 18.50000000000000355, -9.399999999988830623, -207.8820418481726620 ) ) ;
#87101=ORIENTED_EDGE ( 'NONE', *, *, #182108, .T. ) ;
#87106=DIRECTION ( 'NONE',  ( 1.000000000000000000, 2.952720810173289112E-16, -0.000000000000000000 ) ) ;
#87107=DIRECTION ( 'NONE',  ( 0.000000000000000000, -1.000000000000000000, 0.000000000000000000 ) ) ;
#87111=LINE ( 'NONE', #150957, #95077 ) ;
#87114=VERTEX_POINT ( 'NONE', #34541 ) ;
#87128=EDGE_LOOP ( 'NONE', ( #203514, #249606, #51424, #68870 ) ) ;
#87151=VERTEX_POINT ( 'NONE', #189742 ) ;
#87153=CARTESIAN_POINT ( 'NONE',  ( -20.54999999999999716, 1.115600667400684642E-11, -200.9999999999999432 ) ) ;
#87163=DIRECTION ( 'NONE',  ( 0.000000000000000000, 1.000000000000000000, 2.891205793294679805E-16 ) ) ;
#87184=DIRECTION ( 'NONE',  ( -7.304098846218201720E-16, 1.000000000000000000, 0.000000000000000000 ) ) ;
#87209=ADVANCED_FACE ( 'NONE', ( #170233 ), #147471, .T. ) ;
#87216=CYLINDRICAL_SURFACE ( 'NONE', #30430, 0.09999999999998898659 ) ;
#87226=ORIENTED_EDGE ( 'NONE', *, *, #76250, .F. ) ;
#87279=VERTEX_POINT ( 'NONE', #215701 ) ;
#87289=VECTOR ( 'NONE', #115763, 1000.000000000000000 ) ;
#87312=CARTESIAN_POINT ( 'NONE',  ( 23.14999999999999503, 6.550000000011156231, -188.7499999999999716 ) ) ;
#87350=FACE_OUTER_BOUND ( 'NONE', #22039, .T. ) ;
#87357=AXIS2_PLACEMENT_3D ( 'NONE', #78611, #155633, #17376 ) ;
#87376=DIRECTION ( 'NONE',  ( 0.000000000000000000, 1.776356839400306474E-15, 1.000000000000000000 ) ) ;
#87388=EDGE_CURVE ( 'NONE', #255690, #71995, #26529, .T. ) ;
#87408=CARTESIAN_POINT ( 'NONE',  ( 18.44364597020194196, -9.490487317151110602, -174.5579778896838263 ) ) ;
#87420=( BOUNDED_SURFACE ( )  B_SPLINE_SURFACE ( 3, 2, ( 
 ( #55801, #57095, #217457 ),
 ( #136644, #17985, #98774 ),
 ( #195376, #177099, #79230 ),
 ( #194091, #35035, #58374 ),
 ( #137923, #114534, #15450 ),
 ( #16730, #135360, #214910 ),
 ( #6115, #223877, #103921 ),
 ( #165208, #221307, #220049 ),
 ( #143058, #201759, #42691 ),
 ( #183494, #123517, #244727 ),
 ( #199210, #4820, #122238 ),
 ( #83060, #66105, #222586 ) ),
 .UNSPECIFIED., .F., .F., .F. ) 
 B_SPLINE_SURFACE_WITH_KNOTS ( ( 4, 2, 2, 2, 2, 4 ),
 ( 3, 3 ),
 ( 3.174653483277205090, 3.943930578431714018, 4.713207673586222946, 5.482484768740731873, 5.867123316317986337, 6.251761863895240801 ),
 ( 0.000000000000000000, 1.000000000000000000 ),
 .UNSPECIFIED. ) 
 GEOMETRIC_REPRESENTATION_ITEM ( )  RATIONAL_B_SPLINE_SURFACE ( (
 ( 1.000000000000000000, 0.8659465255642228021, 1.000000000000000000),
 ( 1.000000000000000000, 0.8648614068488911233, 1.000000000000000000),
 ( 1.000000000000000000, 0.8489031841323105843, 1.000000000000000000),
 ( 1.000000000000000000, 0.7927507630162217156, 1.000000000000000000),
 ( 1.000000000000000000, 0.7523013858916698382, 1.000000000000000000),
 ( 1.000000000000000000, 0.6616226951289214675, 1.000000000000000000),
 ( 1.000000000000000000, 0.6112214368573144485, 1.000000000000000000),
 ( 1.000000000000000000, 0.5507684314573975115, 1.000000000000000000),
 ( 1.000000000000000000, 0.5333267243152293169, 1.000000000000000000),
 ( 1.000000000000000000, 0.5084565446480597828, 1.000000000000000000),
 ( 1.000000000000000000, 0.5010722703450565252, 1.000000000000000000),
 ( 1.000000000000000000, 0.5001234037138694299, 1.000000000000000000) ) ) 
 REPRESENTATION_ITEM ( '' )  SURFACE ( )  );
#87430=FACE_OUTER_BOUND ( 'NONE', #98408, .T. ) ;
#87438=DIRECTION ( 'NONE',  ( -0.000000000000000000, -0.9876197685951252359, -0.1568667991644863424 ) ) ;
#87458=EDGE_CURVE ( 'NONE', #244617, #257624, #97549, .T. ) ;
#87484=DIRECTION ( 'NONE',  ( 0.000000000000000000, 0.1495327102803792052, -0.9887567792719320625 ) ) ;
#87503=CARTESIAN_POINT ( 'NONE',  ( -23.15000000000000213, 1.925233644870967487, -188.2697564668738153 ) ) ;
#87524=CIRCLE ( 'NONE', #12739, 11.75000000000000000 ) ;
#87593=CARTESIAN_POINT ( 'NONE',  ( -18.58744394320977378, -9.566385154537556446, -207.8228480538757594 ) ) ;
#87603=ADVANCED_FACE ( 'NONE', ( #217964 ), #56048, .T. ) ;
#87615=DIRECTION ( 'NONE',  ( 1.000000000000000000, 0.000000000000000000, 0.000000000000000000 ) ) ;
#87637=AXIS2_PLACEMENT_3D ( 'NONE', #117641, #195913, #57647 ) ;
#87648=EDGE_LOOP ( 'NONE', ( #156581, #178968, #56054, #31787 ) ) ;
#87672=EDGE_LOOP ( 'NONE', ( #16371, #48737, #193166, #183540 ) ) ;
#87684=EDGE_CURVE ( 'NONE', #232784, #493, #52435, .T. ) ;
#87705=AXIS2_PLACEMENT_3D ( 'NONE', #69192, #190418, #189114 ) ;
#87710=ORIENTED_EDGE ( 'NONE', *, *, #44094, .T. ) ;
#87720=ADVANCED_FACE ( 'NONE', ( #246535 ), #177578, .T. ) ;
#87722=AXIS2_PLACEMENT_3D ( 'NONE', #208563, #226815, #127733 ) ;
#87726=DIRECTION ( 'NONE',  ( 0.000000000000000000, 0.9274965247785529332, 0.3738317757009255171 ) ) ;
#87741=CARTESIAN_POINT ( 'NONE',  ( -20.64999999999999858, 7.250000000011155521, -179.7499999999999716 ) ) ;
#87794=DIRECTION ( 'NONE',  ( 0.000000000000000000, 0.000000000000000000, 1.000000000000000000 ) ) ;
#87804=AXIS2_PLACEMENT_3D ( 'NONE', #218100, #240266, #39521 ) ;
#87826=FACE_OUTER_BOUND ( 'NONE', #230882, .T. ) ;
#87832=FACE_OUTER_BOUND ( 'NONE', #121356, .T. ) ;
#87871=LINE ( 'NONE', #185724, #60159 ) ;
#87894=FACE_OUTER_BOUND ( 'NONE', #148379, .T. ) ;
#87900=VECTOR ( 'NONE', #29624, 1000.000000000000000 ) ;
#87956=AXIS2_PLACEMENT_3D ( 'NONE', #144055, #3261, #26722 ) ;
#88010=DIRECTION ( 'NONE',  ( -0.000000000000000000, -1.897661533703519897E-16, 1.000000000000000000 ) ) ;
#88043=EDGE_CURVE ( 'NONE', #169886, #208902, #23637, .T. ) ;
#88062=CARTESIAN_POINT ( 'NONE',  ( -23.15000000000000213, 2.000000000011154189, -188.2753780772378889 ) ) ;
#88083=CARTESIAN_POINT ( 'NONE',  ( 21.05000000000000071, 1.115600667400684642E-11, -167.4999999999999716 ) ) ;
#88089=PLANE ( 'NONE',  #90673 ) ;
#88090=CARTESIAN_POINT ( 'NONE',  ( -20.94403535211772294, 10.30632246271647467, -206.5041836778895288 ) ) ;
#88107=ADVANCED_FACE ( 'NONE', ( #145511 ), #240087, .T. ) ;
#88113=VERTEX_POINT ( 'NONE', #247176 ) ;
#88117=ADVANCED_FACE ( 'NONE', ( #185930 ), #190201, .T. ) ;
#88125=DIRECTION ( 'NONE',  ( 0.000000000000000000, -1.000000000000000000, 0.000000000000000000 ) ) ;
#88160=FACE_OUTER_BOUND ( 'NONE', #100718, .T. ) ;
#88177=AXIS2_PLACEMENT_3D ( 'NONE', #234109, #136271, #93319 ) ;
#88180=EDGE_CURVE ( 'NONE', #251640, #141132, #231707, .T. ) ;
#88181=EDGE_LOOP ( 'NONE', ( #61465, #210259, #2101, #135394 ) ) ;
#88184=CARTESIAN_POINT ( 'NONE',  ( 20.84999999999998721, -11.74999999998884448, -200.9999999999999432 ) ) ;
#88255=EDGE_CURVE ( 'NONE', #224848, #2364, #214469, .T. ) ;
#88260=LINE ( 'NONE', #248645, #19246 ) ;
#88265=ORIENTED_EDGE ( 'NONE', *, *, #129836, .T. ) ;
#88309=VECTOR ( 'NONE', #43115, 1000.000000000000114 ) ;
#88330=ORIENTED_EDGE ( 'NONE', *, *, #71738, .F. ) ;
#88341=AXIS2_PLACEMENT_3D ( 'NONE', #26556, #106046, #146465 ) ;
#88366=LINE ( 'NONE', #87089, #182481 ) ;
#88368=ORIENTED_EDGE ( 'NONE', *, *, #214270, .T. ) ;
#88374=CIRCLE ( 'NONE', #175732, 2.000000000000002665 ) ;
#88397=DIRECTION ( 'NONE',  ( 0.000000000000000000, -1.000000000000000000, 0.000000000000000000 ) ) ;
#88398=ORIENTED_EDGE ( 'NONE', *, *, #110503, .F. ) ;
#88404=CARTESIAN_POINT ( 'NONE',  ( 21.14999999999999858, 1.115600667400684642E-11, -160.9593430482987344 ) ) ;
#88414=CARTESIAN_POINT ( 'NONE',  ( -22.50000000000000000, 1.115600667400684642E-11, -167.3999999999999773 ) ) ;
#88424=DIRECTION ( 'NONE',  ( 1.000000000000000000, -0.000000000000000000, -0.000000000000000000 ) ) ;
#88429=EDGE_CURVE ( 'NONE', #230164, #257624, #227209, .T. ) ;
#88456=EDGE_LOOP ( 'NONE', ( #68739, #149107, #157701, #223964, #236799 ) ) ;
#88482=ADVANCED_FACE ( 'NONE', ( #185629 ), #104767, .T. ) ;
#88505=DIRECTION ( 'NONE',  ( 0.000000000000000000, -1.000000000000000000, 0.000000000000000000 ) ) ;
#88536=CARTESIAN_POINT ( 'NONE',  ( -23.15000000000000213, -11.48912529306489994, -197.9999999999999432 ) ) ;
#88553=DIRECTION ( 'NONE',  ( 0.000000000000000000, -0.8660254037844411501, -0.4999999999999956146 ) ) ;
#88563=DIRECTION ( 'NONE',  ( -1.000000000000000000, 0.000000000000000000, 0.000000000000000000 ) ) ;
#88575=CARTESIAN_POINT ( 'NONE',  ( 23.14999999999999503, 11.65000000001116298, -188.8499999999999659 ) ) ;
#88577=DIRECTION ( 'NONE',  ( 0.000000000000000000, 1.000000000000000000, -6.308085367188393199E-16 ) ) ;
#88594=ORIENTED_EDGE ( 'NONE', *, *, #5128, .T. ) ;
#88605=CARTESIAN_POINT ( 'NONE',  ( -22.50047199487879368, 0.04490605193130675632, -155.7499525810887633 ) ) ;
#88622=DIRECTION ( 'NONE',  ( 1.000000000000000000, 0.000000000000000000, 0.000000000000000000 ) ) ;
#88626=CARTESIAN_POINT ( 'NONE',  ( 18.39999999999999858, -9.599999999988842347, -174.5320693966996259 ) ) ;
#88633=ADVANCED_BREP_SHAPE_REPRESENTATION ( '', ( #110572, #2425 ), #252581 ) ;
#88653=AXIS2_PLACEMENT_3D ( 'NONE', #254960, #76374, #155957 ) ;
#88663=EDGE_CURVE ( 'NONE', #227765, #202185, #119459, .T. ) ;
#88676=DIRECTION ( 'NONE',  ( 0.000000000000000000, 0.000000000000000000, 1.000000000000000000 ) ) ;
#88677=CARTESIAN_POINT ( 'NONE',  ( 18.49999999999999289, -9.419209763398093571, -174.7477694627588392 ) ) ;
#88704=EDGE_LOOP ( 'NONE', ( #77370, #53536, #54421, #201209 ) ) ;
#88712=FACE_OUTER_BOUND ( 'NONE', #226183, .T. ) ;
#88714=DIRECTION ( 'NONE',  ( 0.000000000000000000, -1.000000000000000000, 0.000000000000000000 ) ) ;
#88723=CARTESIAN_POINT ( 'NONE',  ( -21.04999999999999361, 11.75000000001115374, -174.2838656629781156 ) ) ;
#88783=DIRECTION ( 'NONE',  ( 0.000000000000000000, 0.000000000000000000, -1.000000000000000000 ) ) ;
#88793=DIRECTION ( 'NONE',  ( -1.000000000000000000, 0.000000000000000000, 0.000000000000000000 ) ) ;
#88832=CYLINDRICAL_SURFACE ( 'NONE', #155521, 0.09999999999999939493 ) ;
#88845=DIRECTION ( 'NONE',  ( -0.000000000000000000, -0.1350103645451904977, 0.9908441862701596881 ) ) ;
#88846=ORIENTED_EDGE ( 'NONE', *, *, #249591, .T. ) ;
#88883=CARTESIAN_POINT ( 'NONE',  ( -18.59999999999999787, -1.249999999988843369, -175.4999999999999716 ) ) ;
#88892=PRODUCT_DEFINITION_SHAPE ( 'NONE', 'NONE',  #236527 ) ;
#88926=CARTESIAN_POINT ( 'NONE',  ( -18.50000000000000000, -1.736257131586239844, -179.0686523290174819 ) ) ;
#88951=VERTEX_POINT ( 'NONE', #139298 ) ;
#88976=CARTESIAN_POINT ( 'NONE',  ( 22.39999999999999858, 0.1000000000111554016, -159.7092204016265669 ) ) ;
#88997=ORIENTED_EDGE ( 'NONE', *, *, #217181, .T. ) ;
#89013=DIRECTION ( 'NONE',  ( 1.000000000000000000, -0.000000000000000000, -0.000000000000000000 ) ) ;
#89081=EDGE_CURVE ( 'NONE', #87080, #130316, #93001, .T. ) ;
#89102=DIRECTION ( 'NONE',  ( 0.000000000000000000, -1.000000000000000000, 0.000000000000000000 ) ) ;
#89120=CARTESIAN_POINT ( 'NONE',  ( 20.99749315643151348, 11.75000000001115907, -193.9851942312420192 ) ) ;
#89132=AXIS2_PLACEMENT_3D ( 'NONE', #4219, #202437, #2934 ) ;
#89136=AXIS2_PLACEMENT_3D ( 'NONE', #141566, #221095, #64590 ) ;
#89160=EDGE_CURVE ( 'NONE', #135358, #95624, #60042, .T. ) ;
#89161=CARTESIAN_POINT ( 'NONE',  ( 21.14999999999999503, 1.115600667400684642E-11, -167.4999999999999716 ) ) ;
#89167=AXIS2_PLACEMENT_3D ( 'NONE', #28272, #166496, #247266 ) ;
#89183=EDGE_CURVE ( 'NONE', #116440, #123667, #147348, .T. ) ;
#89188=AXIS2_PLACEMENT_3D ( 'NONE', #50949, #88793, #168410 ) ;
#89210=AXIS2_PLACEMENT_3D ( 'NONE', #94691, #75167, #137652 ) ;
#89232=AXIS2_PLACEMENT_3D ( 'NONE', #13176, #229651, #50977 ) ;
#89233=DIRECTION ( 'NONE',  ( -0.000000000000000000, -0.000000000000000000, -1.000000000000000000 ) ) ;
#89249=CARTESIAN_POINT ( 'NONE',  ( -20.64999999999999858, -9.499999999988846255, -191.1060308773475356 ) ) ;
#89256=CARTESIAN_POINT ( 'NONE',  ( -21.45000000000000284, 7.708578643773852157, -179.8499999999999943 ) ) ;
#89281=VECTOR ( 'NONE', #169221, 1000.000000000000114 ) ;
#89302=ORIENTED_EDGE ( 'NONE', *, *, #196568, .T. ) ;
#89312=CARTESIAN_POINT ( 'NONE',  ( 20.89192007715127986, 10.32898536001801304, -206.5826683222763904 ) ) ;
#89332=CARTESIAN_POINT ( 'NONE',  ( 21.05000005001280172, 8.871279691782062216, -179.6779475882455870 ) ) ;
#89376=AXIS2_PLACEMENT_3D ( 'NONE', #15414, #14138, #93649 ) ;
#89392=VECTOR ( 'NONE', #29632, 1000.000000000000000 ) ;
#89431=EDGE_LOOP ( 'NONE', ( #208743, #242886, #124885, #154427 ) ) ;
#89436=DIRECTION ( 'NONE',  ( 1.000000000000000000, -7.304098846218133681E-16, -2.111765289898285610E-31 ) ) ;
#89480=DIRECTION ( 'NONE',  ( 0.000000000000000000, 0.000000000000000000, -1.000000000000000000 ) ) ;
#89482=ORIENTED_EDGE ( 'NONE', *, *, #43435, .T. ) ;
#89506=VECTOR ( 'NONE', #107863, 1000.000000000000000 ) ;
#89515=CARTESIAN_POINT ( 'NONE',  ( -20.94999999999999929, -1.736257131586239844, -179.0686523290174819 ) ) ;
#89550=AXIS2_PLACEMENT_3D ( 'NONE', #242128, #63483, #12535 ) ;
#89612=ORIENTED_EDGE ( 'NONE', *, *, #86466, .F. ) ;
#89633=CARTESIAN_POINT ( 'NONE',  ( 20.94999999999999929, -11.48912529306489994, -197.9999999999999432 ) ) ;
#89670=DIRECTION ( 'NONE',  ( 0.000000000000000000, 1.000000000000000000, -0.000000000000000000 ) ) ;
#89671=CIRCLE ( 'NONE', #14708, 0.09999999999998898659 ) ;
#89673=CARTESIAN_POINT ( 'NONE',  ( 23.15000000000000213, -11.64999999998883595, -197.8999999999999773 ) ) ;
#89692=DIRECTION ( 'NONE',  ( 0.000000000000000000, 0.000000000000000000, -1.000000000000000000 ) ) ;
#89708=DIRECTION ( 'NONE',  ( 0.000000000000000000, 0.000000000000000000, 1.000000000000000000 ) ) ;
#89729=ORIENTED_EDGE ( 'NONE', *, *, #254472, .T. ) ;
#89768=ADVANCED_FACE ( 'NONE', ( #71208 ), #235032, .F. ) ;
#89784=ORIENTED_EDGE ( 'NONE', *, *, #99604, .T. ) ;
#89789=EDGE_CURVE ( 'NONE', #132941, #180362, #14470, .T. ) ;
#89799=PLANE ( 'NONE',  #20303 ) ;
#89814=ORIENTED_EDGE ( 'NONE', *, *, #54123, .F. ) ;
#89832=AXIS2_PLACEMENT_3D ( 'NONE', #158975, #179807, #79387 ) ;
#89863=DIRECTION ( 'NONE',  ( 0.000000000000000000, -1.000000000000000000, 0.000000000000000000 ) ) ;
#89904=VERTEX_POINT ( 'NONE', #42036 ) ;
#89959=ORIENTED_EDGE ( 'NONE', *, *, #248886, .T. ) ;
#90014=CARTESIAN_POINT ( 'NONE',  ( -20.54999999999999716, -11.74999999998884448, -184.2499999999999716 ) ) ;
#90019=CARTESIAN_POINT ( 'NONE',  ( -21.00219873199047171, 11.60538868788763089, -174.4126474282949744 ) ) ;
#90021=B_SPLINE_CURVE_WITH_KNOTS ( 'NONE', 3,
 ( #50242, #32007, #47673, #90658 ),
 .UNSPECIFIED., .F., .F.,
 ( 4, 4 ),
 ( 0.000000000000000000, 0.001767853679387121216 ),
 .UNSPECIFIED. ) ;
#90025=AXIS2_PLACEMENT_3D ( 'NONE', #16912, #63383, #140355 ) ;
#90046=DIRECTION ( 'NONE',  ( 0.000000000000000000, 0.000000000000000000, 1.000000000000000000 ) ) ;
#90069=VECTOR ( 'NONE', #236321, 1000.000000000000000 ) ;
#90071=LINE ( 'NONE', #249177, #56729 ) ;
#90095=CARTESIAN_POINT ( 'NONE',  ( -23.25000000000000000, -1.736705739456431807, -212.5174225876236846 ) ) ;
#90105=AXIS2_PLACEMENT_3D ( 'NONE', #139977, #470, #120477 ) ;
#90121=DIRECTION ( 'NONE',  ( 1.000000000000000000, 0.000000000000000000, -0.000000000000000000 ) ) ;
#90128=CYLINDRICAL_SURFACE ( 'NONE', #44058, 0.09999999999998898659 ) ;
#90169=CIRCLE ( 'NONE', #36032, 0.09999999999998898659 ) ;
#90170=CARTESIAN_POINT ( 'NONE',  ( -20.54999999999999716, -11.74999999998884448, -188.6499999999999488 ) ) ;
#90194=EDGE_LOOP ( 'NONE', ( #251812, #159224, #38416, #77818, #50693 ) ) ;
#90207=AXIS2_PLACEMENT_3D ( 'NONE', #65984, #245915, #189788 ) ;
#90213=CIRCLE ( 'NONE', #2740, 2.000000000000001776 ) ;
#90232=AXIS2_PLACEMENT_3D ( 'NONE', #234600, #16858, #217582 ) ;
#90259=DIRECTION ( 'NONE',  ( -0.9880948137434723000, 0.1538461538461483591, -0.000000000000000000 ) ) ;
#90277=ORIENTED_EDGE ( 'NONE', *, *, #239841, .T. ) ;
#90295=VECTOR ( 'NONE', #91574, 1000.000000000000000 ) ;
#90309=EDGE_CURVE ( 'NONE', #252199, #16613, #160401, .T. ) ;
#90327=VERTEX_POINT ( 'NONE', #8999 ) ;
#90337=AXIS2_PLACEMENT_3D ( 'NONE', #89673, #252602, #114391 ) ;
#90361=CIRCLE ( 'NONE', #248579, 0.09999999999999939493 ) ;
#90380=DIRECTION ( 'NONE',  ( 0.000000000000000000, 0.000000000000000000, -1.000000000000000000 ) ) ;
#90382=CIRCLE ( 'NONE', #186071, 0.09999999999999491240 ) ;
#90387=AXIS2_PLACEMENT_3D ( 'NONE', #134883, #220565, #174090 ) ;
#90398=CARTESIAN_POINT ( 'NONE',  ( 21.04386569057696121, 11.75000000001181988, -194.1428373517797468 ) ) ;
#90413=DIRECTION ( 'NONE',  ( 0.000000000000000000, 0.000000000000000000, -1.000000000000000000 ) ) ;
#90431=ORIENTED_EDGE ( 'NONE', *, *, #189237, .T. ) ;
#90449=ORIENTED_EDGE ( 'NONE', *, *, #225000, .T. ) ;
#90455=VERTEX_POINT ( 'NONE', #126377 ) ;
#90458=AXIS2_PLACEMENT_3D ( 'NONE', #54432, #188811, #153593 ) ;
#90463=AXIS2_PLACEMENT_3D ( 'NONE', #133070, #35290, #136909 ) ;
#90486=ORIENTED_EDGE ( 'NONE', *, *, #1010, .T. ) ;
#90491=LINE ( 'NONE', #170087, #239065 ) ;
#90528=CARTESIAN_POINT ( 'NONE',  ( -21.05000000000000071, 14.05000000001115623, -173.0136950707609458 ) ) ;
#90565=CARTESIAN_POINT ( 'NONE',  ( -18.59999999999999787, 11.65000000001115232, -179.7499999999999716 ) ) ;
#90589=DIRECTION ( 'NONE',  ( 0.000000000000000000, -0.1298341882520022694, -0.9915357197604852679 ) ) ;
#90592=DIRECTION ( 'NONE',  ( 0.000000000000000000, 0.000000000000000000, 1.000000000000000000 ) ) ;
#90593=CARTESIAN_POINT ( 'NONE',  ( 20.84999999999998721, 10.33248238083634440, -206.5948465439131496 ) ) ;
#90631=ORIENTED_EDGE ( 'NONE', *, *, #6709, .T. ) ;
#90658=CARTESIAN_POINT ( 'NONE',  ( 21.14999999999999858, 1.115600667400684642E-11, -160.9593430482987344 ) ) ;
#90662=DIRECTION ( 'NONE',  ( 0.000000000000000000, 0.000000000000000000, -1.000000000000000000 ) ) ;
#90668=EDGE_CURVE ( 'NONE', #57200, #185004, #43962, .T. ) ;
#90673=AXIS2_PLACEMENT_3D ( 'NONE', #142937, #167689, #46416 ) ;
#90679=CARTESIAN_POINT ( 'NONE',  ( -20.85000000000000142, 10.33248238083634440, -206.5948465439131496 ) ) ;
#90711=CARTESIAN_POINT ( 'NONE',  ( 21.04999999999999716, 6.496686585778529199, -167.5146561185098619 ) ) ;
#90736=VERTEX_POINT ( 'NONE', #148195 ) ;
#90741=CARTESIAN_POINT ( 'NONE',  ( -18.59999999999999787, 9.150000000011157653, -155.7499999999999716 ) ) ;
#90765=CYLINDRICAL_SURFACE ( 'NONE', #18293, 0.09999999999998898659 ) ;
#90795=DIRECTION ( 'NONE',  ( -1.000000000000000000, -3.265361837132813093E-16, 0.000000000000000000 ) ) ;
#90808=LINE ( 'NONE', #153412, #172446 ) ;
#90829=AXIS2_PLACEMENT_3D ( 'NONE', #214109, #173753, #35506 ) ;
#90840=CARTESIAN_POINT ( 'NONE',  ( 21.13461538461538325, 8.885417037985616773, -179.8499999999999943 ) ) ;
#90877=ORIENTED_EDGE ( 'NONE', *, *, #103176, .T. ) ;
#90890=CARTESIAN_POINT ( 'NONE',  ( -18.59999999999999787, 9.350000000011156942, -179.7499999999999716 ) ) ;
#90905=ORIENTED_EDGE ( 'NONE', *, *, #53689, .T. ) ;
#90925=DIRECTION ( 'NONE',  ( 0.000000000000000000, 0.000000000000000000, 1.000000000000000000 ) ) ;
#90934=VERTEX_POINT ( 'NONE', #39834 ) ;
#90972=DIRECTION ( 'NONE',  ( 0.000000000000000000, -0.000000000000000000, 1.000000000000000000 ) ) ;
#90987=AXIS2_PLACEMENT_3D ( 'NONE', #62856, #142389, #232848 ) ;
#90990=ORIENTED_EDGE ( 'NONE', *, *, #116594, .F. ) ;
#91012=CIRCLE ( 'NONE', #203442, 12.87499999999999822 ) ;
#91013=CIRCLE ( 'NONE', #99175, 0.9750000000000036415 ) ;
#91024=CARTESIAN_POINT ( 'NONE',  ( -23.25000000000000000, 6.933893972137497030, -204.7856458343735255 ) ) ;
#91031=CARTESIAN_POINT ( 'NONE',  ( -23.25000000000000000, 6.982009704867601307, -204.6961521182562649 ) ) ;
#91037=ORIENTED_EDGE ( 'NONE', *, *, #108531, .F. ) ;
#91061=DIRECTION ( 'NONE',  ( 0.000000000000000000, 0.000000000000000000, -1.000000000000000000 ) ) ;
#91062=AXIS2_PLACEMENT_3D ( 'NONE', #166075, #83889, #243000 ) ;
#91084=VERTEX_POINT ( 'NONE', #50077 ) ;
#91121=CARTESIAN_POINT ( 'NONE',  ( -21.44999999999999929, 7.350000000011155166, -188.6499999999999488 ) ) ;
#91124=ADVANCED_FACE ( 'NONE', ( #87894 ), #172694, .T. ) ;
#91171=VERTEX_POINT ( 'NONE', #146585 ) ;
#91203=CARTESIAN_POINT ( 'NONE',  ( -22.45437739390954590, 1.115488181425289271E-11, -155.8504291884057693 ) ) ;
#91222=VECTOR ( 'NONE', #102900, 1000.000000000000000 ) ;
#91234=EDGE_LOOP ( 'NONE', ( #175241, #82851, #128823, #108738 ) ) ;
#91236=AXIS2_PLACEMENT_3D ( 'NONE', #74913, #172747, #175301 ) ;
#91255=LINE ( 'NONE', #92516, #128207 ) ;
#91307=VERTEX_POINT ( 'NONE', #57770 ) ;
#91309=DIRECTION ( 'NONE',  ( -1.000000000000000000, -0.000000000000000000, 0.000000000000000000 ) ) ;
#91324=DIRECTION ( 'NONE',  ( 0.000000000000000000, 0.000000000000000000, 1.000000000000000000 ) ) ;
#91330=CARTESIAN_POINT ( 'NONE',  ( -23.15000000000000213, -11.64999999998884483, -197.8999999999999773 ) ) ;
#91372=CARTESIAN_POINT ( 'NONE',  ( 20.95289811251229750, 8.893168004469748311, -176.0018094939185005 ) ) ;
#91384=CIRCLE ( 'NONE', #153788, 0.09999999999999939493 ) ;
#91412=AXIS2_PLACEMENT_3D ( 'NONE', #130051, #47950, #170536 ) ;
#91423=DIRECTION ( 'NONE',  ( 1.000000000000000000, 0.000000000000000000, 0.000000000000000000 ) ) ;
#91449=B_SPLINE_CURVE_WITH_KNOTS ( 'NONE', 3,
 ( #81870, #41525, #80596, #255353, #79320, #235838, #76767, #117191, #13285, #37674, #238416, #196714, #119779, #59748, #161468, #18079, #139290, #20674, #141875 ),
 .UNSPECIFIED., .F., .F.,
 ( 4, 3, 3, 3, 3, 3, 4 ),
 ( 0.000000000000000000, 1.655171619026302737E-05, 2.773500582847661863E-05, 5.941817267377570179E-05, 0.0001114174635873301661, 0.0001914169455916044462, 0.0002627181070750214849 ),
 .UNSPECIFIED. ) ;
#91466=CARTESIAN_POINT ( 'NONE',  ( 20.94999999999999574, -1.360870587180885716, -175.5729979270909382 ) ) ;
#91492=FACE_OUTER_BOUND ( 'NONE', #208878, .T. ) ;
#91494=ORIENTED_EDGE ( 'NONE', *, *, #157329, .F. ) ;
#91512=DIRECTION ( 'NONE',  ( 1.000000000000000000, 0.000000000000000000, 0.000000000000000000 ) ) ;
#91537=EDGE_CURVE ( 'NONE', #162728, #194468, #193682, .T. ) ;
#91539=FACE_OUTER_BOUND ( 'NONE', #134200, .T. ) ;
#91541=ORIENTED_EDGE ( 'NONE', *, *, #165798, .T. ) ;
#91563=EDGE_LOOP ( 'NONE', ( #150523, #188996, #32876, #44871, #5511 ) ) ;
#91574=DIRECTION ( 'NONE',  ( 0.000000000000000000, -1.000000000000000000, 0.000000000000000000 ) ) ;
#91586=CIRCLE ( 'NONE', #153998, 0.09999999999999939493 ) ;
#91616=CARTESIAN_POINT ( 'NONE',  ( -23.15000000000000213, -9.499999999988846255, -191.1060308773475356 ) ) ;
#91631=CARTESIAN_POINT ( 'NONE',  ( -21.14999999999999858, 1.115600667400684642E-11, -160.9593430482987344 ) ) ;
#91634=EDGE_CURVE ( 'NONE', #87151, #234897, #135393, .T. ) ;
#91648=CARTESIAN_POINT ( 'NONE',  ( -20.64999999999999858, 1.115600667400684642E-11, -188.1249999999999716 ) ) ;
#91679=DIRECTION ( 'NONE',  ( 1.000000000000000000, -0.000000000000000000, 0.000000000000000000 ) ) ;
#91696=DIRECTION ( 'NONE',  ( -3.469446951953635015E-14, 1.000000000000000000, 0.000000000000000000 ) ) ;
#91715=CARTESIAN_POINT ( 'NONE',  ( -20.54999999999999716, -8.730841121484170131, -191.4019252810156217 ) ) ;
#91726=CARTESIAN_POINT ( 'NONE',  ( -23.15000000000000213, 4.150000000011156764, -188.6499999999999488 ) ) ;
#91757=EDGE_CURVE ( 'NONE', #107478, #231520, #23011, .T. ) ;
#91763=EDGE_CURVE ( 'NONE', #51917, #192876, #214688, .T. ) ;
#91768=CARTESIAN_POINT ( 'NONE',  ( -20.85000000000000142, 0.1610488207298751417, -200.7158101556397582 ) ) ;
#91797=AXIS2_PLACEMENT_3D ( 'NONE', #42775, #2345, #23242 ) ;
#91800=AXIS2_PLACEMENT_3D ( 'NONE', #246237, #104130, #106701 ) ;
#91839=AXIS2_PLACEMENT_3D ( 'NONE', #59458, #101139, #22972 ) ;
#91882=DIRECTION ( 'NONE',  ( 0.000000000000000000, 0.9915357197604972583, -0.1298341882519109536 ) ) ;
#91887=CARTESIAN_POINT ( 'NONE',  ( -20.54999999999999716, 1.115600667400684642E-11, -167.4999999999999716 ) ) ;
#91908=CARTESIAN_POINT ( 'NONE',  ( 21.04105312098506531, 8.875332623054768888, -179.8285067472120033 ) ) ;
#91920=DIRECTION ( 'NONE',  ( 0.000000000000000000, -1.000000000000000000, -0.000000000000000000 ) ) ;
#91955=DIRECTION ( 'NONE',  ( 0.000000000000000000, 0.000000000000000000, 1.000000000000000000 ) ) ;
#91957=DIRECTION ( 'NONE',  ( -1.000000000000000000, 0.000000000000000000, -0.000000000000000000 ) ) ;
#91967=CYLINDRICAL_SURFACE ( 'NONE', #111533, 0.5000000000000004441 ) ;
#91968=CARTESIAN_POINT ( 'NONE',  ( -20.88420186297724612, 10.33025634372637391, -206.5870929282638429 ) ) ;
#91975=CARTESIAN_POINT ( 'NONE',  ( 18.49999999999999645, 1.866714910068465239, -179.2526752462819672 ) ) ;
#91998=CARTESIAN_POINT ( 'NONE',  ( 21.05000000000034177, 6.300183336278641022, -167.4486725676592869 ) ) ;
#92007=CARTESIAN_POINT ( 'NONE',  ( -18.50000000000000000, 11.65000000001115232, -179.6499999999999773 ) ) ;
#92042=CARTESIAN_POINT ( 'NONE',  ( -18.50000000000000000, -1.164121893230052995, -208.9148480855715775 ) ) ;
#92081=ORIENTED_EDGE ( 'NONE', *, *, #181465, .F. ) ;
#92106=( BOUNDED_SURFACE ( )  B_SPLINE_SURFACE ( 3, 2, ( 
 ( #219379, #43333, #39511 ),
 ( #40789, #142417, #21224 ),
 ( #100691, #180275, #221930 ),
 ( #45887, #50991, #6761 ),
 ( #208819, #187978, #30198 ),
 ( #189262, #150145, #227081 ),
 ( #107137, #186701, #128002 ),
 ( #9326, #86272, #10622 ) ),
 .UNSPECIFIED., .F., .F., .T. ) 
 B_SPLINE_SURFACE_WITH_KNOTS ( ( 4, 2, 2, 4 ),
 ( 3, 3 ),
 ( 0.0001704874539069911317, 0.0003809798300636659538, 0.0004862260181420033920, 0.0005914722062203408301 ),
 ( 0.000000000000000000, 1.000000000000000000 ),
 .UNSPECIFIED. ) 
 GEOMETRIC_REPRESENTATION_ITEM ( )  RATIONAL_B_SPLINE_SURFACE ( (
 ( 1.000000000000000000, 0.7071067811864942820, 1.000000000000000000),
 ( 1.000000000000000000, 0.7670648383579508067, 1.000000000000000000),
 ( 1.000000000000000000, 0.8204820770248304473, 1.000000000000000000),
 ( 1.000000000000000000, 0.8877218296116144991, 1.000000000000000000),
 ( 1.000000000000000000, 0.9080815932663784951, 1.000000000000000000),
 ( 1.000000000000000000, 0.9395541505863417298, 1.000000000000000000),
 ( 1.000000000000000000, 0.9506520335377867115, 1.000000000000000000),
 ( 1.000000000000000000, 0.9504532311154454405, 1.000000000000000000) ) ) 
 REPRESENTATION_ITEM ( '' )  SURFACE ( )  );
#92204=CARTESIAN_POINT ( 'NONE',  ( 21.07094088545303734, 6.320167221927647461, -167.4011062974477682 ) ) ;
#92241=LINE ( 'NONE', #252599, #100146 ) ;
#92261=DIRECTION ( 'NONE',  ( 4.026293107431335996E-15, -0.8700118002898359348, 0.4930308989875165082 ) ) ;
#92283=EDGE_CURVE ( 'NONE', #156526, #76578, #35837, .T. ) ;
#92339=DIRECTION ( 'NONE',  ( 1.000000000000000000, -0.000000000000000000, -0.000000000000000000 ) ) ;
#92356=FACE_OUTER_BOUND ( 'NONE', #109567, .T. ) ;
#92373=LINE ( 'NONE', #35019, #157796 ) ;
#92472=ORIENTED_EDGE ( 'NONE', *, *, #231304, .T. ) ;
#92477=ORIENTED_EDGE ( 'NONE', *, *, #133935, .T. ) ;
#92515=DIRECTION ( 'NONE',  ( 0.000000000000000000, 0.000000000000000000, 1.000000000000000000 ) ) ;
#92516=CARTESIAN_POINT ( 'NONE',  ( 23.24999999999999645, 5.600000000011153389, -155.7499999999999716 ) ) ;
#92521=CARTESIAN_POINT ( 'NONE',  ( -20.64999999999999858, -9.499999999988846255, -191.1060308773475356 ) ) ;
#92524=ORIENTED_EDGE ( 'NONE', *, *, #122440, .T. ) ;
#92546=AXIS2_PLACEMENT_3D ( 'NONE', #145851, #29810, #71490 ) ;
#92595=AXIS2_PLACEMENT_3D ( 'NONE', #8343, #167429, #227370 ) ;
#92600=DIRECTION ( 'NONE',  ( 0.000000000000000000, 0.4930308989875230585, 0.8700118002898322711 ) ) ;
#92606=EDGE_CURVE ( 'NONE', #9648, #112737, #11059, .T. ) ;
#92618=AXIS2_PLACEMENT_3D ( 'NONE', #21748, #41328, #97382 ) ;
#92656=ORIENTED_EDGE ( 'NONE', *, *, #171619, .F. ) ;
#92674=DIRECTION ( 'NONE',  ( 1.000000000000000000, -0.000000000000000000, -0.000000000000000000 ) ) ;
#92726=DIRECTION ( 'NONE',  ( -1.000000000000000000, -0.000000000000000000, 0.000000000000000000 ) ) ;
#92752=CARTESIAN_POINT ( 'NONE',  ( 22.48660254037843842, 11.75000000001115730, -167.4499999999999318 ) ) ;
#92772=ORIENTED_EDGE ( 'NONE', *, *, #53225, .F. ) ;
#92781=DIRECTION ( 'NONE',  ( 0.000000000000000000, 0.000000000000000000, 1.000000000000000000 ) ) ;
#92836=DIRECTION ( 'NONE',  ( 0.000000000000000000, 0.000000000000000000, -1.000000000000000000 ) ) ;
#92837=EDGE_CURVE ( 'NONE', #64487, #249408, #86232, .T. ) ;
#92891=EDGE_CURVE ( 'NONE', #49571, #36105, #202770, .T. ) ;
#92916=DIRECTION ( 'NONE',  ( 0.000000000000000000, -0.1298341882520124002, -0.9915357197604841577 ) ) ;
#92970=DIRECTION ( 'NONE',  ( 0.000000000000000000, -1.000000000000000000, 0.000000000000000000 ) ) ;
#92987=ORIENTED_EDGE ( 'NONE', *, *, #227098, .T. ) ;
#93001=CIRCLE ( 'NONE', #176417, 0.09999999999998898659 ) ;
#93014=CARTESIAN_POINT ( 'NONE',  ( -20.94999999999999929, 5.850000000011160495, -190.8675027757220448 ) ) ;
#93024=FACE_OUTER_BOUND ( 'NONE', #65900, .T. ) ;
#93026=ADVANCED_FACE ( 'NONE', ( #115677 ), #93535, .T. ) ;
#93038=DIRECTION ( 'NONE',  ( 1.000000000000000000, 0.000000000000000000, 0.000000000000000000 ) ) ;
#93040=ADVANCED_FACE ( 'NONE', ( #233079 ), #213482, .T. ) ;
#93042=CIRCLE ( 'NONE', #30525, 0.09999999999998898659 ) ;
#93067=CARTESIAN_POINT ( 'NONE',  ( 23.14999999999999858, 5.500000000011153745, -188.5947339810868755 ) ) ;
#93098=CONICAL_SURFACE ( 'NONE', #251886, 7.750000000000034639, 0.7853981633974531640 ) ;
#93108=DIRECTION ( 'NONE',  ( 1.000000000000000000, -0.000000000000000000, -0.000000000000000000 ) ) ;
#93126=CARTESIAN_POINT ( 'NONE',  ( -20.85000000000000142, -11.64999999998884483, -198.0999999999999659 ) ) ;
#93128=ORIENTED_EDGE ( 'NONE', *, *, #40302, .T. ) ;
#93167=VERTEX_POINT ( 'NONE', #2124 ) ;
#93184=EDGE_CURVE ( 'NONE', #202185, #181381, #177314, .T. ) ;
#93233=CARTESIAN_POINT ( 'NONE',  ( -18.42609945526400139, -9.499999710479540838, -174.4993624902488136 ) ) ;
#93239=EDGE_CURVE ( 'NONE', #156566, #12588, #182126, .T. ) ;
#93311=AXIS2_PLACEMENT_3D ( 'NONE', #15507, #74213, #78008 ) ;
#93319=DIRECTION ( 'NONE',  ( -2.978066053179067751E-16, 1.000000000000000000, 0.000000000000000000 ) ) ;
#93339=VECTOR ( 'NONE', #102991, 1000.000000000000000 ) ;
#93377=ORIENTED_EDGE ( 'NONE', *, *, #113794, .F. ) ;
#93387=EDGE_LOOP ( 'NONE', ( #189744, #177213, #186456, #74576 ) ) ;
#93402=ORIENTED_EDGE ( 'NONE', *, *, #44572, .T. ) ;
#93416=ORIENTED_EDGE ( 'NONE', *, *, #218696, .F. ) ;
#93494=DIRECTION ( 'NONE',  ( 0.000000000000000000, -0.000000000000000000, 1.000000000000000000 ) ) ;
#93496=EDGE_CURVE ( 'NONE', #10380, #241874, #19823, .T. ) ;
#93522=CIRCLE ( 'NONE', #6028, 0.2000000000000057288 ) ;
#93535=SPHERICAL_SURFACE ( 'NONE', #90337, 0.1000000000000000056 ) ;
#93540=FACE_OUTER_BOUND ( 'NONE', #225039, .T. ) ;
#93569=FACE_OUTER_BOUND ( 'NONE', #220339, .T. ) ;
#93577=B_SPLINE_CURVE_WITH_KNOTS ( 'NONE', 3,
 ( #230420, #70092, #229145, #51754, #132611, #50468 ),
 .UNSPECIFIED., .F., .F.,
 ( 4, 2, 4 ),
 ( 0.000000000000000000, 0.0002113392456166048581, 0.0004226784912332097162 ),
 .UNSPECIFIED. ) ;
#93598=ADVANCED_FACE ( 'NONE', ( #40991 ), #28395, .T. ) ;
#93646=DIRECTION ( 'NONE',  ( 0.000000000000000000, -0.4999999999999478195, 0.8660254037844686836 ) ) ;
#93649=DIRECTION ( 'NONE',  ( 0.000000000000000000, 0.000000000000000000, -1.000000000000000000 ) ) ;
#93658=AXIS2_PLACEMENT_3D ( 'NONE', #30629, #110134, #166298 ) ;
#93691=LINE ( 'NONE', #173283, #198774 ) ;
#93709=AXIS2_PLACEMENT_3D ( 'NONE', #208198, #49094, #205595 ) ;
#93710=CARTESIAN_POINT ( 'NONE',  ( 18.59999999999999076, 10.20857864377385127, -192.1499999999999488 ) ) ;
#93749=CARTESIAN_POINT ( 'NONE',  ( -22.39999999999999858, 1.115600667400684642E-11, -167.4999999999999716 ) ) ;
#93755=EDGE_CURVE ( 'NONE', #154754, #159944, #82616, .T. ) ;
#93816=EDGE_CURVE ( 'NONE', #228990, #46891, #42254, .T. ) ;
#93822=FACE_OUTER_BOUND ( 'NONE', #667, .T. ) ;
#93853=DIRECTION ( 'NONE',  ( -0.000000000000000000, 0.7397360091702694929, 0.6728971962616898672 ) ) ;
#93915=PRODUCT_CONTEXT ( 'NONE', #198973, 'mechanical' ) ;
#93919=AXIS2_PLACEMENT_3D ( 'NONE', #11658, #109437, #151163 ) ;
#93924=CARTESIAN_POINT ( 'NONE',  ( 20.95483826173900255, 8.876166204781142710, -176.0462755528994876 ) ) ;
#93928=ADVANCED_FACE ( 'NONE', ( #68230 ), #171230, .T. ) ;
#93968=CARTESIAN_POINT ( 'NONE',  ( 23.14999999999999503, 6.650000000011155876, -179.7499999999999716 ) ) ;
#94043=ADVANCED_FACE ( 'NONE', ( #214161 ), #99259, .T. ) ;
#94050=ORIENTED_EDGE ( 'NONE', *, *, #78955, .F. ) ;
#94093=DIRECTION ( 'NONE',  ( 0.000000000000000000, 1.000000000000000000, 0.000000000000000000 ) ) ;
#94106=ORIENTED_EDGE ( 'NONE', *, *, #88429, .T. ) ;
#94162=EDGE_LOOP ( 'NONE', ( #19406, #15370, #181615 ) ) ;
#94173=CYLINDRICAL_SURFACE ( 'NONE', #74733, 0.1000000000000089567 ) ;
#94183=DIRECTION ( 'NONE',  ( 0.000000000000000000, 0.1350103645451876666, 0.9908441862701600211 ) ) ;
#94202=AXIS2_PLACEMENT_3D ( 'NONE', #110985, #35340, #32772 ) ;
#94206=CARTESIAN_POINT ( 'NONE',  ( 19.75857864376268935, 11.75000000001118927, -192.2499999999999432 ) ) ;
#94224=CARTESIAN_POINT ( 'NONE',  ( 21.00000000000000000, 9.750000000011153745, -179.8499999999999943 ) ) ;
#94232=FACE_OUTER_BOUND ( 'NONE', #139655, .T. ) ;
#94279=CARTESIAN_POINT ( 'NONE',  ( -18.39999999999999858, -9.599999999988845900, -207.7001893912220112 ) ) ;
#94298=ORIENTED_EDGE ( 'NONE', *, *, #90309, .T. ) ;
#94337=AXIS2_PLACEMENT_3D ( 'NONE', #215041, #35164, #235876 ) ;
#94380=ORIENTED_EDGE ( 'NONE', *, *, #158983, .T. ) ;
#94392=DIRECTION ( 'NONE',  ( 0.000000000000000000, 0.000000000000000000, -1.000000000000000000 ) ) ;
#94403=EDGE_CURVE ( 'NONE', #131118, #52856, #215956, .T. ) ;
#94411=ORIENTED_EDGE ( 'NONE', *, *, #117445, .T. ) ;
#94423=CARTESIAN_POINT ( 'NONE',  ( -20.94999999999999929, 1.162701749949165642, -175.4999999999999716 ) ) ;
#94436=CARTESIAN_POINT ( 'NONE',  ( -21.05000000000000071, 1.835341550235567887, -179.0551512925629538 ) ) ;
#94453=ORIENTED_EDGE ( 'NONE', *, *, #60606, .T. ) ;
#94482=DIRECTION ( 'NONE',  ( 1.000000000000000000, -0.000000000000000000, -0.000000000000000000 ) ) ;
#94502=DIRECTION ( 'NONE',  ( -1.000000000000000000, 0.000000000000000000, 0.000000000000000000 ) ) ;
#94527=ORIENTED_EDGE ( 'NONE', *, *, #237235, .F. ) ;
#94537=CARTESIAN_POINT ( 'NONE',  ( -18.50000000000000000, -9.419084502802133940, -207.8299078070253927 ) ) ;
#94541=ORIENTED_EDGE ( 'NONE', *, *, #58578, .T. ) ;
#94555=ORIENTED_EDGE ( 'NONE', *, *, #94810, .T. ) ;
#94561=FACE_OUTER_BOUND ( 'NONE', #43736, .T. ) ;
#94565=ORIENTED_EDGE ( 'NONE', *, *, #62797, .F. ) ;
#94602=ORIENTED_EDGE ( 'NONE', *, *, #208067, .T. ) ;
#94619=VERTEX_POINT ( 'NONE', #153287 ) ;
#94622=CARTESIAN_POINT ( 'NONE',  ( -20.54999999999999716, 7.150000000011155876, -188.6499999999999488 ) ) ;
#94624=CARTESIAN_POINT ( 'NONE',  ( 18.59999999999999787, -10.35479209691423996, -194.7565409830737337 ) ) ;
#94653=EDGE_CURVE ( 'NONE', #29202, #93167, #121838, .T. ) ;
#94663=AXIS2_PLACEMENT_3D ( 'NONE', #166737, #105405, #24656 ) ;
#94686=CIRCLE ( 'NONE', #173869, 0.09999999999998898659 ) ;
#94691=CARTESIAN_POINT ( 'NONE',  ( -20.94999999999999929, 5.850000000011105428, -177.6324972242779268 ) ) ;
#94735=ORIENTED_EDGE ( 'NONE', *, *, #224421, .T. ) ;
#94757=CARTESIAN_POINT ( 'NONE',  ( -22.39999999999999858, 11.75000000001115552, -167.4999999999999716 ) ) ;
#94810=EDGE_CURVE ( 'NONE', #55017, #152124, #103523, .T. ) ;
#94823=ORIENTED_EDGE ( 'NONE', *, *, #194355, .T. ) ;
#94826=CARTESIAN_POINT ( 'NONE',  ( 20.85000000000000142, 7.021664781911246322, -204.8335654018972605 ) ) ;
#94827=ORIENTED_EDGE ( 'NONE', *, *, #5739, .T. ) ;
#94829=DIRECTION ( 'NONE',  ( -1.000000000000000000, 0.000000000000000000, 0.000000000000000000 ) ) ;
#94831=DIRECTION ( 'NONE',  ( 0.7071359030028288029, 0.000000000000000000, -0.7070776581708504427 ) ) ;
#94837=DIRECTION ( 'NONE',  ( 1.000000000000000000, 0.000000000000000000, 0.000000000000000000 ) ) ;
#94849=ADVANCED_FACE ( 'NONE', ( #43577 ), #99049, .T. ) ;
#94880=DIRECTION ( 'NONE',  ( 0.000000000000000000, 0.2605042016806672911, -0.9654727137038716656 ) ) ;
#94957=PLANE ( 'NONE',  #221897 ) ;
#95005=ORIENTED_EDGE ( 'NONE', *, *, #61637, .F. ) ;
#95008=CARTESIAN_POINT ( 'NONE',  ( -21.14999999999999858, -11.64999999998884483, -167.4999999999999432 ) ) ;
#95014=ADVANCED_FACE ( 'NONE', ( #210364 ), #129538, .T. ) ;
#95045=ORIENTED_EDGE ( 'NONE', *, *, #109894, .F. ) ;
#95048=VERTEX_POINT ( 'NONE', #134640 ) ;
#95077=VECTOR ( 'NONE', #8878, 1000.000000000000000 ) ;
#95113=DIRECTION ( 'NONE',  ( 2.952720810173289112E-16, -1.000000000000000000, 0.000000000000000000 ) ) ;
#95117=CARTESIAN_POINT ( 'NONE',  ( -18.42554971533677133, -9.497159669426594064, -174.5398269135486089 ) ) ;
#95154=CARTESIAN_POINT ( 'NONE',  ( 22.49999999999999645, 0.1000000000111554016, -155.8504291924551808 ) ) ;
#95158=CARTESIAN_POINT ( 'NONE',  ( 18.59999999999997655, 11.75000000001115552, -200.9999999999999432 ) ) ;
#95193=EDGE_CURVE ( 'NONE', #129423, #88113, #140774, .T. ) ;
#95196=CARTESIAN_POINT ( 'NONE',  ( -21.59142135623730852, 7.850000000011158718, -179.7499999999999716 ) ) ;
#95208=DIRECTION ( 'NONE',  ( 0.000000000000000000, 0.000000000000000000, -1.000000000000000000 ) ) ;
#95240=ORIENTED_EDGE ( 'NONE', *, *, #173448, .F. ) ;
#95249=AXIS2_PLACEMENT_3D ( 'NONE', #115311, #198706, #117877 ) ;
#95255=B_SPLINE_CURVE_WITH_KNOTS ( 'NONE', 3,
 ( #184370, #143961, #83944, #146518 ),
 .UNSPECIFIED., .F., .F.,
 ( 4, 4 ),
 ( 3.469446951953614189E-18, 0.0001058379652594853209 ),
 .UNSPECIFIED. ) ;
#95260=ADVANCED_FACE ( 'NONE', ( #124106 ), #82362, .T. ) ;
#95289=FACE_OUTER_BOUND ( 'NONE', #248900, .T. ) ;
#95311=ORIENTED_EDGE ( 'NONE', *, *, #93496, .T. ) ;
#95353=ORIENTED_EDGE ( 'NONE', *, *, #215703, .F. ) ;
#95383=CARTESIAN_POINT ( 'NONE',  ( 22.00411653889210584, 0.09903810579733299257, -160.2465571323595555 ) ) ;
#95406=CYLINDRICAL_SURFACE ( 'NONE', #107774, 0.09999999999999939493 ) ;
#95420=VERTEX_POINT ( 'NONE', #36584 ) ;
#95434=VERTEX_POINT ( 'NONE', #177376 ) ;
#95440=LINE ( 'NONE', #175036, #248847 ) ;
#95451=CARTESIAN_POINT ( 'NONE',  ( 21.07928932188134397, 1.115600667400684642E-11, -167.4999999999999716 ) ) ;
#95466=EDGE_CURVE ( 'NONE', #10380, #185627, #211887, .T. ) ;
#95470=CIRCLE ( 'NONE', #228758, 0.09999999999998898659 ) ;
#95496=CARTESIAN_POINT ( 'NONE',  ( 20.04142135391667168, 11.75000000001116263, -192.2025068656294309 ) ) ;
#95507=ORIENTED_EDGE ( 'NONE', *, *, #105555, .F. ) ;
#95538=CARTESIAN_POINT ( 'NONE',  ( -18.50000000000000000, -1.164121893230052995, -208.7148480855715604 ) ) ;
#95584=DIRECTION ( 'NONE',  ( 1.000000000000000000, 0.000000000000000000, 0.000000000000000000 ) ) ;
#95606=SPHERICAL_SURFACE ( 'NONE', #96856, 0.1000000000000000056 ) ;
#95624=VERTEX_POINT ( 'NONE', #183761 ) ;
#95636=ORIENTED_EDGE ( 'NONE', *, *, #45079, .T. ) ;
#95641=ADVANCED_FACE ( 'NONE', ( #220329 ), #161831, .T. ) ;
#95676=VERTEX_POINT ( 'NONE', #44260 ) ;
#95701=ORIENTED_EDGE ( 'NONE', *, *, #55422, .T. ) ;
#95703=CARTESIAN_POINT ( 'NONE',  ( -20.64999999999999858, 7.250000000011155521, -188.6499999999999488 ) ) ;
#95705=EDGE_CURVE ( 'NONE', #213950, #119397, #228455, .T. ) ;
#95794=FACE_OUTER_BOUND ( 'NONE', #152361, .T. ) ;
#95796=ORIENTED_EDGE ( 'NONE', *, *, #33740, .F. ) ;
#95826=CONICAL_SURFACE ( 'NONE', #166806, 4.299999999999970512, 0.7853981633974466137 ) ;
#95832=CARTESIAN_POINT ( 'NONE',  ( -22.59999999999999787, 11.64957080755595520, -167.3999999999999773 ) ) ;
#95838=ORIENTED_EDGE ( 'NONE', *, *, #7888, .F. ) ;
#95844=EDGE_CURVE ( 'NONE', #95048, #132728, #12845, .T. ) ;
#95861=ORIENTED_EDGE ( 'NONE', *, *, #152964, .F. ) ;
#95863=CARTESIAN_POINT ( 'NONE',  ( 21.87500000000000355, 9.750000000011153745, -179.8499999999999943 ) ) ;
#95887=EDGE_CURVE ( 'NONE', #12940, #99065, #74725, .T. ) ;
#95893=CIRCLE ( 'NONE', #162570, 0.09999999999999939493 ) ;
#95931=EDGE_CURVE ( 'NONE', #166220, #57378, #203686, .T. ) ;
#95939=LINE ( 'NONE', #234169, #151238 ) ;
#95944=EDGE_CURVE ( 'NONE', #129705, #117379, #253547, .T. ) ;
#95964=DIRECTION ( 'NONE',  ( 0.7071067811865475727, -0.7071067811865475727, 0.000000000000000000 ) ) ;
#95982=DIRECTION ( 'NONE',  ( 0.000000000000000000, 0.000000000000000000, -1.000000000000000000 ) ) ;
#95991=CARTESIAN_POINT ( 'NONE',  ( -18.50000000000000000, 9.150000000011157653, -188.6499999999999488 ) ) ;
#96027=CARTESIAN_POINT ( 'NONE',  ( -21.05000000000000071, -11.64999999998884306, -197.8999999999999773 ) ) ;
#96032=CARTESIAN_POINT ( 'NONE',  ( -23.25000000000000000, 2.600000000011156054, -180.7246219227620543 ) ) ;
#96073=CARTESIAN_POINT ( 'NONE',  ( 20.84999999999999432, -1.164121893230052995, -208.9148480855715775 ) ) ;
#96080=CARTESIAN_POINT ( 'NONE',  ( -23.15000000000000213, 4.350000000011156054, -179.6499999999999773 ) ) ;
#96081=TOROIDAL_SURFACE ( 'NONE', #250040, 11.65000000000000036, 0.1000000000000000056 ) ;
#96166=ADVANCED_FACE ( 'NONE', ( #127321 ), #204767, .T. ) ;
#96189=AXIS2_PLACEMENT_3D ( 'NONE', #67080, #113584, #13216 ) ;
#96220=EDGE_CURVE ( 'NONE', #239082, #77400, #152042, .T. ) ;
#96246=ORIENTED_EDGE ( 'NONE', *, *, #22907, .F. ) ;
#96262=DIRECTION ( 'NONE',  ( 0.000000000000000000, -1.000000000000000000, 0.000000000000000000 ) ) ;
#96272=DIRECTION ( 'NONE',  ( 1.000000000000000000, 7.304098846218135653E-16, 0.000000000000000000 ) ) ;
#96294=DIRECTION ( 'NONE',  ( 0.000000000000000000, 1.598721155460229520E-14, 1.000000000000000000 ) ) ;
#96298=AXIS2_PLACEMENT_3D ( 'NONE', #79204, #200456, #141751 ) ;
#96331=EDGE_CURVE ( 'NONE', #127614, #165621, #149732, .T. ) ;
#96336=B_SPLINE_CURVE_WITH_KNOTS ( 'NONE', 3,
 ( #242966, #64348, #59161, #218254, #39672, #111179, #185570 ),
 .UNSPECIFIED., .F., .F.,
 ( 4, 3, 4 ),
 ( 0.000000000000000000, 1.860045280646151707E-05, 5.251155757305330614E-05 ),
 .UNSPECIFIED. ) ;
#96337=CIRCLE ( 'NONE', #212895, 0.09999999999998898659 ) ;
#96377=CARTESIAN_POINT ( 'NONE',  ( 18.59999999999997655, 1.115600667400684642E-11, -208.8999999999999488 ) ) ;
#96389=CARTESIAN_POINT ( 'NONE',  ( -21.05000000000000071, -11.48912529306489994, -198.0999999999999659 ) ) ;
#96458=CARTESIAN_POINT ( 'NONE',  ( -18.59999999999999787, 7.021664781911246322, -204.7335654018972662 ) ) ;
#96470=ADVANCED_FACE ( 'NONE', ( #40560 ), #22257, .F. ) ;
#96480=CARTESIAN_POINT ( 'NONE',  ( 20.94999999999999929, -8.999999999988842703, -191.1060308773475072 ) ) ;
#96498=CYLINDRICAL_SURFACE ( 'NONE', #254040, 0.09999999999999817368 ) ;
#96532=DIRECTION ( 'NONE',  ( -4.408576920032448588E-17, 0.1350103645451876666, -0.9908441862701600211 ) ) ;
#96541=VERTEX_POINT ( 'NONE', #23565 ) ;
#96590=FACE_BOUND ( 'NONE', #29117, .T. ) ;
#96602=EDGE_LOOP ( 'NONE', ( #141548, #31315, #42776, #31561 ) ) ;
#96605=ADVANCED_FACE ( 'NONE', ( #203449 ), #178787, .T. ) ;
#96608=VERTEX_POINT ( 'NONE', #109458 ) ;
#96631=CARTESIAN_POINT ( 'NONE',  ( -20.54999999999999716, 1.940186915899004161, -188.1708807889466470 ) ) ;
#96649=ADVANCED_FACE ( 'NONE', ( #86023 ), #186455, .F. ) ;
#96651=AXIS2_PLACEMENT_3D ( 'NONE', #216521, #237378, #15793 ) ;
#96663=CARTESIAN_POINT ( 'NONE',  ( -20.85000000000000142, -1.164121893230052995, -208.9148480855715775 ) ) ;
#96692=CARTESIAN_POINT ( 'NONE',  ( -22.39999999999999858, 0.1000000000111554016, -159.7092204016265384 ) ) ;
#96703=DIRECTION ( 'NONE',  ( 0.000000000000000000, 0.000000000000000000, 1.000000000000000000 ) ) ;
#96723=VECTOR ( 'NONE', #115497, 1000.000000000000000 ) ;
#96736=AXIS2_PLACEMENT_3D ( 'NONE', #73966, #119486, #218549 ) ;
#96739=DIRECTION ( 'NONE',  ( 0.000000000000000000, -1.000000000000000000, 0.000000000000000000 ) ) ;
#96747=CARTESIAN_POINT ( 'NONE',  ( 18.49999999999999289, 10.32573593129922607, -192.3499999999999659 ) ) ;
#96751=LINE ( 'NONE', #232469, #229424 ) ;
#96785=TOROIDAL_SURFACE ( 'NONE', #213323, 6.258578643762712446, 0.1000000000000000056 ) ;
#96810=AXIS2_PLACEMENT_3D ( 'NONE', #79541, #59977, #139525 ) ;
#96822=CARTESIAN_POINT ( 'NONE',  ( -20.54999999999999716, 1.115600667400684642E-11, -167.4999999999999716 ) ) ;
#96839=ORIENTED_EDGE ( 'NONE', *, *, #75537, .F. ) ;
#96847=EDGE_CURVE ( 'NONE', #47818, #191501, #175063, .T. ) ;
#96856=AXIS2_PLACEMENT_3D ( 'NONE', #113889, #31819, #111330 ) ;
#96859=ORIENTED_EDGE ( 'NONE', *, *, #139444, .F. ) ;
#96880=AXIS2_PLACEMENT_3D ( 'NONE', #118414, #58394, #197923 ) ;
#96892=CARTESIAN_POINT ( 'NONE',  ( -23.25000000000000000, -8.596261682231835621, -176.9501275171502641 ) ) ;
#96900=ORIENTED_EDGE ( 'NONE', *, *, #191736, .T. ) ;
#96901=EDGE_CURVE ( 'NONE', #254691, #153829, #108551, .T. ) ;
#96910=VERTEX_POINT ( 'NONE', #121063 ) ;
#96959=EDGE_CURVE ( 'NONE', #117714, #95434, #145953, .T. ) ;
#96962=CARTESIAN_POINT ( 'NONE',  ( 23.25000000000000000, -11.64999999998883595, -197.8999999999999773 ) ) ;
#96982=VECTOR ( 'NONE', #200632, 1000.000000000000114 ) ;
#97019=ORIENTED_EDGE ( 'NONE', *, *, #56358, .T. ) ;
#97023=EDGE_CURVE ( 'NONE', #71184, #107478, #220965, .T. ) ;
#97030=ORIENTED_EDGE ( 'NONE', *, *, #170322, .F. ) ;
#97054=DIRECTION ( 'NONE',  ( 1.000000000000000000, -0.000000000000000000, -0.000000000000000000 ) ) ;
#97055=CARTESIAN_POINT ( 'NONE',  ( 21.05000000000000071, -0.09999999998884338825, -167.4999999999999716 ) ) ;
#97084=CARTESIAN_POINT ( 'NONE',  ( 20.95262331984772430, 10.50415726280109219, -175.0608883295932401 ) ) ;
#97106=CARTESIAN_POINT ( 'NONE',  ( 21.05000000000000071, -11.74999999998883560, -197.8999999999999773 ) ) ;
#97155=DIRECTION ( 'NONE',  ( 1.000000000000000000, 0.000000000000000000, -0.000000000000000000 ) ) ;
#97318=EDGE_CURVE ( 'NONE', #208842, #152772, #250842, .T. ) ;
#97364=ORIENTED_EDGE ( 'NONE', *, *, #10589, .F. ) ;
#97382=DIRECTION ( 'NONE',  ( 0.000000000000000000, 0.1350103645451876666, -0.9908441862701600211 ) ) ;
#97455=CARTESIAN_POINT ( 'NONE',  ( 18.59999999999996945, 10.33248238083634440, -206.5948465439131496 ) ) ;
#97461=AXIS2_PLACEMENT_3D ( 'NONE', #183420, #240826, #244658 ) ;
#97481=UNCERTAINTY_MEASURE_WITH_UNIT (LENGTH_MEASURE( 1.000000000000000082E-05 ), #129485, 'distance_accuracy_value', 'NONE');
#97499=AXIS2_PLACEMENT_3D ( 'NONE', #51972, #128973, #208521 ) ;
#97500=CYLINDRICAL_SURFACE ( 'NONE', #179791, 0.09999999999999939493 ) ;
#97549=CIRCLE ( 'NONE', #14412, 0.09999999999999363565 ) ;
#97625=ORIENTED_EDGE ( 'NONE', *, *, #148095, .F. ) ;
#97639=AXIS2_PLACEMENT_3D ( 'NONE', #254754, #172750, #216945 ) ;
#97642=ORIENTED_EDGE ( 'NONE', *, *, #241818, .T. ) ;
#97716=DIRECTION ( 'NONE',  ( 0.000000000000000000, 0.000000000000000000, -1.000000000000000000 ) ) ;
#97736=CIRCLE ( 'NONE', #106115, 0.5999999999999998668 ) ;
#97746=DIRECTION ( 'NONE',  ( 0.000000000000000000, 0.000000000000000000, -1.000000000000000000 ) ) ;
#97750=CARTESIAN_POINT ( 'NONE',  ( 21.04999999999998650, 6.650000000011155876, -179.7499999999999716 ) ) ;
#97751=VECTOR ( 'NONE', #248010, 1000.000000000000000 ) ;
#97822=VERTEX_POINT ( 'NONE', #108244 ) ;
#97824=CIRCLE ( 'NONE', #127074, 7.900000000000000355 ) ;
#97829=ORIENTED_EDGE ( 'NONE', *, *, #195457, .T. ) ;
#97845=DIRECTION ( 'NONE',  ( -1.000000000000000000, -2.952720810173289112E-16, 0.000000000000000000 ) ) ;
#97868=ORIENTED_EDGE ( 'NONE', *, *, #198556, .F. ) ;
#97896=EDGE_CURVE ( 'NONE', #70888, #185004, #180140, .T. ) ;
#97905=EDGE_CURVE ( 'NONE', #99065, #12940, #51088, .T. ) ;
#97907=CARTESIAN_POINT ( 'NONE',  ( 22.14074124539698829, 7.390077851054901892, -167.4009471041559038 ) ) ;
#97917=CARTESIAN_POINT ( 'NONE',  ( 21.07016717457012689, 1.115540062193308597E-11, -161.1790591618990618 ) ) ;
#97921=ORIENTED_EDGE ( 'NONE', *, *, #214884, .F. ) ;
#97925=ORIENTED_EDGE ( 'NONE', *, *, #120997, .F. ) ;
#97926=ORIENTED_EDGE ( 'NONE', *, *, #97896, .T. ) ;
#97940=ORIENTED_EDGE ( 'NONE', *, *, #8246, .T. ) ;
#97957=ORIENTED_EDGE ( 'NONE', *, *, #152458, .F. ) ;
#97974=CIRCLE ( 'NONE', #56291, 0.09999999999998898659 ) ;
#97992=CARTESIAN_POINT ( 'NONE',  ( -18.50000000000000000, 9.250000000011157297, -179.8499999999999943 ) ) ;
#98022=ADVANCED_FACE ( 'NONE', ( #23284 ), #121105, .T. ) ;
#98077=FACE_BOUND ( 'NONE', #238503, .T. ) ;
#98084=FACE_OUTER_BOUND ( 'NONE', #29143, .T. ) ;
#98091=EDGE_LOOP ( 'NONE', ( #142758, #150928, #145081, #83374 ) ) ;
#98116=( BOUNDED_SURFACE ( )  B_SPLINE_SURFACE ( 3, 2, ( 
 ( #19824, #132369, #211924 ),
 ( #58897, #93233, #170266 ),
 ( #249753, #33311, #252298 ),
 ( #73709, #51515, #131080 ),
 ( #112811, #139729, #39400 ),
 ( #191087, #219277, #177626 ),
 ( #12446, #216713, #60199 ),
 ( #192348, #232772, #217975 ) ),
 .UNSPECIFIED., .F., .F., .F. ) 
 B_SPLINE_SURFACE_WITH_KNOTS ( ( 4, 2, 2, 4 ),
 ( 3, 3 ),
 ( 0.0001723339234021422576, 0.0002782939632049988201, 0.0003842540030078554097, 0.0005961740826135685347 ),
 ( 0.000000000000000000, 1.000000000000000000 ),
 .UNSPECIFIED. ) 
 GEOMETRIC_REPRESENTATION_ITEM ( )  RATIONAL_B_SPLINE_SURFACE ( (
 ( 1.000000000000000000, 0.9504532311154454405, 1.000000000000000000),
 ( 1.000000000000000000, 0.9506023220707116028, 1.000000000000000000),
 ( 1.000000000000000000, 0.9395774818185572697, 1.000000000000000000),
 ( 1.000000000000000000, 0.9079328464643486862, 1.000000000000000000),
 ( 1.000000000000000000, 0.8875702416205991652, 1.000000000000000000),
 ( 1.000000000000000000, 0.8205919608039309310, 1.000000000000000000),
 ( 1.000000000000000000, 0.7666842783598621924, 1.000000000000000000),
 ( 1.000000000000000000, 0.7071067811865253683, 1.000000000000000000) ) ) 
 REPRESENTATION_ITEM ( '' )  SURFACE ( )  );
#98119=ORIENTED_EDGE ( 'NONE', *, *, #97905, .T. ) ;
#98151=EDGE_CURVE ( 'NONE', #112231, #190860, #163736, .T. ) ;
#98152=CARTESIAN_POINT ( 'NONE',  ( -20.54999999999999716, 2.000000000011154189, -187.7753780772378889 ) ) ;
#98172=ADVANCED_FACE ( 'NONE', ( #224007 ), #107919, .F. ) ;
#98175=ORIENTED_EDGE ( 'NONE', *, *, #171941, .T. ) ;
#98179=CARTESIAN_POINT ( 'NONE',  ( 23.24999999999999289, 11.65000000001116298, -193.9851942293460070 ) ) ;
#98199=EDGE_LOOP ( 'NONE', ( #82401, #152026, #151236, #116605 ) ) ;
#98201=ORIENTED_EDGE ( 'NONE', *, *, #83448, .T. ) ;
#98235=CIRCLE ( 'NONE', #2398, 0.09999999999998898659 ) ;
#98267=AXIS2_PLACEMENT_3D ( 'NONE', #191539, #113251, #153721 ) ;
#98276=CARTESIAN_POINT ( 'NONE',  ( -23.15000000000000213, 1.115600667400684642E-11, -203.0999999999999375 ) ) ;
#98280=CIRCLE ( 'NONE', #27459, 0.09999999999998898659 ) ;
#98314=EDGE_CURVE ( 'NONE', #215838, #169929, #67878, .T. ) ;
#98316=ORIENTED_EDGE ( 'NONE', *, *, #70841, .F. ) ;
#98324=DIRECTION ( 'NONE',  ( 0.000000000000000000, -0.000000000000000000, -1.000000000000000000 ) ) ;
#98326=LINE ( 'NONE', #74989, #54444 ) ;
#98329=VERTEX_POINT ( 'NONE', #56895 ) ;
#98371=CARTESIAN_POINT ( 'NONE',  ( 18.49999999999999289, 10.20857864377385127, -192.1499999999999488 ) ) ;
#98374=AXIS2_PLACEMENT_3D ( 'NONE', #90014, #69206, #170903 ) ;
#98408=EDGE_LOOP ( 'NONE', ( #157971, #105336, #2736, #243997 ) ) ;
#98440=DIRECTION ( 'NONE',  ( 0.000000000000000000, -0.000000000000000000, 1.000000000000000000 ) ) ;
#98450=ORIENTED_EDGE ( 'NONE', *, *, #225730, .T. ) ;
#98461=CARTESIAN_POINT ( 'NONE',  ( 21.05000000000000071, 8.776282895303632259, -167.4999999999999716 ) ) ;
#98488=AXIS2_PLACEMENT_3D ( 'NONE', #213463, #195221, #175641 ) ;
#98496=AXIS2_PLACEMENT_3D ( 'NONE', #58145, #215943, #218499 ) ;
#98520=EDGE_CURVE ( 'NONE', #33688, #145192, #120783, .T. ) ;
#98525=ADVANCED_FACE ( 'NONE', ( #43791 ), #256347, .T. ) ;
#98570=EDGE_LOOP ( 'NONE', ( #52452, #230176 ) ) ;
#98588=ORIENTED_EDGE ( 'NONE', *, *, #179140, .F. ) ;
#98600=FACE_OUTER_BOUND ( 'NONE', #50109, .T. ) ;
#98625=AXIS2_PLACEMENT_3D ( 'NONE', #125311, #24944, #103149 ) ;
#98654=ORIENTED_EDGE ( 'NONE', *, *, #185441, .F. ) ;
#98673=CARTESIAN_POINT ( 'NONE',  ( 23.15000000000000213, -8.999999999988842703, -191.1060308773475072 ) ) ;
#98681=ORIENTED_EDGE ( 'NONE', *, *, #161398, .T. ) ;
#98726=CARTESIAN_POINT ( 'NONE',  ( 18.59999999999999432, -1.162701749926853712, -175.5999999999999659 ) ) ;
#98774=CARTESIAN_POINT ( 'NONE',  ( 20.74625933824108870, 8.882913521095431975, -176.0551710241120418 ) ) ;
#98786=CARTESIAN_POINT ( 'NONE',  ( -23.15000000000000213, 4.150000000011156764, -179.8499999999999943 ) ) ;
#98804=EDGE_CURVE ( 'NONE', #250208, #178866, #8985, .T. ) ;
#98808=CARTESIAN_POINT ( 'NONE',  ( -21.14999999999999858, -0.09999999998884338825, -160.9593430482987344 ) ) ;
#98829=EDGE_LOOP ( 'NONE', ( #805, #132543, #105882 ) ) ;
#98835=FACE_OUTER_BOUND ( 'NONE', #58276, .T. ) ;
#98846=EDGE_CURVE ( 'NONE', #22594, #129337, #114147, .T. ) ;
#98856=EDGE_CURVE ( 'NONE', #19120, #195524, #100532, .T. ) ;
#98860=ORIENTED_EDGE ( 'NONE', *, *, #106647, .T. ) ;
#98861=EDGE_CURVE ( 'NONE', #16613, #100689, #179691, .T. ) ;
#98888=CARTESIAN_POINT ( 'NONE',  ( 23.15000000000000213, -11.74999999998883737, -188.8499999999999659 ) ) ;
#98920=EDGE_CURVE ( 'NONE', #57491, #96608, #233845, .T. ) ;
#98925=CYLINDRICAL_SURFACE ( 'NONE', #18103, 11.80000000000000426 ) ;
#98937=DIRECTION ( 'NONE',  ( 0.000000000000000000, -0.8660254037844411501, -0.4999999999999956146 ) ) ;
#98965=DIRECTION ( 'NONE',  ( 0.000000000000000000, 0.000000000000000000, -1.000000000000000000 ) ) ;
#98987=CARTESIAN_POINT ( 'NONE',  ( -23.25000000000000000, 1.115650265596050101E-11, -163.4499999999999886 ) ) ;
#98990=CIRCLE ( 'NONE', #49119, 0.1000000000000001860 ) ;
#99000=EDGE_CURVE ( 'NONE', #164666, #29202, #142565, .T. ) ;
#99004=DIRECTION ( 'NONE',  ( 0.000000000000000000, -0.9908441862701782288, -0.1350103645450542456 ) ) ;
#99007=FACE_OUTER_BOUND ( 'NONE', #94162, .T. ) ;
#99020=AXIS2_PLACEMENT_3D ( 'NONE', #15174, #95964, #52995 ) ;
#99041=CARTESIAN_POINT ( 'NONE',  ( -21.44999999999999929, 7.250000000011155521, -188.6499999999999488 ) ) ;
#99049=TOROIDAL_SURFACE ( 'NONE', #111550, 0.2000000000000000111, 0.1000000000000000056 ) ;
#99051=FACE_OUTER_BOUND ( 'NONE', #167837, .T. ) ;
#99061=FACE_OUTER_BOUND ( 'NONE', #44840, .T. ) ;
#99065=VERTEX_POINT ( 'NONE', #228556 ) ;
#99080=DIRECTION ( 'NONE',  ( 1.000000000000000000, -0.000000000000000000, -0.000000000000000000 ) ) ;
#99102=LINE ( 'NONE', #17, #76555 ) ;
#99139=ORIENTED_EDGE ( 'NONE', *, *, #2397, .T. ) ;
#99158=VECTOR ( 'NONE', #133222, 1000.000000000000000 ) ;
#99175=AXIS2_PLACEMENT_3D ( 'NONE', #202721, #98440, #118050 ) ;
#99207=ORIENTED_EDGE ( 'NONE', *, *, #67026, .F. ) ;
#99215=CARTESIAN_POINT ( 'NONE',  ( -21.09096482362080138, 0.03944827878515646397, -161.1364556345951655 ) ) ;
#99259=TOROIDAL_SURFACE ( 'NONE', #249142, 3.899999999999999467, 0.1000000000000000056 ) ;
#99286=VERTEX_POINT ( 'NONE', #110526 ) ;
#99394=AXIS2_PLACEMENT_3D ( 'NONE', #10757, #130690, #225911 ) ;
#99415=DIRECTION ( 'NONE',  ( 1.000000000000000000, 0.000000000000000000, -0.000000000000000000 ) ) ;
#99418=ORIENTED_EDGE ( 'NONE', *, *, #49750, .T. ) ;
#99450=EDGE_CURVE ( 'NONE', #208426, #82909, #133497, .T. ) ;
#99466=ORIENTED_EDGE ( 'NONE', *, *, #188313, .T. ) ;
#99475=EDGE_CURVE ( 'NONE', #36019, #233212, #92241, .T. ) ;
#99492=AXIS2_PLACEMENT_3D ( 'NONE', #145936, #24751, #143376 ) ;
#99505=ORIENTED_EDGE ( 'NONE', *, *, #50722, .T. ) ;
#99520=ORIENTED_EDGE ( 'NONE', *, *, #21293, .F. ) ;
#99579=VERTEX_POINT ( 'NONE', #23016 ) ;
#99604=EDGE_CURVE ( 'NONE', #16272, #117714, #240761, .T. ) ;
#99611=CIRCLE ( 'NONE', #78773, 2.099999999999990763 ) ;
#99628=ORIENTED_EDGE ( 'NONE', *, *, #218929, .T. ) ;
#99639=CARTESIAN_POINT ( 'NONE',  ( 23.24999999999997513, 11.65000000001116298, -193.9851942293460070 ) ) ;
#99646=EDGE_CURVE ( 'NONE', #87279, #215011, #175405, .T. ) ;
#99653=VECTOR ( 'NONE', #186, 1000.000000000000000 ) ;
#99665=CARTESIAN_POINT ( 'NONE',  ( 21.05000000000000071, 10.56271494673944211, -174.9568021056444138 ) ) ;
#99672=DIRECTION ( 'NONE',  ( 1.000000000000000000, -0.000000000000000000, -0.000000000000000000 ) ) ;
#99685=CARTESIAN_POINT ( 'NONE',  ( -18.59999999999999787, -9.321008403350132809, -174.7359382490778614 ) ) ;
#99689=CARTESIAN_POINT ( 'NONE',  ( 20.94999999999999574, 10.47338541492405994, -175.0786544642485012 ) ) ;
#99712=ORIENTED_EDGE ( 'NONE', *, *, #38475, .F. ) ;
#99720=CIRCLE ( 'NONE', #16564, 12.87499999999999822 ) ;
#99763=COLOUR_RGB ( '', 0.09019608, 0.27058824, 0.51372549) ;
#99788=CIRCLE ( 'NONE', #45663, 0.09999999999999939493 ) ;
#99804=DIRECTION ( 'NONE',  ( 1.000000000000000000, 0.000000000000000000, 0.000000000000000000 ) ) ;
#99819=ORIENTED_EDGE ( 'NONE', *, *, #129594, .T. ) ;
#99846=DIRECTION ( 'NONE',  ( 0.000000000000000000, 0.000000000000000000, -1.000000000000000000 ) ) ;
#99873=CARTESIAN_POINT ( 'NONE',  ( 21.05000000000000071, -11.48912529306490349, -170.3999999999999773 ) ) ;
#99883=CARTESIAN_POINT ( 'NONE',  ( 20.12500000000000355, 9.258049272928479567, -175.8633388371424076 ) ) ;
#99887=CARTESIAN_POINT ( 'NONE',  ( -20.85000000000000142, 1.115600667400684642E-11, -200.9999999999999432 ) ) ;
#99890=EDGE_LOOP ( 'NONE', ( #21561, #43426, #83466, #199111 ) ) ;
#99904=ORIENTED_EDGE ( 'NONE', *, *, #685, .F. ) ;
#99923=CARTESIAN_POINT ( 'NONE',  ( -18.59999999999999787, -1.637172712959223952, -179.0821533654719815 ) ) ;
#99926=CARTESIAN_POINT ( 'NONE',  ( -22.59999999999999787, 11.74987124438766273, -167.4345704089863034 ) ) ;
#99933=DIRECTION ( 'NONE',  ( 0.000000000000000000, 1.000000000000000000, 2.891205793294679805E-16 ) ) ;
#99935=EDGE_LOOP ( 'NONE', ( #156613, #222023, #141775, #147171 ) ) ;
#99958=FACE_OUTER_BOUND ( 'NONE', #210842, .T. ) ;
#100000=ORIENTED_EDGE ( 'NONE', *, *, #22946, .F. ) ;
#100045=EDGE_CURVE ( 'NONE', #215705, #70620, #25551, .T. ) ;
#100059=ORIENTED_EDGE ( 'NONE', *, *, #60433, .T. ) ;
#100100=DIRECTION ( 'NONE',  ( 0.000000000000000000, 0.000000000000000000, 1.000000000000000000 ) ) ;
#100125=CARTESIAN_POINT ( 'NONE',  ( -20.64999999999999858, 4.250000000011156409, -179.8499999999999943 ) ) ;
#100144=CIRCLE ( 'NONE', #91800, 0.09999999999999939493 ) ;
#100146=VECTOR ( 'NONE', #74015, 1000.000000000000000 ) ;
#100176=EDGE_LOOP ( 'NONE', ( #50720, #121179, #200515, #146539 ) ) ;
#100177=CARTESIAN_POINT ( 'NONE',  ( 23.15000000000000213, -11.64999999998883595, -197.9999999999999432 ) ) ;
#100183=DIRECTION ( 'NONE',  ( -1.000000000000000000, 0.000000000000000000, 0.000000000000000000 ) ) ;
#100184=ORIENTED_EDGE ( 'NONE', *, *, #5843, .T. ) ;
#100190=ORIENTED_EDGE ( 'NONE', *, *, #182228, .T. ) ;
#100214=VERTEX_POINT ( 'NONE', #65648 ) ;
#100249=FACE_OUTER_BOUND ( 'NONE', #215985, .T. ) ;
#100254=ADVANCED_FACE ( 'NONE', ( #228312 ), #50917, .T. ) ;
#100293=CARTESIAN_POINT ( 'NONE',  ( 22.50000000000000000, 7.790779598384538929, -167.3999999999999773 ) ) ;
#100310=DIRECTION ( 'NONE',  ( -1.000000000000000000, 3.469446951953635015E-14, 0.000000000000000000 ) ) ;
#100323=CYLINDRICAL_SURFACE ( 'NONE', #163380, 0.09999999999998898659 ) ;
#100325=CARTESIAN_POINT ( 'NONE',  ( 23.15000000000000213, -11.48912529306489994, -197.9999999999999432 ) ) ;
#100349=CARTESIAN_POINT ( 'NONE',  ( -23.15000000000000213, 11.65000000001115588, -179.6499999999999773 ) ) ;
#100357=ADVANCED_FACE ( 'NONE', ( #6676 ), #245304, .F. ) ;
#100368=CARTESIAN_POINT ( 'NONE',  ( 23.14999999999999503, 11.65000000001116298, -193.9851942293460070 ) ) ;
#100381=LINE ( 'NONE', #80824, #15951 ) ;
#100392=AXIS2_PLACEMENT_3D ( 'NONE', #94624, #13816, #229022 ) ;
#100400=DIRECTION ( 'NONE',  ( -1.000000000000000000, 0.000000000000000000, 0.000000000000000000 ) ) ;
#100403=CYLINDRICAL_SURFACE ( 'NONE', #96651, 0.09999999999998898659 ) ;
#100430=CARTESIAN_POINT ( 'NONE',  ( -21.93642651522410247, 7.327166239336959208, -167.4999999999999716 ) ) ;
#100439=VERTEX_POINT ( 'NONE', #13118 ) ;
#100441=ORIENTED_EDGE ( 'NONE', *, *, #72612, .T. ) ;
#100457=DIRECTION ( 'NONE',  ( 0.000000000000000000, 1.000000000000000000, 2.891205793294679805E-16 ) ) ;
#100476=ORIENTED_EDGE ( 'NONE', *, *, #6385, .F. ) ;
#100479=CARTESIAN_POINT ( 'NONE',  ( 22.42357213249528769, 7.672932386371071445, -167.4009130359983999 ) ) ;
#100511=FACE_OUTER_BOUND ( 'NONE', #228470, .T. ) ;
#100532=CIRCLE ( 'NONE', #217244, 11.89999999999999325 ) ;
#100533=EDGE_CURVE ( 'NONE', #69026, #233212, #79859, .T. ) ;
#100571=DIRECTION ( 'NONE',  ( 0.000000000000000000, 0.000000000000000000, -1.000000000000000000 ) ) ;
#100595=CARTESIAN_POINT ( 'NONE',  ( 18.59999999999999787, -11.74999999998883737, -192.3499999999999659 ) ) ;
#100630=AXIS2_PLACEMENT_3D ( 'NONE', #20615, #100100, #194122 ) ;
#100659=ADVANCED_FACE ( 'NONE', ( #174162 ), #188391, .T. ) ;
#100662=ADVANCED_FACE ( 'NONE', ( #133698 ), #54152, .T. ) ;
#100681=CARTESIAN_POINT ( 'NONE',  ( -1.739115166359751801E-14, 11.65000000001114699, -179.7499999999999716 ) ) ;
#100685=ORIENTED_EDGE ( 'NONE', *, *, #168237, .T. ) ;
#100689=VERTEX_POINT ( 'NONE', #73755 ) ;
#100691=CARTESIAN_POINT ( 'NONE',  ( 18.49351773456767134, -9.443025695134084074, -174.6853255260267872 ) ) ;
#100696=EDGE_CURVE ( 'NONE', #171236, #191879, #150996, .T. ) ;
#100718=EDGE_LOOP ( 'NONE', ( #256993, #100685, #236488 ) ) ;
#100729=DIRECTION ( 'NONE',  ( 0.000000000000000000, -1.000000000000000000, 0.000000000000000000 ) ) ;
#100735=FACE_OUTER_BOUND ( 'NONE', #113760, .T. ) ;
#100746=ORIENTED_EDGE ( 'NONE', *, *, #219347, .F. ) ;
#100755=ADVANCED_FACE ( 'NONE', ( #253628 ), #154583, .T. ) ;
#100764=EDGE_CURVE ( 'NONE', #147015, #22594, #171875, .T. ) ;
#100765=DIRECTION ( 'NONE',  ( 0.000000000000000000, -0.8660254037844383745, 0.5000000000000003331 ) ) ;
#100789=CARTESIAN_POINT ( 'NONE',  ( -21.05000000000000071, 5.900000000011102586, -177.7190997646563915 ) ) ;
#100801=ADVANCED_FACE ( 'NONE', ( #198803 ), #96785, .T. ) ;
#100805=AXIS2_PLACEMENT_3D ( 'NONE', #37179, #17580, #257427 ) ;
#100839=CARTESIAN_POINT ( 'NONE',  ( -18.56579813702276027, 10.33025634372637569, -206.5870929282638429 ) ) ;
#100867=ADVANCED_FACE ( 'NONE', ( #202659 ), #106104, .T. ) ;
#100870=ORIENTED_EDGE ( 'NONE', *, *, #78522, .T. ) ;
#100898=ORIENTED_EDGE ( 'NONE', *, *, #194184, .F. ) ;
#100925=CARTESIAN_POINT ( 'NONE',  ( 21.05000000000000071, 10.48459288120550070, -174.9567135705834460 ) ) ;
#100948=CARTESIAN_POINT ( 'NONE',  ( 20.95265033839679347, 10.51225083247831371, -175.0657637560299236 ) ) ;
#100965=CARTESIAN_POINT ( 'NONE',  ( 18.59999999999997655, -1.164121893230052995, -208.9148480855715775 ) ) ;
#100979=EDGE_CURVE ( 'NONE', #152772, #140846, #30386, .T. ) ;
#100980=CIRCLE ( 'NONE', #55204, 0.1000000000000096922 ) ;
#100985=ADVANCED_FACE ( 'NONE', ( #87826 ), #167416, .F. ) ;
#100991=ADVANCED_FACE ( 'NONE', ( #252061 ), #250775, .T. ) ;
#101088=CARTESIAN_POINT ( 'NONE',  ( -23.15000000000000213, 11.75000000001115552, -179.7499999999999716 ) ) ;
#101098=ORIENTED_EDGE ( 'NONE', *, *, #398, .F. ) ;
#101130=AXIS2_PLACEMENT_3D ( 'NONE', #153520, #251267, #133896 ) ;
#101135=AXIS2_PLACEMENT_3D ( 'NONE', #218453, #238028, #221029 ) ;
#101139=DIRECTION ( 'NONE',  ( 0.000000000000000000, 0.2605042016806715099, 0.9654727137038706664 ) ) ;
#101144=DIRECTION ( 'NONE',  ( 0.000000000000000000, 0.000000000000000000, -1.000000000000000000 ) ) ;
#101147=TOROIDAL_SURFACE ( 'NONE', #188508, 0.2000000000000000111, 0.1000000000000000056 ) ;
#101159=CYLINDRICAL_SURFACE ( 'NONE', #243386, 0.09999999999999939493 ) ;
#101194=CARTESIAN_POINT ( 'NONE',  ( -22.57320508075687115, 11.75000000001115552, -167.4999999999999716 ) ) ;
#101350=ORIENTED_EDGE ( 'NONE', *, *, #187712, .T. ) ;
#101379=EDGE_CURVE ( 'NONE', #214529, #147404, #13156, .T. ) ;
#101411=DIRECTION ( 'NONE',  ( 0.000000000000000000, 0.000000000000000000, -1.000000000000000000 ) ) ;
#101445=CARTESIAN_POINT ( 'NONE',  ( 20.94999999999999929, 10.72371710471867701, -188.7499999999999716 ) ) ;
#101457=EDGE_CURVE ( 'NONE', #235213, #145941, #131804, .T. ) ;
#101462=CARTESIAN_POINT ( 'NONE',  ( 23.14999999999999858, 1.115600667400684642E-11, -200.9999999999999432 ) ) ;
#101476=DIRECTION ( 'NONE',  ( 1.000000000000000000, -0.000000000000000000, -0.000000000000000000 ) ) ;
#101502=ORIENTED_EDGE ( 'NONE', *, *, #158983, .F. ) ;
#101535=EDGE_LOOP ( 'NONE', ( #222283, #135377, #198912, #239340 ) ) ;
#101543=AXIS2_PLACEMENT_3D ( 'NONE', #162894, #23389, #239847 ) ;
#101557=AXIS2_PLACEMENT_3D ( 'NONE', #251072, #188544, #171581 ) ;
#101561=( BOUNDED_SURFACE ( )  B_SPLINE_SURFACE ( 3, 2, ( 
 ( #86823, #162557, #184654 ),
 ( #123412, #163826, #245930 ),
 ( #144232, #64714, #122132 ),
 ( #202939, #161268, #204219 ),
 ( #141679, #24329, #62157 ),
 ( #206798, #25602, #223776 ) ),
 .UNSPECIFIED., .F., .F., .F. ) 
 B_SPLINE_SURFACE_WITH_KNOTS ( ( 4, 2, 4 ),
 ( 3, 3 ),
 ( 3.141592653589793116, 3.926990816987241395, 4.712388980384689674 ),
 ( 0.000000000000000000, 1.000000000000000000 ),
 .UNSPECIFIED. ) 
 GEOMETRIC_REPRESENTATION_ITEM ( )  RATIONAL_B_SPLINE_SURFACE ( (
 ( 1.000000000000000000, 0.9238795325112820755, 1.000000000000000000),
 ( 1.000000000000000000, 0.9240297172239192447, 1.000000000000000000),
 ( 1.000000000000000000, 0.9038128468044981378, 1.000000000000000000),
 ( 1.000000000000000000, 0.8282379607644450026, 1.000000000000000000),
 ( 1.000000000000000000, 0.7727932973495568181, 1.000000000000000000),
 ( 1.000000000000000000, 0.7071067811864494290, 1.000000000000000000) ) ) 
 REPRESENTATION_ITEM ( '' )  SURFACE ( )  );
#101569=CIRCLE ( 'NONE', #89132, 0.09999999999998898659 ) ;
#101570=EDGE_CURVE ( 'NONE', #76299, #122995, #113748, .T. ) ;
#101575=ORIENTED_EDGE ( 'NONE', *, *, #85405, .T. ) ;
#101577=DIRECTION ( 'NONE',  ( -1.000000000000000000, -0.000000000000000000, -0.000000000000000000 ) ) ;
#101580=FACE_OUTER_BOUND ( 'NONE', #59207, .T. ) ;
#101596=CYLINDRICAL_SURFACE ( 'NONE', #245341, 0.09999999999999939493 ) ;
#101597=EDGE_CURVE ( 'NONE', #135643, #138430, #1307, .T. ) ;
#101604=VECTOR ( 'NONE', #79609, 1000.000000000000000 ) ;
#101617=CARTESIAN_POINT ( 'NONE',  ( 23.25000000000000000, -11.74999999998883560, -155.7499999999999716 ) ) ;
#101645=EDGE_CURVE ( 'NONE', #149929, #5997, #30755, .T. ) ;
#101651=CIRCLE ( 'NONE', #139063, 0.1000000000000002554 ) ;
#101666=CIRCLE ( 'NONE', #172485, 0.09999999999999817368 ) ;
#101706=DIRECTION ( 'NONE',  ( 1.000000000000000000, -0.000000000000000000, -0.000000000000000000 ) ) ;
#101708=AXIS2_PLACEMENT_3D ( 'NONE', #202667, #104816, #168737 ) ;
#101727=DIRECTION ( 'NONE',  ( -0.000000000000000000, -2.891205793294679805E-16, 1.000000000000000000 ) ) ;
#101763=DIRECTION ( 'NONE',  ( 0.000000000000000000, 1.000000000000000000, 2.891205793294679805E-16 ) ) ;
#101774=DIRECTION ( 'NONE',  ( 1.734723475976817507E-14, 0.000000000000000000, -1.000000000000000000 ) ) ;
#101818=AXIS2_PLACEMENT_3D ( 'NONE', #184906, #225288, #63667 ) ;
#101843=EDGE_CURVE ( 'NONE', #56940, #138993, #43217, .T. ) ;
#101848=CIRCLE ( 'NONE', #122561, 0.1000000000000089567 ) ;
#101858=CIRCLE ( 'NONE', #10123, 0.09999999999999817368 ) ;
#101869=CARTESIAN_POINT ( 'NONE',  ( 18.47688499308725696, -9.464855950272969665, -207.7013477531374406 ) ) ;
#101875=VECTOR ( 'NONE', #55794, 1000.000000000000000 ) ;
#101917=CARTESIAN_POINT ( 'NONE',  ( 22.39999999999999858, 0.1000000000111554016, -159.7092204016265669 ) ) ;
#101986=AXIS2_PLACEMENT_3D ( 'NONE', #47020, #87438, #211254 ) ;
#102005=ORIENTED_EDGE ( 'NONE', *, *, #46092, .T. ) ;
#102033=DIRECTION ( 'NONE',  ( 0.000000000000000000, 0.000000000000000000, -1.000000000000000000 ) ) ;
#102035=CIRCLE ( 'NONE', #235327, 11.80000000000000426 ) ;
#102043=ADVANCED_FACE ( 'NONE', ( #137894 ), #217427, .F. ) ;
#102099=EDGE_CURVE ( 'NONE', #54306, #50212, #105892, .T. ) ;
#102108=DIRECTION ( 'NONE',  ( 0.000000000000000000, -1.000000000000000000, 0.000000000000000000 ) ) ;
#102136=CARTESIAN_POINT ( 'NONE',  ( -18.58222699835055280, 10.33200063080771969, -206.5931674956642610 ) ) ;
#102149=EDGE_CURVE ( 'NONE', #59445, #224509, #214073, .T. ) ;
#102179=DIRECTION ( 'NONE',  ( 1.000000000000000000, 1.875376730785737719E-16, 0.000000000000000000 ) ) ;
#102204=DIRECTION ( 'NONE',  ( 1.000000000000000000, 2.952720810173289112E-16, -0.000000000000000000 ) ) ;
#102211=CARTESIAN_POINT ( 'NONE',  ( -20.94999999999999929, -1.835341550213255957, -179.0551512925629538 ) ) ;
#102214=CARTESIAN_POINT ( 'NONE',  ( 21.09706851349342216, 8.775842513484549912, -179.7355662163996328 ) ) ;
#102229=CIRCLE ( 'NONE', #110646, 0.09999999999999817368 ) ;
#102237=CARTESIAN_POINT ( 'NONE',  ( -23.15000000000000213, -9.599999999988844124, -155.7499999999999716 ) ) ;
#102248=CARTESIAN_POINT ( 'NONE',  ( 20.95496329884391784, 10.56743320610419623, -175.0743099322847911 ) ) ;
#102262=EDGE_CURVE ( 'NONE', #168057, #133004, #205876, .T. ) ;
#102277=ADVANCED_FACE ( 'NONE', ( #9954, #169070 ), #45228, .T. ) ;
#102392=CARTESIAN_POINT ( 'NONE',  ( -20.94999999999999929, 1.835341550235569663, -179.0551512925629538 ) ) ;
#102413=DIRECTION ( 'NONE',  ( 0.000000000000000000, 0.000000000000000000, -1.000000000000000000 ) ) ;
#102496=CARTESIAN_POINT ( 'NONE',  ( -21.05000000000000071, 1.115650877919449575E-11, -205.0999999999999375 ) ) ;
#102524=VERTEX_POINT ( 'NONE', #240261 ) ;
#102533=DIRECTION ( 'NONE',  ( 0.000000000000000000, 0.000000000000000000, -1.000000000000000000 ) ) ;
#102552=VECTOR ( 'NONE', #168132, 1000.000000000000000 ) ;
#102589=ORIENTED_EDGE ( 'NONE', *, *, #172270, .F. ) ;
#102595=CIRCLE ( 'NONE', #152925, 0.1000000000000096922 ) ;
#102620=CARTESIAN_POINT ( 'NONE',  ( -20.94999999999999929, 11.65000000001115232, -194.2161343370218560 ) ) ;
#102626=ORIENTED_EDGE ( 'NONE', *, *, #111611, .T. ) ;
#102631=EDGE_LOOP ( 'NONE', ( #202513, #224363, #77981, #41296 ) ) ;
#102686=ADVANCED_FACE ( 'NONE', ( #95289 ), #174884, .T. ) ;
#102698=CARTESIAN_POINT ( 'NONE',  ( 21.14999999999999503, 11.75000000001115552, -167.4999999999999716 ) ) ;
#102723=ORIENTED_EDGE ( 'NONE', *, *, #173967, .F. ) ;
#102725=CARTESIAN_POINT ( 'NONE',  ( -23.15000000000000213, 2.000000000011154189, -187.7753780772378889 ) ) ;
#102748=CIRCLE ( 'NONE', #85997, 0.5999999999999894307 ) ;
#102750=EDGE_LOOP ( 'NONE', ( #124273, #230725, #28247, #124382 ) ) ;
#102754=ORIENTED_EDGE ( 'NONE', *, *, #11070, .F. ) ;
#102755=ORIENTED_EDGE ( 'NONE', *, *, #179759, .F. ) ;
#102785=FACE_OUTER_BOUND ( 'NONE', #216247, .T. ) ;
#102800=CARTESIAN_POINT ( 'NONE',  ( 18.54271179734040942, -9.624084290087520088, -207.7409648527003299 ) ) ;
#102805=VERTEX_POINT ( 'NONE', #198234 ) ;
#102817=CARTESIAN_POINT ( 'NONE',  ( -21.07928932188134041, 6.328516656409858498, -167.4011048543453342 ) ) ;
#102880=ADVANCED_FACE ( 'NONE', ( #203384 ), #164571, .T. ) ;
#102900=DIRECTION ( 'NONE',  ( 1.000000000000000000, -0.000000000000000000, -0.000000000000000000 ) ) ;
#102991=DIRECTION ( 'NONE',  ( 1.000000000000000000, -0.000000000000000000, -0.000000000000000000 ) ) ;
#102994=DIRECTION ( 'NONE',  ( -1.000000000000000000, 0.000000000000000000, 0.000000000000000000 ) ) ;
#103010=CARTESIAN_POINT ( 'NONE',  ( -21.70464131381649509, 7.095358018979010417, -167.4999999999999716 ) ) ;
#103030=EDGE_CURVE ( 'NONE', #48880, #252796, #11612, .T. ) ;
#103077=CYLINDRICAL_SURFACE ( 'NONE', #156442, 0.09999999999999939493 ) ;
#103084=ORIENTED_EDGE ( 'NONE', *, *, #91757, .F. ) ;
#103095=EDGE_LOOP ( 'NONE', ( #44039, #157981, #166285, #257262 ) ) ;
#103128=FACE_OUTER_BOUND ( 'NONE', #98829, .T. ) ;
#103149=DIRECTION ( 'NONE',  ( 0.000000000000000000, -1.000000000000000000, 0.000000000000000000 ) ) ;
#103155=DIRECTION ( 'NONE',  ( 0.000000000000000000, 0.9915357197604971473, -0.1298341882519111479 ) ) ;
#103174=VERTEX_POINT ( 'NONE', #135374 ) ;
#103176=EDGE_CURVE ( 'NONE', #234175, #236406, #31320, .T. ) ;
#103201=VERTEX_POINT ( 'NONE', #136656 ) ;
#103204=DIRECTION ( 'NONE',  ( 4.408576920032447355E-17, -0.1350103645451876666, -0.9908441862701600211 ) ) ;
#103206=DIRECTION ( 'NONE',  ( -0.000000000000000000, 0.000000000000000000, 1.000000000000000000 ) ) ;
#103220=DIRECTION ( 'NONE',  ( -1.000000000000000000, -0.000000000000000000, -0.000000000000000000 ) ) ;
#103222=EDGE_CURVE ( 'NONE', #238413, #237228, #143876, .T. ) ;
#103228=DIRECTION ( 'NONE',  ( 1.000000000000000000, 0.000000000000000000, 0.000000000000000000 ) ) ;
#103258=CIRCLE ( 'NONE', #249042, 0.09999999999999939493 ) ;
#103303=LINE ( 'NONE', #86298, #122916 ) ;
#103344=ORIENTED_EDGE ( 'NONE', *, *, #22129, .T. ) ;
#103358=AXIS2_PLACEMENT_3D ( 'NONE', #208609, #226863, #27426 ) ;
#103388=VECTOR ( 'NONE', #199777, 1000.000000000000000 ) ;
#103401=EDGE_CURVE ( 'NONE', #145808, #154503, #81488, .T. ) ;
#103454=AXIS2_PLACEMENT_3D ( 'NONE', #142166, #101727, #61349 ) ;
#103504=FACE_OUTER_BOUND ( 'NONE', #249531, .T. ) ;
#103506=DIRECTION ( 'NONE',  ( 0.000000000000000000, -1.000000000000000000, 0.000000000000000000 ) ) ;
#103523=LINE ( 'NONE', #83927, #40683 ) ;
#103526=DIRECTION ( 'NONE',  ( 1.000000000000000000, 2.952720810173289112E-16, -0.000000000000000000 ) ) ;
#103531=CARTESIAN_POINT ( 'NONE',  ( 21.12769345151713196, 10.71928767695172624, -179.7474803461974489 ) ) ;
#103534=DIRECTION ( 'NONE',  ( -1.000000000000000000, -3.265361837132813093E-16, 0.000000000000000000 ) ) ;
#103586=DIRECTION ( 'NONE',  ( 1.441126678808781001E-14, 0.9876197685951252359, 0.1568667991644863424 ) ) ;
#103620=VECTOR ( 'NONE', #75252, 1000.000000000000000 ) ;
#103641=VERTEX_POINT ( 'NONE', #178077 ) ;
#103683=CYLINDRICAL_SURFACE ( 'NONE', #39846, 0.09999999999999817368 ) ;
#103690=FACE_OUTER_BOUND ( 'NONE', #135799, .T. ) ;
#103729=ORIENTED_EDGE ( 'NONE', *, *, #239841, .F. ) ;
#103738=ORIENTED_EDGE ( 'NONE', *, *, #109596, .F. ) ;
#103748=DIRECTION ( 'NONE',  ( 0.000000000000000000, 0.000000000000000000, -1.000000000000000000 ) ) ;
#103815=EDGE_CURVE ( 'NONE', #71995, #69705, #209167, .T. ) ;
#103835=CARTESIAN_POINT ( 'NONE',  ( 23.25000000000000000, -8.596261682231833845, -176.9501275171502641 ) ) ;
#103869=FACE_OUTER_BOUND ( 'NONE', #47519, .T. ) ;
#103890=AXIS2_PLACEMENT_3D ( 'NONE', #34957, #58307, #174487 ) ;
#103892=VECTOR ( 'NONE', #182634, 1000.000000000000000 ) ;
#103901=VERTEX_POINT ( 'NONE', #93067 ) ;
#103921=CARTESIAN_POINT ( 'NONE',  ( 20.21567752745019320, 10.19811410124265905, -175.3826203476516241 ) ) ;
#103983=CARTESIAN_POINT ( 'NONE',  ( -21.05000000000000071, -11.64999999998884306, -198.0999999999999659 ) ) ;
#104000=EDGE_LOOP ( 'NONE', ( #3210, #185292, #161842, #131647 ) ) ;
#104002=EDGE_CURVE ( 'NONE', #255780, #163705, #63605, .T. ) ;
#104018=CARTESIAN_POINT ( 'NONE',  ( -21.64999999999999858, 7.350000000011155166, -179.7499999999999716 ) ) ;
#104030=CIRCLE ( 'NONE', #49887, 7.800000000000001599 ) ;
#104051=PLANE ( 'NONE',  #49269 ) ;
#104056=DIRECTION ( 'NONE',  ( 0.000000000000000000, -0.1455152366551721865, -0.9893560106964475187 ) ) ;
#104071=DIRECTION ( 'NONE',  ( 0.000000000000000000, 0.000000000000000000, 1.000000000000000000 ) ) ;
#104100=CARTESIAN_POINT ( 'NONE',  ( -21.05000000000000071, 6.304961112695768755, -167.5213855659370665 ) ) ;
#104130=DIRECTION ( 'NONE',  ( -0.000000000000000000, -0.000000000000000000, 1.000000000000000000 ) ) ;
#104148=DIRECTION ( 'NONE',  ( 1.000000000000000000, -0.000000000000000000, -0.000000000000000000 ) ) ;
#104155=DIRECTION ( 'NONE',  ( 1.000000000000000000, -0.000000000000000000, -0.000000000000000000 ) ) ;
#104162=CARTESIAN_POINT ( 'NONE',  ( 22.49436431346199683, 11.64995094766461392, -167.4330964702777180 ) ) ;
#104175=DIRECTION ( 'NONE',  ( 0.000000000000000000, 0.000000000000000000, 1.000000000000000000 ) ) ;
#104182=LINE ( 'NONE', #143319, #147306 ) ;
#104190=LINE ( 'NONE', #165482, #91222 ) ;
#104201=AXIS2_PLACEMENT_3D ( 'NONE', #100368, #236054, #155274 ) ;
#104202=DIRECTION ( 'NONE',  ( -1.000000000000000000, 0.000000000000000000, 0.000000000000000000 ) ) ;
#104225=FACE_OUTER_BOUND ( 'NONE', #119448, .T. ) ;
#104253=DIRECTION ( 'NONE',  ( 0.000000000000000000, 0.000000000000000000, 1.000000000000000000 ) ) ;
#104255=ORIENTED_EDGE ( 'NONE', *, *, #240748, .F. ) ;
#104265=CARTESIAN_POINT ( 'NONE',  ( 20.95512820512820440, 10.62384868372303259, -179.6499999999999773 ) ) ;
#104283=VECTOR ( 'NONE', #227217, 999.9999999999998863 ) ;
#104346=VERTEX_POINT ( 'NONE', #95991 ) ;
#104362=EDGE_CURVE ( 'NONE', #59075, #143156, #85559, .T. ) ;
#104384=DIRECTION ( 'NONE',  ( 0.000000000000000000, 0.000000000000000000, -1.000000000000000000 ) ) ;
#104396=ORIENTED_EDGE ( 'NONE', *, *, #14294, .F. ) ;
#104405=ORIENTED_EDGE ( 'NONE', *, *, #125972, .F. ) ;
#104422=DIRECTION ( 'NONE',  ( 0.000000000000000000, -0.000000000000000000, 1.000000000000000000 ) ) ;
#104430=CARTESIAN_POINT ( 'NONE',  ( -20.85000000000000142, -1.164121893230052995, -208.9148480855715775 ) ) ;
#104443=AXIS2_PLACEMENT_3D ( 'NONE', #4016, #58828, #123982 ) ;
#104444=EDGE_CURVE ( 'NONE', #5997, #160190, #206670, .T. ) ;
#104448=VECTOR ( 'NONE', #56961, 1000.000000000000227 ) ;
#104498=ADVANCED_FACE ( 'NONE', ( #107554 ), #103683, .F. ) ;
#104560=AXIS2_PLACEMENT_3D ( 'NONE', #251237, #70081, #173051 ) ;
#104629=DIRECTION ( 'NONE',  ( 0.000000000000000000, -0.7397360091702744889, 0.6728971962616842051 ) ) ;
#104636=ORIENTED_EDGE ( 'NONE', *, *, #19690, .T. ) ;
#104672=DIRECTION ( 'NONE',  ( -1.000000000000000000, -0.000000000000000000, -0.000000000000000000 ) ) ;
#104691=CARTESIAN_POINT ( 'NONE',  ( 20.95512820512820440, 10.62384868372303615, -179.6499999999999773 ) ) ;
#104730=ORIENTED_EDGE ( 'NONE', *, *, #58228, .T. ) ;
#104767=CYLINDRICAL_SURFACE ( 'NONE', #202287, 0.09999999999999939493 ) ;
#104772=CARTESIAN_POINT ( 'NONE',  ( 21.05000000000000071, 1.115600667400684642E-11, -200.9999999999999432 ) ) ;
#104785=CARTESIAN_POINT ( 'NONE',  ( -20.15000000000000568, 9.291421356248463326, -188.7499999999999716 ) ) ;
#104797=FACE_OUTER_BOUND ( 'NONE', #177, .T. ) ;
#104799=CARTESIAN_POINT ( 'NONE',  ( 18.59999999999999787, -1.835341550213255957, -179.0551512925629538 ) ) ;
#104805=CARTESIAN_POINT ( 'NONE',  ( -23.15000000000000213, 1.115600667400684642E-11, -200.9999999999999432 ) ) ;
#104815=FACE_OUTER_BOUND ( 'NONE', #238072, .T. ) ;
#104816=DIRECTION ( 'NONE',  ( 1.000000000000000000, 0.000000000000000000, 0.000000000000000000 ) ) ;
#104817=ORIENTED_EDGE ( 'NONE', *, *, #153999, .F. ) ;
#104823=CARTESIAN_POINT ( 'NONE',  ( 18.51024323315077069, 10.31104185824063713, -206.5204516983105520 ) ) ;
#104830=CARTESIAN_POINT ( 'NONE',  ( -23.25000000000000000, 1.115600667400684642E-11, -167.4999999999999716 ) ) ;
#104834=CYLINDRICAL_SURFACE ( 'NONE', #211368, 4.000000000000003553 ) ;
#104864=CARTESIAN_POINT ( 'NONE',  ( 23.15000000000000213, -9.499999999988844479, -191.1060308773475072 ) ) ;
#104865=TOROIDAL_SURFACE ( 'NONE', #155016, 2.100000000000002309, 0.1000000000000000056 ) ;
#104868=DIRECTION ( 'NONE',  ( -2.940209281316621016E-16, 1.000000000000000000, -4.704334850106593625E-15 ) ) ;
#104881=EDGE_CURVE ( 'NONE', #254577, #49571, #239734, .T. ) ;
#104941=CIRCLE ( 'NONE', #209212, 0.09999999999998898659 ) ;
#104958=DIRECTION ( 'NONE',  ( -0.7071067811865388020, 0.7071067811865561215, 0.000000000000000000 ) ) ;
#104967=DIRECTION ( 'NONE',  ( -1.000000000000000000, -0.000000000000000000, -0.000000000000000000 ) ) ;
#105032=VERTEX_POINT ( 'NONE', #79668 ) ;
#105062=CIRCLE ( 'NONE', #109179, 0.5000000000000004441 ) ;
#105063=AXIS2_PLACEMENT_3D ( 'NONE', #136908, #138171, #238575 ) ;
#105100=CARTESIAN_POINT ( 'NONE',  ( -18.59999999999999787, 1.851028230152016674, -179.1539132694224463 ) ) ;
#105122=ORIENTED_EDGE ( 'NONE', *, *, #153689, .F. ) ;
#105138=DIRECTION ( 'NONE',  ( -1.000000000000000000, 0.000000000000000000, 0.000000000000000000 ) ) ;
#105139=CARTESIAN_POINT ( 'NONE',  ( 21.04999999999999716, 8.871279686006802834, -176.0586289951408787 ) ) ;
#105144=EDGE_CURVE ( 'NONE', #154991, #61597, #181387, .T. ) ;
#105241=CARTESIAN_POINT ( 'NONE',  ( 23.14999999999998437, -11.74999999998884448, -167.4999999999999432 ) ) ;
#105262=ORIENTED_EDGE ( 'NONE', *, *, #165055, .T. ) ;
#105266=EDGE_CURVE ( 'NONE', #257620, #213934, #226899, .T. ) ;
#105288=DIRECTION ( 'NONE',  ( -3.469446951953604722E-14, -0.9999176327611370985, -0.01283462868040260302 ) ) ;
#105317=ORIENTED_EDGE ( 'NONE', *, *, #251615, .T. ) ;
#105336=ORIENTED_EDGE ( 'NONE', *, *, #181626, .F. ) ;
#105341=ADVANCED_FACE ( 'NONE', ( #250317 ), #69138, .T. ) ;
#105351=CARTESIAN_POINT ( 'NONE',  ( 18.50000000000000711, -9.421074344976677395, -207.8244720594301498 ) ) ;
#105360=DIRECTION ( 'NONE',  ( 0.000000000000000000, 0.000000000000000000, 1.000000000000000000 ) ) ;
#105405=DIRECTION ( 'NONE',  ( 0.000000000000000000, 0.000000000000000000, 1.000000000000000000 ) ) ;
#105429=CARTESIAN_POINT ( 'NONE',  ( 20.94999999999999929, -8.999999999988842703, -191.1060308773475072 ) ) ;
#105431=DIRECTION ( 'NONE',  ( -1.000000000000000000, -0.000000000000000000, -0.000000000000000000 ) ) ;
#105476=ADVANCED_FACE ( 'NONE', ( #115952 ), #134206, .F. ) ;
#105486=ORIENTED_EDGE ( 'NONE', *, *, #61995, .T. ) ;
#105497=DIRECTION ( 'NONE',  ( 0.000000000000000000, -0.8660254037844247188, 0.5000000000000245359 ) ) ;
#105511=ADVANCED_FACE ( 'NONE', ( #257966 ), #138053, .F. ) ;
#105524=CARTESIAN_POINT ( 'NONE',  ( -20.94999999999999929, 1.115650877919449575E-11, -205.0999999999999375 ) ) ;
#105527=AXIS2_PLACEMENT_3D ( 'NONE', #56306, #154189, #14655 ) ;
#105543=FACE_OUTER_BOUND ( 'NONE', #224466, .T. ) ;
#105544=ORIENTED_EDGE ( 'NONE', *, *, #243166, .T. ) ;
#105545=VERTEX_POINT ( 'NONE', #139331 ) ;
#105555=EDGE_CURVE ( 'NONE', #45677, #27613, #119814, .T. ) ;
#105574=CIRCLE ( 'NONE', #122178, 0.1000000000000089567 ) ;
#105643=CARTESIAN_POINT ( 'NONE',  ( 19.97071067811864609, 11.72071067812981404, -192.1499999999999488 ) ) ;
#105650=DIRECTION ( 'NONE',  ( -0.000000000000000000, 0.8660254037844411501, 0.4999999999999956701 ) ) ;
#105684=CARTESIAN_POINT ( 'NONE',  ( 20.99142135623731065, 11.60000000001116049, -194.0717967697245001 ) ) ;
#105709=FACE_OUTER_BOUND ( 'NONE', #40120, .T. ) ;
#105763=DIRECTION ( 'NONE',  ( 1.000000000000000000, 0.000000000000000000, 0.000000000000000000 ) ) ;
#105790=AXIS2_PLACEMENT_3D ( 'NONE', #255573, #160410, #54840 ) ;
#105818=DIRECTION ( 'NONE',  ( 0.000000000000000000, 0.000000000000000000, -1.000000000000000000 ) ) ;
#105853=ADVANCED_FACE ( 'NONE', ( #143843 ), #19720, .F. ) ;
#105868=CARTESIAN_POINT ( 'NONE',  ( -23.25000000000000000, 1.115600667400684642E-11, -200.9999999999999432 ) ) ;
#105869=ORIENTED_EDGE ( 'NONE', *, *, #222352, .F. ) ;
#105882=ORIENTED_EDGE ( 'NONE', *, *, #37975, .T. ) ;
#105892=CIRCLE ( 'NONE', #151750, 0.09999999999998898659 ) ;
#105921=EDGE_LOOP ( 'NONE', ( #150166, #232553, #213116, #20454 ) ) ;
#105923=DIRECTION ( 'NONE',  ( 0.000000000000000000, -0.1298341882520022694, -0.9915357197604853789 ) ) ;
#105925=EDGE_LOOP ( 'NONE', ( #45733, #131493, #108297, #120750 ) ) ;
#105965=DIRECTION ( 'NONE',  ( 0.000000000000000000, -0.5907332058517320572, 0.8068669527896995541 ) ) ;
#105998=DIRECTION ( 'NONE',  ( -1.000000000000000000, 0.000000000000000000, 0.000000000000000000 ) ) ;
#106029=DIRECTION ( 'NONE',  ( -1.000000000000000000, -0.000000000000000000, 0.000000000000000000 ) ) ;
#106035=ORIENTED_EDGE ( 'NONE', *, *, #203304, .F. ) ;
#106046=DIRECTION ( 'NONE',  ( 0.000000000000000000, 0.000000000000000000, -1.000000000000000000 ) ) ;
#106058=CARTESIAN_POINT ( 'NONE',  ( 20.94999999999999929, 1.115600667400684642E-11, -200.9999999999999432 ) ) ;
#106073=CARTESIAN_POINT ( 'NONE',  ( 21.10320863425824811, 6.400277386470322405, -167.4749777487728579 ) ) ;
#106084=DIRECTION ( 'NONE',  ( -1.000000000000000000, 0.000000000000000000, 0.000000000000000000 ) ) ;
#106104=CYLINDRICAL_SURFACE ( 'NONE', #42647, 0.09999999999999939493 ) ;
#106112=( NAMED_UNIT ( * ) SI_UNIT ( $, .STERADIAN. ) SOLID_ANGLE_UNIT ( ) );
#106115=AXIS2_PLACEMENT_3D ( 'NONE', #921, #80454, #117066 ) ;
#106158=EDGE_CURVE ( 'NONE', #170879, #45677, #57284, .T. ) ;
#106162=AXIS2_PLACEMENT_3D ( 'NONE', #135402, #214953, #112024 ) ;
#106192=EDGE_CURVE ( 'NONE', #29625, #162728, #95440, .T. ) ;
#106213=DIRECTION ( 'NONE',  ( -1.000000000000000000, -2.952720810173289112E-16, 0.000000000000000000 ) ) ;
#106229=FACE_OUTER_BOUND ( 'NONE', #132585, .T. ) ;
#106233=LINE ( 'NONE', #5852, #256109 ) ;
#106247=CIRCLE ( 'NONE', #127116, 0.09999999999998898659 ) ;
#106250=ORIENTED_EDGE ( 'NONE', *, *, #195130, .F. ) ;
#106258=CARTESIAN_POINT ( 'NONE',  ( -21.05000000000000426, 11.60000000001115872, -174.4282032302755283 ) ) ;
#106269=EDGE_CURVE ( 'NONE', #257620, #15539, #36518, .T. ) ;
#106276=DIRECTION ( 'NONE',  ( 1.000000000000000000, 0.000000000000000000, 0.000000000000000000 ) ) ;
#106287=ORIENTED_EDGE ( 'NONE', *, *, #187807, .T. ) ;
#106290=DIRECTION ( 'NONE',  ( 0.000000000000000000, 0.000000000000000000, 1.000000000000000000 ) ) ;
#106291=AXIS2_PLACEMENT_3D ( 'NONE', #78584, #79850, #76023 ) ;
#106321=LINE ( 'NONE', #122067, #22658 ) ;
#106351=ADVANCED_FACE ( 'NONE', ( #211237 ), #169774, .T. ) ;
#106364=ORIENTED_EDGE ( 'NONE', *, *, #192329, .F. ) ;
#106406=DIRECTION ( 'NONE',  ( 0.000000000000000000, 0.000000000000000000, 1.000000000000000000 ) ) ;
#106496=EDGE_CURVE ( 'NONE', #209946, #188501, #199136, .T. ) ;
#106500=ADVANCED_FACE ( 'NONE', ( #78127 ), #45008, .F. ) ;
#106509=ADVANCED_FACE ( 'NONE', ( #237224 ), #124981, .F. ) ;
#106535=LINE ( 'NONE', #227783, #87900 ) ;
#106552=FACE_BOUND ( 'NONE', #30007, .T. ) ;
#106616=ORIENTED_EDGE ( 'NONE', *, *, #19165, .T. ) ;
#106623=LINE ( 'NONE', #222731, #253482 ) ;
#106630=DIRECTION ( 'NONE',  ( -1.000000000000000000, -0.000000000000000000, 0.000000000000000000 ) ) ;
#106634=FACE_OUTER_BOUND ( 'NONE', #21025, .T. ) ;
#106646=ADVANCED_FACE ( 'NONE', ( #221481 ), #41823, .F. ) ;
#106647=EDGE_CURVE ( 'NONE', #39612, #257620, #87111, .T. ) ;
#106656=EDGE_LOOP ( 'NONE', ( #61449, #9965, #190846, #244191 ) ) ;
#106681=EDGE_CURVE ( 'NONE', #50099, #213687, #182405, .T. ) ;
#106686=ADVANCED_FACE ( 'NONE', ( #131383 ), #11458, .T. ) ;
#106701=DIRECTION ( 'NONE',  ( -1.000000000000000000, 6.938893903907270030E-14, 0.000000000000000000 ) ) ;
#106714=DIRECTION ( 'NONE',  ( -1.000000000000000000, -2.952720810173289112E-16, 0.000000000000000000 ) ) ;
#106753=EDGE_LOOP ( 'NONE', ( #222286, #220749, #255321, #64666 ) ) ;
#106766=EDGE_CURVE ( 'NONE', #156566, #181381, #75296, .T. ) ;
#106774=CIRCLE ( 'NONE', #206735, 0.1000000000000001860 ) ;
#106800=DIRECTION ( 'NONE',  ( 0.000000000000000000, 0.000000000000000000, -1.000000000000000000 ) ) ;
#106819=DIRECTION ( 'NONE',  ( 1.000000000000000000, 1.836970198721029934E-16, 0.000000000000000000 ) ) ;
#106834=( GEOMETRIC_REPRESENTATION_CONTEXT ( 3 ) GLOBAL_UNCERTAINTY_ASSIGNED_CONTEXT ( ( #97481 ) ) GLOBAL_UNIT_ASSIGNED_CONTEXT ( ( #129485, #85172, #126914 ) ) REPRESENTATION_CONTEXT ( 'NONE', 'WORKASPACE' ) );
#106849=CIRCLE ( 'NONE', #248510, 0.09999999999998898659 ) ;
#106870=EDGE_CURVE ( 'NONE', #2364, #178867, #132499, .T. ) ;
#106896=CARTESIAN_POINT ( 'NONE',  ( -22.40000000000000213, 1.115488287304407678E-11, -155.7495671075413668 ) ) ;
#106954=AXIS2_PLACEMENT_3D ( 'NONE', #63370, #240755, #123369 ) ;
#106975=AXIS2_PLACEMENT_3D ( 'NONE', #80383, #26563, #206466 ) ;
#106985=DIRECTION ( 'NONE',  ( 0.000000000000000000, 1.000000000000000000, 0.000000000000000000 ) ) ;
#106988=ORIENTED_EDGE ( 'NONE', *, *, #215932, .F. ) ;
#106993=ORIENTED_EDGE ( 'NONE', *, *, #172323, .T. ) ;
#106999=DIRECTION ( 'NONE',  ( 1.000000000000000000, 0.000000000000000000, 0.000000000000000000 ) ) ;
#107011=DIRECTION ( 'NONE',  ( 1.000000000000000000, 0.000000000000000000, 0.000000000000000000 ) ) ;
#107019=ORIENTED_EDGE ( 'NONE', *, *, #138552, .T. ) ;
#107038=DIRECTION ( 'NONE',  ( -1.000000000000000000, -2.952720810173289112E-16, 0.000000000000000000 ) ) ;
#107064=EDGE_CURVE ( 'NONE', #52702, #85372, #182590, .T. ) ;
#107070=PLANE ( 'NONE',  #12234 ) ;
#107091=CARTESIAN_POINT ( 'NONE',  ( -23.15000000000000213, -11.48912529306489994, -197.8999999999999773 ) ) ;
#107111=ORIENTED_EDGE ( 'NONE', *, *, #133935, .F. ) ;
#107137=CARTESIAN_POINT ( 'NONE',  ( 18.41789779300690455, -9.499999999988844479, -174.5320696663606554 ) ) ;
#107155=ADVANCED_FACE ( 'NONE', ( #139727 ), #160627, .T. ) ;
#107167=CARTESIAN_POINT ( 'NONE',  ( 21.05000000000000071, 8.776282895303632259, -175.9880007215843136 ) ) ;
#107185=CARTESIAN_POINT ( 'NONE',  ( 20.94999999999999929, 7.120270961708750512, -204.6595630418393057 ) ) ;
#107216=DIRECTION ( 'NONE',  ( 1.000000000000000000, 0.000000000000000000, 0.000000000000000000 ) ) ;
#107217=ORIENTED_EDGE ( 'NONE', *, *, #120059, .F. ) ;
#107233=FACE_OUTER_BOUND ( 'NONE', #19439, .T. ) ;
#107248=CIRCLE ( 'NONE', #173946, 4.000000000000003553 ) ;
#107262=ADVANCED_FACE ( 'NONE', ( #242688 ), #79151, .T. ) ;
#107275=EDGE_CURVE ( 'NONE', #174631, #42715, #58475, .T. ) ;
#107285=AXIS2_PLACEMENT_3D ( 'NONE', #91887, #107597, #90592 ) ;
#107335=ORIENTED_EDGE ( 'NONE', *, *, #34875, .T. ) ;
#107351=FACE_OUTER_BOUND ( 'NONE', #139001, .T. ) ;
#107378=CARTESIAN_POINT ( 'NONE',  ( 21.08376601933332495, 6.341947271286813681, -167.4362239890699584 ) ) ;
#107382=VECTOR ( 'NONE', #171648, 1000.000000000000000 ) ;
#107396=ORIENTED_EDGE ( 'NONE', *, *, #117789, .T. ) ;
#107398=CARTESIAN_POINT ( 'NONE',  ( 21.05933563467872105, 10.72452471209247626, -179.6936477489558968 ) ) ;
#107405=EDGE_CURVE ( 'NONE', #223354, #207624, #50118, .T. ) ;
#107413=AXIS2_PLACEMENT_3D ( 'NONE', #232667, #37041, #133544 ) ;
#107414=ORIENTED_EDGE ( 'NONE', *, *, #220135, .F. ) ;
#107466=VERTEX_POINT ( 'NONE', #61122 ) ;
#107469=CIRCLE ( 'NONE', #253212, 0.09999999999998898659 ) ;
#107478=VERTEX_POINT ( 'NONE', #160260 ) ;
#107506=EDGE_CURVE ( 'NONE', #250279, #103901, #116758, .T. ) ;
#107512=EDGE_CURVE ( 'NONE', #68890, #138726, #183414, .T. ) ;
#107548=ORIENTED_EDGE ( 'NONE', *, *, #42730, .F. ) ;
#107554=FACE_OUTER_BOUND ( 'NONE', #238200, .T. ) ;
#107582=DIRECTION ( 'NONE',  ( -1.000000000000000000, 0.000000000000000000, 0.000000000000000000 ) ) ;
#107597=DIRECTION ( 'NONE',  ( -1.000000000000000000, 0.000000000000000000, 0.000000000000000000 ) ) ;
#107604=AXIS2_PLACEMENT_3D ( 'NONE', #43252, #81069, #44544 ) ;
#107622=CARTESIAN_POINT ( 'NONE',  ( 21.04999999999999716, 8.871279686006799281, -179.6499999999999488 ) ) ;
#107630=AXIS2_PLACEMENT_3D ( 'NONE', #230806, #67852, #211219 ) ;
#107675=ORIENTED_EDGE ( 'NONE', *, *, #25915, .F. ) ;
#107702=DIRECTION ( 'NONE',  ( 0.000000000000000000, -1.000000000000000000, 0.000000000000000000 ) ) ;
#107721=CARTESIAN_POINT ( 'NONE',  ( -23.15000000000000213, 11.65000000001115588, -179.6499999999999773 ) ) ;
#107722=CARTESIAN_POINT ( 'NONE',  ( 21.14999999999999858, 11.75000000001116263, -167.5999999999999659 ) ) ;
#107774=AXIS2_PLACEMENT_3D ( 'NONE', #140971, #157997, #117539 ) ;
#107778=CARTESIAN_POINT ( 'NONE',  ( -18.59999999999999787, 11.75000000001115197, -179.6499999999999773 ) ) ;
#107811=AXIS2_PLACEMENT_3D ( 'NONE', #257788, #59612, #38811 ) ;
#107817=CARTESIAN_POINT ( 'NONE',  ( 21.07928932188134397, 0.09889514566555242248, -161.1714833436066385 ) ) ;
#107820=CARTESIAN_POINT ( 'NONE',  ( 23.24999999999999645, 4.775700934590591196, -189.1512318959539982 ) ) ;
#107826=VECTOR ( 'NONE', #144578, 1000.000000000000000 ) ;
#107832=CARTESIAN_POINT ( 'NONE',  ( 21.05000000000000071, -9.399999999988846611, -177.3939691226524076 ) ) ;
#107863=DIRECTION ( 'NONE',  ( -1.000000000000000000, 0.000000000000000000, 0.000000000000000000 ) ) ;
#107877=DIRECTION ( 'NONE',  ( 0.000000000000000000, 0.000000000000000000, 1.000000000000000000 ) ) ;
#107913=ORIENTED_EDGE ( 'NONE', *, *, #152705, .F. ) ;
#107919=PLANE ( 'NONE',  #26381 ) ;
#107923=ORIENTED_EDGE ( 'NONE', *, *, #133972, .F. ) ;
#107945=AXIS2_PLACEMENT_3D ( 'NONE', #96822, #238945, #60283 ) ;
#107952=CARTESIAN_POINT ( 'NONE',  ( -20.00857864376270001, 9.150000000011157653, -188.7499999999999716 ) ) ;
#107958=CIRCLE ( 'NONE', #236950, 0.09999999999998898659 ) ;
#107994=ORIENTED_EDGE ( 'NONE', *, *, #57751, .F. ) ;
#108012=LINE ( 'NONE', #88414, #108511 ) ;
#108013=DIRECTION ( 'NONE',  ( 1.000000000000000000, 0.000000000000000000, 0.000000000000000000 ) ) ;
#108022=ADVANCED_FACE ( 'NONE', ( #230158 ), #168949, .F. ) ;
#108064=DIRECTION ( 'NONE',  ( -1.000000000000000000, 0.000000000000000000, 0.000000000000000000 ) ) ;
#108097=TOROIDAL_SURFACE ( 'NONE', #12430, 0.2000000000000000111, 0.1000000000000000056 ) ;
#108107=DIRECTION ( 'NONE',  ( 0.000000000000000000, 1.000000000000000000, -0.000000000000000000 ) ) ;
#108161=VERTEX_POINT ( 'NONE', #119210 ) ;
#108167=DIRECTION ( 'NONE',  ( 1.000000000000000000, -0.000000000000000000, -0.000000000000000000 ) ) ;
#108168=EDGE_CURVE ( 'NONE', #111061, #2364, #85821, .T. ) ;
#108184=FACE_OUTER_BOUND ( 'NONE', #32745, .T. ) ;
#108202=DIRECTION ( 'NONE',  ( 0.000000000000000000, 0.000000000000000000, 1.000000000000000000 ) ) ;
#108203=VERTEX_POINT ( 'NONE', #216997 ) ;
#108238=ORIENTED_EDGE ( 'NONE', *, *, #93184, .F. ) ;
#108244=CARTESIAN_POINT ( 'NONE',  ( -21.07928932188134041, 0.09889514566555068775, -161.1714833436066669 ) ) ;
#108281=CARTESIAN_POINT ( 'NONE',  ( 18.41356215285961540, -9.499999999988867572, -174.5320693966995691 ) ) ;
#108292=SPHERICAL_SURFACE ( 'NONE', #3721, 0.1000000000000000056 ) ;
#108297=ORIENTED_EDGE ( 'NONE', *, *, #173304, .F. ) ;
#108306=ORIENTED_EDGE ( 'NONE', *, *, #36675, .T. ) ;
#108307=CARTESIAN_POINT ( 'NONE',  ( -20.94999999999999929, -1.249999999988843369, -175.4999999999999716 ) ) ;
#108342=TOROIDAL_SURFACE ( 'NONE', #66826, 0.2000000000000000111, 0.1000000000000000056 ) ;
#108347=ORIENTED_EDGE ( 'NONE', *, *, #223582, .F. ) ;
#108361=ORIENTED_EDGE ( 'NONE', *, *, #16367, .F. ) ;
#108362=CARTESIAN_POINT ( 'NONE',  ( -22.39999999999999858, 7.790779598384560245, -167.3999999999999773 ) ) ;
#108380=CARTESIAN_POINT ( 'NONE',  ( -20.64999999999999858, 7.150000000011155876, -188.6499999999999488 ) ) ;
#108504=DIRECTION ( 'NONE',  ( 0.000000000000000000, 5.329070518200764016E-15, -1.000000000000000000 ) ) ;
#108510=TOROIDAL_SURFACE ( 'NONE', #70950, 11.90000000000000391, 0.1000000000000000056 ) ;
#108511=VECTOR ( 'NONE', #209678, 1000.000000000000000 ) ;
#108518=FACE_OUTER_BOUND ( 'NONE', #241567, .T. ) ;
#108528=CARTESIAN_POINT ( 'NONE',  ( 20.94999999999999574, 6.400000000011158541, -177.4304246300615375 ) ) ;
#108531=EDGE_CURVE ( 'NONE', #3198, #20715, #248134, .T. ) ;
#108550=EDGE_CURVE ( 'NONE', #197017, #51917, #3764, .T. ) ;
#108551=CIRCLE ( 'NONE', #162556, 0.2000000000000057288 ) ;
#108562=CARTESIAN_POINT ( 'NONE',  ( 21.14999999999999858, 10.71339244341104013, -179.8499999999999943 ) ) ;
#108591=CARTESIAN_POINT ( 'NONE',  ( -18.59999999999999787, 11.65000000001115232, -188.7499999999999716 ) ) ;
#108622=EDGE_LOOP ( 'NONE', ( #204019, #245123, #74591, #65932 ) ) ;
#108643=FACE_BOUND ( 'NONE', #1102, .T. ) ;
#108681=CARTESIAN_POINT ( 'NONE',  ( 21.10710606213542206, 8.776894023904366904, -179.7409965263994138 ) ) ;
#108687=FACE_OUTER_BOUND ( 'NONE', #143618, .T. ) ;
#108738=ORIENTED_EDGE ( 'NONE', *, *, #51891, .F. ) ;
#108740=B_SPLINE_CURVE_WITH_KNOTS ( 'NONE', 3,
 ( #31331, #132977, #95117, #211212, #130381, #170861, #190388, #33914, #30037, #74307 ),
 .UNSPECIFIED., .F., .F.,
 ( 4, 2, 2, 2, 4 ),
 ( 0.000000000000000000, 3.990160268013856579E-05, 7.980320536027713158E-05, 0.0001596064107205558895, 0.0003192128214411109116 ),
 .UNSPECIFIED. ) ;
#108743=CARTESIAN_POINT ( 'NONE',  ( -21.05000000000000071, 1.115653327213047955E-11, -163.2000000000000171 ) ) ;
#108752=VERTEX_POINT ( 'NONE', #28512 ) ;
#108799=ORIENTED_EDGE ( 'NONE', *, *, #169041, .F. ) ;
#108814=EDGE_CURVE ( 'NONE', #114401, #213950, #60365, .T. ) ;
#108871=DIRECTION ( 'NONE',  ( 0.000000000000000000, -1.000000000000000000, 0.000000000000000000 ) ) ;
#108887=ORIENTED_EDGE ( 'NONE', *, *, #161900, .F. ) ;
#108888=EDGE_LOOP ( 'NONE', ( #63837, #193221, #223059, #3880 ) ) ;
#108927=EDGE_LOOP ( 'NONE', ( #35568, #188381, #26144, #30879 ) ) ;
#108989=CARTESIAN_POINT ( 'NONE',  ( -18.59999999999999787, 9.350000000011156942, -188.6499999999999488 ) ) ;
#109001=CARTESIAN_POINT ( 'NONE',  ( -23.24999999999999645, -9.599999999988845900, -207.6001893912220169 ) ) ;
#109025=CARTESIAN_POINT ( 'NONE',  ( -22.48660254037843131, 11.65000000001115588, -167.4499999999999886 ) ) ;
#109054=ORIENTED_EDGE ( 'NONE', *, *, #136614, .F. ) ;
#109063=CARTESIAN_POINT ( 'NONE',  ( -20.85000000000000142, -1.851617760457748618, -212.6031897196036198 ) ) ;
#109078=ADVANCED_FACE ( 'NONE', ( #145520 ), #88089, .F. ) ;
#109109=ORIENTED_EDGE ( 'NONE', *, *, #134453, .T. ) ;
#109134=DIRECTION ( 'NONE',  ( 0.000000000000000000, -1.000000000000000000, 0.000000000000000000 ) ) ;
#109156=CARTESIAN_POINT ( 'NONE',  ( -22.47120815636973745, 0.02890382191504724946, -155.8500680112464920 ) ) ;
#109168=DIRECTION ( 'NONE',  ( 1.000000000000000000, 3.265361837132813093E-16, -0.000000000000000000 ) ) ;
#109179=AXIS2_PLACEMENT_3D ( 'NONE', #213998, #20956, #194454 ) ;
#109207=AXIS2_PLACEMENT_3D ( 'NONE', #85335, #222273, #223572 ) ;
#109214=EDGE_CURVE ( 'NONE', #225193, #140280, #194764, .T. ) ;
#109217=ORIENTED_EDGE ( 'NONE', *, *, #227097, .F. ) ;
#109223=CARTESIAN_POINT ( 'NONE',  ( 21.05000000000000071, -8.730841121484171907, -177.0980747189843214 ) ) ;
#109245=DIRECTION ( 'NONE',  ( 0.000000000000000000, 0.000000000000000000, -1.000000000000000000 ) ) ;
#109249=DIRECTION ( 'NONE',  ( 0.000000000000000000, 0.9887567792719341719, -0.1495327102803664099 ) ) ;
#109256=VECTOR ( 'NONE', #247489, 1000.000000000000000 ) ;
#109278=ADVANCED_FACE ( 'NONE', ( #191100 ), #91967, .F. ) ;
#109289=DIRECTION ( 'NONE',  ( 0.000000000000000000, 0.000000000000000000, 1.000000000000000000 ) ) ;
#109298=CIRCLE ( 'NONE', #71918, 0.09999999999999939493 ) ;
#109309=AXIS2_PLACEMENT_3D ( 'NONE', #188999, #213686, #209852 ) ;
#109359=CARTESIAN_POINT ( 'NONE',  ( -21.05000000000000071, 1.115600667400684642E-11, -167.4999999999999716 ) ) ;
#109360=EDGE_CURVE ( 'NONE', #98329, #85452, #107248, .T. ) ;
#109437=DIRECTION ( 'NONE',  ( 0.000000000000000000, -1.000000000000000000, -1.734723475976807292E-15 ) ) ;
#109458=CARTESIAN_POINT ( 'NONE',  ( 21.05000000000000071, 4.813084112160680661, -179.4415177565237798 ) ) ;
#109471=EDGE_CURVE ( 'NONE', #165951, #256132, #65919, .T. ) ;
#109481=( BOUNDED_CURVE ( )  B_SPLINE_CURVE ( 3, ( #105643, #147368, #7875, #207356 ),
 .UNSPECIFIED., .F., .F. ) 
 B_SPLINE_CURVE_WITH_KNOTS ( ( 4, 4 ),
 ( 0.000000000000000000, 1.570796326794916320 ),
 .UNSPECIFIED. ) 
 CURVE ( )  GEOMETRIC_REPRESENTATION_ITEM ( )  RATIONAL_B_SPLINE_CURVE ( ( 1.000000000000000000, 0.8047378541243603856, 0.8047378541243603856, 1.000000000000000000 ) ) 
 REPRESENTATION_ITEM ( '' )  );
#109516=EDGE_LOOP ( 'NONE', ( #111473, #225707, #9957, #145773 ) ) ;
#109523=ORIENTED_EDGE ( 'NONE', *, *, #158614, .T. ) ;
#109567=EDGE_LOOP ( 'NONE', ( #38021, #149863, #152932, #181167 ) ) ;
#109576=ORIENTED_EDGE ( 'NONE', *, *, #9369, .T. ) ;
#109584=DIRECTION ( 'NONE',  ( 1.000000000000000000, 2.952720810173289112E-16, -0.000000000000000000 ) ) ;
#109596=EDGE_CURVE ( 'NONE', #251611, #149929, #111713, .T. ) ;
#109608=DIRECTION ( 'NONE',  ( 1.000000000000000000, 0.000000000000000000, 0.000000000000000000 ) ) ;
#109614=ORIENTED_EDGE ( 'NONE', *, *, #122329, .F. ) ;
#109633=EDGE_CURVE ( 'NONE', #93167, #87114, #74718, .T. ) ;
#109646=CARTESIAN_POINT ( 'NONE',  ( -18.59999999999999787, -9.499999999988849808, -175.5999999999999659 ) ) ;
#109760=ORIENTED_EDGE ( 'NONE', *, *, #26455, .F. ) ;
#109762=VECTOR ( 'NONE', #218508, 1000.000000000000000 ) ;
#109798=SPHERICAL_SURFACE ( 'NONE', #152548, 0.1000000000000000056 ) ;
#109800=DIRECTION ( 'NONE',  ( 0.000000000000000000, 0.1495327102803792052, -0.9887567792719320625 ) ) ;
#109822=ORIENTED_EDGE ( 'NONE', *, *, #156571, .F. ) ;
#109831=CARTESIAN_POINT ( 'NONE',  ( 18.59999999999999787, -9.399999999988843058, -207.8820418481726620 ) ) ;
#109894=EDGE_CURVE ( 'NONE', #202583, #245309, #66104, .T. ) ;
#109908=ADVANCED_FACE ( 'NONE', ( #244002 ), #53642, .F. ) ;
#109950=CARTESIAN_POINT ( 'NONE',  ( -21.29999999999995808, 1.115600667400684642E-11, -171.5499999999999829 ) ) ;
#109992=ADVANCED_FACE ( 'NONE', ( #53520 ), #220048, .F. ) ;
#109994=EDGE_CURVE ( 'NONE', #169487, #160579, #57719, .T. ) ;
#109996=CARTESIAN_POINT ( 'NONE',  ( -22.39999999999999858, 7.790779598384559357, -167.4999999999999432 ) ) ;
#110029=EDGE_CURVE ( 'NONE', #17724, #27168, #212324, .T. ) ;
#110035=VECTOR ( 'NONE', #66009, 1000.000000000000000 ) ;
#110039=AXIS2_PLACEMENT_3D ( 'NONE', #51720, #192556, #131286 ) ;
#110044=CARTESIAN_POINT ( 'NONE',  ( 18.59999999999999076, -1.149570369564537842, -208.8159124845019221 ) ) ;
#110079=DIRECTION ( 'NONE',  ( -1.000000000000000000, -0.000000000000000000, -0.000000000000000000 ) ) ;
#110101=EDGE_LOOP ( 'NONE', ( #249396, #20474, #241931, #17179, #208860 ) ) ;
#110104=FACE_OUTER_BOUND ( 'NONE', #77559, .T. ) ;
#110129=ADVANCED_FACE ( 'NONE', ( #40412 ), #174801, .T. ) ;
#110134=DIRECTION ( 'NONE',  ( 1.000000000000000000, 0.000000000000000000, 0.000000000000000000 ) ) ;
#110143=DIRECTION ( 'NONE',  ( 0.000000000000000000, 0.000000000000000000, -1.000000000000000000 ) ) ;
#110156=AXIS2_PLACEMENT_3D ( 'NONE', #150274, #126842, #31628 ) ;
#110165=CARTESIAN_POINT ( 'NONE',  ( 20.91682497891423154, 10.32263460347359185, -206.5605957968671476 ) ) ;
#110186=FACE_OUTER_BOUND ( 'NONE', #184463, .T. ) ;
#110247=CARTESIAN_POINT ( 'NONE',  ( -20.90851465518105812, 10.32532329027886320, -206.5699343018359002 ) ) ;
#110249=AXIS2_PLACEMENT_3D ( 'NONE', #30272, #211461, #107216 ) ;
#110273=AXIS2_PLACEMENT_3D ( 'NONE', #61004, #118435, #177139 ) ;
#110275=CARTESIAN_POINT ( 'NONE',  ( 21.04999999999953886, 6.441084688482137111, -167.5177194333097646 ) ) ;
#110291=CARTESIAN_POINT ( 'NONE',  ( 20.85000000000000142, 11.65000000001115943, -194.2161343370218560 ) ) ;
#110307=CIRCLE ( 'NONE', #26955, 0.09999999999999939493 ) ;
#110347=DIRECTION ( 'NONE',  ( -1.000000000000000000, 0.000000000000000000, 0.000000000000000000 ) ) ;
#110394=ORIENTED_EDGE ( 'NONE', *, *, #45803, .F. ) ;
#110451=CARTESIAN_POINT ( 'NONE',  ( -22.49917693094574389, 0.08522996423282774847, -155.8502042154692901 ) ) ;
#110489=CARTESIAN_POINT ( 'NONE',  ( -22.59999999999999787, 11.74956712350054744, -167.3991416309012550 ) ) ;
#110492=DIRECTION ( 'NONE',  ( 1.000000000000000000, 0.000000000000000000, 0.000000000000000000 ) ) ;
#110494=CARTESIAN_POINT ( 'NONE',  ( 18.59999999999999787, -1.249999999988843369, -208.8004807544150481 ) ) ;
#110503=EDGE_CURVE ( 'NONE', #157637, #199601, #39778, .T. ) ;
#110526=CARTESIAN_POINT ( 'NONE',  ( -21.05000000000000071, 1.115600667400684642E-11, -171.7999999999999545 ) ) ;
#110554=ADVANCED_FACE ( 'NONE', ( #104815 ), #166154, .T. ) ;
#110572=MANIFOLD_SOLID_BREP ( 'Stock-MAS-200-1', #28367 ) ;
#110589=FACE_OUTER_BOUND ( 'NONE', #203223, .T. ) ;
#110591=DIRECTION ( 'NONE',  ( 0.000000000000000000, 0.000000000000000000, -1.000000000000000000 ) ) ;
#110617=ORIENTED_EDGE ( 'NONE', *, *, #181233, .T. ) ;
#110637=CARTESIAN_POINT ( 'NONE',  ( -18.59999999999999787, -9.399999999988851940, -207.8820418481726335 ) ) ;
#110646=AXIS2_PLACEMENT_3D ( 'NONE', #91466, #52306, #15806 ) ;
#110648=AXIS2_PLACEMENT_3D ( 'NONE', #111077, #186786, #189342 ) ;
#110662=LINE ( 'NONE', #11583, #228593 ) ;
#110663=CIRCLE ( 'NONE', #185685, 0.09999999999999939493 ) ;
#110670=LINE ( 'NONE', #54541, #232962 ) ;
#110688=DIRECTION ( 'NONE',  ( 0.000000000000000000, 0.1350103645451904977, 0.9908441862701596881 ) ) ;
#110727=FACE_OUTER_BOUND ( 'NONE', #228422, .T. ) ;
#110763=ORIENTED_EDGE ( 'NONE', *, *, #183604, .F. ) ;
#110769=DIRECTION ( 'NONE',  ( 0.000000000000000000, 0.000000000000000000, -1.000000000000000000 ) ) ;
#110785=ORIENTED_EDGE ( 'NONE', *, *, #73845, .F. ) ;
#110816=DIRECTION ( 'NONE',  ( 0.000000000000000000, 0.000000000000000000, -1.000000000000000000 ) ) ;
#110892=CARTESIAN_POINT ( 'NONE',  ( 20.85000000000000142, -1.835859311432481045, -212.5044391687984842 ) ) ;
#110897=CARTESIAN_POINT ( 'NONE',  ( -23.25000000000000000, 6.982009704867601307, -204.6961521182562649 ) ) ;
#110922=EDGE_CURVE ( 'NONE', #231520, #82701, #228424, .T. ) ;
#110928=DIRECTION ( 'NONE',  ( 0.000000000000000000, -1.000000000000000000, -1.734723475976807292E-15 ) ) ;
#110974=AXIS2_PLACEMENT_3D ( 'NONE', #223679, #26812, #106290 ) ;
#110985=CARTESIAN_POINT ( 'NONE',  ( 18.59999999999999076, 6.450000000011156587, -188.7499999999999716 ) ) ;
#110988=ORIENTED_EDGE ( 'NONE', *, *, #173026, .F. ) ;
#111002=CIRCLE ( 'NONE', #169310, 0.1000000000000098310 ) ;
#111061=VERTEX_POINT ( 'NONE', #44460 ) ;
#111066=ORIENTED_EDGE ( 'NONE', *, *, #138832, .F. ) ;
#111073=SPHERICAL_SURFACE ( 'NONE', #110249, 0.1000000000000000056 ) ;
#111077=CARTESIAN_POINT ( 'NONE',  ( 21.14999999999999858, 11.65000000001115943, -167.5999999999999659 ) ) ;
#111110=ORIENTED_EDGE ( 'NONE', *, *, #143253, .F. ) ;
#111146=CIRCLE ( 'NONE', #98625, 0.1999999999999996503 ) ;
#111148=ORIENTED_EDGE ( 'NONE', *, *, #243834, .F. ) ;
#111159=EDGE_LOOP ( 'NONE', ( #217109, #243522, #205193, #23690 ) ) ;
#111179=CARTESIAN_POINT ( 'NONE',  ( -22.50000000000000000, 11.64976291804307884, -167.4111900236130452 ) ) ;
#111299=ORIENTED_EDGE ( 'NONE', *, *, #191536, .F. ) ;
#111308=TOROIDAL_SURFACE ( 'NONE', #15658, 4.149999999999999467, 0.1000000000000000056 ) ;
#111330=DIRECTION ( 'NONE',  ( 1.000000000000000000, 0.000000000000000000, 0.000000000000000000 ) ) ;
#111346=CARTESIAN_POINT ( 'NONE',  ( 20.94999999999999574, -1.162701749926853712, -175.4999999999999716 ) ) ;
#111351=CIRCLE ( 'NONE', #65372, 7.800000000000001599 ) ;
#111352=AXIS2_PLACEMENT_3D ( 'NONE', #210059, #232196, #31443 ) ;
#111392=TOROIDAL_SURFACE ( 'NONE', #157203, 0.2000000000000000111, 0.1000000000000000056 ) ;
#111396=CARTESIAN_POINT ( 'NONE',  ( 18.59999999999999076, 11.75000000001115907, -155.7499999999999716 ) ) ;
#111421=DIRECTION ( 'NONE',  ( -0.000000000000000000, -0.000000000000000000, -1.000000000000000000 ) ) ;
#111473=ORIENTED_EDGE ( 'NONE', *, *, #12906, .T. ) ;
#111489=CARTESIAN_POINT ( 'NONE',  ( -21.05000000000000071, 1.835341550235567887, -179.0551512925629538 ) ) ;
#111533=AXIS2_PLACEMENT_3D ( 'NONE', #171544, #231500, #52833 ) ;
#111534=ORIENTED_EDGE ( 'NONE', *, *, #28481, .F. ) ;
#111541=ORIENTED_EDGE ( 'NONE', *, *, #177394, .T. ) ;
#111550=AXIS2_PLACEMENT_3D ( 'NONE', #226026, #48698, #64425 ) ;
#111562=DIRECTION ( 'NONE',  ( 0.000000000000000000, 0.1350103645451876666, -0.9908441862701600211 ) ) ;
#111572=AXIS2_PLACEMENT_3D ( 'NONE', #195260, #94837, #152280 ) ;
#111611=EDGE_CURVE ( 'NONE', #79726, #86816, #116356, .T. ) ;
#111656=CARTESIAN_POINT ( 'NONE',  ( -23.15000000000000213, -11.74999999998884448, -155.7499999999999716 ) ) ;
#111674=ORIENTED_EDGE ( 'NONE', *, *, #114300, .F. ) ;
#111698=LINE ( 'NONE', #15178, #185085 ) ;
#111699=CIRCLE ( 'NONE', #236763, 12.87499999999999822 ) ;
#111713=CIRCLE ( 'NONE', #228255, 0.09999999999998898659 ) ;
#111745=CARTESIAN_POINT ( 'NONE',  ( -22.47886152344871036, 0.03750093887284929733, -155.8500113569520238 ) ) ;
#111791=CARTESIAN_POINT ( 'NONE',  ( 20.94999999999999574, -11.64999999998883595, -170.5999999999999659 ) ) ;
#111796=CARTESIAN_POINT ( 'NONE',  ( 23.15000000000000213, -11.74999999998883737, -179.7499999999999716 ) ) ;
#111808=CARTESIAN_POINT ( 'NONE',  ( -18.50000000000000355, -1.263275465206102233, -208.9018646667463770 ) ) ;
#111809=ORIENTED_EDGE ( 'NONE', *, *, #236125, .T. ) ;
#111836=CARTESIAN_POINT ( 'NONE',  ( -21.07094088545368749, 0.09889370256337755294, -161.1798327780828402 ) ) ;
#111856=ORIENTED_EDGE ( 'NONE', *, *, #90668, .T. ) ;
#111878=CARTESIAN_POINT ( 'NONE',  ( 21.05000000000000426, 0.06570161033324604938, -161.2416839426679758 ) ) ;
#111887=CIRCLE ( 'NONE', #149303, 0.09999999999999820144 ) ;
#111898=EDGE_CURVE ( 'NONE', #257429, #132941, #248120, .T. ) ;
#111911=CARTESIAN_POINT ( 'NONE',  ( -20.54999999999999716, -8.999999999988846255, -177.3939691226524076 ) ) ;
#111918=AXIS2_PLACEMENT_3D ( 'NONE', #210043, #28871, #33998 ) ;
#111972=CYLINDRICAL_SURFACE ( 'NONE', #244158, 0.09999999999999939493 ) ;
#111975=DIRECTION ( 'NONE',  ( 0.000000000000000000, 0.000000000000000000, -1.000000000000000000 ) ) ;
#111979=ORIENTED_EDGE ( 'NONE', *, *, #171225, .T. ) ;
#111985=DIRECTION ( 'NONE',  ( 0.000000000000000000, 0.000000000000000000, 1.000000000000000000 ) ) ;
#112000=AXIS2_PLACEMENT_3D ( 'NONE', #149073, #210324, #207766 ) ;
#112024=DIRECTION ( 'NONE',  ( 0.000000000000000000, 0.000000000000000000, -1.000000000000000000 ) ) ;
#112032=ORIENTED_EDGE ( 'NONE', *, *, #135238, .F. ) ;
#112043=DIRECTION ( 'NONE',  ( -0.000000000000000000, 1.000000000000000000, -0.000000000000000000 ) ) ;
#112084=CARTESIAN_POINT ( 'NONE',  ( -23.15000000000000213, 1.115649653272650466E-11, -204.9999999999999716 ) ) ;
#112085=DIRECTION ( 'NONE',  ( 3.469446951953728416E-14, -0.8660254037844309360, 0.5000000000000134337 ) ) ;
#112100=EDGE_CURVE ( 'NONE', #23864, #90327, #215416, .T. ) ;
#112115=DIRECTION ( 'NONE',  ( -0.000000000000000000, -0.000000000000000000, -1.000000000000000000 ) ) ;
#112145=CARTESIAN_POINT ( 'NONE',  ( 18.42555734704282600, -9.497158361925556846, -174.5398304977348971 ) ) ;
#112170=AXIS2_PLACEMENT_3D ( 'NONE', #33750, #71570, #114522 ) ;
#112187=CARTESIAN_POINT ( 'NONE',  ( 23.15000000000000213, -8.999999999988844479, -177.3939691226524076 ) ) ;
#112203=CIRCLE ( 'NONE', #87014, 0.09999999999999939493 ) ;
#112230=AXIS2_PLACEMENT_3D ( 'NONE', #245247, #2754, #62751 ) ;
#112231=VERTEX_POINT ( 'NONE', #199733 ) ;
#112240=FACE_OUTER_BOUND ( 'NONE', #157705, .T. ) ;
#112243=AXIS2_PLACEMENT_3D ( 'NONE', #107091, #167110, #246601 ) ;
#112251=DIRECTION ( 'NONE',  ( 0.000000000000000000, 1.734723475976998188E-13, 1.000000000000000000 ) ) ;
#112281=ORIENTED_EDGE ( 'NONE', *, *, #116796, .F. ) ;
#112290=CARTESIAN_POINT ( 'NONE',  ( -20.85000000000000142, -0.3238857010591806307, -200.9575895893139545 ) ) ;
#112299=ORIENTED_EDGE ( 'NONE', *, *, #129445, .T. ) ;
#112307=CARTESIAN_POINT ( 'NONE',  ( -18.59999999999999787, 1.162701749949165642, -175.4999999999999716 ) ) ;
#112309=CARTESIAN_POINT ( 'NONE',  ( 18.49999999999999289, 10.25000000001115552, -188.8499999999999659 ) ) ;
#112326=FACE_OUTER_BOUND ( 'NONE', #195403, .T. ) ;
#112387=ORIENTED_EDGE ( 'NONE', *, *, #238079, .F. ) ;
#112397=VECTOR ( 'NONE', #163911, 1000.000000000000000 ) ;
#112417=EDGE_CURVE ( 'NONE', #178867, #143316, #241606, .T. ) ;
#112420=DIRECTION ( 'NONE',  ( 0.000000000000000000, -1.000000000000000000, -0.000000000000000000 ) ) ;
#112425=DIRECTION ( 'NONE',  ( 1.000000000000000000, 0.000000000000000000, 0.000000000000000000 ) ) ;
#112506=CARTESIAN_POINT ( 'NONE',  ( -18.50000000000000711, 11.75000000001115197, -174.5148057706539930 ) ) ;
#112528=LINE ( 'NONE', #209053, #210915 ) ;
#112530=CIRCLE ( 'NONE', #62471, 0.09999999999998898659 ) ;
#112534=ADVANCED_FACE ( 'NONE', ( #114738 ), #237251, .T. ) ;
#112539=CARTESIAN_POINT ( 'NONE',  ( 21.08035267497491105, 6.331706839794169817, -167.4173113752238464 ) ) ;
#112553=LINE ( 'NONE', #231227, #236119 ) ;
#112559=LINE ( 'NONE', #75989, #253299 ) ;
#112598=CARTESIAN_POINT ( 'NONE',  ( 23.24999999999999289, 6.650000000011155876, -188.8499999999999659 ) ) ;
#112601=CARTESIAN_POINT ( 'NONE',  ( -22.39999999999999858, 0.1000000000111554016, -167.4999999999999716 ) ) ;
#112609=DIRECTION ( 'NONE',  ( 1.000000000000000000, 0.000000000000000000, 0.000000000000000000 ) ) ;
#112612=DIRECTION ( 'NONE',  ( -1.000000000000000000, 0.000000000000000000, 0.000000000000000000 ) ) ;
#112613=ADVANCED_FACE ( 'NONE', ( #81986 ), #108342, .T. ) ;
#112714=EDGE_CURVE ( 'NONE', #229311, #199945, #108012, .T. ) ;
#112736=EDGE_CURVE ( 'NONE', #117217, #48866, #133632, .T. ) ;
#112737=VERTEX_POINT ( 'NONE', #10205 ) ;
#112738=AXIS2_PLACEMENT_3D ( 'NONE', #24044, #223490, #60566 ) ;
#112769=CARTESIAN_POINT ( 'NONE',  ( 20.95512828230152280, 8.876151312336450161, -179.7024302655030965 ) ) ;
#112782=DIRECTION ( 'NONE',  ( -0.000000000000000000, 0.01283462868039629209, -0.9999176327611372095 ) ) ;
#112811=CARTESIAN_POINT ( 'NONE',  ( -18.47079683080347223, -9.471664105233724484, -174.6088605409921968 ) ) ;
#112833=DIRECTION ( 'NONE',  ( 0.000000000000000000, 0.000000000000000000, -1.000000000000000000 ) ) ;
#112865=ADVANCED_FACE ( 'NONE', ( #55690 ), #14059, .T. ) ;
#112869=CARTESIAN_POINT ( 'NONE',  ( 18.49999999999999289, 11.65000000001115943, -155.7499999999999716 ) ) ;
#112872=AXIS2_PLACEMENT_3D ( 'NONE', #121664, #82480, #81206 ) ;
#112877=DIRECTION ( 'NONE',  ( 0.000000000000000000, 1.000000000000000000, -3.469446951953635015E-14 ) ) ;
#112906=DIRECTION ( 'NONE',  ( -1.000000000000000000, 0.000000000000000000, 0.000000000000000000 ) ) ;
#112908=B_SPLINE_CURVE_WITH_KNOTS ( 'NONE', 3,
 ( #196578, #64463, #82695, #136594, #234420, #76633, #216140, #104823, #5735, #3175, #243084, #123152, #57043, #214863, #17940, #77909, #177052, #156208, #97455 ),
 .UNSPECIFIED., .F., .F.,
 ( 4, 3, 3, 3, 3, 3, 4 ),
 ( -2.000416914636979038E-06, 4.235164736271501695E-22, 4.714008503747322393E-05, 9.979203887779805799E-05, 0.0001372215519229540691, 0.0001635031576221083007, 0.0001900083748504232718 ),
 .UNSPECIFIED. ) ;
#112916=DIRECTION ( 'NONE',  ( 0.000000000000000000, -1.000000000000000000, 0.000000000000000000 ) ) ;
#112949=DIRECTION ( 'NONE',  ( 0.000000000000000000, 0.000000000000000000, -1.000000000000000000 ) ) ;
#112962=EDGE_CURVE ( 'NONE', #255868, #226886, #4453, .T. ) ;
#112966=ADVANCED_FACE ( 'NONE', ( #2156 ), #208496, .T. ) ;
#112982=CIRCLE ( 'NONE', #527, 0.09999999999999939493 ) ;
#113039=AXIS2_PLACEMENT_3D ( 'NONE', #100965, #157168, #180564 ) ;
#113062=CARTESIAN_POINT ( 'NONE',  ( 21.05000000000000071, 1.115653327213047955E-11, -171.8000000000000114 ) ) ;
#113075=LINE ( 'NONE', #111796, #212029 ) ;
#113092=ORIENTED_EDGE ( 'NONE', *, *, #164813, .T. ) ;
#113128=CIRCLE ( 'NONE', #117413, 0.09999999999998898659 ) ;
#113132=DIRECTION ( 'NONE',  ( 0.7071067811865474617, 0.7071067811865474617, 0.000000000000000000 ) ) ;
#113138=CIRCLE ( 'NONE', #233763, 0.2000000000000000944 ) ;
#113167=DIRECTION ( 'NONE',  ( 0.000000000000000000, 0.9999631594459056361, -0.008583690987128059571 ) ) ;
#113173=EDGE_LOOP ( 'NONE', ( #189169, #200340, #193501, #2513 ) ) ;
#113207=CARTESIAN_POINT ( 'NONE',  ( 21.05000000000000071, 1.115600667400684642E-11, -200.9999999999999432 ) ) ;
#113251=DIRECTION ( 'NONE',  ( 1.000000000000000000, 0.000000000000000000, -0.000000000000000000 ) ) ;
#113258=AXIS2_PLACEMENT_3D ( 'NONE', #177967, #193671, #76271 ) ;
#113276=CARTESIAN_POINT ( 'NONE',  ( -18.31572283045136729, -9.548437830874727084, -207.8506256510582944 ) ) ;
#113284=EDGE_LOOP ( 'NONE', ( #76882, #218759, #57182, #194481 ) ) ;
#113359=EDGE_CURVE ( 'NONE', #85475, #1689, #226831, .T. ) ;
#113374=VERTEX_POINT ( 'NONE', #186620 ) ;
#113382=ORIENTED_EDGE ( 'NONE', *, *, #248969, .F. ) ;
#113388=ORIENTED_EDGE ( 'NONE', *, *, #91634, .F. ) ;
#113411=EDGE_LOOP ( 'NONE', ( #27974, #232877, #94527, #64635 ) ) ;
#113421=DIRECTION ( 'NONE',  ( -1.000000000000000000, 0.000000000000000000, 0.000000000000000000 ) ) ;
#113431=CARTESIAN_POINT ( 'NONE',  ( 20.94999999999999574, 1.115600667400684642E-11, -167.4999999999999716 ) ) ;
#113432=FACE_OUTER_BOUND ( 'NONE', #226843, .T. ) ;
#113466=ORIENTED_EDGE ( 'NONE', *, *, #37540, .F. ) ;
#113522=AXIS2_PLACEMENT_3D ( 'NONE', #21666, #163744, #64627 ) ;
#113532=CIRCLE ( 'NONE', #76107, 0.09999999999999817368 ) ;
#113555=EDGE_CURVE ( 'NONE', #145192, #223514, #246435, .T. ) ;
#113557=DIRECTION ( 'NONE',  ( 0.000000000000000000, 0.1298341882520022694, 0.9915357197604852679 ) ) ;
#113584=DIRECTION ( 'NONE',  ( 1.000000000000000000, 0.000000000000000000, 0.000000000000000000 ) ) ;
#113615=CARTESIAN_POINT ( 'NONE',  ( -23.15000000000000213, 4.250000000011156409, -188.6499999999999488 ) ) ;
#113626=EDGE_CURVE ( 'NONE', #145347, #204451, #119942, .T. ) ;
#113640=CARTESIAN_POINT ( 'NONE',  ( 18.59999999999999076, 10.20857864377385127, -188.8499999999999659 ) ) ;
#113642=CARTESIAN_POINT ( 'NONE',  ( 19.92426406871192412, 11.75000000001116085, -192.3499999999999375 ) ) ;
#113647=DIRECTION ( 'NONE',  ( -1.000000000000000000, -2.952720810173289112E-16, 0.000000000000000000 ) ) ;
#113665=EDGE_CURVE ( 'NONE', #50465, #200909, #4793, .T. ) ;
#113683=CIRCLE ( 'NONE', #234476, 0.09999999999999939493 ) ;
#113691=CIRCLE ( 'NONE', #176259, 0.09999999999998898659 ) ;
#113748=CIRCLE ( 'NONE', #238844, 0.09999999999999939493 ) ;
#113751=CARTESIAN_POINT ( 'NONE',  ( -21.05000000000000071, -1.162701749926853712, -175.4999999999999716 ) ) ;
#113760=EDGE_LOOP ( 'NONE', ( #208491, #61394, #170968, #202979 ) ) ;
#113780=ORIENTED_EDGE ( 'NONE', *, *, #42330, .T. ) ;
#113794=EDGE_CURVE ( 'NONE', #10283, #188501, #213279, .T. ) ;
#113805=EDGE_CURVE ( 'NONE', #61925, #227290, #84060, .T. ) ;
#113821=CARTESIAN_POINT ( 'NONE',  ( -20.64999999999999858, 1.115600667400684642E-11, -202.8999999999999773 ) ) ;
#113889=CARTESIAN_POINT ( 'NONE',  ( -18.59999999999999787, -1.835859311432481045, -212.5044391687984842 ) ) ;
#113937=ORIENTED_EDGE ( 'NONE', *, *, #170241, .T. ) ;
#113946=AXIS2_PLACEMENT_3D ( 'NONE', #15973, #36824, #56327 ) ;
#113947=TOROIDAL_SURFACE ( 'NONE', #188981, 12.77500000000000036, 0.1000000000000000056 ) ;
#113952=ORIENTED_EDGE ( 'NONE', *, *, #80269, .T. ) ;
#113955=CARTESIAN_POINT ( 'NONE',  ( -23.15000000000000213, 2.000000000011154189, -180.7246219227620543 ) ) ;
#113957=ORIENTED_EDGE ( 'NONE', *, *, #28808, .T. ) ;
#113972=EDGE_LOOP ( 'NONE', ( #135052, #119710, #58645 ) ) ;
#113975=CIRCLE ( 'NONE', #30622, 0.09999999999998898659 ) ;
#113997=DIRECTION ( 'NONE',  ( 0.000000000000000000, 1.000000000000000000, 0.000000000000000000 ) ) ;
#114020=CARTESIAN_POINT ( 'NONE',  ( -21.05000000000000071, 1.115653327213047955E-11, -163.2000000000000171 ) ) ;
#114125=VECTOR ( 'NONE', #70636, 1000.000000000000000 ) ;
#114147=B_SPLINE_CURVE_WITH_KNOTS ( 'NONE', 3,
 ( #121757, #138687, #102136, #21376, #100839, #77444, #1773, #59153, #256049, #482, #119175, #158331, #39663, #198702, #236534, #240407, #57888, #78736, #61761 ),
 .UNSPECIFIED., .F., .F.,
 ( 4, 3, 3, 3, 3, 3, 4 ),
 ( 0.000000000000000000, 2.646747978908900846E-05, 5.271166642128170848E-05, 9.008788829884258422E-05, 0.0001426648776560945301, 0.0001897378458659844771, 0.0001917382627806300734 ),
 .UNSPECIFIED. ) ;
#114184=EDGE_LOOP ( 'NONE', ( #214261, #146242, #164358, #51842 ) ) ;
#114260=EDGE_LOOP ( 'NONE', ( #141450, #184199, #73954, #1326 ) ) ;
#114269=ORIENTED_EDGE ( 'NONE', *, *, #105144, .T. ) ;
#114300=EDGE_CURVE ( 'NONE', #4264, #257620, #155067, .T. ) ;
#114305=PLANE ( 'NONE',  #160726 ) ;
#114321=CARTESIAN_POINT ( 'NONE',  ( 18.59999999999998366, 1.115600667400684642E-11, -200.9999999999999432 ) ) ;
#114358=EDGE_CURVE ( 'NONE', #108161, #86456, #235368, .T. ) ;
#114371=DIRECTION ( 'NONE',  ( 0.000000000000000000, 0.000000000000000000, 1.000000000000000000 ) ) ;
#114376=VECTOR ( 'NONE', #65166, 1000.000000000000000 ) ;
#114380=EDGE_CURVE ( 'NONE', #58178, #100214, #38517, .T. ) ;
#114385=VERTEX_POINT ( 'NONE', #253640 ) ;
#114391=DIRECTION ( 'NONE',  ( 1.000000000000000000, 0.000000000000000000, 0.000000000000000000 ) ) ;
#114401=VERTEX_POINT ( 'NONE', #215796 ) ;
#114407=EDGE_CURVE ( 'NONE', #181739, #82856, #184252, .T. ) ;
#114409=AXIS2_PLACEMENT_3D ( 'NONE', #136147, #236553, #174071 ) ;
#114425=DIRECTION ( 'NONE',  ( 1.000000000000000000, -0.000000000000000000, -0.000000000000000000 ) ) ;
#114433=CARTESIAN_POINT ( 'NONE',  ( 21.05000000000000071, 0.09779029131994770863, -161.2421853895238542 ) ) ;
#114446=CARTESIAN_POINT ( 'NONE',  ( -18.50000000000000000, 1.162701749949165642, -175.5999999999999659 ) ) ;
#114450=ORIENTED_EDGE ( 'NONE', *, *, #106870, .T. ) ;
#114474=EDGE_CURVE ( 'NONE', #122594, #69026, #138989, .T. ) ;
#114475=CARTESIAN_POINT ( 'NONE',  ( 21.05000000000000071, -11.29603075032412995, -170.5478991596638423 ) ) ;
#114495=DIRECTION ( 'NONE',  ( 1.000000000000000000, -0.000000000000000000, -0.000000000000000000 ) ) ;
#114522=DIRECTION ( 'NONE',  ( 0.000000000000000000, 0.000000000000000000, 1.000000000000000000 ) ) ;
#114534=CARTESIAN_POINT ( 'NONE',  ( 20.13684514579856000, 9.495855392757592384, -175.6430316856907723 ) ) ;
#114546=EDGE_CURVE ( 'NONE', #115618, #29625, #151466, .T. ) ;
#114560=VERTEX_POINT ( 'NONE', #215271 ) ;
#114623=DIRECTION ( 'NONE',  ( -1.000000000000000000, 7.304098846218134667E-16, -4.217023435051678980E-16 ) ) ;
#114625=DIRECTION ( 'NONE',  ( -1.000000000000000000, -0.000000000000000000, -0.000000000000000000 ) ) ;
#114670=CARTESIAN_POINT ( 'NONE',  ( 20.94999999999999929, 5.000000000011153745, -188.5947339810868755 ) ) ;
#114678=CARTESIAN_POINT ( 'NONE',  ( -21.65000000000000213, 7.708578643773852157, -188.6499999999999488 ) ) ;
#114738=FACE_OUTER_BOUND ( 'NONE', #86259, .T. ) ;
#114739=DIRECTION ( 'NONE',  ( -1.000000000000000000, 0.000000000000000000, 0.000000000000000000 ) ) ;
#114773=DIRECTION ( 'NONE',  ( 0.000000000000000000, -1.000000000000000000, 0.000000000000000000 ) ) ;
#114785=ADVANCED_FACE ( 'NONE', ( #65172 ), #123885, .F. ) ;
#114794=AXIS2_PLACEMENT_3D ( 'NONE', #106058, #68252, #147794 ) ;
#114817=ORIENTED_EDGE ( 'NONE', *, *, #13962, .F. ) ;
#114856=AXIS2_PLACEMENT_3D ( 'NONE', #129833, #127280, #148129 ) ;
#114859=FACE_OUTER_BOUND ( 'NONE', #7397, .T. ) ;
#114886=DIRECTION ( 'NONE',  ( -0.000000000000000000, -0.000000000000000000, -1.000000000000000000 ) ) ;
#114947=CARTESIAN_POINT ( 'NONE',  ( 21.00023020733505064, 1.115539681028482333E-11, -161.1091307547316092 ) ) ;
#114953=FACE_OUTER_BOUND ( 'NONE', #212781, .T. ) ;
#114954=ORIENTED_EDGE ( 'NONE', *, *, #215007, .F. ) ;
#114956=ORIENTED_EDGE ( 'NONE', *, *, #157951, .T. ) ;
#114981=CARTESIAN_POINT ( 'NONE',  ( -20.94999999999999929, -11.74999999998884448, -170.3999999999999773 ) ) ;
#114993=TOROIDAL_SURFACE ( 'NONE', #69229, 0.9750000000000019762, 0.1000000000000000056 ) ;
#114997=EDGE_LOOP ( 'NONE', ( #203577, #52206, #15287, #217018 ) ) ;
#115000=ORIENTED_EDGE ( 'NONE', *, *, #2583, .F. ) ;
#115006=CARTESIAN_POINT ( 'NONE',  ( 21.05000000000000071, -8.999999999988842703, -191.1060308773475072 ) ) ;
#115032=DIRECTION ( 'NONE',  ( -0.000000000000000000, -1.000000000000000000, 6.308085367188393199E-16 ) ) ;
#115040=CARTESIAN_POINT ( 'NONE',  ( 20.85000000000000142, 6.846123162363745074, -204.7377262668498190 ) ) ;
#115047=EDGE_LOOP ( 'NONE', ( #215218, #164270, #46730, #1539 ) ) ;
#115075=ORIENTED_EDGE ( 'NONE', *, *, #144056, .F. ) ;
#115138=VECTOR ( 'NONE', #197184, 1000.000000000000000 ) ;
#115184=CIRCLE ( 'NONE', #48538, 0.09999999999999917288 ) ;
#115194=CARTESIAN_POINT ( 'NONE',  ( 20.94999999999999929, 5.000000000011153745, -179.9052660189130677 ) ) ;
#115288=CARTESIAN_POINT ( 'NONE',  ( -22.39999999999999858, 0.1000000000111554016, -159.7092204016265384 ) ) ;
#115302=CIRCLE ( 'NONE', #36234, 11.70000000000001528 ) ;
#115311=CARTESIAN_POINT ( 'NONE',  ( -20.64999999999999858, 7.150000000011155876, -179.8499999999999943 ) ) ;
#115342=VERTEX_POINT ( 'NONE', #25135 ) ;
#115345=ORIENTED_EDGE ( 'NONE', *, *, #92606, .T. ) ;
#115351=ORIENTED_EDGE ( 'NONE', *, *, #46232, .T. ) ;
#115354=CIRCLE ( 'NONE', #2921, 0.9750000000000036415 ) ;
#115374=ORIENTED_EDGE ( 'NONE', *, *, #81437, .T. ) ;
#115381=VECTOR ( 'NONE', #55701, 1000.000000000000000 ) ;
#115384=CIRCLE ( 'NONE', #36306, 0.09999999999998898659 ) ;
#115385=DIRECTION ( 'NONE',  ( 0.000000000000000000, 0.6728971962617388280, 0.7397360091702248619 ) ) ;
#115428=DIRECTION ( 'NONE',  ( -0.000000000000000000, -0.000000000000000000, -1.000000000000000000 ) ) ;
#115432=DIRECTION ( 'NONE',  ( 0.000000000000000000, 3.469446951953995998E-14, 1.000000000000000000 ) ) ;
#115463=AXIS2_PLACEMENT_3D ( 'NONE', #124256, #224613, #45982 ) ;
#115491=DIRECTION ( 'NONE',  ( 9.044546369203339308E-15, -0.7397360091702694929, -0.6728971962616898672 ) ) ;
#115497=DIRECTION ( 'NONE',  ( -0.000000000000000000, 0.000000000000000000, -1.000000000000000000 ) ) ;
#115507=VERTEX_POINT ( 'NONE', #27721 ) ;
#115519=EDGE_CURVE ( 'NONE', #181381, #118267, #163403, .T. ) ;
#115558=DIRECTION ( 'NONE',  ( 1.000000000000000000, 1.836970198721029934E-16, -0.000000000000000000 ) ) ;
#115570=AXIS2_PLACEMENT_3D ( 'NONE', #249214, #91423, #250479 ) ;
#115572=CARTESIAN_POINT ( 'NONE',  ( -20.99749315643151348, 11.75000000001115197, -193.9851942312420192 ) ) ;
#115615=AXIS2_PLACEMENT_3D ( 'NONE', #41592, #121136, #200645 ) ;
#115618=VERTEX_POINT ( 'NONE', #73261 ) ;
#115632=EDGE_LOOP ( 'NONE', ( #193188, #70822, #37419, #175213 ) ) ;
#115659=EDGE_CURVE ( 'NONE', #128029, #213316, #100980, .T. ) ;
#115660=DIRECTION ( 'NONE',  ( 1.000000000000000000, 0.000000000000000000, 0.000000000000000000 ) ) ;
#115666=TOROIDAL_SURFACE ( 'NONE', #61505, 4.149999999999999467, 0.1000000000000000056 ) ;
#115671=ORIENTED_EDGE ( 'NONE', *, *, #71738, .T. ) ;
#115677=FACE_OUTER_BOUND ( 'NONE', #17511, .T. ) ;
#115680=DIRECTION ( 'NONE',  ( 1.000000000000000000, -0.000000000000000000, -0.000000000000000000 ) ) ;
#115763=DIRECTION ( 'NONE',  ( -1.000000000000000000, -1.875376730785737719E-16, -0.000000000000000000 ) ) ;
#115765=DIRECTION ( 'NONE',  ( 0.000000000000000000, 0.000000000000000000, -1.000000000000000000 ) ) ;
#115781=EDGE_CURVE ( 'NONE', #141186, #84620, #118786, .T. ) ;
#115805=LINE ( 'NONE', #134068, #142550 ) ;
#115809=ORIENTED_EDGE ( 'NONE', *, *, #228508, .T. ) ;
#115848=LINE ( 'NONE', #257868, #208825 ) ;
#115870=TOROIDAL_SURFACE ( 'NONE', #236656, 0.4000000000000003553, 0.1000000000000000056 ) ;
#115887=EDGE_CURVE ( 'NONE', #68978, #205992, #50760, .T. ) ;
#115910=CARTESIAN_POINT ( 'NONE',  ( -23.25000000000000000, 2.000000000011154189, -187.7753780772378889 ) ) ;
#115917=DIRECTION ( 'NONE',  ( -1.000000000000000000, -2.952720810173289112E-16, 0.000000000000000000 ) ) ;
#115925=DIRECTION ( 'NONE',  ( 3.469446951953243109E-14, 0.4999999999999608646, 0.8660254037844612451 ) ) ;
#115936=ADVANCED_FACE ( 'NONE', ( #9099 ), #203239, .T. ) ;
#115940=ORIENTED_EDGE ( 'NONE', *, *, #120997, .T. ) ;
#115947=ORIENTED_EDGE ( 'NONE', *, *, #27256, .F. ) ;
#115951=DIRECTION ( 'NONE',  ( 0.7070776581709139474, -0.7071359030027652981, -2.453168425935592377E-14 ) ) ;
#115952=FACE_OUTER_BOUND ( 'NONE', #130535, .T. ) ;
#115983=CARTESIAN_POINT ( 'NONE',  ( -18.59999999999999787, 1.115600667400684642E-11, -200.9999999999999432 ) ) ;
#116027=DIRECTION ( 'NONE',  ( 0.000000000000000000, 0.000000000000000000, -1.000000000000000000 ) ) ;
#116028=AXIS2_PLACEMENT_3D ( 'NONE', #164763, #130450, #203876 ) ;
#116031=CARTESIAN_POINT ( 'NONE',  ( 18.59999999999999076, 1.835341550235567887, -179.0551512925629538 ) ) ;
#116063=DIRECTION ( 'NONE',  ( 0.000000000000000000, 0.000000000000000000, -1.000000000000000000 ) ) ;
#116084=VECTOR ( 'NONE', #196895, 1000.000000000000000 ) ;
#116180=CIRCLE ( 'NONE', #120303, 0.09999999999999939493 ) ;
#116192=CIRCLE ( 'NONE', #257562, 0.1000000000000001027 ) ;
#116197=EDGE_LOOP ( 'NONE', ( #65246, #30984, #101098, #71097 ) ) ;
#116199=ADVANCED_FACE ( 'NONE', ( #1048 ), #80589, .T. ) ;
#116227=ADVANCED_FACE ( 'NONE', ( #126146 ), #255283, .T. ) ;
#116232=CARTESIAN_POINT ( 'NONE',  ( 20.04142135623730070, 11.75000000001115907, -192.1499999999999488 ) ) ;
#116275=AXIS2_PLACEMENT_3D ( 'NONE', #192054, #92916, #172523 ) ;
#116285=VERTEX_POINT ( 'NONE', #29662 ) ;
#116307=FACE_OUTER_BOUND ( 'NONE', #45139, .T. ) ;
#116310=DIRECTION ( 'NONE',  ( 0.000000000000000000, -0.9999176327611369874, 0.01283462868041984617 ) ) ;
#116313=DIRECTION ( 'NONE',  ( 6.484947573744954877E-15, 0.9274965247785529332, -0.3738317757009255171 ) ) ;
#116344=ORIENTED_EDGE ( 'NONE', *, *, #2473, .T. ) ;
#116356=CIRCLE ( 'NONE', #3924, 11.70000000000001528 ) ;
#116384=DIRECTION ( 'NONE',  ( 1.000000000000000000, 0.000000000000000000, 0.000000000000000000 ) ) ;
#116386=EDGE_CURVE ( 'NONE', #135869, #119689, #221986, .T. ) ;
#116389=DIRECTION ( 'NONE',  ( 0.000000000000000000, 1.000000000000000000, 0.000000000000000000 ) ) ;
#116430=DIRECTION ( 'NONE',  ( 0.000000000000000000, 0.000000000000000000, -1.000000000000000000 ) ) ;
#116440=VERTEX_POINT ( 'NONE', #131293 ) ;
#116479=CYLINDRICAL_SURFACE ( 'NONE', #149192, 0.5000000000000004441 ) ;
#116572=LINE ( 'NONE', #257304, #222370 ) ;
#116594=EDGE_CURVE ( 'NONE', #68874, #131693, #42459, .T. ) ;
#116601=DIRECTION ( 'NONE',  ( 0.000000000000000000, 0.000000000000000000, -1.000000000000000000 ) ) ;
#116603=CARTESIAN_POINT ( 'NONE',  ( 23.15000000000000213, -11.39257802169451139, -197.9260504201680249 ) ) ;
#116605=ORIENTED_EDGE ( 'NONE', *, *, #95193, .F. ) ;
#116636=AXIS2_PLACEMENT_3D ( 'NONE', #215996, #34842, #176916 ) ;
#116646=ADVANCED_FACE ( 'NONE', ( #166305 ), #65881, .F. ) ;
#116666=CIRCLE ( 'NONE', #58377, 0.09999999999999864553 ) ;
#116673=CARTESIAN_POINT ( 'NONE',  ( 20.85000000000000142, -1.835859311432481045, -212.5044391687984842 ) ) ;
#116758=CIRCLE ( 'NONE', #4322, 0.09999999999999939493 ) ;
#116776=DIRECTION ( 'NONE',  ( 1.000000000000000000, 0.000000000000000000, 0.000000000000000000 ) ) ;
#116796=EDGE_CURVE ( 'NONE', #17335, #50465, #153167, .T. ) ;
#116817=CIRCLE ( 'NONE', #120945, 0.09999999999998898659 ) ;
#116823=ORIENTED_EDGE ( 'NONE', *, *, #136060, .F. ) ;
#116826=VERTEX_POINT ( 'NONE', #95703 ) ;
#116828=ORIENTED_EDGE ( 'NONE', *, *, #70009, .F. ) ;
#116829=FACE_OUTER_BOUND ( 'NONE', #236825, .T. ) ;
#116861=CARTESIAN_POINT ( 'NONE',  ( -20.95000000000000639, 11.75000000001115019, -194.2161343370218560 ) ) ;
#116862=VERTEX_POINT ( 'NONE', #90565 ) ;
#116872=AXIS2_PLACEMENT_3D ( 'NONE', #209447, #30845, #110347 ) ;
#116882=CARTESIAN_POINT ( 'NONE',  ( -20.85000000000000142, -1.835859311432479268, -212.5044391687984842 ) ) ;
#116891=DIRECTION ( 'NONE',  ( 0.000000000000000000, 0.000000000000000000, -1.000000000000000000 ) ) ;
#116903=ORIENTED_EDGE ( 'NONE', *, *, #182721, .F. ) ;
#116990=AXIS2_PLACEMENT_3D ( 'NONE', #133752, #112916, #51620 ) ;
#117026=VERTEX_POINT ( 'NONE', #202206 ) ;
#117042=EDGE_CURVE ( 'NONE', #87114, #164666, #37059, .T. ) ;
#117066=DIRECTION ( 'NONE',  ( 0.000000000000000000, -1.000000000000000000, 0.000000000000000000 ) ) ;
#117104=CARTESIAN_POINT ( 'NONE',  ( -20.54999999999999716, 7.250000000011155521, -179.7499999999999716 ) ) ;
#117141=DIRECTION ( 'NONE',  ( 0.000000000000000000, 0.000000000000000000, -1.000000000000000000 ) ) ;
#117144=CARTESIAN_POINT ( 'NONE',  ( -21.07928932188134041, 0.09889514566555068775, -161.1714833436066669 ) ) ;
#117191=CARTESIAN_POINT ( 'NONE',  ( -21.08376601933334271, 0.06377601094103295398, -161.1580527287242433 ) ) ;
#117217=VERTEX_POINT ( 'NONE', #86070 ) ;
#117225=DIRECTION ( 'NONE',  ( -1.000000000000000000, -0.000000000000000000, 0.000000000000000000 ) ) ;
#117241=CIRCLE ( 'NONE', #54688, 0.09999999999999939493 ) ;
#117243=DIRECTION ( 'NONE',  ( 0.000000000000000000, -0.9915357197604853789, 0.1298341882520022694 ) ) ;
#117251=DIRECTION ( 'NONE',  ( -1.000000000000000000, -0.000000000000000000, -0.000000000000000000 ) ) ;
#117253=VERTEX_POINT ( 'NONE', #10430 ) ;
#117277=DIRECTION ( 'NONE',  ( 0.000000000000000000, -0.000000000000000000, 1.000000000000000000 ) ) ;
#117308=DIRECTION ( 'NONE',  ( 1.000000000000000000, -0.000000000000000000, -0.000000000000000000 ) ) ;
#117312=CARTESIAN_POINT ( 'NONE',  ( 21.00000000000000000, 9.750000000011153745, -188.6499999999999488 ) ) ;
#117322=AXIS2_PLACEMENT_3D ( 'NONE', #98276, #177876, #26504 ) ;
#117347=ADVANCED_FACE ( 'NONE', ( #78081 ), #43517, .T. ) ;
#117369=DIRECTION ( 'NONE',  ( 0.000000000000000000, -0.9999631594459056361, -0.008583690987124413183 ) ) ;
#117371=CARTESIAN_POINT ( 'NONE',  ( -20.54999999999999716, -9.499999999988848032, -177.3939691226524076 ) ) ;
#117379=VERTEX_POINT ( 'NONE', #220178 ) ;
#117383=DIRECTION ( 'NONE',  ( 0.000000000000000000, 0.000000000000000000, -1.000000000000000000 ) ) ;
#117413=AXIS2_PLACEMENT_3D ( 'NONE', #217374, #195293, #156166 ) ;
#117426=ORIENTED_EDGE ( 'NONE', *, *, #26353, .F. ) ;
#117445=EDGE_CURVE ( 'NONE', #68890, #139380, #62386, .T. ) ;
#117466=ADVANCED_FACE ( 'NONE', ( #127491 ), #10113, .F. ) ;
#117479=CARTESIAN_POINT ( 'NONE',  ( -18.50000000000000000, -1.135018845899022466, -208.7169768834322952 ) ) ;
#117500=ORIENTED_EDGE ( 'NONE', *, *, #199516, .T. ) ;
#117515=CARTESIAN_POINT ( 'NONE',  ( 21.53699400384776297, 1.117343393059872131E-11, -160.7122882067608600 ) ) ;
#117521=FACE_OUTER_BOUND ( 'NONE', #235741, .T. ) ;
#117530=DIRECTION ( 'NONE',  ( 1.000000000000000000, -0.000000000000000000, -0.000000000000000000 ) ) ;
#117535=CIRCLE ( 'NONE', #238329, 0.09999999999999917288 ) ;
#117539=DIRECTION ( 'NONE',  ( -1.000000000000000000, 0.000000000000000000, 0.000000000000000000 ) ) ;
#117560=EDGE_CURVE ( 'NONE', #114401, #215804, #87052, .T. ) ;
#117582=CARTESIAN_POINT ( 'NONE',  ( 20.94999999999999929, -8.730841121484171907, -177.0980747189843214 ) ) ;
#117591=CARTESIAN_POINT ( 'NONE',  ( 23.24999999999999645, 5.600000000011153389, -179.9052660189130677 ) ) ;
#117596=ORIENTED_EDGE ( 'NONE', *, *, #97905, .F. ) ;
#117601=DIRECTION ( 'NONE',  ( 0.000000000000000000, 0.000000000000000000, -1.000000000000000000 ) ) ;
#117603=CARTESIAN_POINT ( 'NONE',  ( 18.59999999999999076, 7.070967871809997973, -204.7465642218682547 ) ) ;
#117606=AXIS2_PLACEMENT_3D ( 'NONE', #257984, #117251, #19435 ) ;
#117641=CARTESIAN_POINT ( 'NONE',  ( 23.14999999999999503, 11.65000000001116298, -155.7499999999999716 ) ) ;
#117649=CIRCLE ( 'NONE', #126007, 0.09999999999999939493 ) ;
#117664=AXIS2_PLACEMENT_3D ( 'NONE', #13757, #170311, #231533 ) ;
#117689=CIRCLE ( 'NONE', #192517, 12.77500000000000924 ) ;
#117692=CARTESIAN_POINT ( 'NONE',  ( -18.59999999999999787, 5.950000000011100632, -177.8057023050348278 ) ) ;
#117710=DIRECTION ( 'NONE',  ( 0.000000000000000000, 0.000000000000000000, -1.000000000000000000 ) ) ;
#117714=VERTEX_POINT ( 'NONE', #113062 ) ;
#117721=DIRECTION ( 'NONE',  ( 0.000000000000000000, 0.000000000000000000, -1.000000000000000000 ) ) ;
#117733=EDGE_CURVE ( 'NONE', #86243, #195513, #158326, .T. ) ;
#117736=CARTESIAN_POINT ( 'NONE',  ( -20.64999999999999858, -8.999999999988846255, -177.3939691226524076 ) ) ;
#117760=VERTEX_POINT ( 'NONE', #222389 ) ;
#117781=CIRCLE ( 'NONE', #234303, 0.1000000000000000472 ) ;
#117789=EDGE_CURVE ( 'NONE', #136769, #129423, #137603, .T. ) ;
#117812=DIRECTION ( 'NONE',  ( 0.000000000000000000, 0.000000000000000000, 1.000000000000000000 ) ) ;
#117814=ORIENTED_EDGE ( 'NONE', *, *, #181465, .T. ) ;
#117821=ORIENTED_EDGE ( 'NONE', *, *, #117560, .F. ) ;
#117844=CARTESIAN_POINT ( 'NONE',  ( -20.54999999999999716, 1.115600667400684642E-11, -200.9999999999999432 ) ) ;
#117851=VECTOR ( 'NONE', #7326, 1000.000000000000000 ) ;
#117877=DIRECTION ( 'NONE',  ( 1.000000000000000000, 0.000000000000000000, 0.000000000000000000 ) ) ;
#117881=EDGE_LOOP ( 'NONE', ( #228652, #78582, #8666, #198509 ) ) ;
#117895=CARTESIAN_POINT ( 'NONE',  ( 21.78635804494511419, 0.09900506551883611617, -160.4643385148467871 ) ) ;
#117918=AXIS2_PLACEMENT_3D ( 'NONE', #114981, #12055, #34196 ) ;
#117956=CARTESIAN_POINT ( 'NONE',  ( 21.51976009735019346, 6.910458441670357388, -167.4999999999999716 ) ) ;
#117957=SPHERICAL_SURFACE ( 'NONE', #57619, 0.1000000000000000056 ) ;
#117975=EDGE_CURVE ( 'NONE', #203019, #172330, #3797, .T. ) ;
#117982=ORIENTED_EDGE ( 'NONE', *, *, #76044, .F. ) ;
#118012=FACE_OUTER_BOUND ( 'NONE', #150289, .T. ) ;
#118013=EDGE_LOOP ( 'NONE', ( #181435, #227391, #83855, #77690 ) ) ;
#118040=VERTEX_POINT ( 'NONE', #26369 ) ;
#118042=EDGE_CURVE ( 'NONE', #100689, #243191, #99611, .T. ) ;
#118050=DIRECTION ( 'NONE',  ( 1.000000000000000000, 0.000000000000000000, 0.000000000000000000 ) ) ;
#118060=ORIENTED_EDGE ( 'NONE', *, *, #53519, .F. ) ;
#118063=DIRECTION ( 'NONE',  ( 0.000000000000000000, 0.6728971962617483760, -0.7397360091702162022 ) ) ;
#118080=DIRECTION ( 'NONE',  ( -1.000000000000000000, 0.000000000000000000, 0.000000000000000000 ) ) ;
#118104=DIRECTION ( 'NONE',  ( -1.000000000000000000, -2.952720810173289112E-16, 0.000000000000000000 ) ) ;
#118114=CARTESIAN_POINT ( 'NONE',  ( 20.94999999999999574, 10.42338541492406279, -174.9920519238700649 ) ) ;
#118121=ORIENTED_EDGE ( 'NONE', *, *, #190036, .T. ) ;
#118140=DIRECTION ( 'NONE',  ( -1.000000000000000000, 0.000000000000000000, -0.000000000000000000 ) ) ;
#118143=ORIENTED_EDGE ( 'NONE', *, *, #146864, .T. ) ;
#118164=DIRECTION ( 'NONE',  ( 1.000000000000000000, 3.265361837132813093E-16, -0.000000000000000000 ) ) ;
#118183=ORIENTED_EDGE ( 'NONE', *, *, #256461, .F. ) ;
#118224=DIRECTION ( 'NONE',  ( 0.000000000000000000, -0.9915357197604853789, 0.1298341882520022694 ) ) ;
#118237=DIRECTION ( 'NONE',  ( 0.000000000000000000, -0.1350103645451904977, -0.9908441862701596881 ) ) ;
#118267=VERTEX_POINT ( 'NONE', #166334 ) ;
#118341=CARTESIAN_POINT ( 'NONE',  ( -23.25000000000000000, 2.000000000011154189, -188.3753780772378548 ) ) ;
#118348=EDGE_CURVE ( 'NONE', #100439, #42095, #187331, .T. ) ;
#118353=AXIS2_PLACEMENT_3D ( 'NONE', #72468, #29511, #88125 ) ;
#118361=EDGE_LOOP ( 'NONE', ( #182054, #211063, #196256, #27029 ) ) ;
#118369=EDGE_CURVE ( 'NONE', #208842, #160579, #86732, .T. ) ;
#118414=CARTESIAN_POINT ( 'NONE',  ( 21.05000000000000071, 1.115600667400684642E-11, -167.4999999999999716 ) ) ;
#118416=CARTESIAN_POINT ( 'NONE',  ( 18.54286124688534088, -9.623917578786652882, -207.7412023318626666 ) ) ;
#118435=DIRECTION ( 'NONE',  ( 0.000000000000000000, 1.000000000000000000, 0.000000000000000000 ) ) ;
#118437=AXIS2_PLACEMENT_3D ( 'NONE', #221082, #84095, #22923 ) ;
#118443=DIRECTION ( 'NONE',  ( -1.000000000000000000, 0.000000000000000000, 0.000000000000000000 ) ) ;
#118454=LINE ( 'NONE', #175867, #242026 ) ;
#118471=ORIENTED_EDGE ( 'NONE', *, *, #97023, .T. ) ;
#118485=AXIS2_PLACEMENT_3D ( 'NONE', #183794, #23471, #123829 ) ;
#118492=DIRECTION ( 'NONE',  ( 0.000000000000000000, -0.1568667991644693838, -0.9876197685951279004 ) ) ;
#118497=CARTESIAN_POINT ( 'NONE',  ( 18.59999999999999076, 11.65000000001115943, -192.2499999999999716 ) ) ;
#118507=EDGE_CURVE ( 'NONE', #117253, #21796, #128149, .T. ) ;
#118515=CIRCLE ( 'NONE', #114409, 0.2000000000000057288 ) ;
#118547=CARTESIAN_POINT ( 'NONE',  ( -20.05000000000000426, 9.250000000011157297, -179.8499999999999943 ) ) ;
#118557=DIRECTION ( 'NONE',  ( -1.000000000000000000, 0.000000000000000000, 0.000000000000000000 ) ) ;
#118572=CARTESIAN_POINT ( 'NONE',  ( 20.94999999999999929, 5.500000000011153745, -179.9052660189130677 ) ) ;
#118608=EDGE_LOOP ( 'NONE', ( #138225, #31824, #136502, #39550 ) ) ;
#118634=EDGE_LOOP ( 'NONE', ( #148526, #159202, #173798, #81446 ) ) ;
#118647=VERTEX_POINT ( 'NONE', #104691 ) ;
#118652=CARTESIAN_POINT ( 'NONE',  ( 20.95392731769792150, 8.883061479199918509, -176.0222279795712836 ) ) ;
#118715=ORIENTED_EDGE ( 'NONE', *, *, #134351, .T. ) ;
#118724=EDGE_LOOP ( 'NONE', ( #143895, #121985, #168507, #104817 ) ) ;
#118728=ORIENTED_EDGE ( 'NONE', *, *, #129265, .T. ) ;
#118760=FACE_OUTER_BOUND ( 'NONE', #91234, .T. ) ;
#118786=LINE ( 'NONE', #24839, #242683 ) ;
#118799=AXIS2_PLACEMENT_3D ( 'NONE', #101445, #123637, #21976 ) ;
#118820=CARTESIAN_POINT ( 'NONE',  ( -21.04999999999999716, 0.05132743235259914355, -161.1998166637364420 ) ) ;
#118829=EDGE_LOOP ( 'NONE', ( #40714, #189122, #19146 ) ) ;
#118844=FACE_OUTER_BOUND ( 'NONE', #227916, .T. ) ;
#118851=DIRECTION ( 'NONE',  ( -1.000000000000000000, -0.000000000000000000, 0.000000000000000000 ) ) ;
#118854=ORIENTED_EDGE ( 'NONE', *, *, #248342, .F. ) ;
#118906=DIRECTION ( 'NONE',  ( 1.000000000000000000, 0.000000000000000000, 0.000000000000000000 ) ) ;
#118908=CARTESIAN_POINT ( 'NONE',  ( -22.50000000000000000, 1.115600667400684642E-11, -167.4999999999999716 ) ) ;
#118909=CARTESIAN_POINT ( 'NONE',  ( 23.14999999999999858, 5.000000000011153745, -179.9052660189130677 ) ) ;
#118925=CARTESIAN_POINT ( 'NONE',  ( 21.07928932188134397, 0.09889514566555242248, -161.1714833436066385 ) ) ;
#118940=EDGE_CURVE ( 'NONE', #117217, #75355, #233313, .T. ) ;
#118954=DIRECTION ( 'NONE',  ( 0.000000000000000000, -1.000000000000000000, 0.000000000000000000 ) ) ;
#119006=ORIENTED_EDGE ( 'NONE', *, *, #19165, .F. ) ;
#119014=AXIS2_PLACEMENT_3D ( 'NONE', #180223, #1555, #81087 ) ;
#119059=FACE_OUTER_BOUND ( 'NONE', #221999, .T. ) ;
#119070=EDGE_CURVE ( 'NONE', #9648, #114385, #83415, .T. ) ;
#119118=ORIENTED_EDGE ( 'NONE', *, *, #149528, .T. ) ;
#119135=AXIS2_PLACEMENT_3D ( 'NONE', #128623, #212019, #112906 ) ;
#119145=EDGE_CURVE ( 'NONE', #14186, #115618, #162754, .T. ) ;
#119162=VECTOR ( 'NONE', #161688, 1000.000000000000114 ) ;
#119174=AXIS2_PLACEMENT_3D ( 'NONE', #25492, #184538, #127149 ) ;
#119175=CARTESIAN_POINT ( 'NONE',  ( -18.51697539158857353, 10.31565961587945957, -206.5364194119177910 ) ) ;
#119196=CARTESIAN_POINT ( 'NONE',  ( 22.60000000000000142, 0.04781839071596409585, -155.7499775809527307 ) ) ;
#119199=CARTESIAN_POINT ( 'NONE',  ( 21.07928932188134397, 0.09889514566555242248, -161.1714833436066385 ) ) ;
#119210=CARTESIAN_POINT ( 'NONE',  ( 18.49999999999999289, 11.65000000001115943, -192.3499999999999659 ) ) ;
#119219=EDGE_CURVE ( 'NONE', #196929, #103174, #245956, .T. ) ;
#119239=DIRECTION ( 'NONE',  ( 0.000000000000000000, 0.000000000000000000, -1.000000000000000000 ) ) ;
#119241=ORIENTED_EDGE ( 'NONE', *, *, #206955, .F. ) ;
#119269=ORIENTED_EDGE ( 'NONE', *, *, #225802, .T. ) ;
#119275=DIRECTION ( 'NONE',  ( 0.000000000000000000, 0.000000000000000000, -1.000000000000000000 ) ) ;
#119287=ORIENTED_EDGE ( 'NONE', *, *, #240929, .T. ) ;
#119292=DIRECTION ( 'NONE',  ( 2.952720810173288619E-16, -1.000000000000000000, 0.000000000000000000 ) ) ;
#119294=CARTESIAN_POINT ( 'NONE',  ( 20.95512820512820440, 10.62384868372303615, -175.1649135690875880 ) ) ;
#119308=ORIENTED_EDGE ( 'NONE', *, *, #41453, .T. ) ;
#119334=TOROIDAL_SURFACE ( 'NONE', #240146, 0.4000000000000005773, 0.1000000000000000056 ) ;
#119363=CARTESIAN_POINT ( 'NONE',  ( -21.05000000000000071, 6.257814610487270279, -167.4022097086911742 ) ) ;
#119371=CARTESIAN_POINT ( 'NONE',  ( 22.39999999999999503, 11.75000000001115552, -167.4999999999999716 ) ) ;
#119373=ADVANCED_FACE ( 'NONE', ( #100249 ), #96081, .T. ) ;
#119389=CIRCLE ( 'NONE', #81746, 0.09999999999999939493 ) ;
#119397=VERTEX_POINT ( 'NONE', #239806 ) ;
#119403=ORIENTED_EDGE ( 'NONE', *, *, #11707, .F. ) ;
#119414=ADVANCED_FACE ( 'NONE', ( #123707 ), #199405, .F. ) ;
#119420=EDGE_CURVE ( 'NONE', #112737, #145941, #41959, .T. ) ;
#119448=EDGE_LOOP ( 'NONE', ( #60779, #224612, #196903, #253766 ) ) ;
#119455=ORIENTED_EDGE ( 'NONE', *, *, #119656, .F. ) ;
#119459=CIRCLE ( 'NONE', #7024, 11.75000000000001066 ) ;
#119470=CARTESIAN_POINT ( 'NONE',  ( 20.04142135623730070, 11.65000000001115943, -188.7499999999999716 ) ) ;
#119481=EDGE_LOOP ( 'NONE', ( #160831, #214514, #199651, #197734 ) ) ;
#119486=DIRECTION ( 'NONE',  ( 1.000000000000000000, -0.000000000000000000, -0.000000000000000000 ) ) ;
#119491=ORIENTED_EDGE ( 'NONE', *, *, #44129, .F. ) ;
#119517=ORIENTED_EDGE ( 'NONE', *, *, #255425, .F. ) ;
#119519=EDGE_CURVE ( 'NONE', #58899, #234175, #150285, .T. ) ;
#119573=CARTESIAN_POINT ( 'NONE',  ( -23.25000000000000000, 1.115600667400684642E-11, -167.4999999999999716 ) ) ;
#119579=AXIS2_PLACEMENT_3D ( 'NONE', #252222, #73632, #108871 ) ;
#119605=ORIENTED_EDGE ( 'NONE', *, *, #1010, .F. ) ;
#119608=CARTESIAN_POINT ( 'NONE',  ( 21.11701782572533048, 10.72160911601861244, -179.7450374295111715 ) ) ;
#119656=EDGE_CURVE ( 'NONE', #22594, #60251, #76547, .T. ) ;
#119679=ADVANCED_FACE ( 'NONE', ( #171848 ), #36166, .T. ) ;
#119680=FACE_OUTER_BOUND ( 'NONE', #170029, .T. ) ;
#119689=VERTEX_POINT ( 'NONE', #71445 ) ;
#119710=ORIENTED_EDGE ( 'NONE', *, *, #109894, .T. ) ;
#119726=VECTOR ( 'NONE', #166567, 1000.000000000000000 ) ;
#119737=DIRECTION ( 'NONE',  ( -0.000000000000000000, -0.1298341882520022694, -0.9915357197604853789 ) ) ;
#119739=TOROIDAL_SURFACE ( 'NONE', #115615, 0.2000000000000000111, 0.1000000000000000056 ) ;
#119748=CARTESIAN_POINT ( 'NONE',  ( 18.59999999999999787, -1.263275465206102233, -208.9018646667463770 ) ) ;
#119750=VERTEX_POINT ( 'NONE', #230505 ) ;
#119751=DIRECTION ( 'NONE',  ( 1.000000000000000000, -0.000000000000000000, -0.000000000000000000 ) ) ;
#119758=CARTESIAN_POINT ( 'NONE',  ( -23.24999999999999645, -9.599999999988845900, -207.7001893912220112 ) ) ;
#119779=CARTESIAN_POINT ( 'NONE',  ( -21.10320863425827298, 0.02502225123826237740, -161.0997226135407345 ) ) ;
#119791=DIRECTION ( 'NONE',  ( 0.000000000000000000, 0.000000000000000000, -1.000000000000000000 ) ) ;
#119792=DIRECTION ( 'NONE',  ( -1.000000000000000000, 0.000000000000000000, 0.000000000000000000 ) ) ;
#119808=ORIENTED_EDGE ( 'NONE', *, *, #98520, .T. ) ;
#119814=LINE ( 'NONE', #167599, #223509 ) ;
#119866=CARTESIAN_POINT ( 'NONE',  ( 18.49999999999999645, 1.637172712981537659, -179.0821533654719815 ) ) ;
#119868=CARTESIAN_POINT ( 'NONE',  ( 22.60000000000000142, 1.115600667400684642E-11, -167.4999999999999716 ) ) ;
#119942=LINE ( 'NONE', #25949, #217188 ) ;
#119953=AXIS2_PLACEMENT_3D ( 'NONE', #148075, #67244, #165064 ) ;
#119965=DIRECTION ( 'NONE',  ( 0.000000000000000000, 0.008583690987124100932, -0.9999631594459055250 ) ) ;
#120014=EDGE_CURVE ( 'NONE', #11610, #133529, #183957, .T. ) ;
#120032=PLANE ( 'NONE',  #85056 ) ;
#120059=EDGE_CURVE ( 'NONE', #118267, #159944, #125506, .T. ) ;
#120069=ADVANCED_FACE ( 'NONE', ( #52817 ), #98116, .T. ) ;
#120072=CARTESIAN_POINT ( 'NONE',  ( 21.05000000000000071, -1.162701749926853712, -175.3999999999999773 ) ) ;
#120085=CIRCLE ( 'NONE', #57672, 0.09999999999999939493 ) ;
#120120=VECTOR ( 'NONE', #188404, 1000.000000000000000 ) ;
#120123=FACE_OUTER_BOUND ( 'NONE', #175871, .T. ) ;
#120210=DIRECTION ( 'NONE',  ( 0.000000000000000000, 0.000000000000000000, 1.000000000000000000 ) ) ;
#120294=AXIS2_PLACEMENT_3D ( 'NONE', #186321, #144597, #25965 ) ;
#120303=AXIS2_PLACEMENT_3D ( 'NONE', #82264, #142268, #121461 ) ;
#120312=DIRECTION ( 'NONE',  ( 1.000000000000000000, 0.000000000000000000, -0.000000000000000000 ) ) ;
#120314=CYLINDRICAL_SURFACE ( 'NONE', #70017, 11.80000000000000426 ) ;
#120315=DIRECTION ( 'NONE',  ( 0.000000000000000000, 0.000000000000000000, -1.000000000000000000 ) ) ;
#120320=CIRCLE ( 'NONE', #170207, 0.09999999999998898659 ) ;
#120365=FACE_OUTER_BOUND ( 'NONE', #113173, .T. ) ;
#120387=VECTOR ( 'NONE', #71745, 1000.000000000000000 ) ;
#120393=CIRCLE ( 'NONE', #116275, 0.09999999999999864553 ) ;
#120398=FACE_OUTER_BOUND ( 'NONE', #202120, .T. ) ;
#120420=DIRECTION ( 'NONE',  ( 0.000000000000000000, 1.000000000000000000, 0.000000000000000000 ) ) ;
#120477=DIRECTION ( 'NONE',  ( 0.000000000000000000, 0.01562500000001262185, 0.9998779222360095753 ) ) ;
#120567=CARTESIAN_POINT ( 'NONE',  ( 21.05000000000084626, 10.60832956796496696, -175.0916850132954323 ) ) ;
#120568=DIRECTION ( 'NONE',  ( 0.000000000000000000, -1.000000000000000000, 0.000000000000000000 ) ) ;
#120570=CARTESIAN_POINT ( 'NONE',  ( -20.64999999999999858, -9.399999999988846611, -191.1060308773475356 ) ) ;
#120591=CARTESIAN_POINT ( 'NONE',  ( 20.95052659398289308, 10.47982436779105875, -175.0752387558655698 ) ) ;
#120605=VERTEX_POINT ( 'NONE', #100293 ) ;
#120610=EDGE_LOOP ( 'NONE', ( #29763, #189819, #82475, #245650, #182817 ) ) ;
#120669=ADVANCED_FACE ( 'NONE', ( #85856 ), #188407, .T. ) ;
#120672=EDGE_CURVE ( 'NONE', #165976, #141132, #128882, .T. ) ;
#120697=ORIENTED_EDGE ( 'NONE', *, *, #22946, .T. ) ;
#120742=CARTESIAN_POINT ( 'NONE',  ( -21.14999999999999503, 11.75000000001115197, -174.4191472459587544 ) ) ;
#120750=ORIENTED_EDGE ( 'NONE', *, *, #78739, .T. ) ;
#120757=AXIS2_PLACEMENT_3D ( 'NONE', #139083, #218639, #200383 ) ;
#120760=AXIS2_PLACEMENT_3D ( 'NONE', #202734, #7099, #204018 ) ;
#120783=LINE ( 'NONE', #222386, #150469 ) ;
#120785=CARTESIAN_POINT ( 'NONE',  ( 21.00000000000000000, 9.750000000011153745, -188.6499999999999488 ) ) ;
#120844=CARTESIAN_POINT ( 'NONE',  ( 21.04999999999999716, -0.01759718699757174473, -161.0592291063375967 ) ) ;
#120863=EDGE_LOOP ( 'NONE', ( #100476, #19127, #97957, #177716 ) ) ;
#120881=DIRECTION ( 'NONE',  ( 1.000000000000000000, 0.000000000000000000, 0.000000000000000000 ) ) ;
#120899=ORIENTED_EDGE ( 'NONE', *, *, #185009, .F. ) ;
#120905=ORIENTED_EDGE ( 'NONE', *, *, #120014, .T. ) ;
#120945=AXIS2_PLACEMENT_3D ( 'NONE', #108362, #249164, #168377 ) ;
#120950=DIRECTION ( 'NONE',  ( 1.000000000000000000, 0.000000000000000000, -0.000000000000000000 ) ) ;
#120997=EDGE_CURVE ( 'NONE', #251640, #41250, #85540, .T. ) ;
#121029=DIRECTION ( 'NONE',  ( 1.000000000000000000, 2.952720810173289112E-16, -0.000000000000000000 ) ) ;
#121040=FACE_OUTER_BOUND ( 'NONE', #88456, .T. ) ;
#121042=DIRECTION ( 'NONE',  ( 0.000000000000000000, 0.000000000000000000, 1.000000000000000000 ) ) ;
#121063=CARTESIAN_POINT ( 'NONE',  ( 22.47071067811865319, 0.09909245471376171288, -159.7799252555019223 ) ) ;
#121096=FACE_OUTER_BOUND ( 'NONE', #121599, .T. ) ;
#121105=CYLINDRICAL_SURFACE ( 'NONE', #134490, 0.09999999999999939493 ) ;
#121133=ORIENTED_EDGE ( 'NONE', *, *, #58445, .T. ) ;
#121134=CARTESIAN_POINT ( 'NONE',  ( 21.00000000000000000, 9.750000000011153745, -179.8499999999999943 ) ) ;
#121136=DIRECTION ( 'NONE',  ( -1.000000000000000000, 0.000000000000000000, 0.000000000000000000 ) ) ;
#121146=ORIENTED_EDGE ( 'NONE', *, *, #32652, .T. ) ;
#121147=ORIENTED_EDGE ( 'NONE', *, *, #206594, .F. ) ;
#121174=ORIENTED_EDGE ( 'NONE', *, *, #73390, .T. ) ;
#121178=FACE_OUTER_BOUND ( 'NONE', #125469, .T. ) ;
#121179=ORIENTED_EDGE ( 'NONE', *, *, #66108, .F. ) ;
#121201=CARTESIAN_POINT ( 'NONE',  ( 18.59999999999999076, 6.550000000011156231, -177.5170271704400022 ) ) ;
#121206=CARTESIAN_POINT ( 'NONE',  ( -21.05000000000000071, -11.64999999998884483, -170.4999999999999716 ) ) ;
#121219=DIRECTION ( 'NONE',  ( 0.000000000000000000, 1.776356839400254803E-15, -1.000000000000000000 ) ) ;
#121244=VECTOR ( 'NONE', #228138, 1000.000000000000000 ) ;
#121255=CARTESIAN_POINT ( 'NONE',  ( 22.45301702632625762, 0.01521087972134078925, -155.8502077757395625 ) ) ;
#121269=ADVANCED_FACE ( 'NONE', ( #82670 ), #236633, .T. ) ;
#121281=ORIENTED_EDGE ( 'NONE', *, *, #24410, .F. ) ;
#121293=VERTEX_POINT ( 'NONE', #41040 ) ;
#121298=ORIENTED_EDGE ( 'NONE', *, *, #210346, .F. ) ;
#121299=EDGE_LOOP ( 'NONE', ( #248784, #94565, #133857, #181494 ) ) ;
#121338=CARTESIAN_POINT ( 'NONE',  ( -21.05000000000000071, 1.115600667400684642E-11, -200.9999999999999432 ) ) ;
#121356=EDGE_LOOP ( 'NONE', ( #97625, #72839, #33306, #172798 ) ) ;
#121379=AXIS2_PLACEMENT_3D ( 'NONE', #228513, #54970, #49853 ) ;
#121382=EDGE_LOOP ( 'NONE', ( #206049, #71770, #239148, #74389 ) ) ;
#121393=CIRCLE ( 'NONE', #229689, 0.1000000000000002554 ) ;
#121412=CARTESIAN_POINT ( 'NONE',  ( -21.05000000000000071, -0.02110330804802081767, -161.1954836707355128 ) ) ;
#121420=ORIENTED_EDGE ( 'NONE', *, *, #3958, .F. ) ;
#121431=DIRECTION ( 'NONE',  ( 0.000000000000000000, 0.000000000000000000, -1.000000000000000000 ) ) ;
#121444=CARTESIAN_POINT ( 'NONE',  ( -20.94999999999999929, -1.162701749926853712, -175.3999999999999773 ) ) ;
#121461=DIRECTION ( 'NONE',  ( -1.000000000000000000, 0.000000000000000000, 0.000000000000000000 ) ) ;
#121464=ORIENTED_EDGE ( 'NONE', *, *, #170160, .T. ) ;
#121506=CYLINDRICAL_SURFACE ( 'NONE', #140255, 0.1000000000000101918 ) ;
#121535=EDGE_LOOP ( 'NONE', ( #120697, #148856, #132658, #28910 ) ) ;
#121546=FACE_OUTER_BOUND ( 'NONE', #175351, .T. ) ;
#121565=CARTESIAN_POINT ( 'NONE',  ( 20.94999999999999929, 1.115600667400684642E-11, -167.4999999999999716 ) ) ;
#121574=ORIENTED_EDGE ( 'NONE', *, *, #185943, .F. ) ;
#121577=ORIENTED_EDGE ( 'NONE', *, *, #156178, .T. ) ;
#121585=CARTESIAN_POINT ( 'NONE',  ( -21.05000000000000071, -11.48912529306490349, -170.4999999999999716 ) ) ;
#121599=EDGE_LOOP ( 'NONE', ( #126442, #71696, #75493, #183352 ) ) ;
#121617=ADVANCED_FACE ( 'NONE', ( #61566, #98084 ), #79814, .T. ) ;
#121663=VERTEX_POINT ( 'NONE', #37235 ) ;
#121664=CARTESIAN_POINT ( 'NONE',  ( 20.85000000000000142, -1.135018845899022466, -208.7169768834322952 ) ) ;
#121708=ORIENTED_EDGE ( 'NONE', *, *, #12893, .F. ) ;
#121737=CARTESIAN_POINT ( 'NONE',  ( -20.94999999999999929, -11.48912529306489994, -198.0999999999999659 ) ) ;
#121744=ORIENTED_EDGE ( 'NONE', *, *, #64860, .T. ) ;
#121750=ORIENTED_EDGE ( 'NONE', *, *, #128961, .F. ) ;
#121757=CARTESIAN_POINT ( 'NONE',  ( -18.59999999999999787, 10.33248238083634440, -206.5948465439131496 ) ) ;
#121794=AXIS2_PLACEMENT_3D ( 'NONE', #249226, #90121, #190551 ) ;
#121814=AXIS2_PLACEMENT_3D ( 'NONE', #234530, #254084, #35096 ) ;
#121821=ADVANCED_FACE ( 'NONE', ( #42359 ), #8377, .F. ) ;
#121834=ADVANCED_FACE ( 'NONE', ( #85302 ), #47470, .T. ) ;
#121838=LINE ( 'NONE', #219627, #194777 ) ;
#121840=CARTESIAN_POINT ( 'NONE',  ( 21.05000000000000426, 6.413826288824131971, -167.5857409370333926 ) ) ;
#121846=CARTESIAN_POINT ( 'NONE',  ( 23.24999999999999289, 4.150000000011154988, -167.4999999999999716 ) ) ;
#121857=ORIENTED_EDGE ( 'NONE', *, *, #211614, .F. ) ;
#121866=CARTESIAN_POINT ( 'NONE',  ( 20.95203847575071521, 10.50106053928516303, -175.0670713486235002 ) ) ;
#121915=ORIENTED_EDGE ( 'NONE', *, *, #26907, .T. ) ;
#121921=CYLINDRICAL_SURFACE ( 'NONE', #7632, 0.09999999999999892308 ) ;
#121931=ORIENTED_EDGE ( 'NONE', *, *, #249591, .F. ) ;
#121948=EDGE_CURVE ( 'NONE', #126189, #88113, #155679, .T. ) ;
#121959=ADVANCED_FACE ( 'NONE', ( #210438 ), #192164, .T. ) ;
#121973=DIRECTION ( 'NONE',  ( 0.000000000000000000, 0.000000000000000000, -1.000000000000000000 ) ) ;
#121985=ORIENTED_EDGE ( 'NONE', *, *, #125328, .F. ) ;
#122023=ORIENTED_EDGE ( 'NONE', *, *, #15667, .T. ) ;
#122025=ORIENTED_EDGE ( 'NONE', *, *, #63270, .T. ) ;
#122067=CARTESIAN_POINT ( 'NONE',  ( 23.24999999999999289, 11.65000000001116298, -155.7499999999999716 ) ) ;
#122132=CARTESIAN_POINT ( 'NONE',  ( 18.49999999999999289, 10.23906162413259402, -192.2543974345975926 ) ) ;
#122145=DIRECTION ( 'NONE',  ( 0.5000000000001141309, 0.000000000000000000, -0.8660254037843729824 ) ) ;
#122163=FACE_OUTER_BOUND ( 'NONE', #195904, .T. ) ;
#122178=AXIS2_PLACEMENT_3D ( 'NONE', #7239, #25550, #86770 ) ;
#122209=CIRCLE ( 'NONE', #230552, 0.09999999999998898659 ) ;
#122238=CARTESIAN_POINT ( 'NONE',  ( 20.86036036209915423, 10.62104277658212048, -175.1663484185077095 ) ) ;
#122253=VERTEX_POINT ( 'NONE', #27665 ) ;
#122260=DIRECTION ( 'NONE',  ( 1.000000000000000000, -0.000000000000000000, -0.000000000000000000 ) ) ;
#122286=LINE ( 'NONE', #162704, #76746 ) ;
#122323=DIRECTION ( 'NONE',  ( 1.000000000000000000, 0.000000000000000000, -0.000000000000000000 ) ) ;
#122329=EDGE_CURVE ( 'NONE', #85197, #86058, #49753, .T. ) ;
#122331=EDGE_CURVE ( 'NONE', #215804, #27481, #80791, .T. ) ;
#122377=CARTESIAN_POINT ( 'NONE',  ( -23.15000000000000213, 2.000000000011154189, -180.7246219227620543 ) ) ;
#122402=ORIENTED_EDGE ( 'NONE', *, *, #172270, .T. ) ;
#122409=CARTESIAN_POINT ( 'NONE',  ( 20.94999999999999929, 1.115600667400684642E-11, -200.9999999999999432 ) ) ;
#122413=ORIENTED_EDGE ( 'NONE', *, *, #45496, .F. ) ;
#122416=VECTOR ( 'NONE', #84255, 1000.000000000000000 ) ;
#122420=CARTESIAN_POINT ( 'NONE',  ( -18.59999999999999787, -1.835341550213255957, -179.0551512925629538 ) ) ;
#122422=CARTESIAN_POINT ( 'NONE',  ( -23.15000000000000213, 11.65000000001115588, -155.7499999999999716 ) ) ;
#122435=CARTESIAN_POINT ( 'NONE',  ( -23.25000000000000000, -8.999999999988844479, -191.7060308773475299 ) ) ;
#122440=EDGE_CURVE ( 'NONE', #236406, #56169, #55837, .T. ) ;
#122465=LINE ( 'NONE', #121206, #175505 ) ;
#122471=ADVANCED_FACE ( 'NONE', ( #85971 ), #120032, .F. ) ;
#122520=LINE ( 'NONE', #165498, #166598 ) ;
#122522=PLANE ( 'NONE',  #227323 ) ;
#122523=ORIENTED_EDGE ( 'NONE', *, *, #233973, .F. ) ;
#122534=AXIS2_PLACEMENT_3D ( 'NONE', #18583, #51563, #57685 ) ;
#122560=DIRECTION ( 'NONE',  ( 0.000000000000000000, 0.000000000000000000, -1.000000000000000000 ) ) ;
#122561=AXIS2_PLACEMENT_3D ( 'NONE', #118114, #135090, #214635 ) ;
#122562=EDGE_LOOP ( 'NONE', ( #99466, #7911, #121574 ) ) ;
#122576=ORIENTED_EDGE ( 'NONE', *, *, #161823, .T. ) ;
#122583=EDGE_CURVE ( 'NONE', #112231, #154754, #122721, .T. ) ;
#122585=ORIENTED_EDGE ( 'NONE', *, *, #149885, .F. ) ;
#122589=AXIS2_PLACEMENT_3D ( 'NONE', #191881, #34100, #11951 ) ;
#122594=VERTEX_POINT ( 'NONE', #239958 ) ;
#122604=CARTESIAN_POINT ( 'NONE',  ( 23.14999999999999858, 5.000000000011153745, -189.0947339810868755 ) ) ;
#122665=CARTESIAN_POINT ( 'NONE',  ( -18.59999999999999787, -1.135018845899022466, -208.7169768834322952 ) ) ;
#122698=ORIENTED_EDGE ( 'NONE', *, *, #147342, .T. ) ;
#122714=CARTESIAN_POINT ( 'NONE',  ( -20.64999999999999858, 2.400000000011155432, -180.7246219227620543 ) ) ;
#122721=CIRCLE ( 'NONE', #43030, 0.09999999999998898659 ) ;
#122753=CARTESIAN_POINT ( 'NONE',  ( 21.00000000000000000, 9.750000000011153745, -188.6499999999999488 ) ) ;
#122766=FACE_OUTER_BOUND ( 'NONE', #87648, .T. ) ;
#122819=DIRECTION ( 'NONE',  ( -4.408576920032448588E-17, 0.1350103645451876944, -0.9908441862701601321 ) ) ;
#122833=FACE_OUTER_BOUND ( 'NONE', #176460, .T. ) ;
#122850=DIRECTION ( 'NONE',  ( 0.000000000000000000, 0.000000000000000000, -1.000000000000000000 ) ) ;
#122853=DIRECTION ( 'NONE',  ( 0.000000000000000000, 0.000000000000000000, -1.000000000000000000 ) ) ;
#122874=DIRECTION ( 'NONE',  ( 0.000000000000000000, 0.000000000000000000, -1.000000000000000000 ) ) ;
#122907=ORIENTED_EDGE ( 'NONE', *, *, #20571, .T. ) ;
#122916=VECTOR ( 'NONE', #146294, 1000.000000000000000 ) ;
#122929=EDGE_CURVE ( 'NONE', #61597, #201908, #55447, .T. ) ;
#122941=DIRECTION ( 'NONE',  ( 0.000000000000000000, -1.776356839400254803E-15, 1.000000000000000000 ) ) ;
#122977=ADVANCED_FACE ( 'NONE', ( #20607 ), #151371, .T. ) ;
#122981=ORIENTED_EDGE ( 'NONE', *, *, #66071, .T. ) ;
#122995=VERTEX_POINT ( 'NONE', #232613 ) ;
#123005=LINE ( 'NONE', #180405, #127747 ) ;
#123033=SPHERICAL_SURFACE ( 'NONE', #53739, 0.1000000000000000056 ) ;
#123073=CARTESIAN_POINT ( 'NONE',  ( -21.44999999999999929, 7.350000000011155166, -188.7499999999999716 ) ) ;
#123095=DIRECTION ( 'NONE',  ( 2.879366945564059217E-14, -0.9875055080513751582, 0.1575844902526747915 ) ) ;
#123143=PRESENTATION_STYLE_ASSIGNMENT (( #186989 ) ) ;
#123146=AXIS2_PLACEMENT_3D ( 'NONE', #121444, #125270, #44457 ) ;
#123152=CARTESIAN_POINT ( 'NONE',  ( 18.54148534481894117, 10.32532329027886853, -206.5699343018359286 ) ) ;
#123159=DIRECTION ( 'NONE',  ( -1.000000000000000000, -0.000000000000000000, 0.000000000000000000 ) ) ;
#123175=VECTOR ( 'NONE', #113132, 1000.000000000000114 ) ;
#123181=CARTESIAN_POINT ( 'NONE',  ( -20.54999999999999716, 4.350000000011156054, -179.8499999999999943 ) ) ;
#123216=ORIENTED_EDGE ( 'NONE', *, *, #67178, .F. ) ;
#123247=DIRECTION ( 'NONE',  ( 0.000000000000000000, -0.6728971962617388280, 0.7397360091702248619 ) ) ;
#123251=CIRCLE ( 'NONE', #98267, 0.09999999999998898659 ) ;
#123256=DIRECTION ( 'NONE',  ( 1.000000000000000000, 0.000000000000000000, -0.000000000000000000 ) ) ;
#123258=DIRECTION ( 'NONE',  ( 0.000000000000000000, 0.000000000000000000, -1.000000000000000000 ) ) ;
#123291=ADVANCED_FACE ( 'NONE', ( #182899 ), #43377, .F. ) ;
#123313=DIRECTION ( 'NONE',  ( 0.000000000000000000, -1.000000000000000000, 0.000000000000000000 ) ) ;
#123315=AXIS2_PLACEMENT_3D ( 'NONE', #4893, #44053, #239690 ) ;
#123333=DIRECTION ( 'NONE',  ( 0.000000000000000000, -0.000000000000000000, 1.000000000000000000 ) ) ;
#123335=CIRCLE ( 'NONE', #194094, 0.09999999999998898659 ) ;
#123367=ORIENTED_EDGE ( 'NONE', *, *, #155904, .T. ) ;
#123369=DIRECTION ( 'NONE',  ( -0.1538461538461510236, 0.9880948137434718559, 0.000000000000000000 ) ) ;
#123371=AXIS2_PLACEMENT_3D ( 'NONE', #147432, #27528, #88714 ) ;
#123389=LINE ( 'NONE', #24306, #3140 ) ;
#123412=CARTESIAN_POINT ( 'NONE',  ( 18.52928932304149967, 10.27928932305266407, -192.1762534328030938 ) ) ;
#123445=ORIENTED_EDGE ( 'NONE', *, *, #96959, .F. ) ;
#123472=CARTESIAN_POINT ( 'NONE',  ( 21.05000000000085336, 8.894723818387976877, -175.9870843231449555 ) ) ;
#123477=EDGE_CURVE ( 'NONE', #180362, #33688, #56193, .T. ) ;
#123517=CARTESIAN_POINT ( 'NONE',  ( 20.72390388899090752, 10.58996311843487348, -175.0113482957463020 ) ) ;
#123533=AXIS2_PLACEMENT_3D ( 'NONE', #96389, #139364, #217613 ) ;
#123577=ORIENTED_EDGE ( 'NONE', *, *, #123477, .T. ) ;
#123589=AXIS2_PLACEMENT_3D ( 'NONE', #251081, #191150, #73772 ) ;
#123597=ORIENTED_EDGE ( 'NONE', *, *, #5488, .T. ) ;
#123607=EDGE_LOOP ( 'NONE', ( #202870, #17200, #180814, #160762 ) ) ;
#123637=DIRECTION ( 'NONE',  ( -0.000000000000000000, -0.000000000000000000, 1.000000000000000000 ) ) ;
#123667=VERTEX_POINT ( 'NONE', #62644 ) ;
#123682=CIRCLE ( 'NONE', #211152, 0.09999999999998898659 ) ;
#123685=FACE_OUTER_BOUND ( 'NONE', #136177, .T. ) ;
#123700=VERTEX_POINT ( 'NONE', #61350 ) ;
#123707=FACE_OUTER_BOUND ( 'NONE', #41149, .T. ) ;
#123708=CYLINDRICAL_SURFACE ( 'NONE', #185038, 0.09999999999999939493 ) ;
#123739=ADVANCED_FACE ( 'NONE', ( #82164 ), #221684, .F. ) ;
#123774=DIRECTION ( 'NONE',  ( -1.000000000000000000, 0.000000000000000000, 0.000000000000000000 ) ) ;
#123794=EDGE_CURVE ( 'NONE', #6262, #17415, #131042, .T. ) ;
#123799=FACE_OUTER_BOUND ( 'NONE', #236085, .T. ) ;
#123802=ORIENTED_EDGE ( 'NONE', *, *, #126280, .T. ) ;
#123806=CARTESIAN_POINT ( 'NONE',  ( -18.59999999999999787, 11.65000000001115232, -174.5148057706539930 ) ) ;
#123829=DIRECTION ( 'NONE',  ( -0.7071067811865388020, 0.7071067811865561215, 0.000000000000000000 ) ) ;
#123846=CARTESIAN_POINT ( 'NONE',  ( 21.05000000000000071, 1.162701749949165642, -175.5999999999999659 ) ) ;
#123885=CYLINDRICAL_SURFACE ( 'NONE', #26240, 0.09999999999998898659 ) ;
#123905=DIRECTION ( 'NONE',  ( 1.000000000000000000, -0.000000000000000000, -0.000000000000000000 ) ) ;
#123924=ORIENTED_EDGE ( 'NONE', *, *, #206618, .T. ) ;
#123948=ORIENTED_EDGE ( 'NONE', *, *, #159548, .F. ) ;
#123955=ORIENTED_EDGE ( 'NONE', *, *, #15796, .T. ) ;
#123956=ORIENTED_EDGE ( 'NONE', *, *, #48648, .F. ) ;
#123967=DIRECTION ( 'NONE',  ( -0.000000000000000000, -0.000000000000000000, 1.000000000000000000 ) ) ;
#123968=ORIENTED_EDGE ( 'NONE', *, *, #97896, .F. ) ;
#123982=DIRECTION ( 'NONE',  ( 0.000000000000000000, 0.000000000000000000, 1.000000000000000000 ) ) ;
#123984=VECTOR ( 'NONE', #253584, 1000.000000000000000 ) ;
#124055=ADVANCED_FACE ( 'NONE', ( #4881 ), #160110, .T. ) ;
#124058=LINE ( 'NONE', #224417, #147177 ) ;
#124078=ADVANCED_FACE ( 'NONE', ( #81841 ), #221369, .F. ) ;
#124106=FACE_OUTER_BOUND ( 'NONE', #23574, .T. ) ;
#124109=( BOUNDED_SURFACE ( )  B_SPLINE_SURFACE ( 3, 2, ( 
 ( #204495, #143242, #141961 ),
 ( #201952, #222773, #183676 ),
 ( #25891, #186240, #126246 ),
 ( #205788, #23339, #104100 ),
 ( #182395, #27195, #80689 ),
 ( #102817, #3739, #162840 ) ),
 .UNSPECIFIED., .F., .F., .F. ) 
 B_SPLINE_SURFACE_WITH_KNOTS ( ( 4, 2, 4 ),
 ( 3, 3 ),
 ( 0.0001300404313046710908, 0.0003183318589266656714, 0.0005066232865486602248 ),
 ( 0.000000000000000000, 1.000000000000000000 ),
 .UNSPECIFIED. ) 
 GEOMETRIC_REPRESENTATION_ITEM ( )  RATIONAL_B_SPLINE_SURFACE ( (
 ( 1.000000000000000000, 0.7071067811865475727, 1.000000000000000000),
 ( 1.000000000000000000, 0.7625113560545213609, 1.000000000000000000),
 ( 1.000000000000000000, 0.8126073484681893833, 1.000000000000000000),
 ( 1.000000000000000000, 0.8923049332738569595, 1.000000000000000000),
 ( 1.000000000000000000, 0.9231914937764841289, 1.000000000000000000),
 ( 1.000000000000000000, 0.9238795325112909573, 1.000000000000000000) ) ) 
 REPRESENTATION_ITEM ( '' )  SURFACE ( )  );
#124148=ORIENTED_EDGE ( 'NONE', *, *, #228314, .F. ) ;
#124149=AXIS2_PLACEMENT_3D ( 'NONE', #186317, #7684, #87184 ) ;
#124162=TOROIDAL_SURFACE ( 'NONE', #132518, 12.97499999999999609, 0.1000000000000000056 ) ;
#124236=ORIENTED_EDGE ( 'NONE', *, *, #209238, .F. ) ;
#124238=CARTESIAN_POINT ( 'NONE',  ( -18.59999999999999787, 1.835341550235567887, -179.1551512925629197 ) ) ;
#124244=EDGE_CURVE ( 'NONE', #160946, #14833, #235502, .T. ) ;
#124256=CARTESIAN_POINT ( 'NONE',  ( 23.14999999999999858, 3.900000000011155432, -200.9999999999999432 ) ) ;
#124258=CARTESIAN_POINT ( 'NONE',  ( -23.15000000000000213, 1.910280373842936141, -180.1313678551989028 ) ) ;
#124273=ORIENTED_EDGE ( 'NONE', *, *, #223183, .T. ) ;
#124341=ORIENTED_EDGE ( 'NONE', *, *, #149885, .T. ) ;
#124377=DIRECTION ( 'NONE',  ( 1.000000000000000000, -7.304098846218135653E-16, 0.000000000000000000 ) ) ;
#124382=ORIENTED_EDGE ( 'NONE', *, *, #183233, .F. ) ;
#124464=VECTOR ( 'NONE', #39139, 1000.000000000000000 ) ;
#124475=DIRECTION ( 'NONE',  ( 0.000000000000000000, -0.1568667991644863147, 0.9876197685951252359 ) ) ;
#124503=PLANE ( 'NONE',  #30139 ) ;
#124525=FACE_OUTER_BOUND ( 'NONE', #201816, .T. ) ;
#124561=DIRECTION ( 'NONE',  ( 1.000000000000000000, 0.000000000000000000, -0.000000000000000000 ) ) ;
#124581=EDGE_CURVE ( 'NONE', #178529, #222295, #31498, .T. ) ;
#124585=CARTESIAN_POINT ( 'NONE',  ( 20.94999999999999929, 1.835341550235569663, -179.0551512925629538 ) ) ;
#124605=ORIENTED_EDGE ( 'NONE', *, *, #31519, .F. ) ;
#124621=CARTESIAN_POINT ( 'NONE',  ( 21.05000000000000071, -11.48912529306489994, -197.9999999999999432 ) ) ;
#124640=ORIENTED_EDGE ( 'NONE', *, *, #51891, .T. ) ;
#124654=EDGE_LOOP ( 'NONE', ( #63653, #84227, #242218, #2849, #206785, #193079 ) ) ;
#124711=CARTESIAN_POINT ( 'NONE',  ( 23.14999999999999858, 1.115600667400684642E-11, -200.9999999999999432 ) ) ;
#124728=CARTESIAN_POINT ( 'NONE',  ( 23.14999999999999503, 6.650000000011155876, -179.6499999999999773 ) ) ;
#124762=DIRECTION ( 'NONE',  ( 0.000000000000000000, 0.000000000000000000, 1.000000000000000000 ) ) ;
#124775=CARTESIAN_POINT ( 'NONE',  ( -20.85000000000000142, 10.33248238083635151, -206.5948465439131496 ) ) ;
#124780=EDGE_CURVE ( 'NONE', #232431, #247867, #182638, .T. ) ;
#124789=CYLINDRICAL_SURFACE ( 'NONE', #161593, 0.5000000000000004441 ) ;
#124820=CIRCLE ( 'NONE', #70679, 0.2000000000000005107 ) ;
#124821=ADVANCED_FACE ( 'NONE', ( #87350 ), #65230, .T. ) ;
#124824=EDGE_LOOP ( 'NONE', ( #104730, #169562, #163304, #74323 ) ) ;
#124842=ORIENTED_EDGE ( 'NONE', *, *, #98314, .F. ) ;
#124861=DIRECTION ( 'NONE',  ( 1.000000000000000000, 0.000000000000000000, -0.000000000000000000 ) ) ;
#124865=AXIS2_PLACEMENT_3D ( 'NONE', #113431, #153895, #98965 ) ;
#124885=ORIENTED_EDGE ( 'NONE', *, *, #114380, .F. ) ;
#124897=CARTESIAN_POINT ( 'NONE',  ( -21.65000000000000213, 7.708578643773852157, -179.8499999999999943 ) ) ;
#124915=ORIENTED_EDGE ( 'NONE', *, *, #100764, .F. ) ;
#124966=EDGE_CURVE ( 'NONE', #46891, #168999, #98235, .T. ) ;
#124981=CYLINDRICAL_SURFACE ( 'NONE', #136575, 0.09999999999998898659 ) ;
#124987=LINE ( 'NONE', #127546, #196740 ) ;
#125034=CARTESIAN_POINT ( 'NONE',  ( -18.39999999999999858, -9.599999999988849453, -207.6001893912220169 ) ) ;
#125054=CIRCLE ( 'NONE', #204315, 0.09999999999999982514 ) ;
#125081=CARTESIAN_POINT ( 'NONE',  ( -20.85000000000000142, 7.021664781911246322, -204.8335654018972605 ) ) ;
#125109=EDGE_CURVE ( 'NONE', #184791, #250208, #14912, .T. ) ;
#125124=ORIENTED_EDGE ( 'NONE', *, *, #67282, .T. ) ;
#125132=CIRCLE ( 'NONE', #196039, 4.049999999999998934 ) ;
#125148=CARTESIAN_POINT ( 'NONE',  ( 21.06280952165543141, 10.62713230061201841, -179.7040538867792918 ) ) ;
#125157=CARTESIAN_POINT ( 'NONE',  ( -22.39999999999999858, 7.790779598384560245, -167.4999999999999716 ) ) ;
#125160=DIRECTION ( 'NONE',  ( 0.000000000000000000, 0.000000000000000000, 1.000000000000000000 ) ) ;
#125177=DIRECTION ( 'NONE',  ( 0.000000000000000000, 0.000000000000000000, 1.000000000000000000 ) ) ;
#125178=CARTESIAN_POINT ( 'NONE',  ( -23.15000000000000213, 11.65000000001115588, -179.6499999999999773 ) ) ;
#125200=DIRECTION ( 'NONE',  ( -1.000000000000000000, -7.304098846218134667E-16, 4.217023435051678980E-16 ) ) ;
#125220=EDGE_CURVE ( 'NONE', #178255, #52759, #153361, .T. ) ;
#125246=ORIENTED_EDGE ( 'NONE', *, *, #247990, .T. ) ;
#125261=CARTESIAN_POINT ( 'NONE',  ( -21.08479644141223019, 6.345038657743042876, -167.4414455574358556 ) ) ;
#125264=DIRECTION ( 'NONE',  ( 0.000000000000000000, 0.000000000000000000, 1.000000000000000000 ) ) ;
#125270=DIRECTION ( 'NONE',  ( 0.000000000000000000, 1.000000000000000000, 0.000000000000000000 ) ) ;
#125302=CARTESIAN_POINT ( 'NONE',  ( -20.85000000000000142, 11.65000000001115232, -194.2161343370218560 ) ) ;
#125311=CARTESIAN_POINT ( 'NONE',  ( 23.24999999999999289, 6.650000000011155876, -188.6499999999999488 ) ) ;
#125313=AXIS2_PLACEMENT_3D ( 'NONE', #19672, #22246, #80896 ) ;
#125328=EDGE_CURVE ( 'NONE', #216004, #251640, #160671, .T. ) ;
#125387=ORIENTED_EDGE ( 'NONE', *, *, #247532, .T. ) ;
#125395=CIRCLE ( 'NONE', #237807, 0.09999999999999939493 ) ;
#125403=DIRECTION ( 'NONE',  ( 1.000000000000000000, -0.000000000000000000, -0.000000000000000000 ) ) ;
#125406=CARTESIAN_POINT ( 'NONE',  ( 20.94999999999999929, -1.835341550213257733, -179.0551512925629538 ) ) ;
#125419=DIRECTION ( 'NONE',  ( 0.000000000000000000, 1.000000000000000000, 0.000000000000000000 ) ) ;
#125429=DIRECTION ( 'NONE',  ( -0.000000000000000000, -0.9875055080513799322, 0.1575844902526464253 ) ) ;
#125459=LINE ( 'NONE', #147581, #189588 ) ;
#125468=CARTESIAN_POINT ( 'NONE',  ( -18.59999999999999787, -9.480686695267820596, -207.9411151687577899 ) ) ;
#125469=EDGE_LOOP ( 'NONE', ( #109523, #96859, #171222, #233396 ) ) ;
#125484=VECTOR ( 'NONE', #177172, 1000.000000000000000 ) ;
#125506=CIRCLE ( 'NONE', #8984, 0.09999999999998898659 ) ;
#125522=CARTESIAN_POINT ( 'NONE',  ( 18.59999999999999076, 6.450000000011156587, -177.5170271704400022 ) ) ;
#125534=VERTEX_POINT ( 'NONE', #73130 ) ;
#125543=VECTOR ( 'NONE', #170130, 1000.000000000000000 ) ;
#125546=AXIS2_PLACEMENT_3D ( 'NONE', #98673, #235652, #196530 ) ;
#125552=LINE ( 'NONE', #245513, #104283 ) ;
#125573=ADVANCED_FACE ( 'NONE', ( #112240 ), #194356, .T. ) ;
#125586=EDGE_CURVE ( 'NONE', #77358, #171611, #90071, .T. ) ;
#125590=ORIENTED_EDGE ( 'NONE', *, *, #151848, .T. ) ;
#125607=AXIS2_PLACEMENT_3D ( 'NONE', #98808, #156292, #217490 ) ;
#125636=FACE_OUTER_BOUND ( 'NONE', #36345, .T. ) ;
#125637=ORIENTED_EDGE ( 'NONE', *, *, #54810, .T. ) ;
#125638=CARTESIAN_POINT ( 'NONE',  ( 21.05000000000000071, -11.64999999998883595, -170.3999999999999773 ) ) ;
#125647=CARTESIAN_POINT ( 'NONE',  ( 20.04142135623730070, 11.65000000001115943, -155.7499999999999716 ) ) ;
#125662=CARTESIAN_POINT ( 'NONE',  ( 21.11101077988997332, 6.423684734737197921, -167.4847147310856599 ) ) ;
#125685=CARTESIAN_POINT ( 'NONE',  ( -18.59999999999999787, 5.341242990002807112, -157.6933497935119419 ) ) ;
#125709=CARTESIAN_POINT ( 'NONE',  ( -20.54999999999999716, -8.730841121484173684, -177.0980747189843214 ) ) ;
#125759=FACE_OUTER_BOUND ( 'NONE', #30912, .T. ) ;
#125781=AXIS2_PLACEMENT_3D ( 'NONE', #2169, #183404, #102533 ) ;
#125805=ORIENTED_EDGE ( 'NONE', *, *, #173026, .T. ) ;
#125855=FACE_OUTER_BOUND ( 'NONE', #240228, .T. ) ;
#125856=CIRCLE ( 'NONE', #67612, 0.09999999999998898659 ) ;
#125894=CIRCLE ( 'NONE', #134277, 0.09999999999999939493 ) ;
#125898=ADVANCED_FACE ( 'NONE', ( #17604 ), #214527, .T. ) ;
#125971=CIRCLE ( 'NONE', #100805, 12.87499999999999822 ) ;
#125972=EDGE_CURVE ( 'NONE', #132861, #236967, #231545, .T. ) ;
#125979=CARTESIAN_POINT ( 'NONE',  ( -18.59999999999999787, -1.162701749926853712, -175.5999999999999659 ) ) ;
#125988=VECTOR ( 'NONE', #214520, 1000.000000000000000 ) ;
#126007=AXIS2_PLACEMENT_3D ( 'NONE', #164517, #184058, #47096 ) ;
#126013=CARTESIAN_POINT ( 'NONE',  ( 18.55857864376267941, 10.36715728753653565, -192.2499999999999432 ) ) ;
#126021=CARTESIAN_POINT ( 'NONE',  ( -18.39999999999999858, -9.599999999988844124, -174.5320693966996259 ) ) ;
#126048=CARTESIAN_POINT ( 'NONE',  ( -21.05000000000000071, 11.60000000001115517, -194.0717967697244717 ) ) ;
#126065=DIRECTION ( 'NONE',  ( -1.000000000000000000, 0.000000000000000000, 0.000000000000000000 ) ) ;
#126132=AXIS2_PLACEMENT_3D ( 'NONE', #221532, #5049, #126302 ) ;
#126146=FACE_OUTER_BOUND ( 'NONE', #142805, .T. ) ;
#126189=VERTEX_POINT ( 'NONE', #36924 ) ;
#126192=DIRECTION ( 'NONE',  ( 1.000000000000000000, 0.000000000000000000, 0.000000000000000000 ) ) ;
#126196=DIRECTION ( 'NONE',  ( 0.000000000000000000, 0.4930308989874718772, 0.8700118002898612479 ) ) ;
#126202=CARTESIAN_POINT ( 'NONE',  ( 23.14999999999999503, 6.650000000011155876, -188.8499999999999659 ) ) ;
#126219=CARTESIAN_POINT ( 'NONE',  ( 20.94999999999999929, -8.999999999988842703, -191.1060308773475072 ) ) ;
#126230=CARTESIAN_POINT ( 'NONE',  ( 18.58725287972330165, -9.566626910680657403, -207.8225048057653055 ) ) ;
#126234=ORIENTED_EDGE ( 'NONE', *, *, #26142, .T. ) ;
#126246=CARTESIAN_POINT ( 'NONE',  ( -21.05000000000000071, 6.413662734880721139, -167.5855928633627343 ) ) ;
#126248=DIRECTION ( 'NONE',  ( 0.000000000000000000, 0.1495327102803792052, 0.9887567792719320625 ) ) ;
#126265=CARTESIAN_POINT ( 'NONE',  ( -20.94999999999999929, -11.41227409413852989, -170.4999999999999716 ) ) ;
#126270=DIRECTION ( 'NONE',  ( -0.000000000000000000, -0.000000000000000000, 1.000000000000000000 ) ) ;
#126280=EDGE_CURVE ( 'NONE', #187086, #155258, #115384, .T. ) ;
#126294=CARTESIAN_POINT ( 'NONE',  ( -21.05000000000000071, 1.851028230152016674, -179.1539132694224463 ) ) ;
#126299=EDGE_LOOP ( 'NONE', ( #251482, #106616, #155224, #244037, #188556, #239411, #230452, #179388, #126362, #98175, #12575, #195773, #21031, #54268, #138339, #257770, #102626, #250529, #229155, #70908, #18495, #178489, #152099, #18781, #105262, #114269, #24082 ) ) ;
#126302=DIRECTION ( 'NONE',  ( 0.000000000000000000, 0.000000000000000000, 1.000000000000000000 ) ) ;
#126323=ORIENTED_EDGE ( 'NONE', *, *, #133226, .T. ) ;
#126325=DIRECTION ( 'NONE',  ( 0.000000000000000000, 0.000000000000000000, 1.000000000000000000 ) ) ;
#126340=PLANE ( 'NONE',  #46264 ) ;
#126362=ORIENTED_EDGE ( 'NONE', *, *, #215445, .F. ) ;
#126377=CARTESIAN_POINT ( 'NONE',  ( -21.14999999999999858, 11.75000000001115552, -174.2838656629781156 ) ) ;
#126380=LINE ( 'NONE', #28623, #137259 ) ;
#126393=DIRECTION ( 'NONE',  ( 0.000000000000000000, 0.000000000000000000, -1.000000000000000000 ) ) ;
#126394=LINE ( 'NONE', #225473, #166104 ) ;
#126403=ORIENTED_EDGE ( 'NONE', *, *, #120014, .F. ) ;
#126412=CARTESIAN_POINT ( 'NONE',  ( 21.13461538461538680, 10.61458296203669427, -179.7500000000000000 ) ) ;
#126427=DIRECTION ( 'NONE',  ( -1.000000000000000000, 0.000000000000000000, 0.000000000000000000 ) ) ;
#126434=ORIENTED_EDGE ( 'NONE', *, *, #84140, .T. ) ;
#126442=ORIENTED_EDGE ( 'NONE', *, *, #100533, .T. ) ;
#126447=LINE ( 'NONE', #22236, #60407 ) ;
#126451=EDGE_CURVE ( 'NONE', #146076, #96541, #157296, .T. ) ;
#126473=ORIENTED_EDGE ( 'NONE', *, *, #238295, .F. ) ;
#126553=EDGE_CURVE ( 'NONE', #6055, #234784, #190613, .T. ) ;
#126593=CARTESIAN_POINT ( 'NONE',  ( 21.00000000000000000, 9.750000000011153745, -188.7499999999999716 ) ) ;
#126597=CARTESIAN_POINT ( 'NONE',  ( 18.41416235934317314, -9.499999999988842703, -207.6001893912219884 ) ) ;
#126617=DIRECTION ( 'NONE',  ( -0.000000000000000000, 0.1350103645451876666, -0.9908441862701600211 ) ) ;
#126621=ORIENTED_EDGE ( 'NONE', *, *, #226340, .F. ) ;
#126639=DIRECTION ( 'NONE',  ( 0.000000000000000000, 1.000000000000000000, 0.000000000000000000 ) ) ;
#126656=DIRECTION ( 'NONE',  ( 0.000000000000000000, -1.000000000000000000, -0.000000000000000000 ) ) ;
#126658=FACE_OUTER_BOUND ( 'NONE', #36457, .T. ) ;
#126700=VECTOR ( 'NONE', #7474, 1000.000000000000000 ) ;
#126740=VECTOR ( 'NONE', #104155, 1000.000000000000000 ) ;
#126745=ORIENTED_EDGE ( 'NONE', *, *, #117042, .T. ) ;
#126748=EDGE_CURVE ( 'NONE', #19120, #23864, #7413, .T. ) ;
#126751=ORIENTED_EDGE ( 'NONE', *, *, #5209, .F. ) ;
#126774=EDGE_CURVE ( 'NONE', #83250, #105032, #19930, .T. ) ;
#126798=CARTESIAN_POINT ( 'NONE',  ( -20.94999999999999929, 11.65000000001115588, -174.5148057706539930 ) ) ;
#126810=CARTESIAN_POINT ( 'NONE',  ( -20.85000000000000142, -1.835859311432481045, -212.5044391687984842 ) ) ;
#126820=ORIENTED_EDGE ( 'NONE', *, *, #196568, .F. ) ;
#126822=EDGE_CURVE ( 'NONE', #182833, #95624, #126380, .T. ) ;
#126823=ORIENTED_EDGE ( 'NONE', *, *, #35719, .F. ) ;
#126836=ORIENTED_EDGE ( 'NONE', *, *, #224996, .T. ) ;
#126842=DIRECTION ( 'NONE',  ( 1.000000000000000000, -0.000000000000000000, -0.000000000000000000 ) ) ;
#126864=EDGE_CURVE ( 'NONE', #20774, #215603, #110670, .T. ) ;
#126867=DIRECTION ( 'NONE',  ( 0.000000000000000000, 0.000000000000000000, -1.000000000000000000 ) ) ;
#126879=CARTESIAN_POINT ( 'NONE',  ( 21.14999999999999858, 11.65000000001116298, -179.6499999999999773 ) ) ;
#126881=EDGE_CURVE ( 'NONE', #57378, #225164, #220484, .T. ) ;
#126914=( NAMED_UNIT ( * ) SI_UNIT ( $, .STERADIAN. ) SOLID_ANGLE_UNIT ( ) );
#126939=ORIENTED_EDGE ( 'NONE', *, *, #38502, .T. ) ;
#126954=CARTESIAN_POINT ( 'NONE',  ( 21.08621493067296626, 6.349294291182826733, -167.4438051605238513 ) ) ;
#127002=ORIENTED_EDGE ( 'NONE', *, *, #214552, .F. ) ;
#127039=TOROIDAL_SURFACE ( 'NONE', #235193, 11.65000000000000036, 0.1000000000000000056 ) ;
#127051=CARTESIAN_POINT ( 'NONE',  ( -21.05000000000000071, 1.162701749949165642, -175.4999999999999716 ) ) ;
#127074=AXIS2_PLACEMENT_3D ( 'NONE', #199684, #216649, #200941 ) ;
#127112=ORIENTED_EDGE ( 'NONE', *, *, #47040, .T. ) ;
#127116=AXIS2_PLACEMENT_3D ( 'NONE', #125034, #148451, #109289 ) ;
#127119=VERTEX_POINT ( 'NONE', #238307 ) ;
#127133=CARTESIAN_POINT ( 'NONE',  ( -21.05000000000000071, 1.250000000011155299, -175.4999999999999716 ) ) ;
#127142=( BOUNDED_SURFACE ( )  B_SPLINE_SURFACE ( 3, 2, ( 
 ( #193330, #94206, #253279 ),
 ( #55064, #156788, #155513 ),
 ( #12143, #134602, #152947 ),
 ( #35558, #235021, #56352 ),
 ( #15995, #171238, #95496 ),
 ( #135887, #36848, #57640 ) ),
 .UNSPECIFIED., .F., .F., .T. ) 
 B_SPLINE_SURFACE_WITH_KNOTS ( ( 4, 2, 4 ),
 ( 3, 3 ),
 ( 4.712388980384689674, 5.497787143782137953, 6.283185307179586232 ),
 ( 0.000000000000000000, 1.000000000000000000 ),
 .UNSPECIFIED. ) 
 GEOMETRIC_REPRESENTATION_ITEM ( )  RATIONAL_B_SPLINE_SURFACE ( (
 ( 1.000000000000000000, 0.7071067811864555352, 1.000000000000000000),
 ( 1.000000000000000000, 0.7727932973496255409, 1.000000000000000000),
 ( 1.000000000000000000, 0.8282379607643716168, 1.000000000000000000),
 ( 1.000000000000000000, 0.9038128468045815156, 1.000000000000000000),
 ( 1.000000000000000000, 0.9240297172238780554, 1.000000000000000000),
 ( 1.000000000000000000, 0.9238795325112914014, 1.000000000000000000) ) ) 
 REPRESENTATION_ITEM ( '' )  SURFACE ( )  );
#127149=DIRECTION ( 'NONE',  ( 1.000000000000000000, 0.000000000000000000, 0.000000000000000000 ) ) ;
#127150=DIRECTION ( 'NONE',  ( 0.000000000000000000, -0.1350103645451904977, 0.9908441862701596881 ) ) ;
#127151=PLANE ( 'NONE',  #19363 ) ;
#127169=AXIS2_PLACEMENT_3D ( 'NONE', #330, #236381, #257175 ) ;
#127190=AXIS2_PLACEMENT_3D ( 'NONE', #234419, #139147, #218694 ) ;
#127194=ORIENTED_EDGE ( 'NONE', *, *, #256763, .F. ) ;
#127231=CARTESIAN_POINT ( 'NONE',  ( -21.44999999999999929, 7.350000000011155166, -179.7499999999999716 ) ) ;
#127280=DIRECTION ( 'NONE',  ( 1.000000000000000000, 2.952720810173289112E-16, -0.000000000000000000 ) ) ;
#127285=CARTESIAN_POINT ( 'NONE',  ( -22.39999999999999858, 1.115600667400684642E-11, -159.7092204016265384 ) ) ;
#127296=DIRECTION ( 'NONE',  ( 1.000000000000000000, 0.000000000000000000, 0.000000000000000000 ) ) ;
#127320=AXIS2_PLACEMENT_3D ( 'NONE', #139209, #179665, #972 ) ;
#127321=FACE_OUTER_BOUND ( 'NONE', #245251, .T. ) ;
#127364=EDGE_LOOP ( 'NONE', ( #161858, #92772, #222527, #53359 ) ) ;
#127389=EDGE_CURVE ( 'NONE', #208842, #220457, #129077, .T. ) ;
#127410=DIRECTION ( 'NONE',  ( 7.304098846218134667E-16, -1.000000000000000000, 0.000000000000000000 ) ) ;
#127419=CIRCLE ( 'NONE', #69193, 0.09999999999999999167 ) ;
#127452=CYLINDRICAL_SURFACE ( 'NONE', #5349, 4.000000000000003553 ) ;
#127483=EDGE_LOOP ( 'NONE', ( #47472, #15511, #245161, #180634 ) ) ;
#127491=FACE_OUTER_BOUND ( 'NONE', #249400, .T. ) ;
#127496=DIRECTION ( 'NONE',  ( 1.000000000000000000, -0.000000000000000000, -0.000000000000000000 ) ) ;
#127531=ORIENTED_EDGE ( 'NONE', *, *, #215185, .T. ) ;
#127546=CARTESIAN_POINT ( 'NONE',  ( 20.95512820512820440, 8.876151316299271343, -188.7499999999999716 ) ) ;
#127560=DIRECTION ( 'NONE',  ( 1.000000000000000000, -0.000000000000000000, -0.000000000000000000 ) ) ;
#127572=CARTESIAN_POINT ( 'NONE',  ( 23.14999999999999858, 5.500000000011153745, -188.5947339810868755 ) ) ;
#127592=AXIS2_PLACEMENT_3D ( 'NONE', #126219, #31017, #87079 ) ;
#127608=AXIS2_PLACEMENT_3D ( 'NONE', #188444, #223702, #86757 ) ;
#127614=VERTEX_POINT ( 'NONE', #206269 ) ;
#127619=CIRCLE ( 'NONE', #165021, 0.09999999999999817368 ) ;
#127659=EDGE_CURVE ( 'NONE', #4296, #256132, #247950, .T. ) ;
#127670=DIRECTION ( 'NONE',  ( 1.000000000000000000, -0.000000000000000000, -0.000000000000000000 ) ) ;
#127673=EDGE_CURVE ( 'NONE', #139380, #145808, #11509, .T. ) ;
#127679=CARTESIAN_POINT ( 'NONE',  ( -23.25000000000000000, 4.350000000011156054, -188.6499999999999488 ) ) ;
#127697=CARTESIAN_POINT ( 'NONE',  ( -20.94999999999999929, -1.360870587180885716, -175.5729979270909382 ) ) ;
#127710=CARTESIAN_POINT ( 'NONE',  ( 20.94999999999999929, 4.813084112160680661, -179.4415177565237798 ) ) ;
#127731=CARTESIAN_POINT ( 'NONE',  ( -20.54999999999999716, 7.150000000011155876, -179.8499999999999943 ) ) ;
#127733=DIRECTION ( 'NONE',  ( 0.000000000000000000, 0.000000000000000000, -1.000000000000000000 ) ) ;
#127747=VECTOR ( 'NONE', #21352, 1000.000000000000000 ) ;
#127758=VECTOR ( 'NONE', #197687, 1000.000000000000000 ) ;
#127775=CIRCLE ( 'NONE', #98488, 0.09999999999999817368 ) ;
#127789=DIRECTION ( 'NONE',  ( -1.000000000000000000, 0.000000000000000000, 0.000000000000000000 ) ) ;
#127814=DIRECTION ( 'NONE',  ( 0.000000000000000000, -0.8660254037844383745, 0.5000000000000003331 ) ) ;
#127820=ORIENTED_EDGE ( 'NONE', *, *, #19690, .F. ) ;
#127873=CARTESIAN_POINT ( 'NONE',  ( -23.25000000000000000, 2.600000000011156054, -187.7753780772378889 ) ) ;
#127888=CARTESIAN_POINT ( 'NONE',  ( 18.45139536634708932, -9.486081720270037820, -207.6405116178106312 ) ) ;
#127892=( BOUNDED_SURFACE ( )  B_SPLINE_SURFACE ( 3, 2, ( 
 ( #206858, #66056, #145587 ),
 ( #43932, #123472, #245993 ),
 ( #146859, #223833, #186010 ),
 ( #67349, #105139, #203001 ) ),
 .UNSPECIFIED., .F., .F., .F. ) 
 B_SPLINE_SURFACE_WITH_KNOTS ( ( 4, 4 ),
 ( 3, 3 ),
 ( 0.0002700421466196765378, 0.0004789321604330627779 ),
 ( 0.000000000000000000, 1.000000000000000000 ),
 .UNSPECIFIED. ) 
 GEOMETRIC_REPRESENTATION_ITEM ( )  RATIONAL_B_SPLINE_SURFACE ( (
 ( 1.000000000000000000, 0.7071067811865475727, 1.000000000000000000),
 ( 1.000000000000000000, 0.7163411249511861811, 1.000000000000000000),
 ( 1.000000000000000000, 0.7221957104841836284, 1.000000000000000000),
 ( 1.000000000000000000, 0.7250110520819876836, 1.000000000000000000) ) ) 
 REPRESENTATION_ITEM ( '' )  SURFACE ( )  );
#127936=CARTESIAN_POINT ( 'NONE',  ( -20.64999999999999858, 2.000000000011154189, -188.2753780772378889 ) ) ;
#127945=ORIENTED_EDGE ( 'NONE', *, *, #239400, .T. ) ;
#127976=CIRCLE ( 'NONE', #219526, 0.1000000000000102612 ) ;
#127977=CARTESIAN_POINT ( 'NONE',  ( -21.05000000000000071, 0.03363273534480442500, -161.2411828053184877 ) ) ;
#128002=CARTESIAN_POINT ( 'NONE',  ( 18.43579564894481138, -9.519327535281362884, -174.4729766438603349 ) ) ;
#128014=EDGE_LOOP ( 'NONE', ( #63852, #89814, #122523, #92081 ) ) ;
#128029=VERTEX_POINT ( 'NONE', #160131 ) ;
#128041=LINE ( 'NONE', #88883, #72398 ) ;
#128056=AXIS2_PLACEMENT_3D ( 'NONE', #245367, #28926, #125419 ) ;
#128089=LINE ( 'NONE', #248021, #14095 ) ;
#128143=VECTOR ( 'NONE', #127560, 1000.000000000000000 ) ;
#128149=B_SPLINE_CURVE_WITH_KNOTS ( 'NONE', 3,
 ( #90593, #167604, #247100, #48908, #29393, #89312, #69785, #209269, #110165, #150593, #191022, #12385, #236528, #155756, #157026, #20075, #235250, #174045, #77440 ),
 .UNSPECIFIED., .F., .F.,
 ( 4, 3, 3, 3, 3, 3, 4 ),
 ( 1.387778780781445676E-17, 2.646747978909242031E-05, 5.271166642130207115E-05, 9.008788829887291478E-05, 0.0001426648776561344830, 0.0001897378458660081940, 0.0001917382627806528145 ),
 .UNSPECIFIED. ) ;
#128207=VECTOR ( 'NONE', #112115, 1000.000000000000000 ) ;
#128216=FACE_OUTER_BOUND ( 'NONE', #253777, .T. ) ;
#128244=VECTOR ( 'NONE', #41136, 1000.000000000000000 ) ;
#128255=CIRCLE ( 'NONE', #74116, 7.899999999999990585 ) ;
#128274=DIRECTION ( 'NONE',  ( 1.000000000000000000, -0.000000000000000000, -0.000000000000000000 ) ) ;
#128276=ORIENTED_EDGE ( 'NONE', *, *, #187537, .T. ) ;
#128285=AXIS2_PLACEMENT_3D ( 'NONE', #200219, #41171, #62000 ) ;
#128341=CARTESIAN_POINT ( 'NONE',  ( -23.15000000000000213, 2.600000000011156054, -155.7499999999999716 ) ) ;
#128348=DIRECTION ( 'NONE',  ( 1.000000000000000000, 3.265361837132813093E-16, -0.000000000000000000 ) ) ;
#128375=DIRECTION ( 'NONE',  ( 1.000000000000000000, 1.875376730785737719E-16, 0.000000000000000000 ) ) ;
#128403=VERTEX_POINT ( 'NONE', #218321 ) ;
#128410=VERTEX_POINT ( 'NONE', #220898 ) ;
#128418=ORIENTED_EDGE ( 'NONE', *, *, #149346, .F. ) ;
#128443=DIRECTION ( 'NONE',  ( -1.000000000000000000, -0.000000000000000000, -0.000000000000000000 ) ) ;
#128464=ORIENTED_EDGE ( 'NONE', *, *, #12196, .T. ) ;
#128507=ORIENTED_EDGE ( 'NONE', *, *, #64973, .F. ) ;
#128523=CIRCLE ( 'NONE', #49409, 12.87499999999999822 ) ;
#128537=CARTESIAN_POINT ( 'NONE',  ( -20.91682497891423154, 10.32263460347359185, -206.5605957968671476 ) ) ;
#128557=EDGE_CURVE ( 'NONE', #187086, #223496, #27306, .T. ) ;
#128570=CIRCLE ( 'NONE', #99492, 0.2000000000000057288 ) ;
#128584=FACE_OUTER_BOUND ( 'NONE', #64913, .T. ) ;
#128588=CIRCLE ( 'NONE', #224258, 0.2000000000000057288 ) ;
#128611=CARTESIAN_POINT ( 'NONE',  ( -22.59999985501179154, 11.74986979301414181, -167.4344013302005862 ) ) ;
#128616=EDGE_LOOP ( 'NONE', ( #38028, #170447, #115374, #2551 ) ) ;
#128619=EDGE_LOOP ( 'NONE', ( #129952, #107396, #72169, #198650, #172364, #11533, #56363 ) ) ;
#128623=CARTESIAN_POINT ( 'NONE',  ( 23.14999999999999147, -4.149999999988843058, -167.4999999999999716 ) ) ;
#128627=CARTESIAN_POINT ( 'NONE',  ( -18.59999999999999787, -1.835341550213255957, -179.0551512925629538 ) ) ;
#128658=DIRECTION ( 'NONE',  ( -0.000000000000000000, 0.000000000000000000, 1.000000000000000000 ) ) ;
#128693=AXIS2_PLACEMENT_3D ( 'NONE', #39596, #1699, #100765 ) ;
#128709=CARTESIAN_POINT ( 'NONE',  ( -21.05000000000000071, 1.261786168576181755, -175.5864989635454378 ) ) ;
#128718=ORIENTED_EDGE ( 'NONE', *, *, #130416, .T. ) ;
#128721=CARTESIAN_POINT ( 'NONE',  ( 23.24999999999999645, 1.115600667400684642E-11, -200.9999999999999432 ) ) ;
#128749=DIRECTION ( 'NONE',  ( 0.000000000000000000, -0.000000000000000000, -1.000000000000000000 ) ) ;
#128757=DIRECTION ( 'NONE',  ( 1.000000000000000000, 0.000000000000000000, 0.000000000000000000 ) ) ;
#128823=ORIENTED_EDGE ( 'NONE', *, *, #98920, .F. ) ;
#128826=CIRCLE ( 'NONE', #91412, 11.65000000000000036 ) ;
#128849=CARTESIAN_POINT ( 'NONE',  ( 23.14999999999999858, 1.115600667400684642E-11, -200.9999999999999432 ) ) ;
#128874=DIRECTION ( 'NONE',  ( 1.000000000000000000, 0.000000000000000000, 0.000000000000000000 ) ) ;
#128880=CARTESIAN_POINT ( 'NONE',  ( -23.25000000000000000, 11.65000000001115588, -167.4999999999999716 ) ) ;
#128882=LINE ( 'NONE', #186289, #171692 ) ;
#128886=PLANE ( 'NONE',  #46285 ) ;
#128904=EDGE_LOOP ( 'NONE', ( #32542, #233013, #229764, #164956 ) ) ;
#128914=SPHERICAL_SURFACE ( 'NONE', #120294, 0.1000000000000000056 ) ;
#128946=CARTESIAN_POINT ( 'NONE',  ( 20.94999999999999929, -1.362429037182151470, -208.8888812479211765 ) ) ;
#128961=EDGE_CURVE ( 'NONE', #69705, #207624, #191132, .T. ) ;
#128973=DIRECTION ( 'NONE',  ( -1.000000000000000000, 0.000000000000000000, -0.000000000000000000 ) ) ;
#128992=LINE ( 'NONE', #127710, #171782 ) ;
#129018=CARTESIAN_POINT ( 'NONE',  ( -18.59999999999999787, 7.250000000011155521, -188.8499999999999659 ) ) ;
#129020=CARTESIAN_POINT ( 'NONE',  ( -22.39999999999999858, 1.115600667400684642E-11, -167.3999999999999773 ) ) ;
#129029=FACE_OUTER_BOUND ( 'NONE', #257357, .T. ) ;
#129036=FACE_OUTER_BOUND ( 'NONE', #8084, .T. ) ;
#129043=CIRCLE ( 'NONE', #58282, 0.09999999999999939493 ) ;
#129048=CARTESIAN_POINT ( 'NONE',  ( -22.59999970745345976, -0.009356377315826230542, -155.7494867923307424 ) ) ;
#129049=EDGE_LOOP ( 'NONE', ( #41878, #48708, #196556, #208934 ) ) ;
#129077=CIRCLE ( 'NONE', #204068, 0.09999999999999939493 ) ;
#129078=EDGE_CURVE ( 'NONE', #50212, #7516, #203757, .T. ) ;
#129121=CARTESIAN_POINT ( 'NONE',  ( -20.54999999999999716, -8.999999999988846255, -177.3939691226524076 ) ) ;
#129205=DIRECTION ( 'NONE',  ( 1.000000000000000000, -0.000000000000000000, -0.000000000000000000 ) ) ;
#129238=DIRECTION ( 'NONE',  ( -1.000000000000000000, 0.000000000000000000, 0.000000000000000000 ) ) ;
#129240=FACE_OUTER_BOUND ( 'NONE', #232380, .T. ) ;
#129265=EDGE_CURVE ( 'NONE', #244617, #145757, #237075, .T. ) ;
#129277=CARTESIAN_POINT ( 'NONE',  ( 18.59999999999999432, -1.162701749926853712, -175.4999999999999716 ) ) ;
#129284=CIRCLE ( 'NONE', #75137, 2.099999999999990763 ) ;
#129285=DIRECTION ( 'NONE',  ( 0.000000000000000000, 0.9908441862701782288, 0.1350103645450542456 ) ) ;
#129296=DIRECTION ( 'NONE',  ( 0.000000000000000000, 0.000000000000000000, -1.000000000000000000 ) ) ;
#129337=VERTEX_POINT ( 'NONE', #129997 ) ;
#129352=ORIENTED_EDGE ( 'NONE', *, *, #225667, .F. ) ;
#129377=AXIS2_PLACEMENT_3D ( 'NONE', #226878, #247729, #67807 ) ;
#129379=EDGE_LOOP ( 'NONE', ( #79028, #119287, #42650, #50650, #96900, #102005, #146653 ) ) ;
#129409=DIRECTION ( 'NONE',  ( -0.000000000000000000, 0.9274965247785350586, 0.3738317757009704811 ) ) ;
#129420=ORIENTED_EDGE ( 'NONE', *, *, #100696, .T. ) ;
#129423=VERTEX_POINT ( 'NONE', #131297 ) ;
#129445=EDGE_CURVE ( 'NONE', #108203, #122253, #133039, .T. ) ;
#129448=DIRECTION ( 'NONE',  ( 0.000000000000000000, 0.000000000000000000, 1.000000000000000000 ) ) ;
#129461=DIRECTION ( 'NONE',  ( -1.000000000000000000, -0.000000000000000000, -0.000000000000000000 ) ) ;
#129480=DIRECTION ( 'NONE',  ( 0.000000000000000000, 0.1298341882520022694, 0.9915357197604852679 ) ) ;
#129485=( LENGTH_UNIT ( ) NAMED_UNIT ( * ) SI_UNIT ( .MILLI., .METRE. ) );
#129492=DIRECTION ( 'NONE',  ( 1.000000000000000000, 0.000000000000000000, 0.000000000000000000 ) ) ;
#129507=AXIS2_PLACEMENT_3D ( 'NONE', #142948, #41338, #40061 ) ;
#129508=DIRECTION ( 'NONE',  ( 0.000000000000000000, 0.000000000000000000, -1.000000000000000000 ) ) ;
#129538=CYLINDRICAL_SURFACE ( 'NONE', #28196, 0.09999999999998898659 ) ;
#129544=CARTESIAN_POINT ( 'NONE',  ( 20.96077737575349786, 11.62390063401585394, -194.1407919571063019 ) ) ;
#129548=CARTESIAN_POINT ( 'NONE',  ( -21.05000000000000071, -11.64999999998884483, -167.4999999999999432 ) ) ;
#129576=FACE_OUTER_BOUND ( 'NONE', #121299, .T. ) ;
#129586=CARTESIAN_POINT ( 'NONE',  ( -21.07928932188134041, 6.328516656404449492, -167.4011048543455615 ) ) ;
#129589=CIRCLE ( 'NONE', #254446, 11.80000000000000426 ) ;
#129593=FACE_OUTER_BOUND ( 'NONE', #67524, .T. ) ;
#129594=EDGE_CURVE ( 'NONE', #98329, #42259, #232995, .T. ) ;
#129653=CARTESIAN_POINT ( 'NONE',  ( 23.24999999999999645, 1.115600667400684642E-11, -200.9999999999999432 ) ) ;
#129705=VERTEX_POINT ( 'NONE', #129713 ) ;
#129713=CARTESIAN_POINT ( 'NONE',  ( -18.59999999999999787, -1.164121893230052995, -208.8148480855715832 ) ) ;
#129795=CARTESIAN_POINT ( 'NONE',  ( 21.14999999999999503, -0.09999999998884338825, -155.8504291924551808 ) ) ;
#129833=CARTESIAN_POINT ( 'NONE',  ( 23.15000000000000213, -8.999999999988842703, -191.1060308773475072 ) ) ;
#129836=EDGE_CURVE ( 'NONE', #77400, #177630, #3625, .T. ) ;
#129837=CARTESIAN_POINT ( 'NONE',  ( 21.05000000000000071, 6.304516329275450914, -167.5211033080591392 ) ) ;
#129838=DIRECTION ( 'NONE',  ( -1.000000000000000000, 0.000000000000000000, 0.000000000000000000 ) ) ;
#129851=CIRCLE ( 'NONE', #138219, 0.09999999999998898659 ) ;
#129875=CIRCLE ( 'NONE', #17459, 0.09999999999998898659 ) ;
#129879=ORIENTED_EDGE ( 'NONE', *, *, #234843, .T. ) ;
#129897=CARTESIAN_POINT ( 'NONE',  ( 20.99999999999997868, 1.115600667400684642E-11, -167.4999999999999716 ) ) ;
#129901=CARTESIAN_POINT ( 'NONE',  ( -18.59999999999999787, 1.866714910068465239, -179.2526752462819672 ) ) ;
#129952=ORIENTED_EDGE ( 'NONE', *, *, #66930, .F. ) ;
#129967=ORIENTED_EDGE ( 'NONE', *, *, #122331, .F. ) ;
#129997=CARTESIAN_POINT ( 'NONE',  ( -18.50000000000000000, 10.29270135741298375, -206.4573618871519045 ) ) ;
#130014=CIRCLE ( 'NONE', #17594, 0.09999999999998807065 ) ;
#130017=TOROIDAL_SURFACE ( 'NONE', #217510, 0.2000000000000000111, 0.1000000000000000056 ) ;
#130038=ADVANCED_FACE ( 'NONE', ( #218207 ), #220801, .F. ) ;
#130051=CARTESIAN_POINT ( 'NONE',  ( 18.49999999999999645, 1.115600667400684642E-11, -200.9999999999999432 ) ) ;
#130058=DIRECTION ( 'NONE',  ( -1.000000000000000000, -3.265361837132813093E-16, 0.000000000000000000 ) ) ;
#130060=CARTESIAN_POINT ( 'NONE',  ( -21.45000000000000284, 7.708578643773852157, -188.7499999999999716 ) ) ;
#130066=CIRCLE ( 'NONE', #84225, 0.09999999999998898659 ) ;
#130077=VERTEX_POINT ( 'NONE', #202527 ) ;
#130094=CARTESIAN_POINT ( 'NONE',  ( -21.53699400384035201, 1.437176978725413726E-11, -160.7122882067533567 ) ) ;
#130100=DIRECTION ( 'NONE',  ( -0.000000000000000000, -0.000000000000000000, 1.000000000000000000 ) ) ;
#130110=ORIENTED_EDGE ( 'NONE', *, *, #245151, .F. ) ;
#130121=CARTESIAN_POINT ( 'NONE',  ( -18.60000000000000142, -9.523954320741637503, -207.8820170568272943 ) ) ;
#130150=EDGE_LOOP ( 'NONE', ( #133878, #110785, #133892, #236540 ) ) ;
#130163=DIRECTION ( 'NONE',  ( 1.000000000000000000, -0.000000000000000000, -0.000000000000000000 ) ) ;
#130187=DIRECTION ( 'NONE',  ( 0.000000000000000000, 0.6728971962617388280, -0.7397360091702248619 ) ) ;
#130188=FACE_OUTER_BOUND ( 'NONE', #205479, .T. ) ;
#130268=DIRECTION ( 'NONE',  ( -1.836970198721029934E-16, 1.000000000000000000, 0.000000000000000000 ) ) ;
#130274=CARTESIAN_POINT ( 'NONE',  ( -21.05000000000000071, 1.851028230152016674, -179.1539132694224463 ) ) ;
#130308=VERTEX_POINT ( 'NONE', #57560 ) ;
#130316=VERTEX_POINT ( 'NONE', #131977 ) ;
#130331=CARTESIAN_POINT ( 'NONE',  ( -23.15000000000000213, 11.65000000001115588, -193.9851942293460070 ) ) ;
#130350=CIRCLE ( 'NONE', #221921, 0.1000000000000019207 ) ;
#130381=CARTESIAN_POINT ( 'NONE',  ( -18.45068461519105441, -9.486506529077933791, -174.5687771689046883 ) ) ;
#130402=CIRCLE ( 'NONE', #188661, 0.09999999999999344136 ) ;
#130411=CARTESIAN_POINT ( 'NONE',  ( 20.04142135623730070, 11.65000000001115943, -188.8499999999999659 ) ) ;
#130416=EDGE_CURVE ( 'NONE', #91084, #57292, #3828, .T. ) ;
#130425=DIRECTION ( 'NONE',  ( -0.000000000000000000, -0.000000000000000000, 1.000000000000000000 ) ) ;
#130434=FACE_OUTER_BOUND ( 'NONE', #205706, .T. ) ;
#130450=DIRECTION ( 'NONE',  ( 1.000000000000000000, 0.000000000000000000, -0.000000000000000000 ) ) ;
#130458=AXIS2_PLACEMENT_3D ( 'NONE', #253749, #75160, #56811 ) ;
#130477=DIRECTION ( 'NONE',  ( -0.7071067811865475727, -0.7071067811865475727, 0.000000000000000000 ) ) ;
#130483=DIRECTION ( 'NONE',  ( 1.000000000000000000, 0.000000000000000000, 0.000000000000000000 ) ) ;
#130535=EDGE_LOOP ( 'NONE', ( #73579, #56449, #15369, #21579 ) ) ;
#130615=VECTOR ( 'NONE', #114623, 1000.000000000000000 ) ;
#130638=AXIS2_PLACEMENT_3D ( 'NONE', #231041, #190629, #91512 ) ;
#130646=CARTESIAN_POINT ( 'NONE',  ( 20.94999999999999929, 1.115600667400684642E-11, -200.9999999999999432 ) ) ;
#130690=DIRECTION ( 'NONE',  ( 1.000000000000000000, -0.000000000000000000, -0.000000000000000000 ) ) ;
#130708=ORIENTED_EDGE ( 'NONE', *, *, #119070, .T. ) ;
#130737=ADVANCED_FACE ( 'NONE', ( #151259 ), #230802, .F. ) ;
#130742=CARTESIAN_POINT ( 'NONE',  ( 18.59999999999998721, 19.85039924724470950, -169.7803030578013477 ) ) ;
#130819=CARTESIAN_POINT ( 'NONE',  ( -21.59142135623730852, 7.850000000011158718, -188.6499999999999488 ) ) ;
#130826=EDGE_CURVE ( 'NONE', #251611, #91084, #138079, .T. ) ;
#130863=ORIENTED_EDGE ( 'NONE', *, *, #45803, .T. ) ;
#130890=DIRECTION ( 'NONE',  ( 0.000000000000000000, -4.440892098500611173E-15, -1.000000000000000000 ) ) ;
#130936=EDGE_CURVE ( 'NONE', #215603, #115618, #237428, .T. ) ;
#130955=PLANE ( 'NONE',  #26379 ) ;
#130980=LINE ( 'NONE', #12342, #154370 ) ;
#131011=ORIENTED_EDGE ( 'NONE', *, *, #206951, .T. ) ;
#131014=ORIENTED_EDGE ( 'NONE', *, *, #41744, .F. ) ;
#131042=CIRCLE ( 'NONE', #201769, 0.09999999999998898659 ) ;
#131080=CARTESIAN_POINT ( 'NONE',  ( -18.52186455168970625, -9.481018481431632949, -174.5250164779141073 ) ) ;
#131090=DIRECTION ( 'NONE',  ( 1.000000000000000000, 7.304098846218134667E-16, -0.000000000000000000 ) ) ;
#131093=CIRCLE ( 'NONE', #18670, 0.09999999999998898659 ) ;
#131118=VERTEX_POINT ( 'NONE', #233982 ) ;
#131128=CARTESIAN_POINT ( 'NONE',  ( 21.05000000000000071, 6.257814610487288043, -167.4022097086911742 ) ) ;
#131130=ORIENTED_EDGE ( 'NONE', *, *, #229262, .F. ) ;
#131150=DIRECTION ( 'NONE',  ( -1.000000000000000000, 0.000000000000000000, 0.000000000000000000 ) ) ;
#131167=EDGE_LOOP ( 'NONE', ( #139264, #20465, #40087, #60881 ) ) ;
#131251=CIRCLE ( 'NONE', #226937, 0.09999999999998898659 ) ;
#131277=EDGE_LOOP ( 'NONE', ( #49967, #154097, #197469, #214444 ) ) ;
#131286=DIRECTION ( 'NONE',  ( 0.000000000000000000, 0.000000000000000000, -1.000000000000000000 ) ) ;
#131293=CARTESIAN_POINT ( 'NONE',  ( 22.48660254037844197, 11.65000000001116298, -167.4499999999999602 ) ) ;
#131297=CARTESIAN_POINT ( 'NONE',  ( 21.87500000000000355, 9.750000000011153745, -188.6499999999999488 ) ) ;
#131329=EDGE_LOOP ( 'NONE', ( #13229, #160472, #121174, #255973, #220129 ) ) ;
#131341=VERTEX_POINT ( 'NONE', #249413 ) ;
#131383=FACE_OUTER_BOUND ( 'NONE', #127364, .T. ) ;
#131386=ORIENTED_EDGE ( 'NONE', *, *, #96901, .F. ) ;
#131391=CARTESIAN_POINT ( 'NONE',  ( -18.59999999999999787, 1.162701749949165642, -175.5999999999999659 ) ) ;
#131407=ORIENTED_EDGE ( 'NONE', *, *, #149346, .T. ) ;
#131421=CARTESIAN_POINT ( 'NONE',  ( 21.05000000000000071, -0.09999999998884338825, -160.9593430482987344 ) ) ;
#131429=ORIENTED_EDGE ( 'NONE', *, *, #216702, .F. ) ;
#131435=DIRECTION ( 'NONE',  ( 0.000000000000000000, 0.4930308989875230585, 0.8700118002898322711 ) ) ;
#131438=CARTESIAN_POINT ( 'NONE',  ( -20.94999999999999929, -11.48912529306490349, -170.3999999999999773 ) ) ;
#131456=VERTEX_POINT ( 'NONE', #14674 ) ;
#131468=FACE_OUTER_BOUND ( 'NONE', #79741, .T. ) ;
#131479=CARTESIAN_POINT ( 'NONE',  ( 22.49999999999999645, 0.08880997639808871358, -155.8502370819680323 ) ) ;
#131483=DIRECTION ( 'NONE',  ( -2.561896900575096011E-15, -0.5907332058517279494, 0.8068669527897025517 ) ) ;
#131491=EDGE_CURVE ( 'NONE', #243191, #100689, #129284, .T. ) ;
#131493=ORIENTED_EDGE ( 'NONE', *, *, #133728, .T. ) ;
#131503=CIRCLE ( 'NONE', #123146, 0.09999999999998898659 ) ;
#131553=CARTESIAN_POINT ( 'NONE',  ( -18.31331870001089612, -9.536294719169530865, -207.8685786909852879 ) ) ;
#131583=CYLINDRICAL_SURFACE ( 'NONE', #93919, 0.09999999999998898659 ) ;
#131633=VECTOR ( 'NONE', #126065, 1000.000000000000000 ) ;
#131647=ORIENTED_EDGE ( 'NONE', *, *, #9369, .F. ) ;
#131653=CARTESIAN_POINT ( 'NONE',  ( 20.94999999999999929, 5.850000000011156942, -190.8675027757220448 ) ) ;
#131667=ORIENTED_EDGE ( 'NONE', *, *, #39800, .F. ) ;
#131693=VERTEX_POINT ( 'NONE', #84848 ) ;
#131717=DIRECTION ( 'NONE',  ( 1.000000000000000000, 0.000000000000000000, 0.000000000000000000 ) ) ;
#131726=CARTESIAN_POINT ( 'NONE',  ( -20.97625342178436014, 11.60000000083177696, -174.4282032298017384 ) ) ;
#131749=ORIENTED_EDGE ( 'NONE', *, *, #221140, .F. ) ;
#131756=ORIENTED_EDGE ( 'NONE', *, *, #207373, .T. ) ;
#131761=CARTESIAN_POINT ( 'NONE',  ( -23.15000000000000213, 1.925233644870972816, -180.2302435331260995 ) ) ;
#131776=CARTESIAN_POINT ( 'NONE',  ( -20.54999999999999716, -9.399999999988846611, -191.1060308773475356 ) ) ;
#131804=LINE ( 'NONE', #47111, #155494 ) ;
#131805=AXIS2_PLACEMENT_3D ( 'NONE', #35580, #218014, #118954 ) ;
#131826=DIRECTION ( 'NONE',  ( -0.000000000000000000, -0.000000000000000000, 1.000000000000000000 ) ) ;
#131843=EDGE_CURVE ( 'NONE', #59716, #77719, #254337, .T. ) ;
#131860=CIRCLE ( 'NONE', #152744, 0.09999999999999971412 ) ;
#131876=LINE ( 'NONE', #10652, #59949 ) ;
#131883=VECTOR ( 'NONE', #115032, 1000.000000000000000 ) ;
#131901=VERTEX_POINT ( 'NONE', #122435 ) ;
#131921=DIRECTION ( 'NONE',  ( -1.000000000000000000, -0.000000000000000000, 0.000000000000000000 ) ) ;
#131948=ORIENTED_EDGE ( 'NONE', *, *, #106870, .F. ) ;
#131950=ORIENTED_EDGE ( 'NONE', *, *, #206835, .F. ) ;
#131953=ORIENTED_EDGE ( 'NONE', *, *, #109596, .T. ) ;
#131971=CYLINDRICAL_SURFACE ( 'NONE', #83586, 12.87499999999999822 ) ;
#131977=CARTESIAN_POINT ( 'NONE',  ( -20.64999999999999858, 4.350000000011156054, -188.7499999999999716 ) ) ;
#131984=DIRECTION ( 'NONE',  ( -2.952720810173289112E-16, 1.000000000000000000, -0.000000000000000000 ) ) ;
#132006=CARTESIAN_POINT ( 'NONE',  ( 18.49999999999999289, 6.450000000011156587, -155.7499999999999716 ) ) ;
#132082=DIRECTION ( 'NONE',  ( 0.000000000000000000, 0.000000000000000000, -1.000000000000000000 ) ) ;
#132103=DIRECTION ( 'NONE',  ( -1.000000000000000000, -0.000000000000000000, -0.000000000000000000 ) ) ;
#132108=CARTESIAN_POINT ( 'NONE',  ( 20.85000000000000142, 11.75000000001115907, -194.2161343370218560 ) ) ;
#132115=EDGE_LOOP ( 'NONE', ( #146424, #138387, #221973, #94541 ) ) ;
#132153=CYLINDRICAL_SURFACE ( 'NONE', #144371, 0.09999999999998898659 ) ;
#132162=DIRECTION ( 'NONE',  ( 0.000000000000000000, 0.000000000000000000, 1.000000000000000000 ) ) ;
#132170=DIRECTION ( 'NONE',  ( -0.000000000000000000, 0.000000000000000000, -1.000000000000000000 ) ) ;
#132171=DIRECTION ( 'NONE',  ( -1.836970198721029934E-16, 1.000000000000000000, 0.000000000000000000 ) ) ;
#132181=CARTESIAN_POINT ( 'NONE',  ( -18.46902351632711614, -9.509470118669717920, -174.4864539342572698 ) ) ;
#132206=AXIS2_PLACEMENT_3D ( 'NONE', #238799, #219216, #229511 ) ;
#132250=EDGE_LOOP ( 'NONE', ( #119118, #214513, #156732, #143463 ) ) ;
#132290=EDGE_CURVE ( 'NONE', #156141, #208842, #226162, .T. ) ;
#132311=DIRECTION ( 'NONE',  ( -0.000000000000000000, -0.000000000000000000, 1.000000000000000000 ) ) ;
#132316=CARTESIAN_POINT ( 'NONE',  ( 20.04142135623730070, 11.65000000001115943, -188.8499999999999659 ) ) ;
#132359=DIRECTION ( 'NONE',  ( -0.000000000000000000, 0.000000000000000000, 1.000000000000000000 ) ) ;
#132369=CARTESIAN_POINT ( 'NONE',  ( -18.40000000000000568, -9.499999999988851584, -174.4993620971800681 ) ) ;
#132399=VERTEX_POINT ( 'NONE', #30518 ) ;
#132499=CIRCLE ( 'NONE', #207707, 12.87500000000000000 ) ;
#132518=AXIS2_PLACEMENT_3D ( 'NONE', #195751, #250552, #191906 ) ;
#132543=ORIENTED_EDGE ( 'NONE', *, *, #170377, .T. ) ;
#132549=DIRECTION ( 'NONE',  ( 1.000000000000000000, 0.000000000000000000, -0.000000000000000000 ) ) ;
#132585=EDGE_LOOP ( 'NONE', ( #156254, #210979 ) ) ;
#132596=AXIS2_PLACEMENT_3D ( 'NONE', #99639, #21447, #240467 ) ;
#132611=CARTESIAN_POINT ( 'NONE',  ( 21.05000000000000426, 10.72371710471867701, -175.0944173916130637 ) ) ;
#132658=ORIENTED_EDGE ( 'NONE', *, *, #47858, .T. ) ;
#132667=ORIENTED_EDGE ( 'NONE', *, *, #100045, .F. ) ;
#132675=DIRECTION ( 'NONE',  ( -2.602085213965226419E-14, -0.000000000000000000, 1.000000000000000000 ) ) ;
#132691=ORIENTED_EDGE ( 'NONE', *, *, #73864, .T. ) ;
#132693=DIRECTION ( 'NONE',  ( -1.000000000000000000, -0.000000000000000000, -0.000000000000000000 ) ) ;
#132713=DIRECTION ( 'NONE',  ( 0.000000000000000000, 0.000000000000000000, 1.000000000000000000 ) ) ;
#132728=VERTEX_POINT ( 'NONE', #6770 ) ;
#132771=DIRECTION ( 'NONE',  ( 0.000000000000000000, -1.000000000000000000, 0.000000000000000000 ) ) ;
#132772=ORIENTED_EDGE ( 'NONE', *, *, #161823, .F. ) ;
#132808=ORIENTED_EDGE ( 'NONE', *, *, #43834, .T. ) ;
#132823=ORIENTED_EDGE ( 'NONE', *, *, #241848, .F. ) ;
#132831=DIRECTION ( 'NONE',  ( 0.000000000000000000, -0.1350103645451876666, -0.9908441862701600211 ) ) ;
#132854=CARTESIAN_POINT ( 'NONE',  ( -18.41817142474042512, -9.498703066590925559, -207.6039654876369696 ) ) ;
#132861=VERTEX_POINT ( 'NONE', #30204 ) ;
#132884=CARTESIAN_POINT ( 'NONE',  ( 23.14999999999999503, 6.450000000011156587, -155.7499999999999716 ) ) ;
#132888=CARTESIAN_POINT ( 'NONE',  ( -18.59999999999999787, -1.162701749926853712, -175.5999999999999659 ) ) ;
#132893=ORIENTED_EDGE ( 'NONE', *, *, #12563, .T. ) ;
#132911=ADVANCED_FACE ( 'NONE', ( #136983 ), #100403, .F. ) ;
#132941=VERTEX_POINT ( 'NONE', #238657 ) ;
#132953=ADVANCED_FACE ( 'NONE', ( #114859 ), #254345, .F. ) ;
#132959=CIRCLE ( 'NONE', #182859, 0.8750000000000007772 ) ;
#132977=CARTESIAN_POINT ( 'NONE',  ( -18.41353343127311959, -9.499999999988849808, -174.5320693966996259 ) ) ;
#133003=DIRECTION ( 'NONE',  ( 0.000000000000000000, -0.6728971962617483760, 0.7397360091702162022 ) ) ;
#133004=VERTEX_POINT ( 'NONE', #105524 ) ;
#133009=DIRECTION ( 'NONE',  ( 0.000000000000000000, 0.000000000000000000, -1.000000000000000000 ) ) ;
#133034=ADVANCED_FACE ( 'NONE', ( #220390 ), #165550, .T. ) ;
#133039=CIRCLE ( 'NONE', #165801, 0.09999999999998898659 ) ;
#133070=CARTESIAN_POINT ( 'NONE',  ( -20.94999999999999929, 1.115600667400684642E-11, -175.3999999999999773 ) ) ;
#133092=ORIENTED_EDGE ( 'NONE', *, *, #5128, .F. ) ;
#133151=LINE ( 'NONE', #127051, #204533 ) ;
#133157=VECTOR ( 'NONE', #146703, 1000.000000000000000 ) ;
#133181=CARTESIAN_POINT ( 'NONE',  ( 22.49533356619864222, 11.65000000631534149, -167.4348774196771501 ) ) ;
#133185=ORIENTED_EDGE ( 'NONE', *, *, #75736, .F. ) ;
#133212=EDGE_LOOP ( 'NONE', ( #243881, #101575, #54788 ) ) ;
#133222=DIRECTION ( 'NONE',  ( -1.000000000000000000, 0.000000000000000000, 0.000000000000000000 ) ) ;
#133226=EDGE_CURVE ( 'NONE', #194728, #220627, #70323, .T. ) ;
#133255=DIRECTION ( 'NONE',  ( -3.265361837132813093E-16, 1.000000000000000000, 0.000000000000000000 ) ) ;
#133301=ORIENTED_EDGE ( 'NONE', *, *, #42703, .F. ) ;
#133368=CARTESIAN_POINT ( 'NONE',  ( -20.85000000000000142, -1.164121893230052995, -208.9148480855715775 ) ) ;
#133411=DIRECTION ( 'NONE',  ( 0.000000000000000000, 0.000000000000000000, -1.000000000000000000 ) ) ;
#133420=CARTESIAN_POINT ( 'NONE',  ( -20.54999999999999716, 7.250000000011155521, -188.6499999999999488 ) ) ;
#133440=DIRECTION ( 'NONE',  ( 0.000000000000000000, 1.000000000000000000, 0.000000000000000000 ) ) ;
#133497=CIRCLE ( 'NONE', #158475, 0.09999999999999939493 ) ;
#133504=ORIENTED_EDGE ( 'NONE', *, *, #209051, .F. ) ;
#133509=VERTEX_POINT ( 'NONE', #43989 ) ;
#133523=DIRECTION ( 'NONE',  ( -1.000000000000000000, 0.000000000000000000, 0.000000000000000000 ) ) ;
#133529=VERTEX_POINT ( 'NONE', #50381 ) ;
#133537=ORIENTED_EDGE ( 'NONE', *, *, #98856, .F. ) ;
#133544=DIRECTION ( 'NONE',  ( 0.000000000000000000, 1.000000000000000000, 0.000000000000000000 ) ) ;
#133563=EDGE_LOOP ( 'NONE', ( #246670, #245887, #109576, #233897, #93128, #23320 ) ) ;
#133571=CYLINDRICAL_SURFACE ( 'NONE', #152913, 0.09999999999999939493 ) ;
#133586=ORIENTED_EDGE ( 'NONE', *, *, #167176, .T. ) ;
#133589=VECTOR ( 'NONE', #96739, 1000.000000000000000 ) ;
#133632=CIRCLE ( 'NONE', #12861, 0.5000000000000013323 ) ;
#133649=CARTESIAN_POINT ( 'NONE',  ( -20.64999999999999858, 2.500000000011156409, -180.7246219227620543 ) ) ;
#133659=DIRECTION ( 'NONE',  ( 1.000000000000000000, -0.000000000000000000, 0.000000000000000000 ) ) ;
#133684=EDGE_CURVE ( 'NONE', #58899, #6554, #95939, .T. ) ;
#133695=DIRECTION ( 'NONE',  ( 1.000000000000000000, 0.000000000000000000, 0.000000000000000000 ) ) ;
#133698=FACE_OUTER_BOUND ( 'NONE', #224289, .T. ) ;
#133728=EDGE_CURVE ( 'NONE', #237228, #2978, #47145, .T. ) ;
#133731=AXIS2_PLACEMENT_3D ( 'NONE', #173179, #66655, #5358 ) ;
#133752=CARTESIAN_POINT ( 'NONE',  ( 21.05000000000000071, 1.115600667400684642E-11, -202.8999999999999773 ) ) ;
#133776=CARTESIAN_POINT ( 'NONE',  ( 23.14999999999999503, 11.75000000001116263, -193.9851942293460070 ) ) ;
#133853=FACE_OUTER_BOUND ( 'NONE', #120863, .T. ) ;
#133857=ORIENTED_EDGE ( 'NONE', *, *, #231304, .F. ) ;
#133866=CARTESIAN_POINT ( 'NONE',  ( 20.94999999999999929, 1.115600667400684642E-11, -204.9999999999999716 ) ) ;
#133875=VECTOR ( 'NONE', #68186, 1000.000000000000000 ) ;
#133878=ORIENTED_EDGE ( 'NONE', *, *, #32695, .T. ) ;
#133881=LINE ( 'NONE', #191328, #233504 ) ;
#133882=VERTEX_POINT ( 'NONE', #161078 ) ;
#133892=ORIENTED_EDGE ( 'NONE', *, *, #223183, .F. ) ;
#133896=DIRECTION ( 'NONE',  ( 0.000000000000000000, 0.000000000000000000, -1.000000000000000000 ) ) ;
#133904=LINE ( 'NONE', #233040, #103620 ) ;
#133927=ORIENTED_EDGE ( 'NONE', *, *, #32695, .F. ) ;
#133935=EDGE_CURVE ( 'NONE', #117760, #116862, #231020, .T. ) ;
#133940=CARTESIAN_POINT ( 'NONE',  ( 23.15000000000000213, -11.64999999998883595, -155.7499999999999716 ) ) ;
#133946=EDGE_LOOP ( 'NONE', ( #29604, #9107, #46278, #44469 ) ) ;
#133953=CARTESIAN_POINT ( 'NONE',  ( 20.94999999999999574, -1.261786168553869603, -175.5864989635454378 ) ) ;
#133972=EDGE_CURVE ( 'NONE', #75721, #20774, #80439, .T. ) ;
#133994=CARTESIAN_POINT ( 'NONE',  ( -21.14999999999999858, 6.540656951712397138, -167.4999999999999716 ) ) ;
#134019=ORIENTED_EDGE ( 'NONE', *, *, #230944, .F. ) ;
#134067=CIRCLE ( 'NONE', #13476, 0.09999999999998898659 ) ;
#134068=CARTESIAN_POINT ( 'NONE',  ( -20.94999999999999929, 11.70000000001115126, -194.2450018504813443 ) ) ;
#134093=DIRECTION ( 'NONE',  ( 0.000000000000000000, 0.000000000000000000, -1.000000000000000000 ) ) ;
#134098=DIRECTION ( 'NONE',  ( 1.000000000000000000, 0.000000000000000000, 0.000000000000000000 ) ) ;
#134116=CARTESIAN_POINT ( 'NONE',  ( 22.39999999999999503, 11.65000000001116298, -167.3999999999999773 ) ) ;
#134122=AXIS2_PLACEMENT_3D ( 'NONE', #254128, #216290, #16837 ) ;
#134139=DIRECTION ( 'NONE',  ( -1.000000000000000000, 0.000000000000000000, 0.000000000000000000 ) ) ;
#134146=ORIENTED_EDGE ( 'NONE', *, *, #170001, .T. ) ;
#134147=LINE ( 'NONE', #29956, #121244 ) ;
#134159=ORIENTED_EDGE ( 'NONE', *, *, #182108, .F. ) ;
#134182=DIRECTION ( 'NONE',  ( 1.000000000000000000, 0.000000000000000000, 0.000000000000000000 ) ) ;
#134200=EDGE_LOOP ( 'NONE', ( #168145, #142328, #162732, #134872 ) ) ;
#134206=CYLINDRICAL_SURFACE ( 'NONE', #94337, 0.1000000000000098310 ) ;
#134217=AXIS2_PLACEMENT_3D ( 'NONE', #59252, #196233, #76282 ) ;
#134224=DIRECTION ( 'NONE',  ( 0.000000000000000000, -0.4999999999999543698, -0.8660254037844650199 ) ) ;
#134270=B_SPLINE_CURVE_WITH_KNOTS ( 'NONE', 3,
 ( #43603, #26628, #68308, #203952, #44888, #244353, #65730, #67014 ),
 .UNSPECIFIED., .F., .F.,
 ( 4, 2, 2, 4 ),
 ( 0.000000000000000000, 0.0002114466876441986436, 0.0003171700314663001880, 0.0004228933752884017866 ),
 .UNSPECIFIED. ) ;
#134277=AXIS2_PLACEMENT_3D ( 'NONE', #33058, #175137, #177683 ) ;
#134287=EDGE_CURVE ( 'NONE', #131118, #180615, #71754, .T. ) ;
#134288=DIRECTION ( 'NONE',  ( 0.000000000000000000, 0.000000000000000000, -1.000000000000000000 ) ) ;
#134351=EDGE_CURVE ( 'NONE', #105032, #29024, #248983, .T. ) ;
#134354=DIRECTION ( 'NONE',  ( 1.000000000000000000, 0.000000000000000000, 0.000000000000000000 ) ) ;
#134362=ADVANCED_FACE ( 'NONE', ( #108184 ), #190294, .T. ) ;
#134390=DIRECTION ( 'NONE',  ( 0.000000000000000000, 0.000000000000000000, -1.000000000000000000 ) ) ;
#134407=ORIENTED_EDGE ( 'NONE', *, *, #160692, .T. ) ;
#134425=ADVANCED_FACE ( 'NONE', ( #252802 ), #52028, .T. ) ;
#134453=EDGE_CURVE ( 'NONE', #12588, #251277, #196805, .T. ) ;
#134465=EDGE_CURVE ( 'NONE', #145757, #255780, #84314, .T. ) ;
#134467=CARTESIAN_POINT ( 'NONE',  ( -23.15000000000000213, 1.115651490242849210E-11, -163.3499999999999943 ) ) ;
#134487=CARTESIAN_POINT ( 'NONE',  ( 22.39999999999999503, 1.115541036281197940E-11, -159.7092204016265669 ) ) ;
#134490=AXIS2_PLACEMENT_3D ( 'NONE', #2384, #42820, #157678 ) ;
#134512=EDGE_CURVE ( 'NONE', #166015, #117026, #180069, .T. ) ;
#134543=EDGE_LOOP ( 'NONE', ( #80786, #24439, #21087, #553 ) ) ;
#134574=EDGE_CURVE ( 'NONE', #182833, #71184, #57154, .T. ) ;
#134579=ORIENTED_EDGE ( 'NONE', *, *, #237754, .F. ) ;
#134589=ADVANCED_FACE ( 'NONE', ( #98835 ), #159232, .T. ) ;
#134592=EDGE_LOOP ( 'NONE', ( #60549, #40040, #78024, #95861 ) ) ;
#134602=CARTESIAN_POINT ( 'NONE',  ( 19.87657994471988587, 11.75000000001115019, -192.2657881246250042 ) ) ;
#134613=CIRCLE ( 'NONE', #38784, 11.69999999999998863 ) ;
#134621=ORIENTED_EDGE ( 'NONE', *, *, #220763, .F. ) ;
#134635=LINE ( 'NONE', #34308, #198103 ) ;
#134640=CARTESIAN_POINT ( 'NONE',  ( 18.49999999999999289, 10.29270135741298731, -206.4573618871519045 ) ) ;
#134653=AXIS2_PLACEMENT_3D ( 'NONE', #125406, #167124, #142386 ) ;
#134655=ADVANCED_FACE ( 'NONE', ( #106552, #121040 ), #4875, .T. ) ;
#134702=CYLINDRICAL_SURFACE ( 'NONE', #135629, 0.09999999999999939493 ) ;
#134712=DIRECTION ( 'NONE',  ( 1.000000000000000000, 0.000000000000000000, 0.000000000000000000 ) ) ;
#134756=VERTEX_POINT ( 'NONE', #170453 ) ;
#134795=DIRECTION ( 'NONE',  ( 1.000000000000000000, 0.000000000000000000, 0.000000000000000000 ) ) ;
#134848=CIRCLE ( 'NONE', #226438, 0.09999999999998898659 ) ;
#134872=ORIENTED_EDGE ( 'NONE', *, *, #23779, .F. ) ;
#134874=CIRCLE ( 'NONE', #101557, 0.09999999999999939493 ) ;
#134883=CARTESIAN_POINT ( 'NONE',  ( 20.94999999999999929, 8.876614585098254295, -175.8850804788446567 ) ) ;
#134893=DIRECTION ( 'NONE',  ( 0.000000000000000000, 0.000000000000000000, -1.000000000000000000 ) ) ;
#134918=CARTESIAN_POINT ( 'NONE',  ( -20.89878130938411616, 10.32747123227773045, -206.5774032850248716 ) ) ;
#134927=CARTESIAN_POINT ( 'NONE',  ( -18.41418431465367433, -9.499999999989068300, -207.6001893912213916 ) ) ;
#134936=CARTESIAN_POINT ( 'NONE',  ( 23.14999999999999503, 11.65000000001116298, -193.9851942293460070 ) ) ;
#134944=EDGE_LOOP ( 'NONE', ( #60126, #97642, #95353, #37386 ) ) ;
#134963=LINE ( 'NONE', #150710, #172531 ) ;
#134988=DIRECTION ( 'NONE',  ( 0.000000000000000000, 0.8660254037844385966, -0.5000000000000003331 ) ) ;
#135015=CIRCLE ( 'NONE', #222513, 0.1000000000000002692 ) ;
#135024=CARTESIAN_POINT ( 'NONE',  ( -21.05000000000000071, 1.115600667400684642E-11, -200.9999999999999432 ) ) ;
#135032=ORIENTED_EDGE ( 'NONE', *, *, #142185, .T. ) ;
#135044=DIRECTION ( 'NONE',  ( 1.000000000000000000, -0.000000000000000000, -0.000000000000000000 ) ) ;
#135052=ORIENTED_EDGE ( 'NONE', *, *, #199185, .F. ) ;
#135053=ORIENTED_EDGE ( 'NONE', *, *, #37650, .T. ) ;
#135090=DIRECTION ( 'NONE',  ( -0.000000000000000000, 0.8660254037844502539, 0.4999999999999799605 ) ) ;
#135105=ORIENTED_EDGE ( 'NONE', *, *, #9033, .T. ) ;
#135147=DIRECTION ( 'NONE',  ( -1.000000000000000000, -0.000000000000000000, -0.000000000000000000 ) ) ;
#135160=DIRECTION ( 'NONE',  ( 0.000000000000000000, 0.000000000000000000, 1.000000000000000000 ) ) ;
#135170=CARTESIAN_POINT ( 'NONE',  ( -21.44999999999999929, 7.150000000011155876, -179.7499999999999716 ) ) ;
#135209=ORIENTED_EDGE ( 'NONE', *, *, #126774, .T. ) ;
#135229=DIRECTION ( 'NONE',  ( 0.000000000000000000, 0.000000000000000000, -1.000000000000000000 ) ) ;
#135237=ORIENTED_EDGE ( 'NONE', *, *, #54687, .T. ) ;
#135238=EDGE_CURVE ( 'NONE', #143070, #119750, #163863, .T. ) ;
#135248=CARTESIAN_POINT ( 'NONE',  ( -18.47140463609787631, -9.671474685209723532, -207.6727604582740696 ) ) ;
#135259=CARTESIAN_POINT ( 'NONE',  ( 21.05000000000000426, 0.03486800302424813980, -161.2299141363108390 ) ) ;
#135263=FACE_OUTER_BOUND ( 'NONE', #216418, .T. ) ;
#135315=CARTESIAN_POINT ( 'NONE',  ( -23.25000000000000000, 1.115600667400684642E-11, -200.9999999999999432 ) ) ;
#135342=AXIS2_PLACEMENT_3D ( 'NONE', #150758, #51615, #148180 ) ;
#135358=VERTEX_POINT ( 'NONE', #42157 ) ;
#135360=CARTESIAN_POINT ( 'NONE',  ( 20.11144452914359348, 9.933610851132206321, -175.3902934539515002 ) ) ;
#135362=AXIS2_PLACEMENT_3D ( 'NONE', #906, #80438, #239562 ) ;
#135374=CARTESIAN_POINT ( 'NONE',  ( -20.94999999999999929, -11.39257802169451672, -170.5739495798319183 ) ) ;
#135377=ORIENTED_EDGE ( 'NONE', *, *, #126553, .T. ) ;
#135393=CIRCLE ( 'NONE', #39767, 0.09999999999998898659 ) ;
#135394=ORIENTED_EDGE ( 'NONE', *, *, #29430, .F. ) ;
#135402=CARTESIAN_POINT ( 'NONE',  ( -20.94999999999999929, -11.48912529306490349, -170.5999999999999659 ) ) ;
#135423=VERTEX_POINT ( 'NONE', #29040 ) ;
#135436=CARTESIAN_POINT ( 'NONE',  ( -23.15000000000000213, 1.115600667400684642E-11, -171.6499999999999773 ) ) ;
#135466=ORIENTED_EDGE ( 'NONE', *, *, #142433, .T. ) ;
#135471=DIRECTION ( 'NONE',  ( 1.000000000000000000, -0.000000000000000000, -0.000000000000000000 ) ) ;
#135492=CARTESIAN_POINT ( 'NONE',  ( -21.05000000000000071, 1.835341550235569663, -179.0551512925629538 ) ) ;
#135509=DIRECTION ( 'NONE',  ( -0.000000000000000000, -0.000000000000000000, -1.000000000000000000 ) ) ;
#135565=CARTESIAN_POINT ( 'NONE',  ( 18.59999999999999076, 11.75000000001115907, -175.5999999999999659 ) ) ;
#135622=DIRECTION ( 'NONE',  ( 0.000000000000000000, 0.000000000000000000, -1.000000000000000000 ) ) ;
#135629=AXIS2_PLACEMENT_3D ( 'NONE', #112601, #195997, #192153 ) ;
#135634=DIRECTION ( 'NONE',  ( 1.000000000000000000, -0.000000000000000000, 0.000000000000000000 ) ) ;
#135643=VERTEX_POINT ( 'NONE', #181037 ) ;
#135646=CARTESIAN_POINT ( 'NONE',  ( 21.14999999999999858, 6.540656951712400691, -167.4999999999999716 ) ) ;
#135650=VERTEX_POINT ( 'NONE', #118497 ) ;
#135688=CARTESIAN_POINT ( 'NONE',  ( 21.05000000000000071, 5.400000000011154988, -191.1060308773475072 ) ) ;
#135720=VECTOR ( 'NONE', #21211, 1000.000000000000000 ) ;
#135735=ORIENTED_EDGE ( 'NONE', *, *, #239391, .T. ) ;
#135750=VERTEX_POINT ( 'NONE', #242262 ) ;
#135775=ORIENTED_EDGE ( 'NONE', *, *, #154041, .T. ) ;
#135780=EDGE_LOOP ( 'NONE', ( #126234, #250292, #182111, #149579 ) ) ;
#135799=EDGE_LOOP ( 'NONE', ( #222032, #157844, #123216, #167352 ) ) ;
#135802=CIRCLE ( 'NONE', #65089, 0.2000000000000057288 ) ;
#135869=VERTEX_POINT ( 'NONE', #17636 ) ;
#135878=CARTESIAN_POINT ( 'NONE',  ( 21.12230431290520016, 0.005209851700173377329, -161.0424333467069573 ) ) ;
#135887=CARTESIAN_POINT ( 'NONE',  ( 19.97071067811865674, 11.72071067812981937, -192.1499999999999488 ) ) ;
#135903=CIRCLE ( 'NONE', #119174, 0.9750000000000036415 ) ;
#135920=SPHERICAL_SURFACE ( 'NONE', #36913, 0.1000000000000000056 ) ;
#135994=FACE_OUTER_BOUND ( 'NONE', #128619, .T. ) ;
#135997=AXIS2_PLACEMENT_3D ( 'NONE', #170271, #28176, #26890 ) ;
#136012=DIRECTION ( 'NONE',  ( 0.000000000000000000, 0.9908441862701782288, -0.1350103645450542456 ) ) ;
#136023=EDGE_CURVE ( 'NONE', #51917, #206366, #87871, .T. ) ;
#136033=CARTESIAN_POINT ( 'NONE',  ( 21.14999999999999503, -0.1008583690875562017, -155.7504328765105868 ) ) ;
#136045=DIRECTION ( 'NONE',  ( 0.000000000000000000, 0.1350103645451876666, -0.9908441862701600211 ) ) ;
#136060=EDGE_CURVE ( 'NONE', #215705, #29202, #55859, .T. ) ;
#136118=CARTESIAN_POINT ( 'NONE',  ( -21.05000000000000071, -11.29603075032412995, -170.5478991596638423 ) ) ;
#136147=CARTESIAN_POINT ( 'NONE',  ( -20.94999999999999929, 7.021664781911246322, -204.8335654018972605 ) ) ;
#136151=AXIS2_PLACEMENT_3D ( 'NONE', #147597, #32831, #191893 ) ;
#136174=DIRECTION ( 'NONE',  ( -1.000000000000000000, 0.000000000000000000, 0.000000000000000000 ) ) ;
#136177=EDGE_LOOP ( 'NONE', ( #234352, #30205, #91541, #240950, #158619 ) ) ;
#136211=DIRECTION ( 'NONE',  ( 1.000000000000000000, 3.265361837132813093E-16, -0.000000000000000000 ) ) ;
#136246=LINE ( 'NONE', #158443, #209493 ) ;
#136263=DIRECTION ( 'NONE',  ( -1.000000000000000000, 0.000000000000000000, 0.000000000000000000 ) ) ;
#136267=CARTESIAN_POINT ( 'NONE',  ( -20.85000000000000142, 6.933893972137497030, -204.7856458343735255 ) ) ;
#136271=DIRECTION ( 'NONE',  ( -1.000000000000000000, -3.265361837132813093E-16, 0.000000000000000000 ) ) ;
#136323=DIRECTION ( 'NONE',  ( 0.000000000000000000, 0.000000000000000000, -1.000000000000000000 ) ) ;
#136325=ORIENTED_EDGE ( 'NONE', *, *, #177611, .T. ) ;
#136375=DIRECTION ( 'NONE',  ( 0.000000000000000000, 0.000000000000000000, -1.000000000000000000 ) ) ;
#136385=ORIENTED_EDGE ( 'NONE', *, *, #96847, .T. ) ;
#136418=CIRCLE ( 'NONE', #248894, 0.1000000000000102612 ) ;
#136465=CARTESIAN_POINT ( 'NONE',  ( -21.05000000000000071, 1.115600667400684642E-11, -196.9999999999999432 ) ) ;
#136485=DIRECTION ( 'NONE',  ( 1.000000000000000000, -0.000000000000000000, 0.000000000000000000 ) ) ;
#136496=CARTESIAN_POINT ( 'NONE',  ( 21.07954640115206502, 0.06600770715081333284, -161.1707123039770408 ) ) ;
#136497=DIRECTION ( 'NONE',  ( 2.694716079187272946E-16, -1.000000000000000000, 0.000000000000000000 ) ) ;
#136502=ORIENTED_EDGE ( 'NONE', *, *, #107405, .F. ) ;
#136503=DIRECTION ( 'NONE',  ( 0.000000000000000000, 0.000000000000000000, -1.000000000000000000 ) ) ;
#136506=CARTESIAN_POINT ( 'NONE',  ( 21.14999999999999858, -0.09999999998884338825, -167.4999999999999716 ) ) ;
#136523=ORIENTED_EDGE ( 'NONE', *, *, #225424, .F. ) ;
#136528=EDGE_CURVE ( 'NONE', #70888, #132861, #239419, .T. ) ;
#136555=EDGE_CURVE ( 'NONE', #19947, #33844, #218537, .T. ) ;
#136575=AXIS2_PLACEMENT_3D ( 'NONE', #140680, #145804, #62439 ) ;
#136593=LINE ( 'NONE', #137873, #77299 ) ;
#136594=CARTESIAN_POINT ( 'NONE',  ( 18.50000972452444969, 10.29326151435342851, -206.4592822510414010 ) ) ;
#136614=EDGE_CURVE ( 'NONE', #12940, #59445, #52149, .T. ) ;
#136637=CARTESIAN_POINT ( 'NONE',  ( 21.30000000000002558, 1.115600667400684642E-11, -163.4499999999999886 ) ) ;
#136644=CARTESIAN_POINT ( 'NONE',  ( 20.77526135991796608, 8.932009016637321608, -175.9685685427218971 ) ) ;
#136646=FACE_OUTER_BOUND ( 'NONE', #101535, .T. ) ;
#136656=CARTESIAN_POINT ( 'NONE',  ( -21.05000000000000071, 1.115649653272650466E-11, -204.9999999999999716 ) ) ;
#136692=EDGE_CURVE ( 'NONE', #254925, #216004, #28278, .T. ) ;
#136697=ORIENTED_EDGE ( 'NONE', *, *, #119420, .F. ) ;
#136707=CARTESIAN_POINT ( 'NONE',  ( 18.59999999999999076, 6.550000000011156231, -188.7499999999999716 ) ) ;
#136708=CARTESIAN_POINT ( 'NONE',  ( 20.94999999999999574, 1.162701749949165642, -175.3999999999999773 ) ) ;
#136737=CARTESIAN_POINT ( 'NONE',  ( -20.94999999999999929, -1.835341550213257733, -179.0551512925629538 ) ) ;
#136751=ORIENTED_EDGE ( 'NONE', *, *, #12650, .F. ) ;
#136757=EDGE_CURVE ( 'NONE', #42612, #163390, #60518, .T. ) ;
#136762=CIRCLE ( 'NONE', #53580, 0.09999999999998898659 ) ;
#136769=VERTEX_POINT ( 'NONE', #212030 ) ;
#136771=CARTESIAN_POINT ( 'NONE',  ( -20.00857864376270001, 9.350000000011156942, -179.8499999999999659 ) ) ;
#136805=DIRECTION ( 'NONE',  ( -1.000000000000000000, 0.000000000000000000, 0.000000000000000000 ) ) ;
#136836=AXIS2_PLACEMENT_3D ( 'NONE', #162710, #242220, #158872 ) ;
#136837=AXIS2_PLACEMENT_3D ( 'NONE', #146189, #66669, #41984 ) ;
#136838=CARTESIAN_POINT ( 'NONE',  ( 22.40000000000010161, 1.020945317880167817E-11, -155.7495671075409973 ) ) ;
#136868=ORIENTED_EDGE ( 'NONE', *, *, #49005, .T. ) ;
#136879=EDGE_CURVE ( 'NONE', #209946, #6520, #147851, .T. ) ;
#136902=ADVANCED_FACE ( 'NONE', ( #242811 ), #181179, .T. ) ;
#136907=LINE ( 'NONE', #97750, #43258 ) ;
#136908=CARTESIAN_POINT ( 'NONE',  ( 18.59999999999999076, 6.650000000011155876, -188.6499999999999488 ) ) ;
#136909=DIRECTION ( 'NONE',  ( 0.000000000000000000, 0.000000000000000000, 1.000000000000000000 ) ) ;
#136945=( BOUNDED_CURVE ( )  B_SPLINE_CURVE ( 3, ( #137102, #142, #240062, #219193 ),
 .UNSPECIFIED., .F., .F. ) 
 B_SPLINE_CURVE_WITH_KNOTS ( ( 4, 4 ),
 ( 4.712388980384689674, 6.231880751915385375 ),
 .UNSPECIFIED. ) 
 CURVE ( )  GEOMETRIC_REPRESENTATION_ITEM ( )  RATIONAL_B_SPLINE_CURVE ( ( 1.000000000000000000, 0.8166740347213230500, 0.8166740347213230500, 1.000000000000000000 ) ) 
 REPRESENTATION_ITEM ( '' )  );
#136958=AXIS2_PLACEMENT_3D ( 'NONE', #38963, #19390, #40262 ) ;
#136983=FACE_OUTER_BOUND ( 'NONE', #96602, .T. ) ;
#136991=AXIS2_PLACEMENT_3D ( 'NONE', #23420, #19548, #200742 ) ;
#137000=FACE_OUTER_BOUND ( 'NONE', #256945, .T. ) ;
#137047=ORIENTED_EDGE ( 'NONE', *, *, #33590, .T. ) ;
#137078=CARTESIAN_POINT ( 'NONE',  ( -20.94999999999999929, 1.162701749949165642, -175.5999999999999659 ) ) ;
#137098=ORIENTED_EDGE ( 'NONE', *, *, #119519, .F. ) ;
#137102=CARTESIAN_POINT ( 'NONE',  ( 20.12500000000000000, 9.750000000011153745, -175.6117712821142618 ) ) ;
#137126=AXIS2_PLACEMENT_3D ( 'NONE', #115910, #157639, #190656 ) ;
#137133=LINE ( 'NONE', #212822, #230573 ) ;
#137170=ORIENTED_EDGE ( 'NONE', *, *, #254640, .T. ) ;
#137210=ORIENTED_EDGE ( 'NONE', *, *, #81200, .F. ) ;
#137252=DIRECTION ( 'NONE',  ( -1.000000000000000000, 0.000000000000000000, -0.000000000000000000 ) ) ;
#137259=VECTOR ( 'NONE', #63844, 1000.000000000000000 ) ;
#137273=FACE_OUTER_BOUND ( 'NONE', #99890, .T. ) ;
#137277=DIRECTION ( 'NONE',  ( 1.000000000000000000, 0.000000000000000000, 0.000000000000000000 ) ) ;
#137300=DIRECTION ( 'NONE',  ( -1.836970198721029934E-16, 1.000000000000000000, 0.000000000000000000 ) ) ;
#137330=AXIS2_PLACEMENT_3D ( 'NONE', #16302, #252301, #119239 ) ;
#137336=AXIS2_PLACEMENT_3D ( 'NONE', #154008, #215209, #195675 ) ;
#137381=DIRECTION ( 'NONE',  ( 0.000000000000000000, 0.000000000000000000, 1.000000000000000000 ) ) ;
#137396=AXIS2_PLACEMENT_3D ( 'NONE', #116031, #27219, #63740 ) ;
#137398=EDGE_CURVE ( 'NONE', #96608, #111061, #128992, .T. ) ;
#137401=CARTESIAN_POINT ( 'NONE',  ( -22.47071067811865319, 0.09909245471376171288, -159.7799252555019223 ) ) ;
#137429=DIRECTION ( 'NONE',  ( -0.000000000000000000, -0.000000000000000000, 1.000000000000000000 ) ) ;
#137451=CARTESIAN_POINT ( 'NONE',  ( 22.01447462590973458, 0.09903700007069084210, -160.2361997987700875 ) ) ;
#137485=LINE ( 'NONE', #159647, #20479 ) ;
#137504=AXIS2_PLACEMENT_3D ( 'NONE', #85912, #147202, #226729 ) ;
#137508=EDGE_CURVE ( 'NONE', #177551, #252063, #46836, .T. ) ;
#137527=DIRECTION ( 'NONE',  ( 0.000000000000000000, 0.000000000000000000, -1.000000000000000000 ) ) ;
#137539=VECTOR ( 'NONE', #233980, 1000.000000000000114 ) ;
#137544=CARTESIAN_POINT ( 'NONE',  ( -18.50000000000000000, 11.65000000001115232, -155.7499999999999716 ) ) ;
#137568=CARTESIAN_POINT ( 'NONE',  ( 21.05000000000000071, -9.499999999988848032, -177.3939691226524076 ) ) ;
#137584=ORIENTED_EDGE ( 'NONE', *, *, #95466, .F. ) ;
#137603=CIRCLE ( 'NONE', #171004, 0.8750000000000007772 ) ;
#137652=DIRECTION ( 'NONE',  ( 0.000000000000000000, -0.4999999999999348299, 0.8660254037844762331 ) ) ;
#137683=CARTESIAN_POINT ( 'NONE',  ( -21.02374657821563275, 11.60000000083177696, -194.0717967701982616 ) ) ;
#137684=EDGE_LOOP ( 'NONE', ( #198326, #37737, #201395, #94602 ) ) ;
#137689=ORIENTED_EDGE ( 'NONE', *, *, #125586, .F. ) ;
#137693=ADVANCED_FACE ( 'NONE', ( #18010 ), #209343, .F. ) ;
#137741=VERTEX_POINT ( 'NONE', #107817 ) ;
#137746=DIRECTION ( 'NONE',  ( 0.000000000000000000, -1.000000000000000000, 0.000000000000000000 ) ) ;
#137760=( BOUNDED_SURFACE ( )  B_SPLINE_SURFACE ( 3, 2, ( 
 ( #134487, #14590, #176226 ),
 ( #254428, #234906, #95383 ),
 ( #232351, #117515, #255692 ),
 ( #114947, #97917, #56236 ) ),
 .UNSPECIFIED., .F., .F., .F. ) 
 B_SPLINE_SURFACE_WITH_KNOTS ( ( 4, 4 ),
 ( 3, 3 ),
 ( -3.469446951953614189E-18, 0.001979672783031532438 ),
 ( 0.000000000000000000, 1.000000000000000000 ),
 .UNSPECIFIED. ) 
 GEOMETRIC_REPRESENTATION_ITEM ( )  RATIONAL_B_SPLINE_SURFACE ( (
 ( 1.000000000000000000, 0.7103081912008198939, 1.000000000000000000),
 ( 1.000000000000000000, 0.7104998333558532053, 1.000000000000000000),
 ( 1.000000000000000000, 0.7107238315755430857, 1.000000000000000000),
 ( 1.000000000000000000, 0.7110073749539379540, 1.000000000000000000) ) ) 
 REPRESENTATION_ITEM ( '' )  SURFACE ( )  );
#137764=DIRECTION ( 'NONE',  ( 0.000000000000000000, 0.000000000000000000, -1.000000000000000000 ) ) ;
#137766=ORIENTED_EDGE ( 'NONE', *, *, #92606, .F. ) ;
#137776=ORIENTED_EDGE ( 'NONE', *, *, #29838, .F. ) ;
#137785=CARTESIAN_POINT ( 'NONE',  ( 21.05000000000000071, 0.01471785653540256221, -161.1552765959100952 ) ) ;
#137796=DIRECTION ( 'NONE',  ( 0.000000000000000000, 0.8660254037844411501, 0.4999999999999956701 ) ) ;
#137813=DIRECTION ( 'NONE',  ( 0.000000000000000000, 0.000000000000000000, -1.000000000000000000 ) ) ;
#137826=CARTESIAN_POINT ( 'NONE',  ( -18.59999999999999787, 11.65000000001115232, -188.8499999999999659 ) ) ;
#137839=EDGE_CURVE ( 'NONE', #77400, #34312, #59455, .T. ) ;
#137842=ORIENTED_EDGE ( 'NONE', *, *, #227098, .F. ) ;
#137873=CARTESIAN_POINT ( 'NONE',  ( -18.59999999999999787, -1.249999999988843369, -208.8004807544150481 ) ) ;
#137887=ORIENTED_EDGE ( 'NONE', *, *, #161785, .F. ) ;
#137888=CARTESIAN_POINT ( 'NONE',  ( 20.94999999999999929, -8.999999999988844479, -177.3939691226524076 ) ) ;
#137894=FACE_OUTER_BOUND ( 'NONE', #185885, .T. ) ;
#137905=CARTESIAN_POINT ( 'NONE',  ( -18.59999999999999787, 6.933893972137497030, -204.7856458343735255 ) ) ;
#137912=DIRECTION ( 'NONE',  ( -0.000000000000000000, 0.8660254037844383745, -0.5000000000000003331 ) ) ;
#137923=CARTESIAN_POINT ( 'NONE',  ( 20.22483756094572271, 9.501904678881089694, -175.6395391287154268 ) ) ;
#137988=CARTESIAN_POINT ( 'NONE',  ( -21.05000000000000071, 1.115600667400684642E-11, -200.9999999999999432 ) ) ;
#138001=EDGE_CURVE ( 'NONE', #175396, #232247, #213627, .T. ) ;
#138017=CARTESIAN_POINT ( 'NONE',  ( 23.14999999999999858, 1.115600667400684642E-11, -200.9999999999999432 ) ) ;
#138025=CARTESIAN_POINT ( 'NONE',  ( 22.39999999999999503, 1.115600667400684642E-11, -159.7092204016265669 ) ) ;
#138035=AXIS2_PLACEMENT_3D ( 'NONE', #237550, #58879, #19800 ) ;
#138053=CYLINDRICAL_SURFACE ( 'NONE', #90232, 0.09999999999998898659 ) ;
#138058=VECTOR ( 'NONE', #137429, 1000.000000000000000 ) ;
#138059=EDGE_LOOP ( 'NONE', ( #232973, #209257, #64178, #138365 ) ) ;
#138079=LINE ( 'NONE', #235899, #216394 ) ;
#138097=CARTESIAN_POINT ( 'NONE',  ( -23.15000000000000213, 4.150000000011156764, -155.7499999999999716 ) ) ;
#138171=DIRECTION ( 'NONE',  ( 1.000000000000000000, 3.265361837132813093E-16, -0.000000000000000000 ) ) ;
#138177=VECTOR ( 'NONE', #248122, 1000.000000000000000 ) ;
#138184=VERTEX_POINT ( 'NONE', #5822 ) ;
#138192=CARTESIAN_POINT ( 'NONE',  ( 20.94999999999999929, 1.115600667400684642E-11, -200.9999999999999432 ) ) ;
#138219=AXIS2_PLACEMENT_3D ( 'NONE', #33159, #110079, #227455 ) ;
#138225=ORIENTED_EDGE ( 'NONE', *, *, #245151, .T. ) ;
#138233=CARTESIAN_POINT ( 'NONE',  ( 23.25000000000000000, -11.64999999998884483, -167.4999999999999432 ) ) ;
#138244=ORIENTED_EDGE ( 'NONE', *, *, #49517, .F. ) ;
#138252=TOROIDAL_SURFACE ( 'NONE', #25857, 2.100000000000002309, 0.1000000000000000056 ) ;
#138263=FACE_OUTER_BOUND ( 'NONE', #9444, .T. ) ;
#138312=CARTESIAN_POINT ( 'NONE',  ( 19.75857864376268935, 11.75000000001115907, -192.3499999999999659 ) ) ;
#138331=VERTEX_POINT ( 'NONE', #136033 ) ;
#138333=EDGE_CURVE ( 'NONE', #253941, #131341, #9793, .T. ) ;
#138339=ORIENTED_EDGE ( 'NONE', *, *, #42529, .F. ) ;
#138347=ORIENTED_EDGE ( 'NONE', *, *, #52879, .F. ) ;
#138359=CIRCLE ( 'NONE', #242425, 12.97499999999998721 ) ;
#138365=ORIENTED_EDGE ( 'NONE', *, *, #9650, .F. ) ;
#138387=ORIENTED_EDGE ( 'NONE', *, *, #49809, .T. ) ;
#138403=FACE_OUTER_BOUND ( 'NONE', #213614, .T. ) ;
#138420=DIRECTION ( 'NONE',  ( -2.915501640297154283E-16, 1.000000000000000000, 0.000000000000000000 ) ) ;
#138430=VERTEX_POINT ( 'NONE', #98179 ) ;
#138437=DIRECTION ( 'NONE',  ( 1.000000000000000000, 0.000000000000000000, 0.000000000000000000 ) ) ;
#138442=FACE_OUTER_BOUND ( 'NONE', #55703, .T. ) ;
#138456=ORIENTED_EDGE ( 'NONE', *, *, #204406, .F. ) ;
#138493=LINE ( 'NONE', #255855, #199556 ) ;
#138507=CARTESIAN_POINT ( 'NONE',  ( 20.94999999999999574, -1.835341550213255957, -179.0551512925629538 ) ) ;
#138552=EDGE_CURVE ( 'NONE', #85197, #205292, #155596, .T. ) ;
#138555=EDGE_CURVE ( 'NONE', #142940, #206366, #247106, .T. ) ;
#138556=CARTESIAN_POINT ( 'NONE',  ( -21.59142135623730852, 7.850000000011158718, -188.7499999999999716 ) ) ;
#138565=CARTESIAN_POINT ( 'NONE',  ( -20.54999999999999716, 1.115600667400684642E-11, -167.4999999999999716 ) ) ;
#138585=CARTESIAN_POINT ( 'NONE',  ( -20.64999999999999858, 2.000000000011154189, -187.7753780772378889 ) ) ;
#138632=EDGE_CURVE ( 'NONE', #116862, #82909, #134848, .T. ) ;
#138649=CARTESIAN_POINT ( 'NONE',  ( -23.25000000000000000, 1.115600667400684642E-11, -167.4999999999999716 ) ) ;
#138656=ORIENTED_EDGE ( 'NONE', *, *, #74477, .T. ) ;
#138687=CARTESIAN_POINT ( 'NONE',  ( -18.59117750673696889, 10.33248238083634796, -206.5948465439131496 ) ) ;
#138724=VECTOR ( 'NONE', #137252, 1000.000000000000000 ) ;
#138726=VERTEX_POINT ( 'NONE', #119748 ) ;
#138766=DIRECTION ( 'NONE',  ( 1.000000000000000000, 0.000000000000000000, 0.000000000000000000 ) ) ;
#138778=FACE_OUTER_BOUND ( 'NONE', #251261, .T. ) ;
#138801=FACE_OUTER_BOUND ( 'NONE', #245647, .T. ) ;
#138832=EDGE_CURVE ( 'NONE', #133882, #187086, #201827, .T. ) ;
#138840=EDGE_CURVE ( 'NONE', #4495, #51843, #169156, .T. ) ;
#138878=LINE ( 'NONE', #119371, #201161 ) ;
#138916=CARTESIAN_POINT ( 'NONE',  ( 19.75857864376268935, 11.65000000001115943, -192.2499999999999716 ) ) ;
#138923=DIRECTION ( 'NONE',  ( 0.000000000000000000, 0.000000000000000000, -1.000000000000000000 ) ) ;
#138935=ORIENTED_EDGE ( 'NONE', *, *, #67178, .T. ) ;
#138949=EDGE_CURVE ( 'NONE', #138726, #95676, #144391, .T. ) ;
#138963=CARTESIAN_POINT ( 'NONE',  ( -22.50000000000000000, 0.1000000000111554016, -167.4999999999999716 ) ) ;
#138986=EDGE_LOOP ( 'NONE', ( #198159, #29444, #95045, #111110 ) ) ;
#138989=B_SPLINE_CURVE_WITH_KNOTS ( 'NONE', 3,
 ( #99689, #177992, #59262, #120591, #22779, #121866, #100948, #43605, #217077, #239233, #241798, #102248, #257448, #197526, #63145, #222210, #201384, #38464, #200110, #80112, #181831, #119294 ),
 .UNSPECIFIED., .F., .F.,
 ( 4, 3, 3, 3, 3, 3, 3, 4 ),
 ( 0.000000000000000000, 7.307836821080901168E-06, 4.161455748548336644E-05, 7.576591810647893463E-05, 0.0001098090429817568444, 0.0001438003617351259016, 0.0001777914035423789891, 0.0002117966137403338534 ),
 .UNSPECIFIED. ) ;
#138993=VERTEX_POINT ( 'NONE', #11333 ) ;
#138996=CARTESIAN_POINT ( 'NONE',  ( -23.25000000000000000, 11.65000000001115588, -179.6499999999999773 ) ) ;
#139001=EDGE_LOOP ( 'NONE', ( #247883, #198618, #173805, #128464, #139475, #48505, #66566, #89482, #249256, #40003, #57531, #76788 ) ) ;
#139004=CARTESIAN_POINT ( 'NONE',  ( 20.46382478191414833, 8.901379558713770734, -176.0457280948830885 ) ) ;
#139005=CARTESIAN_POINT ( 'NONE',  ( -21.14999999999999858, 6.540656951712397138, -167.4999999999999716 ) ) ;
#139020=ORIENTED_EDGE ( 'NONE', *, *, #6841, .T. ) ;
#139063=AXIS2_PLACEMENT_3D ( 'NONE', #164607, #60350, #100729 ) ;
#139078=ORIENTED_EDGE ( 'NONE', *, *, #112962, .T. ) ;
#139082=CARTESIAN_POINT ( 'NONE',  ( 21.05000000000000071, -1.162701749926853712, -175.5999999999999659 ) ) ;
#139083=CARTESIAN_POINT ( 'NONE',  ( -20.64999999999999858, 7.250000000011155521, -188.6499999999999488 ) ) ;
#139109=EDGE_CURVE ( 'NONE', #100439, #86243, #213595, .T. ) ;
#139115=TOROIDAL_SURFACE ( 'NONE', #197400, 0.2000000000000000111, 0.1000000000000000056 ) ;
#139133=DIRECTION ( 'NONE',  ( 0.000000000000000000, 0.000000000000000000, -1.000000000000000000 ) ) ;
#139147=DIRECTION ( 'NONE',  ( -1.000000000000000000, -0.000000000000000000, -0.000000000000000000 ) ) ;
#139181=LINE ( 'NONE', #80475, #148918 ) ;
#139209=CARTESIAN_POINT ( 'NONE',  ( 18.59999999999999787, -1.835859311432481045, -212.5044391687984842 ) ) ;
#139220=DIRECTION ( 'NONE',  ( -1.000000000000000000, -0.000000000000000000, -0.000000000000000000 ) ) ;
#139250=CARTESIAN_POINT ( 'NONE',  ( 23.14999999999999858, -3.999999999988843147, -200.9999999999999432 ) ) ;
#139251=VECTOR ( 'NONE', #73817, 1000.000000000000000 ) ;
#139258=DIRECTION ( 'NONE',  ( -1.836970198721029934E-16, 1.000000000000000000, 0.000000000000000000 ) ) ;
#139264=ORIENTED_EDGE ( 'NONE', *, *, #146673, .T. ) ;
#139287=ORIENTED_EDGE ( 'NONE', *, *, #10788, .F. ) ;
#139290=CARTESIAN_POINT ( 'NONE',  ( -21.13498764882296044, 0.001656394742484908677, -161.0043818565260096 ) ) ;
#139298=CARTESIAN_POINT ( 'NONE',  ( 21.05000000000000071, 5.500000000011153745, -188.5947339810868755 ) ) ;
#139301=ORIENTED_EDGE ( 'NONE', *, *, #187639, .T. ) ;
#139328=EDGE_LOOP ( 'NONE', ( #77122, #165396, #180940, #116823 ) ) ;
#139331=CARTESIAN_POINT ( 'NONE',  ( -23.15000000000000213, 11.75000000001115552, -193.9851942293460070 ) ) ;
#139336=CARTESIAN_POINT ( 'NONE',  ( -20.54999999999999716, -9.499999999988846255, -191.1060308773475356 ) ) ;
#139345=LINE ( 'NONE', #141927, #247037 ) ;
#139358=DIRECTION ( 'NONE',  ( 0.000000000000000000, -0.9915357197604971473, 0.1298341882519111479 ) ) ;
#139364=DIRECTION ( 'NONE',  ( -0.000000000000000000, 1.000000000000000000, -0.000000000000000000 ) ) ;
#139380=VERTEX_POINT ( 'NONE', #241919 ) ;
#139404=CARTESIAN_POINT ( 'NONE',  ( 21.05000000000000071, 1.115600667400684642E-11, -200.9999999999999432 ) ) ;
#139429=CARTESIAN_POINT ( 'NONE',  ( -20.94999999999999929, -1.164121893230052995, -208.9148480855715775 ) ) ;
#139440=CARTESIAN_POINT ( 'NONE',  ( 21.14999999999999503, 11.65000000001116298, -167.5999999999999659 ) ) ;
#139444=EDGE_CURVE ( 'NONE', #254691, #254440, #47175, .T. ) ;
#139475=ORIENTED_EDGE ( 'NONE', *, *, #230813, .F. ) ;
#139494=DIRECTION ( 'NONE',  ( 1.000000000000000000, 0.000000000000000000, -0.000000000000000000 ) ) ;
#139512=DIRECTION ( 'NONE',  ( 0.000000000000000000, 0.000000000000000000, 1.000000000000000000 ) ) ;
#139525=DIRECTION ( 'NONE',  ( -1.000000000000000000, 0.000000000000000000, 0.000000000000000000 ) ) ;
#139532=CARTESIAN_POINT ( 'NONE',  ( 20.94999999999999929, 1.115600667400684642E-11, -200.9999999999999432 ) ) ;
#139533=CARTESIAN_POINT ( 'NONE',  ( -21.05000000000000071, -1.835341550213255957, -179.1551512925629197 ) ) ;
#139543=DIRECTION ( 'NONE',  ( 0.000000000000000000, 0.000000000000000000, -1.000000000000000000 ) ) ;
#139551=CARTESIAN_POINT ( 'NONE',  ( 18.59999999999999787, -11.74999999998883737, -188.8499999999999659 ) ) ;
#139552=CARTESIAN_POINT ( 'NONE',  ( -23.15000000000000213, 11.65000000001115588, -155.7499999999999716 ) ) ;
#139570=CIRCLE ( 'NONE', #143852, 0.09999999999999817368 ) ;
#139643=ORIENTED_EDGE ( 'NONE', *, *, #166097, .T. ) ;
#139655=EDGE_LOOP ( 'NONE', ( #67028, #190094, #122576, #156697, #182588, #155790 ) ) ;
#139657=CARTESIAN_POINT ( 'NONE',  ( -18.50000000000000000, 1.115600667400684642E-11, -167.4999999999999716 ) ) ;
#139659=DIRECTION ( 'NONE',  ( 1.000000000000000000, 0.000000000000000000, 0.000000000000000000 ) ) ;
#139727=FACE_OUTER_BOUND ( 'NONE', #4628, .T. ) ;
#139729=CARTESIAN_POINT ( 'NONE',  ( -18.49719636458551264, -9.446365359216978064, -174.5716138698830662 ) ) ;
#139885=CARTESIAN_POINT ( 'NONE',  ( 20.94999999999999929, 1.835341550235569663, -179.0551512925629538 ) ) ;
#139901=EDGE_LOOP ( 'NONE', ( #176167, #226834, #135105, #122981 ) ) ;
#139913=AXIS2_PLACEMENT_3D ( 'NONE', #203553, #6628, #5317 ) ;
#139922=DIRECTION ( 'NONE',  ( 1.000000000000000000, -7.304098846218133681E-16, 4.607487905232622991E-31 ) ) ;
#139934=ORIENTED_EDGE ( 'NONE', *, *, #108531, .T. ) ;
#139946=DIRECTION ( 'NONE',  ( -1.000000000000000000, 0.000000000000000000, 0.000000000000000000 ) ) ;
#139956=CARTESIAN_POINT ( 'NONE',  ( -22.57848426163147693, -0.004264329271961049897, -155.7499416931096619 ) ) ;
#139975=( BOUNDED_SURFACE ( )  B_SPLINE_SURFACE ( 3, 2, ( 
 ( #164595, #244109, #125468 ),
 ( #186736, #32496, #8092 ),
 ( #152433, #146297, #87593 ),
 ( #75463, #194118, #225813 ),
 ( #172011, #167190, #211094 ),
 ( #151130, #113276, #192825 ),
 ( #191558, #131553, #153742 ),
 ( #132854, #212392, #33784 ),
 ( #15479, #245417, #173303 ),
 ( #35063, #47180, #231962 ) ),
 .UNSPECIFIED., .F., .F., .F. ) 
 B_SPLINE_SURFACE_WITH_KNOTS ( ( 4, 2, 2, 2, 4 ),
 ( 3, 3 ),
 ( 0.0001836757140119304782, 0.0004000170051583700577, 0.0005081876507315898203, 0.0005622729735181997016, 0.0006163582963048095829 ),
 ( 0.000000000000000000, 1.000000000000000000 ),
 .UNSPECIFIED. ) 
 GEOMETRIC_REPRESENTATION_ITEM ( )  RATIONAL_B_SPLINE_SURFACE ( (
 ( 1.000000000000000000, 0.7071067811865425767, 1.000000000000000000),
 ( 1.000000000000000000, 0.6461995200056629418, 1.000000000000000000),
 ( 1.000000000000000000, 0.5776453529514137264, 1.000000000000000000),
 ( 1.000000000000000000, 0.4585233068370012655, 1.000000000000000000),
 ( 1.000000000000000000, 0.4154092989940034730, 1.000000000000000000),
 ( 1.000000000000000000, 0.3550093145838931763, 1.000000000000000000),
 ( 1.000000000000000000, 0.3354498651688588295, 1.000000000000000000),
 ( 1.000000000000000000, 0.3060347992252818172, 1.000000000000000000),
 ( 1.000000000000000000, 0.2963555829626350335, 1.000000000000000000),
 ( 1.000000000000000000, 0.2966190024563380434, 1.000000000000000000) ) ) 
 REPRESENTATION_ITEM ( '' )  SURFACE ( )  );
#139977=CARTESIAN_POINT ( 'NONE',  ( -21.14999999999999858, 0.09779029131994770863, -161.2421853895238542 ) ) ;
#139981=ORIENTED_EDGE ( 'NONE', *, *, #163597, .F. ) ;
#139990=CARTESIAN_POINT ( 'NONE',  ( 21.14999999999999858, -11.74999999998884448, -179.7499999999999716 ) ) ;
#140036=FACE_OUTER_BOUND ( 'NONE', #181620, .T. ) ;
#140052=AXIS2_PLACEMENT_3D ( 'NONE', #58930, #142344, #43260 ) ;
#140078=CARTESIAN_POINT ( 'NONE',  ( 21.04999999999908411, 8.776282895301829257, -179.6579090026524739 ) ) ;
#140120=ORIENTED_EDGE ( 'NONE', *, *, #78932, .T. ) ;
#140177=CARTESIAN_POINT ( 'NONE',  ( -21.05000000000000426, 6.477046381801004671, -167.5999999999999659 ) ) ;
#140190=AXIS2_PLACEMENT_3D ( 'NONE', #116882, #157321, #158602 ) ;
#140245=ORIENTED_EDGE ( 'NONE', *, *, #66071, .F. ) ;
#140249=EDGE_CURVE ( 'NONE', #154503, #59716, #181287, .T. ) ;
#140255=AXIS2_PLACEMENT_3D ( 'NONE', #161913, #201022, #22400 ) ;
#140278=EDGE_CURVE ( 'NONE', #145487, #50212, #55909, .T. ) ;
#140280=VERTEX_POINT ( 'NONE', #44332 ) ;
#140333=DIRECTION ( 'NONE',  ( -0.000000000000000000, -0.1350103645451928291, -0.9908441862701594660 ) ) ;
#140355=DIRECTION ( 'NONE',  ( 0.000000000000000000, 0.000000000000000000, -1.000000000000000000 ) ) ;
#140440=CARTESIAN_POINT ( 'NONE',  ( 18.52928932188133970, 10.27928932189250411, -192.1499999999999488 ) ) ;
#140483=DIRECTION ( 'NONE',  ( 1.000000000000000000, 7.304098846218134667E-16, 0.000000000000000000 ) ) ;
#140497=CARTESIAN_POINT ( 'NONE',  ( -23.25000000000000000, 4.150000000011156764, -188.6499999999999488 ) ) ;
#140514=TOROIDAL_SURFACE ( 'NONE', #144620, 0.2000000000000000111, 0.1000000000000000056 ) ;
#140533=CARTESIAN_POINT ( 'NONE',  ( -21.95218792049438861, 0.09902843981107177507, -160.2984924387532999 ) ) ;
#140566=CIRCLE ( 'NONE', #61483, 0.09999999999998898659 ) ;
#140615=CARTESIAN_POINT ( 'NONE',  ( -21.05000000000000071, -9.519327731081284938, -174.4729763765593020 ) ) ;
#140641=CIRCLE ( 'NONE', #232257, 2.000000000000002665 ) ;
#140651=CARTESIAN_POINT ( 'NONE',  ( -23.25000000000000000, -9.599999999988845900, -191.1060308773475356 ) ) ;
#140677=DIRECTION ( 'NONE',  ( -1.000000000000000000, 0.000000000000000000, 0.000000000000000000 ) ) ;
#140680=CARTESIAN_POINT ( 'NONE',  ( -23.25000000000000000, 7.021664781911246322, -204.8335654018972605 ) ) ;
#140692=CIRCLE ( 'NONE', #82400, 0.09999999999999062417 ) ;
#140774=CIRCLE ( 'NONE', #32678, 0.09999999999998898659 ) ;
#140776=CARTESIAN_POINT ( 'NONE',  ( 22.41477678272288188, 0.0008238657741001837072, -155.8504147154845612 ) ) ;
#140798=ORIENTED_EDGE ( 'NONE', *, *, #243166, .F. ) ;
#140803=ORIENTED_EDGE ( 'NONE', *, *, #1400, .T. ) ;
#140812=DIRECTION ( 'NONE',  ( -1.000000000000000000, 0.000000000000000000, 0.000000000000000000 ) ) ;
#140822=LINE ( 'NONE', #160412, #10833 ) ;
#140846=VERTEX_POINT ( 'NONE', #218141 ) ;
#140850=CARTESIAN_POINT ( 'NONE',  ( -21.14999999999999858, 11.65000000001115588, -167.5999999999999659 ) ) ;
#140865=ORIENTED_EDGE ( 'NONE', *, *, #18326, .F. ) ;
#140887=AXIS2_PLACEMENT_3D ( 'NONE', #171919, #148473, #72811 ) ;
#140910=CARTESIAN_POINT ( 'NONE',  ( -18.39999999999999858, -9.399999999988850163, -155.7499999999999716 ) ) ;
#140915=CIRCLE ( 'NONE', #240868, 0.09999999999999939493 ) ;
#140937=VERTEX_POINT ( 'NONE', #96892 ) ;
#140948=CARTESIAN_POINT ( 'NONE',  ( -21.05000000000000071, 0.01485563490490060361, -161.1556409579560523 ) ) ;
#140971=CARTESIAN_POINT ( 'NONE',  ( 23.14999999999999503, 11.65000000001116298, -155.7499999999999716 ) ) ;
#140975=AXIS2_PLACEMENT_3D ( 'NONE', #206729, #243273, #103748 ) ;
#140976=CARTESIAN_POINT ( 'NONE',  ( -22.59999999999999787, 1.115600667400684642E-11, -167.4999999999999716 ) ) ;
#140978=ORIENTED_EDGE ( 'NONE', *, *, #240803, .F. ) ;
#141022=DIRECTION ( 'NONE',  ( 1.000000000000000000, 0.000000000000000000, 0.000000000000000000 ) ) ;
#141048=ORIENTED_EDGE ( 'NONE', *, *, #180396, .T. ) ;
#141054=FACE_OUTER_BOUND ( 'NONE', #73964, .T. ) ;
#141069=CIRCLE ( 'NONE', #49484, 0.1000000000000106914 ) ;
#141132=VERTEX_POINT ( 'NONE', #34129 ) ;
#141140=CIRCLE ( 'NONE', #245181, 0.09999999999999939493 ) ;
#141186=VERTEX_POINT ( 'NONE', #150202 ) ;
#141192=EDGE_CURVE ( 'NONE', #220454, #191282, #97974, .T. ) ;
#141198=AXIS2_PLACEMENT_3D ( 'NONE', #151060, #15409, #130187 ) ;
#141200=VERTEX_POINT ( 'NONE', #35414 ) ;
#141212=ORIENTED_EDGE ( 'NONE', *, *, #101570, .F. ) ;
#141289=AXIS2_PLACEMENT_3D ( 'NONE', #180115, #165354, #144476 ) ;
#141308=ORIENTED_EDGE ( 'NONE', *, *, #157951, .F. ) ;
#141342=CARTESIAN_POINT ( 'NONE',  ( -23.25000000000000000, -0.09999999998884338825, -155.8504291924551808 ) ) ;
#141343=CARTESIAN_POINT ( 'NONE',  ( 23.14999999999999858, 5.000000000011153745, -188.5947339810868755 ) ) ;
#141374=DIRECTION ( 'NONE',  ( -4.408576920032448588E-17, 0.1350103645451876666, 0.9908441862701600211 ) ) ;
#141395=AXIS2_PLACEMENT_3D ( 'NONE', #248588, #32136, #191213 ) ;
#141423=ORIENTED_EDGE ( 'NONE', *, *, #40686, .T. ) ;
#141450=ORIENTED_EDGE ( 'NONE', *, *, #203262, .T. ) ;
#141482=CARTESIAN_POINT ( 'NONE',  ( 21.05000000000000071, 8.876614585098254295, -175.8850804788446567 ) ) ;
#141548=ORIENTED_EDGE ( 'NONE', *, *, #142104, .F. ) ;
#141566=CARTESIAN_POINT ( 'NONE',  ( 18.59999999999997655, 1.115600667400684642E-11, -200.9999999999999432 ) ) ;
#141602=EDGE_CURVE ( 'NONE', #176027, #27481, #218819, .T. ) ;
#141607=ORIENTED_EDGE ( 'NONE', *, *, #48184, .F. ) ;
#141646=DIRECTION ( 'NONE',  ( 0.000000000000000000, 0.000000000000000000, -1.000000000000000000 ) ) ;
#141648=CARTESIAN_POINT ( 'NONE',  ( -22.59999999999999787, 11.74956712350054744, -167.3991416309012550 ) ) ;
#141672=DIRECTION ( 'NONE',  ( 0.000000000000000000, 0.000000000000000000, -1.000000000000000000 ) ) ;
#141676=DIRECTION ( 'NONE',  ( 0.000000000000000000, 0.000000000000000000, -1.000000000000000000 ) ) ;
#141679=CARTESIAN_POINT ( 'NONE',  ( 18.58143601961907976, 10.43572941510573315, -192.2499999999999716 ) ) ;
#141689=CARTESIAN_POINT ( 'NONE',  ( -22.57320508075687115, 11.65000000001115588, -167.5000000000000000 ) ) ;
#141735=DIRECTION ( 'NONE',  ( 0.000000000000000000, 0.000000000000000000, -1.000000000000000000 ) ) ;
#141751=DIRECTION ( 'NONE',  ( 0.000000000000000000, 0.000000000000000000, -1.000000000000000000 ) ) ;
#141775=ORIENTED_EDGE ( 'NONE', *, *, #255425, .T. ) ;
#141792=EDGE_CURVE ( 'NONE', #77947, #223496, #239850, .T. ) ;
#141819=DIRECTION ( 'NONE',  ( 0.000000000000000000, 0.000000000000000000, -1.000000000000000000 ) ) ;
#141824=AXIS2_PLACEMENT_3D ( 'NONE', #36189, #114425, #214798 ) ;
#141832=DIRECTION ( 'NONE',  ( 1.000000000000000000, -0.000000000000000000, -0.000000000000000000 ) ) ;
#141875=CARTESIAN_POINT ( 'NONE',  ( -21.14999999999999858, 1.115600667400684642E-11, -160.9593430482987344 ) ) ;
#141888=ORIENTED_EDGE ( 'NONE', *, *, #101843, .F. ) ;
#141923=VECTOR ( 'NONE', #43238, 1000.000000000000000 ) ;
#141927=CARTESIAN_POINT ( 'NONE',  ( -20.94999999999999929, 11.65000000001115232, -200.9999999999999432 ) ) ;
#141933=DIRECTION ( 'NONE',  ( -0.000000000000000000, 1.000000000000000000, 0.000000000000000000 ) ) ;
#141961=CARTESIAN_POINT ( 'NONE',  ( -21.05000000000000071, 6.540656951712400691, -167.5999999999999659 ) ) ;
#141966=DIRECTION ( 'NONE',  ( 1.000000000000000000, -0.000000000000000000, -0.000000000000000000 ) ) ;
#141979=CYLINDRICAL_SURFACE ( 'NONE', #206751, 0.09999999999999939493 ) ;
#142010=VECTOR ( 'NONE', #160455, 1000.000000000000000 ) ;
#142058=DIRECTION ( 'NONE',  ( -0.7071067811865474617, -0.7071067811865474617, -0.000000000000000000 ) ) ;
#142069=ADVANCED_FACE ( 'NONE', ( #76439 ), #244355, .T. ) ;
#142076=ADVANCED_FACE ( 'NONE', ( #133853 ), #16497, .T. ) ;
#142099=DIRECTION ( 'NONE',  ( -0.000000000000000000, 0.000000000000000000, 1.000000000000000000 ) ) ;
#142104=EDGE_CURVE ( 'NONE', #121663, #156856, #252503, .T. ) ;
#142106=CARTESIAN_POINT ( 'NONE',  ( 23.24999999999999645, 1.115600667400684642E-11, -200.9999999999999432 ) ) ;
#142138=DIRECTION ( 'NONE',  ( 1.000000000000000000, 0.000000000000000000, 0.000000000000000000 ) ) ;
#142166=CARTESIAN_POINT ( 'NONE',  ( -21.44999999999999929, 7.350000000011155166, -179.8499999999999943 ) ) ;
#142177=ORIENTED_EDGE ( 'NONE', *, *, #136614, .T. ) ;
#142185=EDGE_CURVE ( 'NONE', #4326, #15539, #43746, .T. ) ;
#142197=CIRCLE ( 'NONE', #183895, 0.09999999999998898659 ) ;
#142212=CARTESIAN_POINT ( 'NONE',  ( -21.05000000000000071, -0.01465611850164896118, -161.0033134142318261 ) ) ;
#142234=ORIENTED_EDGE ( 'NONE', *, *, #89081, .F. ) ;
#142248=DIRECTION ( 'NONE',  ( -1.000000000000000000, 0.000000000000000000, 0.000000000000000000 ) ) ;
#142255=EDGE_CURVE ( 'NONE', #105545, #51843, #144302, .T. ) ;
#142264=DIRECTION ( 'NONE',  ( 0.000000000000000000, 0.000000000000000000, -1.000000000000000000 ) ) ;
#142268=DIRECTION ( 'NONE',  ( 0.000000000000000000, 0.000000000000000000, -1.000000000000000000 ) ) ;
#142274=DIRECTION ( 'NONE',  ( -0.000000000000000000, 1.000000000000000000, 1.734723475976807292E-15 ) ) ;
#142279=B_SPLINE_CURVE_WITH_KNOTS ( 'NONE', 3,
 ( #217481, #38884, #75457, #118416, #154990, #197926, #214934, #36321 ),
 .UNSPECIFIED., .F., .F.,
 ( 4, 2, 2, 4 ),
 ( 0.000000000000000000, 0.0002181133598169334407, 0.0003271700397253676351, 0.0004362267196338018836 ),
 .UNSPECIFIED. ) ;
#142285=FACE_OUTER_BOUND ( 'NONE', #15190, .T. ) ;
#142296=CYLINDRICAL_SURFACE ( 'NONE', #170609, 0.8750000000000007772 ) ;
#142303=CIRCLE ( 'NONE', #184004, 4.049999999999998934 ) ;
#142328=ORIENTED_EDGE ( 'NONE', *, *, #72592, .T. ) ;
#142336=ADVANCED_FACE ( 'NONE', ( #114953 ), #173444, .T. ) ;
#142344=DIRECTION ( 'NONE',  ( 0.000000000000000000, 0.000000000000000000, -1.000000000000000000 ) ) ;
#142383=CARTESIAN_POINT ( 'NONE',  ( -23.25000000000000000, 1.115600667400684642E-11, -200.9999999999999432 ) ) ;
#142386=DIRECTION ( 'NONE',  ( 0.000000000000000000, -0.9908441862701783398, 0.1350103645450536627 ) ) ;
#142389=DIRECTION ( 'NONE',  ( 0.000000000000000000, 2.891205793294679805E-16, -1.000000000000000000 ) ) ;
#142402=CARTESIAN_POINT ( 'NONE',  ( -20.85000000000000142, 11.75000000001115197, -194.1583993101029080 ) ) ;
#142412=DIRECTION ( 'NONE',  ( 1.000000000000000000, 0.000000000000000000, 0.000000000000000000 ) ) ;
#142417=CARTESIAN_POINT ( 'NONE',  ( 18.51565452909345311, -9.352859338824332625, -174.6949093212327284 ) ) ;
#142433=EDGE_CURVE ( 'NONE', #129337, #157637, #32114, .T. ) ;
#142434=ADVANCED_FACE ( 'NONE', ( #117521 ), #154538, .T. ) ;
#142439=AXIS2_PLACEMENT_3D ( 'NONE', #104830, #123159, #202682 ) ;
#142468=ORIENTED_EDGE ( 'NONE', *, *, #69726, .F. ) ;
#142472=EDGE_LOOP ( 'NONE', ( #19299, #29140, #15236, #239124 ) ) ;
#142495=CARTESIAN_POINT ( 'NONE',  ( 18.49999999999999645, 1.736257131608553550, -179.0686523290174819 ) ) ;
#142512=VERTEX_POINT ( 'NONE', #65243 ) ;
#142550=VECTOR ( 'NONE', #137912, 1000.000000000000114 ) ;
#142565=LINE ( 'NONE', #246808, #133875 ) ;
#142593=ORIENTED_EDGE ( 'NONE', *, *, #92837, .T. ) ;
#142606=DIRECTION ( 'NONE',  ( -1.000000000000000000, 7.304098846218135653E-16, -4.607487905232624742E-31 ) ) ;
#142622=DIRECTION ( 'NONE',  ( -7.304098846218134667E-16, -1.000000000000000000, 0.000000000000000000 ) ) ;
#142623=AXIS2_PLACEMENT_3D ( 'NONE', #243514, #62319, #124861 ) ;
#142729=ORIENTED_EDGE ( 'NONE', *, *, #134351, .F. ) ;
#142742=DIRECTION ( 'NONE',  ( 0.000000000000000000, -1.000000000000000000, 0.000000000000000000 ) ) ;
#142758=ORIENTED_EDGE ( 'NONE', *, *, #128557, .T. ) ;
#142763=AXIS2_PLACEMENT_3D ( 'NONE', #53869, #249512, #90413 ) ;
#142805=EDGE_LOOP ( 'NONE', ( #224766, #139020, #211684, #159636 ) ) ;
#142848=ADVANCED_FACE ( 'NONE', ( #174673 ), #111392, .T. ) ;
#142879=DIRECTION ( 'NONE',  ( 0.000000000000000000, 0.000000000000000000, -1.000000000000000000 ) ) ;
#142881=AXIS2_PLACEMENT_3D ( 'NONE', #212133, #11356, #153481 ) ;
#142882=ORIENTED_EDGE ( 'NONE', *, *, #94653, .F. ) ;
#142897=EDGE_CURVE ( 'NONE', #168999, #176585, #18108, .T. ) ;
#142901=ORIENTED_EDGE ( 'NONE', *, *, #248969, .T. ) ;
#142908=CARTESIAN_POINT ( 'NONE',  ( 21.05000000000000071, 1.115600667400684642E-11, -202.9999999999999716 ) ) ;
#142937=CARTESIAN_POINT ( 'NONE',  ( -23.25000000000000000, -11.74999999998884448, -155.7499999999999716 ) ) ;
#142940=VERTEX_POINT ( 'NONE', #64927 ) ;
#142942=CARTESIAN_POINT ( 'NONE',  ( -23.15000000000000213, 4.350000000011156054, -188.6499999999999488 ) ) ;
#142948=CARTESIAN_POINT ( 'NONE',  ( 21.05000000000000071, -11.48912529306489994, -197.8999999999999773 ) ) ;
#142957=CARTESIAN_POINT ( 'NONE',  ( 20.94999999999999929, 5.500000000011153745, -188.5947339810868755 ) ) ;
#142975=CARTESIAN_POINT ( 'NONE',  ( -20.94999999999999929, 14.05000000001115623, -173.0136950707609458 ) ) ;
#142992=LINE ( 'NONE', #222535, #15863 ) ;
#142995=CARTESIAN_POINT ( 'NONE',  ( -20.93284271247462058, 11.75000000001115019, -193.9851942293460070 ) ) ;
#142998=CARTESIAN_POINT ( 'NONE',  ( -21.05000000000000071, -1.249999999988843369, -175.4999999999999716 ) ) ;
#143015=CARTESIAN_POINT ( 'NONE',  ( -21.14999999999999858, 11.75000000001115552, -167.4999999999999716 ) ) ;
#143057=CARTESIAN_POINT ( 'NONE',  ( -22.50000000000000000, 0.1000000000111554016, -155.8504291924551808 ) ) ;
#143058=CARTESIAN_POINT ( 'NONE',  ( 20.59588692710267921, 10.36872342118052259, -175.1390810945102601 ) ) ;
#143070=VERTEX_POINT ( 'NONE', #248713 ) ;
#143141=ORIENTED_EDGE ( 'NONE', *, *, #251446, .T. ) ;
#143146=AXIS2_PLACEMENT_3D ( 'NONE', #34382, #132170, #112609 ) ;
#143156=VERTEX_POINT ( 'NONE', #191335 ) ;
#143197=LINE ( 'NONE', #44115, #32781 ) ;
#143205=CARTESIAN_POINT ( 'NONE',  ( 18.49999999999999289, 11.65000000001115588, -200.9999999999999432 ) ) ;
#143212=CYLINDRICAL_SURFACE ( 'NONE', #164101, 0.09999999999999939493 ) ;
#143223=CARTESIAN_POINT ( 'NONE',  ( 18.49362639424903776, -9.442604367876930027, -207.7644409335117359 ) ) ;
#143226=ORIENTED_EDGE ( 'NONE', *, *, #241033, .F. ) ;
#143227=ORIENTED_EDGE ( 'NONE', *, *, #179597, .T. ) ;
#143239=CARTESIAN_POINT ( 'NONE',  ( -22.47007471830799119, 1.115783626517291571E-11, -159.7792893480734904 ) ) ;
#143242=CARTESIAN_POINT ( 'NONE',  ( -21.05000000000000071, 6.540656951712399803, -167.4999999999999716 ) ) ;
#143253=EDGE_CURVE ( 'NONE', #157944, #202583, #182318, .T. ) ;
#143260=ORIENTED_EDGE ( 'NONE', *, *, #53468, .F. ) ;
#143278=VECTOR ( 'NONE', #3995, 1000.000000000000000 ) ;
#143279=CIRCLE ( 'NONE', #76637, 0.09999999999998898659 ) ;
#143311=ORIENTED_EDGE ( 'NONE', *, *, #146118, .T. ) ;
#143316=VERTEX_POINT ( 'NONE', #215979 ) ;
#143319=CARTESIAN_POINT ( 'NONE',  ( -22.50000000000000000, 11.65000000001113278, -167.4999999999999716 ) ) ;
#143326=DIRECTION ( 'NONE',  ( 1.000000000000000000, 0.000000000000000000, 0.000000000000000000 ) ) ;
#143333=AXIS2_PLACEMENT_3D ( 'NONE', #163043, #123905, #183867 ) ;
#143376=DIRECTION ( 'NONE',  ( 0.000000000000000000, 0.000000000000000000, 1.000000000000000000 ) ) ;
#143392=CIRCLE ( 'NONE', #226775, 2.000000000000002665 ) ;
#143410=CARTESIAN_POINT ( 'NONE',  ( 21.13461538461538325, 10.61458296203669427, -179.8499999999999943 ) ) ;
#143418=EDGE_LOOP ( 'NONE', ( #201939, #193801, #146340 ) ) ;
#143463=ORIENTED_EDGE ( 'NONE', *, *, #193503, .T. ) ;
#143506=DIRECTION ( 'NONE',  ( 0.000000000000000000, 1.897661533703519897E-16, -1.000000000000000000 ) ) ;
#143537=TOROIDAL_SURFACE ( 'NONE', #101818, 11.70000000000000639, 0.1000000000000000056 ) ;
#143547=DIRECTION ( 'NONE',  ( 0.000000000000000000, -1.000000000000000000, -0.000000000000000000 ) ) ;
#143550=ADVANCED_FACE ( 'NONE', ( #149324 ), #228846, .T. ) ;
#143585=ADVANCED_FACE ( 'NONE', ( #46925 ), #61702, .F. ) ;
#143610=ORIENTED_EDGE ( 'NONE', *, *, #172745, .T. ) ;
#143613=EDGE_LOOP ( 'NONE', ( #205967, #152839, #194146 ) ) ;
#143618=EDGE_LOOP ( 'NONE', ( #237751, #46774, #228445, #111674 ) ) ;
#143634=CARTESIAN_POINT ( 'NONE',  ( -20.54999999999999716, 1.115600667400684642E-11, -200.9999999999999432 ) ) ;
#143652=DIRECTION ( 'NONE',  ( -1.000000000000000000, -0.000000000000000000, -0.000000000000000000 ) ) ;
#143740=ORIENTED_EDGE ( 'NONE', *, *, #116386, .F. ) ;
#143747=CIRCLE ( 'NONE', #127190, 0.5000000000000004441 ) ;
#143774=AXIS2_PLACEMENT_3D ( 'NONE', #93710, #175839, #57125 ) ;
#143810=ORIENTED_EDGE ( 'NONE', *, *, #142897, .F. ) ;
#143843=FACE_OUTER_BOUND ( 'NONE', #118013, .T. ) ;
#143852=AXIS2_PLACEMENT_3D ( 'NONE', #181158, #2487, #99004 ) ;
#143856=DIRECTION ( 'NONE',  ( 0.000000000000000000, 1.000000000000000000, 0.000000000000000000 ) ) ;
#143876=CIRCLE ( 'NONE', #35589, 0.09999999999999939493 ) ;
#143895=ORIENTED_EDGE ( 'NONE', *, *, #218081, .T. ) ;
#143920=DIRECTION ( 'NONE',  ( 0.000000000000000000, 0.1575844902526835067, 0.9875055080513738259 ) ) ;
#143940=CARTESIAN_POINT ( 'NONE',  ( 18.49999999999999645, 1.728086936805617757, -154.3844350051677452 ) ) ;
#143951=DIRECTION ( 'NONE',  ( 0.000000000000000000, 1.000000000000000000, 0.000000000000000000 ) ) ;
#143961=CARTESIAN_POINT ( 'NONE',  ( 22.59080734064468743, 11.75000000001115552, -167.4692502919029096 ) ) ;
#143981=ORIENTED_EDGE ( 'NONE', *, *, #100764, .T. ) ;
#144055=CARTESIAN_POINT ( 'NONE',  ( 23.14999999999999858, 1.115600667400684642E-11, -200.9999999999999432 ) ) ;
#144056=EDGE_CURVE ( 'NONE', #215838, #229311, #7112, .T. ) ;
#144059=EDGE_CURVE ( 'NONE', #125534, #10380, #166619, .T. ) ;
#144064=CARTESIAN_POINT ( 'NONE',  ( 21.05000000000000071, 1.115600667400684642E-11, -179.6499999999999773 ) ) ;
#144070=ORIENTED_EDGE ( 'NONE', *, *, #133684, .F. ) ;
#144096=ORIENTED_EDGE ( 'NONE', *, *, #58578, .F. ) ;
#144103=VECTOR ( 'NONE', #218494, 1000.000000000000000 ) ;
#144105=DIRECTION ( 'NONE',  ( 1.000000000000000000, 0.000000000000000000, 0.000000000000000000 ) ) ;
#144135=CARTESIAN_POINT ( 'NONE',  ( -21.05000000000000071, -1.835341550213257733, -179.0551512925629538 ) ) ;
#144159=FACE_OUTER_BOUND ( 'NONE', #12193, .T. ) ;
#144176=ORIENTED_EDGE ( 'NONE', *, *, #247522, .T. ) ;
#144200=DIRECTION ( 'NONE',  ( 1.000000000000000000, 0.000000000000000000, 0.000000000000000000 ) ) ;
#144232=CARTESIAN_POINT ( 'NONE',  ( 18.53691006697058796, 10.30215155716188669, -192.2021987172990407 ) ) ;
#144242=DIRECTION ( 'NONE',  ( 0.000000000000000000, 0.000000000000000000, -1.000000000000000000 ) ) ;
#144246=ORIENTED_EDGE ( 'NONE', *, *, #215643, .T. ) ;
#144253=ORIENTED_EDGE ( 'NONE', *, *, #232078, .T. ) ;
#144254=CARTESIAN_POINT ( 'NONE',  ( 21.05315837717736827, 11.75000001535411798, -194.1583560219148978 ) ) ;
#144284=DIRECTION ( 'NONE',  ( 0.000000000000000000, 1.000000000000000000, 0.000000000000000000 ) ) ;
#144296=ORIENTED_EDGE ( 'NONE', *, *, #112736, .T. ) ;
#144302=CIRCLE ( 'NONE', #48476, 0.09999999999999939493 ) ;
#144317=CARTESIAN_POINT ( 'NONE',  ( -18.50000000000000000, 11.65000000001115232, -155.7499999999999716 ) ) ;
#144319=DIRECTION ( 'NONE',  ( 0.000000000000000000, 0.000000000000000000, -1.000000000000000000 ) ) ;
#144322=CARTESIAN_POINT ( 'NONE',  ( -23.25000000000000000, -8.596261682231832069, -191.5498724828496790 ) ) ;
#144352=EDGE_CURVE ( 'NONE', #128029, #146076, #8499, .T. ) ;
#144371=AXIS2_PLACEMENT_3D ( 'NONE', #53903, #133440, #171336 ) ;
#144391=LINE ( 'NONE', #70046, #126700 ) ;
#144409=DIRECTION ( 'NONE',  ( -1.000000000000000000, -2.952720810173289112E-16, 0.000000000000000000 ) ) ;
#144443=ADVANCED_FACE ( 'NONE', ( #231402 ), #171455, .F. ) ;
#144455=CIRCLE ( 'NONE', #44542, 0.09999999999998898659 ) ;
#144476=DIRECTION ( 'NONE',  ( 0.000000000000000000, 1.000000000000000000, 0.000000000000000000 ) ) ;
#144487=ORIENTED_EDGE ( 'NONE', *, *, #36143, .T. ) ;
#144488=EDGE_CURVE ( 'NONE', #169929, #80509, #148988, .T. ) ;
#144493=AXIS2_PLACEMENT_3D ( 'NONE', #89256, #9720, #249641 ) ;
#144498=CARTESIAN_POINT ( 'NONE',  ( 18.36493879433156451, -9.500000806182013591, -207.9221486603419748 ) ) ;
#144562=FACE_OUTER_BOUND ( 'NONE', #22646, .T. ) ;
#144578=DIRECTION ( 'NONE',  ( 0.000000000000000000, 0.000000000000000000, -1.000000000000000000 ) ) ;
#144597=DIRECTION ( 'NONE',  ( 0.000000000000000000, 1.000000000000000000, 0.000000000000000000 ) ) ;
#144607=ORIENTED_EDGE ( 'NONE', *, *, #247522, .F. ) ;
#144620=AXIS2_PLACEMENT_3D ( 'NONE', #94826, #192663, #190091 ) ;
#144627=DIRECTION ( 'NONE',  ( 0.000000000000000000, 0.000000000000000000, -1.000000000000000000 ) ) ;
#144680=DIRECTION ( 'NONE',  ( 0.000000000000000000, 0.000000000000000000, -1.000000000000000000 ) ) ;
#144690=DIRECTION ( 'NONE',  ( 0.000000000000000000, 0.000000000000000000, -1.000000000000000000 ) ) ;
#144704=CARTESIAN_POINT ( 'NONE',  ( -23.15000000000000213, 11.65000000001115588, -188.7499999999999716 ) ) ;
#144730=ORIENTED_EDGE ( 'NONE', *, *, #11828, .T. ) ;
#144750=CARTESIAN_POINT ( 'NONE',  ( -20.85000000000000142, -1.164121893230052995, -208.9148480855715775 ) ) ;
#144751=ORIENTED_EDGE ( 'NONE', *, *, #141192, .F. ) ;
#144763=EDGE_LOOP ( 'NONE', ( #12304, #177138, #237107, #217513 ) ) ;
#144775=B_SPLINE_CURVE_WITH_KNOTS ( 'NONE', 3,
 ( #131421, #210969, #174458, #32364, #231827, #135259, #111878, #114433 ),
 .UNSPECIFIED., .F., .F.,
 ( 4, 2, 2, 4 ),
 ( 0.000000000000000000, 0.0001881495939909273306, 0.0002822243909863910230, 0.0003762991879818546612 ),
 .UNSPECIFIED. ) ;
#144825=DIRECTION ( 'NONE',  ( 0.000000000000000000, 0.000000000000000000, 1.000000000000000000 ) ) ;
#144868=DIRECTION ( 'NONE',  ( 2.952720810173289112E-16, -1.000000000000000000, 0.000000000000000000 ) ) ;
#144898=EDGE_LOOP ( 'NONE', ( #186052, #25771, #82024, #137098, #52586 ) ) ;
#144921=CARTESIAN_POINT ( 'NONE',  ( -23.15000000000000213, 11.75000000001115552, -167.4999999999999716 ) ) ;
#144941=EDGE_CURVE ( 'NONE', #113374, #119750, #155444, .T. ) ;
#144948=DIRECTION ( 'NONE',  ( 1.000000000000000000, 0.000000000000000000, 0.000000000000000000 ) ) ;
#144964=DIRECTION ( 'NONE',  ( 0.000000000000000000, 0.1575844902526560010, 0.9875055080513781558 ) ) ;
#144971=FACE_OUTER_BOUND ( 'NONE', #205163, .T. ) ;
#144985=( BOUNDED_CURVE ( )  B_SPLINE_CURVE ( 3, ( #240658, #120742, #63296, #162425 ),
 .UNSPECIFIED., .F., .F. ) 
 B_SPLINE_CURVE_WITH_KNOTS ( ( 4, 4 ),
 ( 1.570796326794895448, 3.141592653589791784 ),
 .UNSPECIFIED. ) 
 CURVE ( )  GEOMETRIC_REPRESENTATION_ITEM ( )  RATIONAL_B_SPLINE_CURVE ( ( 1.000000000000000000, 0.8047378541243650485, 0.8047378541243650485, 1.000000000000000000 ) ) 
 REPRESENTATION_ITEM ( '' )  );
#144993=CARTESIAN_POINT ( 'NONE',  ( 23.14999999999999147, 1.115600667400684642E-11, -167.4999999999999716 ) ) ;
#145071=DIRECTION ( 'NONE',  ( -0.000000000000000000, -0.8660254037844459241, -0.4999999999999873990 ) ) ;
#145081=ORIENTED_EDGE ( 'NONE', *, *, #185242, .F. ) ;
#145101=ORIENTED_EDGE ( 'NONE', *, *, #10589, .T. ) ;
#145112=AXIS2_PLACEMENT_3D ( 'NONE', #8043, #189244, #105818 ) ;
#145133=CARTESIAN_POINT ( 'NONE',  ( 21.05000000000000071, 4.850467289730772791, -179.5342674090016430 ) ) ;
#145153=ADVANCED_FACE ( 'NONE', ( #207386 ), #151263, .F. ) ;
#145166=ADVANCED_FACE ( 'NONE', ( #168291 ), #13047, .F. ) ;
#145170=SURFACE_STYLE_USAGE ( .BOTH. , #245583 ) ;
#145175=AXIS2_PLACEMENT_3D ( 'NONE', #182703, #67866, #144825 ) ;
#145189=DIRECTION ( 'NONE',  ( 0.000000000000000000, 0.000000000000000000, -1.000000000000000000 ) ) ;
#145192=VERTEX_POINT ( 'NONE', #9170 ) ;
#145194=DIRECTION ( 'NONE',  ( -1.000000000000000000, -3.265361837132813093E-16, 0.000000000000000000 ) ) ;
#145198=DIRECTION ( 'NONE',  ( -0.000000000000000000, 1.000000000000000000, 2.891205793294679805E-16 ) ) ;
#145204=AXIS2_PLACEMENT_3D ( 'NONE', #50681, #71584, #46839 ) ;
#145211=VECTOR ( 'NONE', #175865, 1000.000000000000000 ) ;
#145215=DIRECTION ( 'NONE',  ( 0.000000000000000000, 0.000000000000000000, -1.000000000000000000 ) ) ;
#145223=ORIENTED_EDGE ( 'NONE', *, *, #190396, .F. ) ;
#145232=CARTESIAN_POINT ( 'NONE',  ( 21.13507111622890022, 10.71768338700954537, -179.7491685863607529 ) ) ;
#145251=CARTESIAN_POINT ( 'NONE',  ( -23.15000000000000213, -9.499999999988848032, -177.3939691226524360 ) ) ;
#145260=CARTESIAN_POINT ( 'NONE',  ( -21.53752568617683849, 6.786807874514948935, -167.4010255387155439 ) ) ;
#145271=DIRECTION ( 'NONE',  ( 1.000000000000000000, -0.000000000000000000, -0.000000000000000000 ) ) ;
#145276=DIRECTION ( 'NONE',  ( 0.000000000000000000, 0.000000000000000000, -1.000000000000000000 ) ) ;
#145321=ADVANCED_FACE ( 'NONE', ( #98600 ), #81608, .F. ) ;
#145325=AXIS2_PLACEMENT_3D ( 'NONE', #20888, #99080, #11559 ) ;
#145339=ORIENTED_EDGE ( 'NONE', *, *, #34064, .T. ) ;
#145347=VERTEX_POINT ( 'NONE', #222407 ) ;
#145359=CARTESIAN_POINT ( 'NONE',  ( 21.14999999999999858, 0.09779029131994770863, -161.2421853895238542 ) ) ;
#145385=DIRECTION ( 'NONE',  ( 0.000000000000000000, 0.000000000000000000, -1.000000000000000000 ) ) ;
#145400=ADVANCED_FACE ( 'NONE', ( #208036 ), #182671, .T. ) ;
#145401=FACE_OUTER_BOUND ( 'NONE', #209894, .T. ) ;
#145459=AXIS2_PLACEMENT_3D ( 'NONE', #157709, #255422, #18147 ) ;
#145487=VERTEX_POINT ( 'NONE', #14967 ) ;
#145511=FACE_OUTER_BOUND ( 'NONE', #254721, .T. ) ;
#145520=FACE_OUTER_BOUND ( 'NONE', #32669, .T. ) ;
#145533=EDGE_LOOP ( 'NONE', ( #80912, #55606, #10856, #95838 ) ) ;
#145587=CARTESIAN_POINT ( 'NONE',  ( 20.94999999999999929, 8.926614585098256782, -175.9716830192231214 ) ) ;
#145592=ORIENTED_EDGE ( 'NONE', *, *, #94810, .F. ) ;
#145614=CARTESIAN_POINT ( 'NONE',  ( -20.94999999999999574, 11.62071067812980907, -194.1315833476589887 ) ) ;
#145617=DIRECTION ( 'NONE',  ( 1.000000000000000000, 0.000000000000000000, 0.000000000000000000 ) ) ;
#145631=DIRECTION ( 'NONE',  ( 0.000000000000000000, 0.000000000000000000, -1.000000000000000000 ) ) ;
#145708=DIRECTION ( 'NONE',  ( -1.000000000000000000, 0.000000000000000000, 0.000000000000000000 ) ) ;
#145711=AXIS2_PLACEMENT_3D ( 'NONE', #223450, #123095, #143920 ) ;
#145713=CARTESIAN_POINT ( 'NONE',  ( -20.94999999999999929, 1.115600667400684642E-11, -200.9999999999999432 ) ) ;
#145757=VERTEX_POINT ( 'NONE', #201286 ) ;
#145761=CIRCLE ( 'NONE', #16802, 0.09999999999998898659 ) ;
#145773=ORIENTED_EDGE ( 'NONE', *, *, #130416, .F. ) ;
#145787=CIRCLE ( 'NONE', #66703, 4.299999999999970512 ) ;
#145790=CARTESIAN_POINT ( 'NONE',  ( 18.40916198585732388, -9.499999999988844479, -207.6001896318236390 ) ) ;
#145804=DIRECTION ( 'NONE',  ( 1.000000000000000000, -0.000000000000000000, -0.000000000000000000 ) ) ;
#145808=VERTEX_POINT ( 'NONE', #27826 ) ;
#145812=DIRECTION ( 'NONE',  ( -1.000000000000000000, 0.000000000000000000, 0.000000000000000000 ) ) ;
#145851=CARTESIAN_POINT ( 'NONE',  ( 23.14999999999999858, 6.650000000011155876, -179.8499999999999943 ) ) ;
#145866=CARTESIAN_POINT ( 'NONE',  ( -23.15000000000000213, 1.115600667400684642E-11, -167.4999999999999716 ) ) ;
#145883=CARTESIAN_POINT ( 'NONE',  ( 18.59999999999999076, 1.750000000011155743, -179.1695115579016147 ) ) ;
#145891=DIRECTION ( 'NONE',  ( 1.000000000000000000, -0.000000000000000000, -0.000000000000000000 ) ) ;
#145901=CARTESIAN_POINT ( 'NONE',  ( -20.54999999999999716, 4.350000000011156054, -188.6499999999999488 ) ) ;
#145914=ORIENTED_EDGE ( 'NONE', *, *, #242505, .F. ) ;
#145936=CARTESIAN_POINT ( 'NONE',  ( -20.94999999999999929, -1.164121893230052995, -208.9148480855715775 ) ) ;
#145941=VERTEX_POINT ( 'NONE', #12107 ) ;
#145948=CARTESIAN_POINT ( 'NONE',  ( -23.15000000000000213, 1.115600667400684642E-11, -167.4999999999999716 ) ) ;
#145953=CIRCLE ( 'NONE', #208347, 4.300000000000025580 ) ;
#145968=ADVANCED_FACE ( 'NONE', ( #232438 ), #94173, .T. ) ;
#145970=CARTESIAN_POINT ( 'NONE',  ( 21.05000000000000071, 10.72371710471867701, -179.6499999999999773 ) ) ;
#146008=LINE ( 'NONE', #87312, #81164 ) ;
#146028=CARTESIAN_POINT ( 'NONE',  ( 23.24999999999997513, 11.75000000001116263, -193.9851942293460070 ) ) ;
#146043=DIRECTION ( 'NONE',  ( 0.000000000000000000, 0.000000000000000000, -1.000000000000000000 ) ) ;
#146056=CARTESIAN_POINT ( 'NONE',  ( 20.94999999999999929, 11.65000000001115943, -194.2161343370218560 ) ) ;
#146076=VERTEX_POINT ( 'NONE', #117603 ) ;
#146077=DIRECTION ( 'NONE',  ( -1.000000000000000000, -1.836970198721029934E-16, 0.000000000000000000 ) ) ;
#146104=CARTESIAN_POINT ( 'NONE',  ( 18.47654891039378455, -9.465274948371156682, -174.6259759051946219 ) ) ;
#146118=EDGE_CURVE ( 'NONE', #204695, #12612, #49745, .T. ) ;
#146153=( BOUNDED_CURVE ( )  B_SPLINE_CURVE ( 3, ( #164001, #63601, #6188, #162723 ),
 .UNSPECIFIED., .F., .F. ) 
 B_SPLINE_CURVE_WITH_KNOTS ( ( 4, 4 ),
 ( 3.141592653589793116, 4.712388980384689674 ),
 .UNSPECIFIED. ) 
 CURVE ( )  GEOMETRIC_REPRESENTATION_ITEM ( )  RATIONAL_B_SPLINE_CURVE ( ( 1.000000000000000000, 0.8047378541243649375, 0.8047378541243649375, 1.000000000000000000 ) ) 
 REPRESENTATION_ITEM ( '' )  );
#146154=EDGE_CURVE ( 'NONE', #223354, #113374, #236263, .T. ) ;
#146156=EDGE_CURVE ( 'NONE', #52860, #20901, #83023, .T. ) ;
#146161=AXIS2_PLACEMENT_3D ( 'NONE', #136506, #135229, #94829 ) ;
#146184=CIRCLE ( 'NONE', #112872, 0.09999999999998807065 ) ;
#146189=CARTESIAN_POINT ( 'NONE',  ( 23.15000000000000213, -11.48912529306489816, -197.8999999999999773 ) ) ;
#146198=CIRCLE ( 'NONE', #62997, 0.09999999999998898659 ) ;
#146207=DIRECTION ( 'NONE',  ( 0.000000000000000000, 0.000000000000000000, -1.000000000000000000 ) ) ;
#146215=EDGE_CURVE ( 'NONE', #145192, #130316, #223113, .T. ) ;
#146217=CARTESIAN_POINT ( 'NONE',  ( -20.94999999999999929, 1.250000000011155299, -175.4999999999999716 ) ) ;
#146222=ADVANCED_FACE ( 'NONE', ( #167039 ), #142296, .T. ) ;
#146224=ORIENTED_EDGE ( 'NONE', *, *, #28808, .F. ) ;
#146239=CARTESIAN_POINT ( 'NONE',  ( -23.15000000000000213, -8.663551401858001100, -191.4758988819326646 ) ) ;
#146242=ORIENTED_EDGE ( 'NONE', *, *, #173967, .T. ) ;
#146255=VERTEX_POINT ( 'NONE', #4070 ) ;
#146257=SPHERICAL_SURFACE ( 'NONE', #18246, 0.1000000000000000056 ) ;
#146294=DIRECTION ( 'NONE',  ( -0.000000000000000000, 0.000000000000000000, 1.000000000000000000 ) ) ;
#146297=CARTESIAN_POINT ( 'NONE',  ( -18.44232395689746085, -9.552282557039976751, -207.8422519848059551 ) ) ;
#146340=ORIENTED_EDGE ( 'NONE', *, *, #44655, .T. ) ;
#146356=ORIENTED_EDGE ( 'NONE', *, *, #65461, .T. ) ;
#146378=ORIENTED_EDGE ( 'NONE', *, *, #543, .F. ) ;
#146390=CARTESIAN_POINT ( 'NONE',  ( -23.15000000000000213, 11.75000000001115552, -179.6499999999999773 ) ) ;
#146416=CARTESIAN_POINT ( 'NONE',  ( 20.04142135623730070, 11.65000000001115943, -188.8499999999999659 ) ) ;
#146424=ORIENTED_EDGE ( 'NONE', *, *, #225066, .T. ) ;
#146465=DIRECTION ( 'NONE',  ( -1.000000000000000000, 0.000000000000000000, 0.000000000000000000 ) ) ;
#146468=CARTESIAN_POINT ( 'NONE',  ( -20.64999999999999858, 1.115600667400684642E-11, -200.9999999999999432 ) ) ;
#146493=CARTESIAN_POINT ( 'NONE',  ( 21.12757541349815682, 6.473380571262609351, -167.4948387841902218 ) ) ;
#146497=EDGE_CURVE ( 'NONE', #23197, #3673, #129043, .T. ) ;
#146518=CARTESIAN_POINT ( 'NONE',  ( 22.60000000000000142, 11.74956712350054744, -167.3991416309012550 ) ) ;
#146524=AXIS2_PLACEMENT_3D ( 'NONE', #160729, #218077, #257169 ) ;
#146539=ORIENTED_EDGE ( 'NONE', *, *, #131491, .F. ) ;
#146555=VECTOR ( 'NONE', #31206, 1000.000000000000000 ) ;
#146577=CYLINDRICAL_SURFACE ( 'NONE', #179552, 0.09999999999999939493 ) ;
#146580=ORIENTED_EDGE ( 'NONE', *, *, #4873, .T. ) ;
#146585=CARTESIAN_POINT ( 'NONE',  ( 18.49999999999999645, 5.950000000011100632, -177.8057023050348278 ) ) ;
#146602=EDGE_CURVE ( 'NONE', #121663, #34375, #233294, .T. ) ;
#146617=ORIENTED_EDGE ( 'NONE', *, *, #210907, .T. ) ;
#146645=EDGE_LOOP ( 'NONE', ( #189727, #56086, #188731, #22535, #54347 ) ) ;
#146653=ORIENTED_EDGE ( 'NONE', *, *, #53311, .T. ) ;
#146664=DIRECTION ( 'NONE',  ( 0.000000000000000000, 0.000000000000000000, -1.000000000000000000 ) ) ;
#146673=EDGE_CURVE ( 'NONE', #127119, #29625, #100144, .T. ) ;
#146703=DIRECTION ( 'NONE',  ( -1.000000000000000000, 0.000000000000000000, 0.000000000000000000 ) ) ;
#146737=ORIENTED_EDGE ( 'NONE', *, *, #543, .T. ) ;
#146800=AXIS2_PLACEMENT_3D ( 'NONE', #114678, #211209, #110816 ) ;
#146843=EDGE_LOOP ( 'NONE', ( #80623, #242560, #251376, #215688, #193196 ) ) ;
#146859=CARTESIAN_POINT ( 'NONE',  ( 21.05000000000000071, 8.776282648982402179, -175.9875923785215832 ) ) ;
#146864=EDGE_CURVE ( 'NONE', #103901, #179560, #187568, .T. ) ;
#146885=DIRECTION ( 'NONE',  ( 1.000000000000000000, 0.000000000000000000, 0.000000000000000000 ) ) ;
#146890=LINE ( 'NONE', #28290, #255307 ) ;
#146893=DIRECTION ( 'NONE',  ( 1.000000000000000000, 0.000000000000000000, 0.000000000000000000 ) ) ;
#146902=EDGE_CURVE ( 'NONE', #77358, #208902, #170969, .T. ) ;
#146913=CIRCLE ( 'NONE', #230139, 4.000000000000003553 ) ;
#146924=CARTESIAN_POINT ( 'NONE',  ( 23.14999999999999858, 5.000000000011153745, -188.5947339810868755 ) ) ;
#146926=( BOUNDED_CURVE ( )  B_SPLINE_CURVE ( 3, ( #116232, #253142, #113642, #138312 ),
 .UNSPECIFIED., .F., .T. ) 
 B_SPLINE_CURVE_WITH_KNOTS ( ( 4, 4 ),
 ( 0.000000000000000000, 1.570796326794908992 ),
 .UNSPECIFIED. ) 
 CURVE ( )  GEOMETRIC_REPRESENTATION_ITEM ( )  RATIONAL_B_SPLINE_CURVE ( ( 1.000000000000000000, 0.8047378541243619399, 0.8047378541243619399, 1.000000000000000000 ) ) 
 REPRESENTATION_ITEM ( '' )  );
#147015=VERTEX_POINT ( 'NONE', #224904 ) ;
#147045=ORIENTED_EDGE ( 'NONE', *, *, #14831, .F. ) ;
#147070=CARTESIAN_POINT ( 'NONE',  ( 18.31325810956164801, -9.536388475995789094, -207.8684402063061896 ) ) ;
#147083=CARTESIAN_POINT ( 'NONE',  ( 20.85000000000000142, -11.64999999998883595, -200.9999999999999432 ) ) ;
#147133=DIRECTION ( 'NONE',  ( 0.000000000000000000, 0.000000000000000000, -1.000000000000000000 ) ) ;
#147171=ORIENTED_EDGE ( 'NONE', *, *, #159548, .T. ) ;
#147177=VECTOR ( 'NONE', #201020, 1000.000000000000000 ) ;
#147178=CARTESIAN_POINT ( 'NONE',  ( 21.05000000000000071, 8.776282895303632259, -176.0586289951409071 ) ) ;
#147187=CARTESIAN_POINT ( 'NONE',  ( 18.59999999999999076, 10.49142135624846439, -192.3499999999999659 ) ) ;
#147200=CIRCLE ( 'NONE', #55572, 0.09999999999999971412 ) ;
#147202=DIRECTION ( 'NONE',  ( 0.000000000000000000, 1.000000000000000000, 0.000000000000000000 ) ) ;
#147293=ORIENTED_EDGE ( 'NONE', *, *, #177250, .F. ) ;
#147306=VECTOR ( 'NONE', #67639, 1000.000000000000000 ) ;
#147315=CARTESIAN_POINT ( 'NONE',  ( -22.60000000000094289, 0.1008583691096561347, -155.7504328765105583 ) ) ;
#147340=CARTESIAN_POINT ( 'NONE',  ( -23.25000000000000000, -11.64999999998884483, -170.5999999999999659 ) ) ;
#147342=EDGE_CURVE ( 'NONE', #128410, #212963, #83581, .T. ) ;
#147344=FACE_OUTER_BOUND ( 'NONE', #14488, .T. ) ;
#147348=CIRCLE ( 'NONE', #201500, 0.09999999999999939493 ) ;
#147352=CARTESIAN_POINT ( 'NONE',  ( -21.04999999999999716, -0.01771943329755231583, -161.0589153115292902 ) ) ;
#147368=CARTESIAN_POINT ( 'NONE',  ( 19.97071067811865674, 11.72071067812981759, -192.2085786437626496 ) ) ;
#147394=CARTESIAN_POINT ( 'NONE',  ( -21.05000000000000071, -1.261786168553869603, -175.5864989635454378 ) ) ;
#147404=VERTEX_POINT ( 'NONE', #224222 ) ;
#147432=CARTESIAN_POINT ( 'NONE',  ( 23.14999999999999858, 1.115600667400684642E-11, -200.9999999999999432 ) ) ;
#147446=EDGE_CURVE ( 'NONE', #80509, #131693, #77269, .T. ) ;
#147471=TOROIDAL_SURFACE ( 'NONE', #243140, 11.65000000000000036, 0.1000000000000000056 ) ;
#147475=B_SPLINE_CURVE_WITH_KNOTS ( 'NONE', 3,
 ( #160969, #64428, #121840, #183099, #163522, #61859 ),
 .UNSPECIFIED., .F., .F.,
 ( 4, 2, 4 ),
 ( 0.000000000000000000, 0.0001895189928937344179, 0.0003790379857874688358 ),
 .UNSPECIFIED. ) ;
#147483=CARTESIAN_POINT ( 'NONE',  ( -20.94999999999999929, -11.29603075032412995, -170.5478991596638423 ) ) ;
#147560=ADVANCED_FACE ( 'NONE', ( #53301 ), #186407, .F. ) ;
#147580=AXIS2_PLACEMENT_3D ( 'NONE', #172434, #56274, #15914 ) ;
#147581=CARTESIAN_POINT ( 'NONE',  ( 21.05000000000000071, -1.249999999988843369, -175.3999999999999773 ) ) ;
#147597=CARTESIAN_POINT ( 'NONE',  ( -18.59999999999999787, 7.021664781911246322, -204.8335654018972605 ) ) ;
#147615=AXIS2_PLACEMENT_3D ( 'NONE', #131391, #132693, #32331 ) ;
#147645=DIRECTION ( 'NONE',  ( 1.000000000000000000, 0.000000000000000000, -0.000000000000000000 ) ) ;
#147673=ORIENTED_EDGE ( 'NONE', *, *, #218926, .T. ) ;
#147689=EDGE_CURVE ( 'NONE', #209275, #215804, #142279, .T. ) ;
#147711=DIRECTION ( 'NONE',  ( 0.000000000000000000, 0.000000000000000000, 1.000000000000000000 ) ) ;
#147763=ORIENTED_EDGE ( 'NONE', *, *, #224514, .F. ) ;
#147766=PRESENTATION_STYLE_ASSIGNMENT (( #145170 ) ) ;
#147780=FACE_OUTER_BOUND ( 'NONE', #131329, .T. ) ;
#147794=DIRECTION ( 'NONE',  ( 0.000000000000000000, 0.000000000000000000, -1.000000000000000000 ) ) ;
#147819=CARTESIAN_POINT ( 'NONE',  ( 21.05000000000000071, 5.000000000011153745, -179.9052660189130677 ) ) ;
#147838=CYLINDRICAL_SURFACE ( 'NONE', #196129, 4.000000000000003553 ) ;
#147851=CIRCLE ( 'NONE', #160521, 0.5000000000000004441 ) ;
#147904=CARTESIAN_POINT ( 'NONE',  ( 20.85000000000000142, 1.115600667400684642E-11, -200.9999999999999432 ) ) ;
#147916=CARTESIAN_POINT ( 'NONE',  ( 23.25000000000000000, -9.599999999988845900, -177.3939691226524076 ) ) ;
#147926=VERTEX_POINT ( 'NONE', #169119 ) ;
#147971=VECTOR ( 'NONE', #184524, 1000.000000000000000 ) ;
#147993=DIRECTION ( 'NONE',  ( 0.000000000000000000, 0.000000000000000000, -1.000000000000000000 ) ) ;
#148007=CYLINDRICAL_SURFACE ( 'NONE', #30235, 4.000000000000003553 ) ;
#148075=CARTESIAN_POINT ( 'NONE',  ( 18.59999999999999076, 1.115600667400684642E-11, -200.9999999999999432 ) ) ;
#148095=EDGE_CURVE ( 'NONE', #62075, #202760, #202761, .T. ) ;
#148096=AXIS2_PLACEMENT_3D ( 'NONE', #42696, #199216, #963 ) ;
#148101=CARTESIAN_POINT ( 'NONE',  ( -20.54999999999999716, 1.115600667400684642E-11, -188.1249999999999716 ) ) ;
#148105=CARTESIAN_POINT ( 'NONE',  ( -20.94983749550516450, 10.29766095125288494, -206.4743663933275286 ) ) ;
#148129=DIRECTION ( 'NONE',  ( 0.000000000000000000, -1.000000000000000000, -5.551115123125777653E-14 ) ) ;
#148152=PLANE ( 'NONE',  #41347 ) ;
#148156=CARTESIAN_POINT ( 'NONE',  ( -20.05000000000000426, 9.250000000011157297, -188.6499999999999488 ) ) ;
#148176=CARTESIAN_POINT ( 'NONE',  ( -20.94999999999999929, 1.115600667400684642E-11, -200.9999999999999432 ) ) ;
#148180=DIRECTION ( 'NONE',  ( -1.000000000000000000, 0.000000000000000000, 0.000000000000000000 ) ) ;
#148185=DIRECTION ( 'NONE',  ( 0.000000000000000000, 0.000000000000000000, -1.000000000000000000 ) ) ;
#148186=LINE ( 'NONE', #25683, #150146 ) ;
#148195=CARTESIAN_POINT ( 'NONE',  ( 21.14999999999999858, 8.786607556611267356, -179.7499999999999716 ) ) ;
#148209=AXIS2_PLACEMENT_3D ( 'NONE', #102725, #122323, #201854 ) ;
#148214=VECTOR ( 'NONE', #66388, 1000.000000000000000 ) ;
#148215=CARTESIAN_POINT ( 'NONE',  ( 18.39999999999999858, -9.499999999988842703, -207.6001893912220169 ) ) ;
#148230=DIRECTION ( 'NONE',  ( -1.000000000000000000, -0.000000000000000000, -0.000000000000000000 ) ) ;
#148261=AXIS2_PLACEMENT_3D ( 'NONE', #29176, #65685, #86501 ) ;
#148316=VERTEX_POINT ( 'NONE', #232626 ) ;
#148327=AXIS2_PLACEMENT_3D ( 'NONE', #71702, #92515, #172108 ) ;
#148340=DIRECTION ( 'NONE',  ( 0.000000000000000000, 1.000000000000000000, 1.265107689135680095E-16 ) ) ;
#148379=EDGE_LOOP ( 'NONE', ( #71202, #255047, #178819, #192143 ) ) ;
#148398=DIRECTION ( 'NONE',  ( -1.000000000000000000, 0.000000000000000000, 0.000000000000000000 ) ) ;
#148431=DIRECTION ( 'NONE',  ( 0.000000000000000000, 0.000000000000000000, -1.000000000000000000 ) ) ;
#148442=CARTESIAN_POINT ( 'NONE',  ( -21.44999999999999929, 7.250000000011155521, -179.8499999999999943 ) ) ;
#148443=LINE ( 'NONE', #91024, #223522 ) ;
#148451=DIRECTION ( 'NONE',  ( 1.000000000000000000, -0.000000000000000000, 0.000000000000000000 ) ) ;
#148473=DIRECTION ( 'NONE',  ( -0.000000000000000000, 0.000000000000000000, 1.000000000000000000 ) ) ;
#148490=CIRCLE ( 'NONE', #123533, 0.09999999999998898659 ) ;
#148495=DIRECTION ( 'NONE',  ( 0.000000000000000000, 0.000000000000000000, -1.000000000000000000 ) ) ;
#148521=CARTESIAN_POINT ( 'NONE',  ( 23.15000000000000213, -9.599999999988842347, -191.1060308773475072 ) ) ;
#148526=ORIENTED_EDGE ( 'NONE', *, *, #220011, .T. ) ;
#148576=DIRECTION ( 'NONE',  ( 0.000000000000000000, 0.000000000000000000, 1.000000000000000000 ) ) ;
#148601=DIRECTION ( 'NONE',  ( 0.000000000000000000, 1.000000000000000000, 0.000000000000000000 ) ) ;
#148627=ORIENTED_EDGE ( 'NONE', *, *, #215128, .F. ) ;
#148629=AXIS2_PLACEMENT_3D ( 'NONE', #161549, #199394, #158994 ) ;
#148633=DIRECTION ( 'NONE',  ( 0.000000000000000000, -6.308085367188393199E-16, -1.000000000000000000 ) ) ;
#148642=ORIENTED_EDGE ( 'NONE', *, *, #244944, .T. ) ;
#148658=CARTESIAN_POINT ( 'NONE',  ( 23.14999999999999503, 6.550000000011156231, -179.8499999999999943 ) ) ;
#148675=AXIS2_PLACEMENT_3D ( 'NONE', #224419, #109608, #6654 ) ;
#148697=DIRECTION ( 'NONE',  ( 0.000000000000000000, 0.000000000000000000, -1.000000000000000000 ) ) ;
#148701=CIRCLE ( 'NONE', #44631, 0.09999999999999939493 ) ;
#148704=EDGE_LOOP ( 'NONE', ( #138935, #122698, #22459, #221754 ) ) ;
#148707=DIRECTION ( 'NONE',  ( 0.000000000000000000, 0.000000000000000000, -1.000000000000000000 ) ) ;
#148710=DIRECTION ( 'NONE',  ( 0.000000000000000000, 0.000000000000000000, 1.000000000000000000 ) ) ;
#148727=DIRECTION ( 'NONE',  ( 0.000000000000000000, 0.000000000000000000, -1.000000000000000000 ) ) ;
#148734=DIRECTION ( 'NONE',  ( 1.000000000000000000, 0.000000000000000000, 0.000000000000000000 ) ) ;
#148750=EDGE_CURVE ( 'NONE', #14880, #61925, #240334, .T. ) ;
#148779=CARTESIAN_POINT ( 'NONE',  ( -20.64999999999999858, 7.250000000011155521, -179.8499999999999943 ) ) ;
#148829=EDGE_CURVE ( 'NONE', #115507, #119750, #190274, .T. ) ;
#148856=ORIENTED_EDGE ( 'NONE', *, *, #125586, .T. ) ;
#148878=ORIENTED_EDGE ( 'NONE', *, *, #120672, .F. ) ;
#148918=VECTOR ( 'NONE', #200471, 1000.000000000000000 ) ;
#148937=EDGE_LOOP ( 'NONE', ( #3919, #89959, #194752 ) ) ;
#148988=CIRCLE ( 'NONE', #228093, 0.09999999999998986089 ) ;
#149073=CARTESIAN_POINT ( 'NONE',  ( -23.25000000000000000, 1.115600667400684642E-11, -167.4999999999999716 ) ) ;
#149092=DIRECTION ( 'NONE',  ( 1.000000000000000000, 3.469446951953704435E-14, -2.003086131649669752E-14 ) ) ;
#149105=CARTESIAN_POINT ( 'NONE',  ( 21.14999999999999858, 6.540656951712400691, -167.4999999999999716 ) ) ;
#149107=ORIENTED_EDGE ( 'NONE', *, *, #82862, .T. ) ;
#149121=CARTESIAN_POINT ( 'NONE',  ( 21.07189867249812210, 10.72498027010430377, -179.7124514422767163 ) ) ;
#149170=B_SPLINE_CURVE_WITH_KNOTS ( 'NONE', 3,
 ( #91631, #188168, #171217, #227281 ),
 .UNSPECIFIED., .F., .F.,
 ( 4, 4 ),
 ( 0.000000000000000000, 0.001767853679387143117 ),
 .UNSPECIFIED. ) ;
#149172=EDGE_LOOP ( 'NONE', ( #220366, #253691, #102754, #133301 ) ) ;
#149179=CARTESIAN_POINT ( 'NONE',  ( 21.14999999999999858, 1.115600667400684642E-11, -167.5999999999999659 ) ) ;
#149192=AXIS2_PLACEMENT_3D ( 'NONE', #98152, #235141, #236416 ) ;
#149198=FACE_OUTER_BOUND ( 'NONE', #157916, .T. ) ;
#149201=DIRECTION ( 'NONE',  ( 0.000000000000000000, 0.000000000000000000, -1.000000000000000000 ) ) ;
#149214=CARTESIAN_POINT ( 'NONE',  ( 20.85000000000000142, 6.933893972137497030, -204.7856458343735255 ) ) ;
#149225=AXIS2_PLACEMENT_3D ( 'NONE', #30149, #189209, #48396 ) ;
#149238=FACE_OUTER_BOUND ( 'NONE', #76569, .T. ) ;
#149246=DIRECTION ( 'NONE',  ( 0.000000000000000000, 0.9998779222360096863, -0.01562500000001061998 ) ) ;
#149262=DIRECTION ( 'NONE',  ( -1.000000000000000000, -0.000000000000000000, 0.000000000000000000 ) ) ;
#149291=FACE_OUTER_BOUND ( 'NONE', #62512, .T. ) ;
#149303=AXIS2_PLACEMENT_3D ( 'NONE', #236008, #211323, #53526 ) ;
#149307=DIRECTION ( 'NONE',  ( 1.000000000000000000, -0.000000000000000000, -0.000000000000000000 ) ) ;
#149313=ORIENTED_EDGE ( 'NONE', *, *, #187938, .T. ) ;
#149324=FACE_OUTER_BOUND ( 'NONE', #133563, .T. ) ;
#149346=EDGE_CURVE ( 'NONE', #32118, #132728, #65721, .T. ) ;
#149403=EDGE_LOOP ( 'NONE', ( #72776, #201082, #228031, #16705 ) ) ;
#149404=DIRECTION ( 'NONE',  ( -1.000000000000000000, 0.000000000000000000, 0.000000000000000000 ) ) ;
#149430=CARTESIAN_POINT ( 'NONE',  ( 20.85000000000000142, 1.115600667400684642E-11, -200.9999999999999432 ) ) ;
#149441=ORIENTED_EDGE ( 'NONE', *, *, #103030, .T. ) ;
#149446=ADVANCED_FACE ( 'NONE', ( #155709 ), #161610, .F. ) ;
#149453=CIRCLE ( 'NONE', #174433, 11.75000000000001066 ) ;
#149461=CIRCLE ( 'NONE', #166034, 0.09999999999998807065 ) ;
#149478=DIRECTION ( 'NONE',  ( 0.000000000000000000, 0.000000000000000000, -1.000000000000000000 ) ) ;
#149518=EDGE_CURVE ( 'NONE', #56940, #232936, #4287, .T. ) ;
#149528=EDGE_CURVE ( 'NONE', #148316, #255690, #25176, .T. ) ;
#149559=ORIENTED_EDGE ( 'NONE', *, *, #57006, .T. ) ;
#149579=ORIENTED_EDGE ( 'NONE', *, *, #69778, .F. ) ;
#149595=AXIS2_PLACEMENT_3D ( 'NONE', #139657, #142248, #4021 ) ;
#149622=EDGE_LOOP ( 'NONE', ( #107923, #202307, #77946, #60746 ) ) ;
#149643=ORIENTED_EDGE ( 'NONE', *, *, #76250, .T. ) ;
#149711=DIRECTION ( 'NONE',  ( 0.000000000000000000, 1.000000000000000000, -1.224646799147353207E-16 ) ) ;
#149722=CARTESIAN_POINT ( 'NONE',  ( -18.39999999999999858, -9.682403433465239573, -207.6568433774127413 ) ) ;
#149732=CIRCLE ( 'NONE', #187307, 0.09999999999999939493 ) ;
#149754=DIRECTION ( 'NONE',  ( 0.000000000000000000, 0.008583690987127625890, 0.9999631594459055250 ) ) ;
#149755=CARTESIAN_POINT ( 'NONE',  ( 23.25000000000000000, -11.48912529306489994, -197.8999999999999773 ) ) ;
#149759=ORIENTED_EDGE ( 'NONE', *, *, #190670, .F. ) ;
#149760=CARTESIAN_POINT ( 'NONE',  ( -23.25000000000000000, -1.736705739456431807, -212.5174225876236846 ) ) ;
#149774=DIRECTION ( 'NONE',  ( 0.000000000000000000, 1.000000000000000000, 0.000000000000000000 ) ) ;
#149785=DIRECTION ( 'NONE',  ( 0.000000000000000000, -1.000000000000000000, 0.000000000000000000 ) ) ;
#149788=CIRCLE ( 'NONE', #174760, 11.64999999999999325 ) ;
#149789=DIRECTION ( 'NONE',  ( -1.000000000000000000, -8.673617379884087537E-15, 0.000000000000000000 ) ) ;
#149842=ORIENTED_EDGE ( 'NONE', *, *, #34975, .F. ) ;
#149843=CARTESIAN_POINT ( 'NONE',  ( -21.44999999999999929, 7.250000000011155521, -188.7499999999999716 ) ) ;
#149863=ORIENTED_EDGE ( 'NONE', *, *, #184448, .T. ) ;
#149885=EDGE_CURVE ( 'NONE', #90455, #245420, #174283, .T. ) ;
#149913=AXIS2_PLACEMENT_3D ( 'NONE', #92007, #89436, #30785 ) ;
#149914=CARTESIAN_POINT ( 'NONE',  ( -23.15000000000000213, 1.115600667400684642E-11, -200.9999999999999432 ) ) ;
#149929=VERTEX_POINT ( 'NONE', #160532 ) ;
#149971=B_SPLINE_CURVE_WITH_KNOTS ( 'NONE', 3,
 ( #73281, #100479, #241320, #18404, #97907, #178806, #3974, #220473, #40579, #112 ),
 .UNSPECIFIED., .F., .F.,
 ( 4, 3, 3, 4 ),
 ( 0.000000000000000000, 0.0002000000000002884074, 0.001000000000045112589, 0.001967863649472103085 ),
 .UNSPECIFIED. ) ;
#150028=CARTESIAN_POINT ( 'NONE',  ( -20.94999999999999929, 11.60000000001115339, -174.4282032302755283 ) ) ;
#150030=EDGE_CURVE ( 'NONE', #86816, #157570, #40983, .T. ) ;
#150045=VERTEX_POINT ( 'NONE', #148658 ) ;
#150073=EDGE_CURVE ( 'NONE', #118267, #112231, #170829, .T. ) ;
#150076=CARTESIAN_POINT ( 'NONE',  ( 20.95159278453404283, 8.907896337960206523, -175.9847201851092109 ) ) ;
#150096=ORIENTED_EDGE ( 'NONE', *, *, #4086, .F. ) ;
#150116=DIRECTION ( 'NONE',  ( 0.000000000000000000, 0.000000000000000000, 1.000000000000000000 ) ) ;
#150139=DIRECTION ( 'NONE',  ( -0.000000000000000000, 0.000000000000000000, 1.000000000000000000 ) ) ;
#150145=CARTESIAN_POINT ( 'NONE',  ( 18.45036689428329524, -9.490184143317863530, -174.5126958274863114 ) ) ;
#150146=VECTOR ( 'NONE', #8681, 1000.000000000000000 ) ;
#150161=CARTESIAN_POINT ( 'NONE',  ( 18.39999999999999858, -9.599999999988845900, -207.6001893912220169 ) ) ;
#150166=ORIENTED_EDGE ( 'NONE', *, *, #106681, .T. ) ;
#150202=CARTESIAN_POINT ( 'NONE',  ( -20.94999999999999929, 5.900000000011102586, -177.7190997646563915 ) ) ;
#150206=ORIENTED_EDGE ( 'NONE', *, *, #253933, .F. ) ;
#150218=ORIENTED_EDGE ( 'NONE', *, *, #126881, .F. ) ;
#150229=AXIS2_PLACEMENT_3D ( 'NONE', #142942, #178276, #137813 ) ;
#150274=CARTESIAN_POINT ( 'NONE',  ( -18.59999999999999787, 1.115600667400684642E-11, -167.4999999999999716 ) ) ;
#150276=CARTESIAN_POINT ( 'NONE',  ( -21.05000000000000071, -11.74999999998884448, -197.9999999999999432 ) ) ;
#150284=DIRECTION ( 'NONE',  ( -1.000000000000000000, 0.000000000000000000, 0.000000000000000000 ) ) ;
#150285=CIRCLE ( 'NONE', #158673, 0.09999999999999939493 ) ;
#150289=EDGE_LOOP ( 'NONE', ( #157738, #94823, #149441, #52151 ) ) ;
#150318=CARTESIAN_POINT ( 'NONE',  ( 22.50000000000000000, 7.750000000011162626, -167.3999999999999773 ) ) ;
#150363=DIRECTION ( 'NONE',  ( 0.000000000000000000, -1.000000000000000000, 6.308085367188393199E-16 ) ) ;
#150378=CARTESIAN_POINT ( 'NONE',  ( -23.15000000000000213, 11.65000000001115588, -193.9851942293460070 ) ) ;
#150391=ORIENTED_EDGE ( 'NONE', *, *, #73520, .F. ) ;
#150399=DIRECTION ( 'NONE',  ( 0.000000000000000000, 0.000000000000000000, -1.000000000000000000 ) ) ;
#150424=CYLINDRICAL_SURFACE ( 'NONE', #176801, 0.09999999999998898659 ) ;
#150432=CARTESIAN_POINT ( 'NONE',  ( 18.49999999999999645, 1.162701749949165642, -175.5999999999999659 ) ) ;
#150469=VECTOR ( 'NONE', #158628, 1000.000000000000000 ) ;
#150474=CARTESIAN_POINT ( 'NONE',  ( -18.60000000000001208, -9.364240527579751117, -174.6802485818407433 ) ) ;
#150514=LINE ( 'NONE', #171394, #155615 ) ;
#150517=DIRECTION ( 'NONE',  ( 0.000000000000000000, 0.01562500000001262185, 0.9998779222360095753 ) ) ;
#150523=ORIENTED_EDGE ( 'NONE', *, *, #252795, .T. ) ;
#150556=ORIENTED_EDGE ( 'NONE', *, *, #220263, .F. ) ;
#150593=CARTESIAN_POINT ( 'NONE',  ( 20.92356734117541706, 10.31973158071402175, -206.5505334713353989 ) ) ;
#150615=CARTESIAN_POINT ( 'NONE',  ( 21.09787244211752011, 8.775370707348422172, -179.7392533843176068 ) ) ;
#150633=AXIS2_PLACEMENT_3D ( 'NONE', #37093, #3051, #180430 ) ;
#150647=CARTESIAN_POINT ( 'NONE',  ( -21.05000000000000071, -1.162701749926853712, -175.3999999999999773 ) ) ;
#150676=CIRCLE ( 'NONE', #34185, 0.09999999999999996392 ) ;
#150707=FACE_OUTER_BOUND ( 'NONE', #5818, .T. ) ;
#150710=CARTESIAN_POINT ( 'NONE',  ( -23.15000000000000213, 11.75000000001115552, -155.7499999999999716 ) ) ;
#150729=VECTOR ( 'NONE', #46698, 1000.000000000000000 ) ;
#150738=CARTESIAN_POINT ( 'NONE',  ( -22.49544290803713764, 11.74987023786927764, -167.4346880407416336 ) ) ;
#150758=CARTESIAN_POINT ( 'NONE',  ( 20.85000000000000142, -11.64999999998883595, -200.9999999999999432 ) ) ;
#150775=CARTESIAN_POINT ( 'NONE',  ( -20.94999999999999929, -11.64999999998884483, -170.4999999999999716 ) ) ;
#150787=EDGE_CURVE ( 'NONE', #163089, #182339, #128255, .T. ) ;
#150795=ORIENTED_EDGE ( 'NONE', *, *, #182007, .T. ) ;
#150849=ORIENTED_EDGE ( 'NONE', *, *, #49482, .F. ) ;
#150865=CARTESIAN_POINT ( 'NONE',  ( -22.50000000000000000, 0.1000000000111554016, -155.8504291924551808 ) ) ;
#150866=DIRECTION ( 'NONE',  ( -1.000000000000000000, -0.000000000000000000, -0.000000000000000000 ) ) ;
#150891=TOROIDAL_SURFACE ( 'NONE', #105063, 0.2000000000000000111, 0.1000000000000000056 ) ;
#150895=ORIENTED_EDGE ( 'NONE', *, *, #116796, .T. ) ;
#150907=CARTESIAN_POINT ( 'NONE',  ( 21.93340585971920831, 7.324147022865878043, -167.4999999999999432 ) ) ;
#150922=DIRECTION ( 'NONE',  ( 0.000000000000000000, 8.881784197000778021E-16, 1.000000000000000000 ) ) ;
#150928=ORIENTED_EDGE ( 'NONE', *, *, #214696, .F. ) ;
#150935=CARTESIAN_POINT ( 'NONE',  ( -21.14999999999999858, -0.1008583690875562017, -155.7504328765105868 ) ) ;
#150957=CARTESIAN_POINT ( 'NONE',  ( 20.94999999999999929, 11.65000000001115943, -194.1583993101029364 ) ) ;
#150996=CIRCLE ( 'NONE', #117664, 0.09999999999999749367 ) ;
#151004=LINE ( 'NONE', #84883, #246172 ) ;
#151012=CARTESIAN_POINT ( 'NONE',  ( -21.55000000000000426, 7.750000000011159074, -188.7499999999999716 ) ) ;
#151017=DIRECTION ( 'NONE',  ( -1.000000000000000000, -0.000000000000000000, -0.000000000000000000 ) ) ;
#151041=CARTESIAN_POINT ( 'NONE',  ( 18.49999999999999289, 6.650000000011155876, -188.8499999999999659 ) ) ;
#151060=CARTESIAN_POINT ( 'NONE',  ( -23.15000000000000213, -8.596261682231830292, -191.5498724828496790 ) ) ;
#151084=LINE ( 'NONE', #15435, #37594 ) ;
#151116=VERTEX_POINT ( 'NONE', #228323 ) ;
#151130=CARTESIAN_POINT ( 'NONE',  ( -18.44204374631831911, -9.491036389587209854, -207.6262012702209745 ) ) ;
#151146=VECTOR ( 'NONE', #223864, 1000.000000000000000 ) ;
#151163=DIRECTION ( 'NONE',  ( 0.000000000000000000, 0.000000000000000000, -1.000000000000000000 ) ) ;
#151164=DIRECTION ( 'NONE',  ( -0.000000000000000000, -0.000000000000000000, -1.000000000000000000 ) ) ;
#151171=CARTESIAN_POINT ( 'NONE',  ( 20.94999999999999929, 1.115600667400684642E-11, -200.9999999999999432 ) ) ;
#151186=CARTESIAN_POINT ( 'NONE',  ( 21.87500000000000355, 9.750000000011153745, -188.7499999999999716 ) ) ;
#151203=DIRECTION ( 'NONE',  ( 0.000000000000000000, -0.000000000000000000, 1.000000000000000000 ) ) ;
#151225=EDGE_LOOP ( 'NONE', ( #185244, #246401, #27631, #231233 ) ) ;
#151235=CARTESIAN_POINT ( 'NONE',  ( -20.85000000000000142, 1.115600667400684642E-11, -200.9999999999999432 ) ) ;
#151236=ORIENTED_EDGE ( 'NONE', *, *, #228816, .F. ) ;
#151238=VECTOR ( 'NONE', #78927, 1000.000000000000000 ) ;
#151259=FACE_OUTER_BOUND ( 'NONE', #154687, .T. ) ;
#151263=CYLINDRICAL_SURFACE ( 'NONE', #61853, 0.5000000000000004441 ) ;
#151284=EDGE_LOOP ( 'NONE', ( #233835, #122023, #249348, #217812, #118715, #187015, #11895, #43575 ) ) ;
#151308=CARTESIAN_POINT ( 'NONE',  ( -23.15000000000000213, 1.115600667400684642E-11, -196.9999999999999432 ) ) ;
#151315=FACE_OUTER_BOUND ( 'NONE', #142472, .T. ) ;
#151321=TOROIDAL_SURFACE ( 'NONE', #51305, 0.4000000000000012990, 0.1000000000000000056 ) ;
#151326=DIRECTION ( 'NONE',  ( -3.440080580676165868E-14, -0.1298341882520124002, -0.9915357197604841577 ) ) ;
#151330=DIRECTION ( 'NONE',  ( 0.000000000000000000, -0.8700118002898321601, 0.4930308989875230030 ) ) ;
#151340=ORIENTED_EDGE ( 'NONE', *, *, #79596, .T. ) ;
#151351=CARTESIAN_POINT ( 'NONE',  ( -20.64999999999999858, 1.940186915899009490, -180.3291192110532961 ) ) ;
#151365=DIRECTION ( 'NONE',  ( 1.000000000000000000, 0.000000000000000000, 0.000000000000000000 ) ) ;
#151370=DIRECTION ( 'NONE',  ( 0.000000000000000000, 1.734723475976997999E-14, -1.000000000000000000 ) ) ;
#151371=TOROIDAL_SURFACE ( 'NONE', #255529, 12.77499999999999858, 0.1000000000000000056 ) ;
#151377=DIRECTION ( 'NONE',  ( 2.710505431213777355E-16, -1.000000000000000000, 0.000000000000000000 ) ) ;
#151395=DIRECTION ( 'NONE',  ( 1.000000000000000000, 0.000000000000000000, 0.000000000000000000 ) ) ;
#151416=ORIENTED_EDGE ( 'NONE', *, *, #244680, .T. ) ;
#151466=LINE ( 'NONE', #233564, #209383 ) ;
#151475=ORIENTED_EDGE ( 'NONE', *, *, #12650, .T. ) ;
#151476=AXIS2_PLACEMENT_3D ( 'NONE', #65531, #225863, #69413 ) ;
#151481=DIRECTION ( 'NONE',  ( -1.000000000000000000, 0.000000000000000000, 0.000000000000000000 ) ) ;
#151501=ORIENTED_EDGE ( 'NONE', *, *, #14646, .F. ) ;
#151514=ORIENTED_EDGE ( 'NONE', *, *, #14647, .F. ) ;
#151546=ORIENTED_EDGE ( 'NONE', *, *, #232804, .F. ) ;
#151607=FACE_OUTER_BOUND ( 'NONE', #217142, .T. ) ;
#151620=AXIS2_PLACEMENT_3D ( 'NONE', #79173, #55740, #36243 ) ;
#151630=ORIENTED_EDGE ( 'NONE', *, *, #146215, .F. ) ;
#151683=CARTESIAN_POINT ( 'NONE',  ( -22.39999999999999858, 1.115600667400684642E-11, -155.8504291924551808 ) ) ;
#151703=DIRECTION ( 'NONE',  ( -1.000000000000000000, 0.000000000000000000, 0.000000000000000000 ) ) ;
#151724=ORIENTED_EDGE ( 'NONE', *, *, #216243, .F. ) ;
#151727=CARTESIAN_POINT ( 'NONE',  ( -23.25000000000000000, 11.75000000001115552, -200.9999999999999432 ) ) ;
#151732=ORIENTED_EDGE ( 'NONE', *, *, #107405, .T. ) ;
#151750=AXIS2_PLACEMENT_3D ( 'NONE', #257805, #197878, #4790 ) ;
#151771=DIRECTION ( 'NONE',  ( 0.000000000000000000, 0.000000000000000000, -1.000000000000000000 ) ) ;
#151795=AXIS2_PLACEMENT_3D ( 'NONE', #210415, #246941, #172607 ) ;
#151805=DIRECTION ( 'NONE',  ( 1.875376730785737719E-16, -1.000000000000000000, 0.000000000000000000 ) ) ;
#151842=ORIENTED_EDGE ( 'NONE', *, *, #117975, .T. ) ;
#151848=EDGE_CURVE ( 'NONE', #220627, #116826, #250789, .T. ) ;
#151866=AXIS2_PLACEMENT_3D ( 'NONE', #244858, #250004, #208332 ) ;
#151903=AXIS2_PLACEMENT_3D ( 'NONE', #179871, #200706, #97716 ) ;
#151990=CARTESIAN_POINT ( 'NONE',  ( -18.46907102845854354, -9.473727364752949853, -207.6760347387364618 ) ) ;
#152011=EDGE_CURVE ( 'NONE', #188501, #203019, #16383, .T. ) ;
#152026=ORIENTED_EDGE ( 'NONE', *, *, #253632, .T. ) ;
#152041=DIRECTION ( 'NONE',  ( 1.000000000000000000, 0.000000000000000000, 0.000000000000000000 ) ) ;
#152042=LINE ( 'NONE', #100681, #216325 ) ;
#152049=ORIENTED_EDGE ( 'NONE', *, *, #57006, .F. ) ;
#152099=ORIENTED_EDGE ( 'NONE', *, *, #251396, .T. ) ;
#152124=VERTEX_POINT ( 'NONE', #146239 ) ;
#152127=TOROIDAL_SURFACE ( 'NONE', #39702, 11.70000000000000639, 0.1000000000000000056 ) ;
#152129=AXIS2_PLACEMENT_3D ( 'NONE', #253674, #154624, #149478 ) ;
#152181=CARTESIAN_POINT ( 'NONE',  ( -22.43310005002225438, 0.005636942152031573783, -155.8503378728655662 ) ) ;
#152203=EDGE_CURVE ( 'NONE', #82821, #252796, #99720, .T. ) ;
#152249=CARTESIAN_POINT ( 'NONE',  ( 22.39999999999999503, -0.1008583690875579364, -155.7504328765105868 ) ) ;
#152256=EDGE_LOOP ( 'NONE', ( #105317, #238337, #30615, #106035 ) ) ;
#152270=EDGE_LOOP ( 'NONE', ( #159711, #43820, #1164, #189348 ) ) ;
#152275=AXIS2_PLACEMENT_3D ( 'NONE', #102392, #144105, #146664 ) ;
#152280=DIRECTION ( 'NONE',  ( 0.000000000000000000, 0.000000000000000000, -1.000000000000000000 ) ) ;
#152331=VERTEX_POINT ( 'NONE', #93968 ) ;
#152338=ORIENTED_EDGE ( 'NONE', *, *, #246538, .T. ) ;
#152361=EDGE_LOOP ( 'NONE', ( #222716, #100190, #7898, #189362 ) ) ;
#152397=DIRECTION ( 'NONE',  ( 1.000000000000000000, 0.000000000000000000, 0.000000000000000000 ) ) ;
#152409=VECTOR ( 'NONE', #166616, 1000.000000000000000 ) ;
#152412=ADVANCED_FACE ( 'NONE', ( #15762 ), #79528, .F. ) ;
#152433=CARTESIAN_POINT ( 'NONE',  ( -18.49372193242257012, -9.442484523346656999, -207.7647812600339989 ) ) ;
#152442=DIRECTION ( 'NONE',  ( -1.000000000000000000, -2.952720810173289112E-16, 0.000000000000000000 ) ) ;
#152446=EDGE_LOOP ( 'NONE', ( #90905, #53117, #23804, #231382 ) ) ;
#152450=VERTEX_POINT ( 'NONE', #17028 ) ;
#152458=EDGE_CURVE ( 'NONE', #138430, #199092, #75020, .T. ) ;
#152472=FACE_OUTER_BOUND ( 'NONE', #24870, .T. ) ;
#152475=DIRECTION ( 'NONE',  ( 0.000000000000000000, 0.000000000000000000, -1.000000000000000000 ) ) ;
#152513=VERTEX_POINT ( 'NONE', #3866 ) ;
#152524=ORIENTED_EDGE ( 'NONE', *, *, #227097, .T. ) ;
#152548=AXIS2_PLACEMENT_3D ( 'NONE', #126810, #189359, #169832 ) ;
#152584=VERTEX_POINT ( 'NONE', #22167 ) ;
#152617=CIRCLE ( 'NONE', #2714, 0.09999999999998898659 ) ;
#152648=ORIENTED_EDGE ( 'NONE', *, *, #118369, .F. ) ;
#152668=AXIS2_PLACEMENT_3D ( 'NONE', #125685, #243061, #226037 ) ;
#152676=CARTESIAN_POINT ( 'NONE',  ( -21.14999999999999858, 11.75000000001115552, -167.5999999999999659 ) ) ;
#152701=AXIS2_PLACEMENT_3D ( 'NONE', #12379, #90589, #91882 ) ;
#152705=EDGE_CURVE ( 'NONE', #152450, #180362, #208508, .T. ) ;
#152744=AXIS2_PLACEMENT_3D ( 'NONE', #205109, #201272, #217296 ) ;
#152746=EDGE_CURVE ( 'NONE', #52759, #2978, #151084, .T. ) ;
#152772=VERTEX_POINT ( 'NONE', #20572 ) ;
#152776=ORIENTED_EDGE ( 'NONE', *, *, #237255, .T. ) ;
#152790=AXIS2_PLACEMENT_3D ( 'NONE', #256214, #116776, #17663 ) ;
#152811=VECTOR ( 'NONE', #108167, 1000.000000000000000 ) ;
#152839=ORIENTED_EDGE ( 'NONE', *, *, #30883, .T. ) ;
#152862=TOROIDAL_SURFACE ( 'NONE', #206990, 0.4000000000000015210, 0.1000000000000000056 ) ;
#152874=CARTESIAN_POINT ( 'NONE',  ( 23.24999999999999645, 1.115600667400684642E-11, -167.4999999999999716 ) ) ;
#152899=DIRECTION ( 'NONE',  ( 1.000000000000000000, 0.000000000000000000, 0.000000000000000000 ) ) ;
#152905=ORIENTED_EDGE ( 'NONE', *, *, #249208, .F. ) ;
#152913=AXIS2_PLACEMENT_3D ( 'NONE', #71055, #34499, #113997 ) ;
#152919=VECTOR ( 'NONE', #6213, 1000.000000000000000 ) ;
#152925=AXIS2_PLACEMENT_3D ( 'NONE', #85357, #223599, #202773 ) ;
#152932=ORIENTED_EDGE ( 'NONE', *, *, #229554, .F. ) ;
#152934=ORIENTED_EDGE ( 'NONE', *, *, #240631, .T. ) ;
#152947=CARTESIAN_POINT ( 'NONE',  ( 19.90621891164687440, 11.75000000001116263, -192.3284452778769662 ) ) ;
#152964=EDGE_CURVE ( 'NONE', #56940, #242287, #204735, .T. ) ;
#152973=FACE_OUTER_BOUND ( 'NONE', #184884, .T. ) ;
#153021=CARTESIAN_POINT ( 'NONE',  ( 21.14999999999999858, 6.540656951712400691, -167.5999999999999659 ) ) ;
#153038=AXIS2_PLACEMENT_3D ( 'NONE', #142957, #63436, #42602 ) ;
#153154=ORIENTED_EDGE ( 'NONE', *, *, #61637, .T. ) ;
#153167=LINE ( 'NONE', #190991, #39074 ) ;
#153210=CARTESIAN_POINT ( 'NONE',  ( 21.05000000000000071, 10.72371710471867701, -179.6499999999999773 ) ) ;
#153213=DIRECTION ( 'NONE',  ( -1.000000000000000000, -0.000000000000000000, -0.000000000000000000 ) ) ;
#153224=ORIENTED_EDGE ( 'NONE', *, *, #139109, .F. ) ;
#153246=CARTESIAN_POINT ( 'NONE',  ( -21.05000000000000071, 5.900000000011162093, -190.7809002353436085 ) ) ;
#153247=CARTESIAN_POINT ( 'NONE',  ( -21.14999999999999858, -0.09999999998884338825, -161.2499999999999716 ) ) ;
#153286=DIRECTION ( 'NONE',  ( -1.000000000000000000, 0.000000000000000000, 0.000000000000000000 ) ) ;
#153287=CARTESIAN_POINT ( 'NONE',  ( 23.24999999999999289, 6.450000000011156587, -179.8499999999999943 ) ) ;
#153292=ORIENTED_EDGE ( 'NONE', *, *, #228617, .T. ) ;
#153336=B_SPLINE_CURVE_WITH_KNOTS ( 'NONE', 3,
 ( #163324, #242848, #167201, #229712, #188024, #30241 ),
 .UNSPECIFIED., .F., .F.,
 ( 4, 2, 4 ),
 ( 0.000000000000000000, 0.0001497467027049249823, 0.0002994934054098499646 ),
 .UNSPECIFIED. ) ;
#153348=VECTOR ( 'NONE', #53824, 1000.000000000000000 ) ;
#153361=LINE ( 'NONE', #232874, #193977 ) ;
#153362=EDGE_CURVE ( 'NONE', #62638, #252199, #12844, .T. ) ;
#153412=CARTESIAN_POINT ( 'NONE',  ( 20.94999999999999574, -1.249999999988843369, -175.4999999999999716 ) ) ;
#153421=AXIS2_PLACEMENT_3D ( 'NONE', #96480, #151365, #76935 ) ;
#153425=CARTESIAN_POINT ( 'NONE',  ( 23.24999999999999645, 5.000000000011153745, -188.5947339810868755 ) ) ;
#153434=EDGE_CURVE ( 'NONE', #206366, #7452, #133151, .T. ) ;
#153440=DIRECTION ( 'NONE',  ( 0.000000000000000000, 0.000000000000000000, -1.000000000000000000 ) ) ;
#153464=CARTESIAN_POINT ( 'NONE',  ( 23.24999999999999645, -2.099999999988846344, -200.9999999999999432 ) ) ;
#153468=AXIS2_PLACEMENT_3D ( 'NONE', #141342, #177917, #217011 ) ;
#153470=EDGE_CURVE ( 'NONE', #185697, #222817, #196157, .T. ) ;
#153481=DIRECTION ( 'NONE',  ( 0.000000000000000000, 0.000000000000000000, -1.000000000000000000 ) ) ;
#153494=FACE_OUTER_BOUND ( 'NONE', #185510, .T. ) ;
#153510=DIRECTION ( 'NONE',  ( 1.000000000000000000, 0.000000000000000000, 0.000000000000000000 ) ) ;
#153513=CARTESIAN_POINT ( 'NONE',  ( 0.000000000000000000, 0.000000000000000000, 0.000000000000000000 ) ) ;
#153520=CARTESIAN_POINT ( 'NONE',  ( -22.47071067811865319, 1.115600667400684642E-11, -167.4999999999999716 ) ) ;
#153529=CYLINDRICAL_SURFACE ( 'NONE', #241540, 0.09999999999999939493 ) ;
#153551=ORIENTED_EDGE ( 'NONE', *, *, #76329, .T. ) ;
#153593=DIRECTION ( 'NONE',  ( 0.000000000000000000, 0.000000000000000000, -1.000000000000000000 ) ) ;
#153654=ORIENTED_EDGE ( 'NONE', *, *, #188288, .F. ) ;
#153669=CARTESIAN_POINT ( 'NONE',  ( 18.50000000000000000, -9.499999999988842703, -207.6001893912220169 ) ) ;
#153681=CARTESIAN_POINT ( 'NONE',  ( 23.24999999999999289, 5.950000000011163692, -190.6942976949651438 ) ) ;
#153689=EDGE_CURVE ( 'NONE', #132861, #145347, #21404, .T. ) ;
#153721=DIRECTION ( 'NONE',  ( 0.000000000000000000, 0.000000000000000000, -1.000000000000000000 ) ) ;
#153728=CARTESIAN_POINT ( 'NONE',  ( -23.15000000000000213, -8.999999999988846255, -177.3939691226524076 ) ) ;
#153742=CARTESIAN_POINT ( 'NONE',  ( -18.46919391072053074, -9.670724388266537019, -207.6738035317995639 ) ) ;
#153788=AXIS2_PLACEMENT_3D ( 'NONE', #175138, #169998, #91696 ) ;
#153811=ORIENTED_EDGE ( 'NONE', *, *, #177148, .F. ) ;
#153829=VERTEX_POINT ( 'NONE', #251494 ) ;
#153835=DIRECTION ( 'NONE',  ( 0.000000000000000000, 0.000000000000000000, 1.000000000000000000 ) ) ;
#153859=CARTESIAN_POINT ( 'NONE',  ( -21.44999999999999929, 7.150000000011155876, -179.8499999999999943 ) ) ;
#153869=CIRCLE ( 'NONE', #45477, 12.87499999999999822 ) ;
#153878=ORIENTED_EDGE ( 'NONE', *, *, #95887, .F. ) ;
#153895=DIRECTION ( 'NONE',  ( 1.000000000000000000, 0.000000000000000000, 0.000000000000000000 ) ) ;
#153917=DIRECTION ( 'NONE',  ( 1.000000000000000000, 0.000000000000000000, 0.000000000000000000 ) ) ;
#153945=EDGE_CURVE ( 'NONE', #125534, #99579, #212916, .T. ) ;
#153952=CARTESIAN_POINT ( 'NONE',  ( 20.94999999999999929, 10.72371710471867701, -175.1649135690875880 ) ) ;
#153956=CARTESIAN_POINT ( 'NONE',  ( 20.95443524775735256, 8.878554263883970066, -176.0337222756001267 ) ) ;
#153967=DIRECTION ( 'NONE',  ( 0.000000000000000000, -0.5000000000000004441, -0.8660254037844384856 ) ) ;
#153973=ORIENTED_EDGE ( 'NONE', *, *, #61995, .F. ) ;
#153998=AXIS2_PLACEMENT_3D ( 'NONE', #58373, #157552, #36297 ) ;
#153999=EDGE_CURVE ( 'NONE', #195524, #102524, #115848, .T. ) ;
#154008=CARTESIAN_POINT ( 'NONE',  ( -21.14999999999999858, -0.09999999998884338825, -155.8504291924551808 ) ) ;
#154015=CARTESIAN_POINT ( 'NONE',  ( -20.85000000000000142, 6.846123162363745074, -204.7377262668498190 ) ) ;
#154023=CARTESIAN_POINT ( 'NONE',  ( 22.50000000000000000, 1.115600667400684642E-11, -167.4999999999999716 ) ) ;
#154041=EDGE_CURVE ( 'NONE', #231547, #85475, #192263, .T. ) ;
#154054=CARTESIAN_POINT ( 'NONE',  ( 23.24999999999999645, 3.900000000011155432, -200.9999999999999432 ) ) ;
#154097=ORIENTED_EDGE ( 'NONE', *, *, #134512, .T. ) ;
#154103=ORIENTED_EDGE ( 'NONE', *, *, #106269, .T. ) ;
#154107=AXIS2_PLACEMENT_3D ( 'NONE', #139551, #60015, #102994 ) ;
#154136=ORIENTED_EDGE ( 'NONE', *, *, #142255, .F. ) ;
#154189=DIRECTION ( 'NONE',  ( 0.000000000000000000, 0.000000000000000000, 1.000000000000000000 ) ) ;
#154199=DIRECTION ( 'NONE',  ( -1.000000000000000000, 0.000000000000000000, -0.000000000000000000 ) ) ;
#154211=DIRECTION ( 'NONE',  ( 0.000000000000000000, 0.000000000000000000, -1.000000000000000000 ) ) ;
#154242=FACE_OUTER_BOUND ( 'NONE', #219523, .T. ) ;
#154263=DIRECTION ( 'NONE',  ( 0.000000000000000000, -1.000000000000000000, 0.000000000000000000 ) ) ;
#154271=AXIS2_PLACEMENT_3D ( 'NONE', #198750, #39714, #219590 ) ;
#154272=CARTESIAN_POINT ( 'NONE',  ( -23.15000000000000213, 5.900000000011162093, -190.7809002353436085 ) ) ;
#154359=ORIENTED_EDGE ( 'NONE', *, *, #238012, .T. ) ;
#154366=CARTESIAN_POINT ( 'NONE',  ( -23.25000000000000000, 11.65000000001115588, -193.9851942293460070 ) ) ;
#154370=VECTOR ( 'NONE', #72306, 1000.000000000000000 ) ;
#154427=ORIENTED_EDGE ( 'NONE', *, *, #220343, .F. ) ;
#154448=ADVANCED_FACE ( 'NONE', ( #152973 ), #10865, .T. ) ;
#154469=CARTESIAN_POINT ( 'NONE',  ( -20.64999999999999858, 1.925233644870967487, -188.2697564668738153 ) ) ;
#154479=ADVANCED_FACE ( 'NONE', ( #13435 ), #242498, .F. ) ;
#154499=CARTESIAN_POINT ( 'NONE',  ( 21.22070241538126467, 0.09891903054618129965, -161.0300537271303654 ) ) ;
#154503=VERTEX_POINT ( 'NONE', #238513 ) ;
#154510=CARTESIAN_POINT ( 'NONE',  ( 23.14999999999999858, 1.115600667400684642E-11, -167.4999999999999716 ) ) ;
#154518=CIRCLE ( 'NONE', #200277, 0.09999999999998898659 ) ;
#154520=CIRCLE ( 'NONE', #254415, 4.000000000000003553 ) ;
#154522=ORIENTED_EDGE ( 'NONE', *, *, #204406, .T. ) ;
#154536=LINE ( 'NONE', #215734, #158520 ) ;
#154538=( BOUNDED_SURFACE ( )  B_SPLINE_SURFACE ( 3, 2, ( 
 ( #197040, #61396, #217878 ),
 ( #39294, #118820, #220486 ),
 ( #99215, #140948, #121412 ),
 ( #186489, #147352, #242588 ),
 ( #26136, #142212, #207342 ),
 ( #163088, #204743, #63969 ) ),
 .UNSPECIFIED., .F., .F., .F. ) 
 B_SPLINE_SURFACE_WITH_KNOTS ( ( 4, 2, 4 ),
 ( 3, 3 ),
 ( 0.0001792624049599519573, 0.0003686986002124681460, 0.0005581347954649843075 ),
 ( 0.000000000000000000, 1.000000000000000000 ),
 .UNSPECIFIED. ) 
 GEOMETRIC_REPRESENTATION_ITEM ( )  RATIONAL_B_SPLINE_SURFACE ( (
 ( 1.000000000000000000, 0.9238795325112673096, 1.000000000000000000),
 ( 1.000000000000000000, 0.9229318695242666459, 1.000000000000000000),
 ( 1.000000000000000000, 0.8926288119225271878, 1.000000000000000000),
 ( 1.000000000000000000, 0.8123777807276841845, 1.000000000000000000),
 ( 1.000000000000000000, 0.7629087100927172127, 1.000000000000000000),
 ( 1.000000000000000000, 0.7071067811865352493, 1.000000000000000000) ) ) 
 REPRESENTATION_ITEM ( '' )  SURFACE ( )  );
#154557=CARTESIAN_POINT ( 'NONE',  ( 21.93642651522410603, 7.327166239336949438, -167.4999999999999716 ) ) ;
#154569=DIRECTION ( 'NONE',  ( -1.000000000000000000, 0.000000000000000000, 0.000000000000000000 ) ) ;
#154570=CARTESIAN_POINT ( 'NONE',  ( 21.05000000000000071, 10.62950747927176387, -175.1279793999966898 ) ) ;
#154583=CYLINDRICAL_SURFACE ( 'NONE', #50996, 0.09999999999999817368 ) ;
#154596=TOROIDAL_SURFACE ( 'NONE', #83785, 0.4000000000000003553, 0.1000000000000000056 ) ;
#154602=VERTEX_POINT ( 'NONE', #5981 ) ;
#154618=CIRCLE ( 'NONE', #96298, 0.09999999999998898659 ) ;
#154624=DIRECTION ( 'NONE',  ( 1.000000000000000000, 0.000000000000000000, 0.000000000000000000 ) ) ;
#154636=ORIENTED_EDGE ( 'NONE', *, *, #51725, .F. ) ;
#154687=EDGE_LOOP ( 'NONE', ( #131667, #68115, #22563, #194416 ) ) ;
#154695=ORIENTED_EDGE ( 'NONE', *, *, #207240, .F. ) ;
#154703=PLANE ( 'NONE',  #99020 ) ;
#154754=VERTEX_POINT ( 'NONE', #77494 ) ;
#154784=DIRECTION ( 'NONE',  ( 1.000000000000000000, 0.000000000000000000, -0.000000000000000000 ) ) ;
#154789=LINE ( 'NONE', #110494, #86868 ) ;
#154805=DIRECTION ( 'NONE',  ( 1.000000000000000000, -0.000000000000000000, -0.000000000000000000 ) ) ;
#154933=CARTESIAN_POINT ( 'NONE',  ( -20.94999999999999929, 5.850000000011108092, -177.6324972242779268 ) ) ;
#154971=DIRECTION ( 'NONE',  ( 1.000000000000000000, 7.304098846218133681E-16, -4.607487905232622991E-31 ) ) ;
#154981=ORIENTED_EDGE ( 'NONE', *, *, #190710, .F. ) ;
#154990=CARTESIAN_POINT ( 'NONE',  ( 18.52351027002948314, -9.642162904684017377, -207.7150469505097021 ) ) ;
#154991=VERTEX_POINT ( 'NONE', #125638 ) ;
#154998=ADVANCED_FACE ( 'NONE', ( #107351, #108643, #9534 ), #168673, .F. ) ;
#155016=AXIS2_PLACEMENT_3D ( 'NONE', #6541, #83481, #44405 ) ;
#155018=DIRECTION ( 'NONE',  ( 0.000000000000000000, 0.000000000000000000, -1.000000000000000000 ) ) ;
#155067=CIRCLE ( 'NONE', #230049, 0.09999999999999939493 ) ;
#155094=DIRECTION ( 'NONE',  ( 1.000000000000000000, -7.304098846218134667E-16, 4.607487905232622991E-31 ) ) ;
#155127=ORIENTED_EDGE ( 'NONE', *, *, #214473, .F. ) ;
#155136=ADVANCED_FACE ( 'NONE', ( #160641 ), #62796, .T. ) ;
#155141=AXIS2_PLACEMENT_3D ( 'NONE', #182852, #162002, #241515 ) ;
#155172=DIRECTION ( 'NONE',  ( -1.000000000000000000, -0.000000000000000000, -0.000000000000000000 ) ) ;
#155197=AXIS2_PLACEMENT_3D ( 'NONE', #56460, #132171, #112612 ) ;
#155223=DIRECTION ( 'NONE',  ( 1.000000000000000000, 0.000000000000000000, 0.000000000000000000 ) ) ;
#155224=ORIENTED_EDGE ( 'NONE', *, *, #165580, .T. ) ;
#155258=VERTEX_POINT ( 'NONE', #9234 ) ;
#155262=AXIS2_PLACEMENT_3D ( 'NONE', #158701, #180809, #161249 ) ;
#155274=DIRECTION ( 'NONE',  ( 0.000000000000000000, 0.4999999999999608646, 0.8660254037844612451 ) ) ;
#155275=DIRECTION ( 'NONE',  ( -1.000000000000000000, 0.000000000000000000, 0.000000000000000000 ) ) ;
#155289=AXIS2_PLACEMENT_3D ( 'NONE', #204894, #103220, #181517 ) ;
#155296=CARTESIAN_POINT ( 'NONE',  ( 22.39999999999999503, 1.115600667400684642E-11, -159.7499999999999432 ) ) ;
#155303=DIRECTION ( 'NONE',  ( 1.000000000000000000, 0.000000000000000000, 0.000000000000000000 ) ) ;
#155386=LINE ( 'NONE', #232345, #99158 ) ;
#155401=DIRECTION ( 'NONE',  ( -1.000000000000000000, 0.000000000000000000, 0.000000000000000000 ) ) ;
#155418=VECTOR ( 'NONE', #112949, 1000.000000000000000 ) ;
#155436=FACE_OUTER_BOUND ( 'NONE', #26018, .T. ) ;
#155444=LINE ( 'NONE', #175017, #19988 ) ;
#155494=VECTOR ( 'NONE', #92674, 1000.000000000000000 ) ;
#155513=CARTESIAN_POINT ( 'NONE',  ( 19.83283456528359423, 11.75000000001116263, -192.3499999994177472 ) ) ;
#155521=AXIS2_PLACEMENT_3D ( 'NONE', #186694, #150139, #28937 ) ;
#155529=EDGE_LOOP ( 'NONE', ( #221424, #220285, #203858, #27521 ) ) ;
#155557=DIRECTION ( 'NONE',  ( 1.000000000000000000, 0.000000000000000000, -0.000000000000000000 ) ) ;
#155570=ORIENTED_EDGE ( 'NONE', *, *, #68389, .T. ) ;
#155596=CIRCLE ( 'NONE', #226243, 0.1999999999999996503 ) ;
#155615=VECTOR ( 'NONE', #89233, 1000.000000000000000 ) ;
#155620=CARTESIAN_POINT ( 'NONE',  ( -20.94999999999999929, -1.835341550213255957, -179.1551512925629197 ) ) ;
#155633=DIRECTION ( 'NONE',  ( -4.336808689941752679E-15, 0.8660254037844482555, 0.4999999999999837907 ) ) ;
#155640=CARTESIAN_POINT ( 'NONE',  ( -18.59999999999999787, 1.340746217944851715, -157.2271374945787841 ) ) ;
#155675=ORIENTED_EDGE ( 'NONE', *, *, #128557, .F. ) ;
#155679=CIRCLE ( 'NONE', #143146, 0.9750000000000036415 ) ;
#155681=ORIENTED_EDGE ( 'NONE', *, *, #209416, .T. ) ;
#155698=DIRECTION ( 'NONE',  ( 0.000000000000000000, 0.4999999999999543698, 0.8660254037844650199 ) ) ;
#155709=FACE_OUTER_BOUND ( 'NONE', #35683, .T. ) ;
#155716=ADVANCED_FACE ( 'NONE', ( #165457 ), #85871, .T. ) ;
#155756=CARTESIAN_POINT ( 'NONE',  ( 20.94788355080263997, 10.30207779525983547, -206.4895520716781903 ) ) ;
#155763=CARTESIAN_POINT ( 'NONE',  ( -23.25000000000000000, 1.115600667400684642E-11, -200.9999999999999432 ) ) ;
#155776=CARTESIAN_POINT ( 'NONE',  ( -20.54999999999999716, 2.000000000011154189, -188.1753780772378946 ) ) ;
#155783=ORIENTED_EDGE ( 'NONE', *, *, #66930, .T. ) ;
#155787=EDGE_LOOP ( 'NONE', ( #217565, #193113, #144730, #18140 ) ) ;
#155790=ORIENTED_EDGE ( 'NONE', *, *, #220263, .T. ) ;
#155801=FACE_OUTER_BOUND ( 'NONE', #69487, .T. ) ;
#155827=CARTESIAN_POINT ( 'NONE',  ( 22.39999999999999503, 7.790779598384535376, -167.4999999999999716 ) ) ;
#155831=DIRECTION ( 'NONE',  ( 1.000000000000000000, 0.000000000000000000, -0.000000000000000000 ) ) ;
#155838=SPHERICAL_SURFACE ( 'NONE', #66923, 0.1000000000000000056 ) ;
#155868=CARTESIAN_POINT ( 'NONE',  ( -20.00857864376270001, 9.350000000011156942, -188.7499999999999716 ) ) ;
#155870=DIRECTION ( 'NONE',  ( 0.000000000000000000, 0.9908441862701782288, -0.1350103645450542456 ) ) ;
#155890=CARTESIAN_POINT ( 'NONE',  ( -21.05000000000000071, 5.850000000011105428, -177.6324972242779268 ) ) ;
#155904=EDGE_CURVE ( 'NONE', #128410, #34141, #188499, .T. ) ;
#155924=AXIS2_PLACEMENT_3D ( 'NONE', #218358, #39779, #119292 ) ;
#155925=FACE_OUTER_BOUND ( 'NONE', #13610, .T. ) ;
#155951=CARTESIAN_POINT ( 'NONE',  ( 21.14999999999999503, -11.64999999998883595, -155.7499999999999716 ) ) ;
#155957=DIRECTION ( 'NONE',  ( 0.000000000000000000, 0.000000000000000000, -1.000000000000000000 ) ) ;
#155972=DIRECTION ( 'NONE',  ( -1.000000000000000000, 0.000000000000000000, 0.000000000000000000 ) ) ;
#156012=CARTESIAN_POINT ( 'NONE',  ( -20.85000000000000142, 11.75000000001115197, -194.2161343370218560 ) ) ;
#156041=ORIENTED_EDGE ( 'NONE', *, *, #252797, .F. ) ;
#156065=ORIENTED_EDGE ( 'NONE', *, *, #69135, .T. ) ;
#156077=ORIENTED_EDGE ( 'NONE', *, *, #126553, .F. ) ;
#156079=CARTESIAN_POINT ( 'NONE',  ( 20.95512820512820440, 8.876151316299271343, -176.0586289951409071 ) ) ;
#156083=DIRECTION ( 'NONE',  ( 0.000000000000000000, 0.000000000000000000, 1.000000000000000000 ) ) ;
#156086=ORIENTED_EDGE ( 'NONE', *, *, #30875, .F. ) ;
#156095=( BOUNDED_SURFACE ( )  B_SPLINE_SURFACE ( 3, 2, ( 
 ( #104265, #203396, #145970 ),
 ( #221646, #45602, #27364 ),
 ( #62600, #125148, #182561 ),
 ( #243797, #43040, #181281 ),
 ( #246370, #183822, #225489 ),
 ( #143410, #126412, #3905 ) ),
 .UNSPECIFIED., .F., .F., .F. ) 
 B_SPLINE_SURFACE_WITH_KNOTS ( ( 4, 2, 4 ),
 ( 3, 3 ),
 ( 0.0001342700090130150253, 0.0002909192928057470397, 0.0004475685765984790000 ),
 ( 0.000000000000000000, 1.000000000000000000 ),
 .UNSPECIFIED. ) 
 GEOMETRIC_REPRESENTATION_ITEM ( )  RATIONAL_B_SPLINE_SURFACE ( (
 ( 1.000000000000000000, 0.7250110520819876836, 1.000000000000000000),
 ( 1.000000000000000000, 0.7257599279136393022, 1.000000000000000000),
 ( 1.000000000000000000, 0.7137594617280778042, 1.000000000000000000),
 ( 1.000000000000000000, 0.6959270178813201646, 1.000000000000000000),
 ( 1.000000000000000000, 0.6919879549336147573, 1.000000000000000000),
 ( 1.000000000000000000, 0.7071067811865475727, 1.000000000000000000) ) ) 
 REPRESENTATION_ITEM ( '' )  SURFACE ( )  );
#156141=VERTEX_POINT ( 'NONE', #167726 ) ;
#156166=DIRECTION ( 'NONE',  ( 0.000000000000000000, 1.224646799142185182E-16, 1.000000000000000000 ) ) ;
#156178=EDGE_CURVE ( 'NONE', #152331, #50174, #213426, .T. ) ;
#156192=DIRECTION ( 'NONE',  ( 0.000000000000000000, -1.000000000000000000, 0.000000000000000000 ) ) ;
#156208=CARTESIAN_POINT ( 'NONE',  ( 18.59117750673696179, 10.33248238083634796, -206.5948465439131496 ) ) ;
#156211=AXIS2_PLACEMENT_3D ( 'NONE', #208078, #185924, #222453 ) ;
#156254=ORIENTED_EDGE ( 'NONE', *, *, #180755, .T. ) ;
#156260=ADVANCED_FACE ( 'NONE', ( #177682 ), #251698, .T. ) ;
#156270=ORIENTED_EDGE ( 'NONE', *, *, #115887, .F. ) ;
#156292=DIRECTION ( 'NONE',  ( -0.000000000000000000, -0.000000000000000000, 1.000000000000000000 ) ) ;
#156320=CARTESIAN_POINT ( 'NONE',  ( 20.85000000000000142, 1.115600667400684642E-11, -200.9999999999999432 ) ) ;
#156367=ORIENTED_EDGE ( 'NONE', *, *, #103222, .F. ) ;
#156368=CARTESIAN_POINT ( 'NONE',  ( 20.94999999999999929, -1.835341550213257733, -179.0551512925629538 ) ) ;
#156372=DIRECTION ( 'NONE',  ( -1.000000000000000000, 0.000000000000000000, 0.000000000000000000 ) ) ;
#156377=AXIS2_PLACEMENT_3D ( 'NONE', #63752, #106714, #62485 ) ;
#156380=ORIENTED_EDGE ( 'NONE', *, *, #33022, .F. ) ;
#156385=DIRECTION ( 'NONE',  ( 0.7071359030027680737, 0.7070776581709111719, 0.000000000000000000 ) ) ;
#156400=CARTESIAN_POINT ( 'NONE',  ( -23.15000000000000213, 1.115600667400684642E-11, -171.5499999999999829 ) ) ;
#156410=DIRECTION ( 'NONE',  ( 1.301042606982683418E-14, -0.8660254037844330455, 0.5000000000000096589 ) ) ;
#156412=DIRECTION ( 'NONE',  ( 0.7071359030027766224, -0.7070776581709024011, 0.000000000000000000 ) ) ;
#156442=AXIS2_PLACEMENT_3D ( 'NONE', #165667, #143506, #241345 ) ;
#156515=FACE_OUTER_BOUND ( 'NONE', #175799, .T. ) ;
#156526=VERTEX_POINT ( 'NONE', #189212 ) ;
#156558=DIRECTION ( 'NONE',  ( 0.000000000000000000, 1.000000000000000000, 0.000000000000000000 ) ) ;
#156566=VERTEX_POINT ( 'NONE', #144921 ) ;
#156571=EDGE_CURVE ( 'NONE', #16272, #190824, #85064, .T. ) ;
#156581=ORIENTED_EDGE ( 'NONE', *, *, #98314, .T. ) ;
#156613=ORIENTED_EDGE ( 'NONE', *, *, #137398, .F. ) ;
#156632=CARTESIAN_POINT ( 'NONE',  ( 22.48660254037844197, 11.65000000001115588, -167.4499999999999602 ) ) ;
#156636=DIRECTION ( 'NONE',  ( 1.000000000000000000, 0.000000000000000000, -0.000000000000000000 ) ) ;
#156697=ORIENTED_EDGE ( 'NONE', *, *, #70009, .T. ) ;
#156712=CARTESIAN_POINT ( 'NONE',  ( 18.59999999999996945, 10.33248238083634440, -206.5948465439131496 ) ) ;
#156727=CIRCLE ( 'NONE', #123371, 3.999999999999999112 ) ;
#156732=ORIENTED_EDGE ( 'NONE', *, *, #103815, .T. ) ;
#156744=EDGE_LOOP ( 'NONE', ( #112387, #208262, #176529, #193851 ) ) ;
#156750=CARTESIAN_POINT ( 'NONE',  ( 21.05000000000000071, -11.64999999998883595, -197.8999999999999773 ) ) ;
#156777=CIRCLE ( 'NONE', #44336, 0.09999999999999062417 ) ;
#156788=CARTESIAN_POINT ( 'NONE',  ( 19.80993210785717196, 11.75000000000834177, -192.2671177488814749 ) ) ;
#156849=ORIENTED_EDGE ( 'NONE', *, *, #42375, .F. ) ;
#156856=VERTEX_POINT ( 'NONE', #248877 ) ;
#156905=ORIENTED_EDGE ( 'NONE', *, *, #42406, .T. ) ;
#156914=ADVANCED_FACE ( 'NONE', ( #175770 ), #234425, .F. ) ;
#156921=DIRECTION ( 'NONE',  ( 0.000000000000000000, 2.168404344971247498E-15, 1.000000000000000000 ) ) ;
#156930=CARTESIAN_POINT ( 'NONE',  ( -20.94999999999999929, -11.64999999998884483, -198.0999999999999659 ) ) ;
#156952=ORIENTED_EDGE ( 'NONE', *, *, #132290, .T. ) ;
#156986=DIRECTION ( 'NONE',  ( -1.000000000000000000, 0.000000000000000000, 0.000000000000000000 ) ) ;
#156990=DIRECTION ( 'NONE',  ( 1.000000000000000000, -0.000000000000000000, -0.000000000000000000 ) ) ;
#157009=CARTESIAN_POINT ( 'NONE',  ( -21.14999999999999858, 6.257814610487270279, -167.4022097086911742 ) ) ;
#157021=ADVANCED_FACE ( 'NONE', ( #130188 ), #255228, .F. ) ;
#157023=AXIS2_PLACEMENT_3D ( 'NONE', #151235, #46964, #87376 ) ;
#157026=CARTESIAN_POINT ( 'NONE',  ( 20.94983749550516450, 10.29766095125288494, -206.4743663933275286 ) ) ;
#157045=CARTESIAN_POINT ( 'NONE',  ( 22.50497660315937054, -0.07871793021434786430, -155.7502044951045548 ) ) ;
#157049=AXIS2_PLACEMENT_3D ( 'NONE', #212870, #36831, #94183 ) ;
#157060=VERTEX_POINT ( 'NONE', #153681 ) ;
#157072=FACE_OUTER_BOUND ( 'NONE', #37142, .T. ) ;
#157109=DIRECTION ( 'NONE',  ( 0.000000000000000000, 0.7397360091702777085, -0.6728971962616808744 ) ) ;
#157110=DIRECTION ( 'NONE',  ( 0.000000000000000000, 1.000000000000000000, 0.000000000000000000 ) ) ;
#157126=CARTESIAN_POINT ( 'NONE',  ( 20.95595012432474746, 10.60417921308754607, -175.0957693302182463 ) ) ;
#157129=DIRECTION ( 'NONE',  ( 0.000000000000000000, 0.000000000000000000, 1.000000000000000000 ) ) ;
#157145=CARTESIAN_POINT ( 'NONE',  ( 22.39999999999999503, -0.1008583690875579364, -155.7504328765105868 ) ) ;
#157152=DIRECTION ( 'NONE',  ( 2.342056488767301376E-15, -0.1350103645451904977, -0.9908441862701596881 ) ) ;
#157160=VECTOR ( 'NONE', #81981, 1000.000000000000000 ) ;
#157168=DIRECTION ( 'NONE',  ( 1.000000000000000000, 3.265361837132813093E-16, -0.000000000000000000 ) ) ;
#157203=AXIS2_PLACEMENT_3D ( 'NONE', #57211, #100183, #196739 ) ;
#157225=ORIENTED_EDGE ( 'NONE', *, *, #106496, .T. ) ;
#157230=DIRECTION ( 'NONE',  ( 1.000000000000000000, -0.000000000000000000, -0.000000000000000000 ) ) ;
#157267=CARTESIAN_POINT ( 'NONE',  ( 23.14999999999999503, 11.75000000001116263, -179.6499999999999773 ) ) ;
#157296=CIRCLE ( 'NONE', #128056, 0.1000000000000002554 ) ;
#157299=CARTESIAN_POINT ( 'NONE',  ( -20.99780126800952829, 11.60538868788763089, -194.0873525717049972 ) ) ;
#157321=DIRECTION ( 'NONE',  ( -0.000000000000000000, -0.1298341882519805091, -0.9915357197604881545 ) ) ;
#157329=EDGE_CURVE ( 'NONE', #127614, #239082, #177073, .T. ) ;
#157330=VECTOR ( 'NONE', #8832, 1000.000000000000000 ) ;
#157353=CARTESIAN_POINT ( 'NONE',  ( 18.59999999999999076, 11.65000000001115943, -155.7499999999999716 ) ) ;
#157386=PLANE ( 'NONE',  #218409 ) ;
#157399=ADVANCED_FACE ( 'NONE', ( #71223 ), #174200, .F. ) ;
#157409=CARTESIAN_POINT ( 'NONE',  ( 21.04999999999999716, 0.09843750001147316686, -161.2007690899076806 ) ) ;
#157416=DIRECTION ( 'NONE',  ( 0.000000000000000000, 0.000000000000000000, -1.000000000000000000 ) ) ;
#157433=ORIENTED_EDGE ( 'NONE', *, *, #114380, .T. ) ;
#157452=DIRECTION ( 'NONE',  ( 0.000000000000000000, 0.000000000000000000, 1.000000000000000000 ) ) ;
#157476=DIRECTION ( 'NONE',  ( 0.000000000000000000, 0.1350103645451876666, -0.9908441862701600211 ) ) ;
#157499=CARTESIAN_POINT ( 'NONE',  ( -21.05000000000000071, -1.162701749926853712, -175.4999999999999716 ) ) ;
#157552=DIRECTION ( 'NONE',  ( 0.000000000000000000, -0.000000000000000000, -1.000000000000000000 ) ) ;
#157554=CARTESIAN_POINT ( 'NONE',  ( -20.54999999999999716, 2.400000000011155432, -187.7753780772378889 ) ) ;
#157560=AXIS2_PLACEMENT_3D ( 'NONE', #170570, #33619, #55654 ) ;
#157570=VERTEX_POINT ( 'NONE', #41091 ) ;
#157604=AXIS2_PLACEMENT_3D ( 'NONE', #203350, #242458, #224181 ) ;
#157607=LINE ( 'NONE', #37637, #145211 ) ;
#157628=EDGE_LOOP ( 'NONE', ( #181560, #72418, #17102, #189535 ) ) ;
#157637=VERTEX_POINT ( 'NONE', #3200 ) ;
#157639=DIRECTION ( 'NONE',  ( 1.000000000000000000, 0.000000000000000000, -0.000000000000000000 ) ) ;
#157678=DIRECTION ( 'NONE',  ( 0.000000000000000000, 1.000000000000000000, 0.000000000000000000 ) ) ;
#157701=ORIENTED_EDGE ( 'NONE', *, *, #126864, .T. ) ;
#157705=EDGE_LOOP ( 'NONE', ( #216621, #78472, #173756, #51660 ) ) ;
#157709=CARTESIAN_POINT ( 'NONE',  ( 20.94999999999999929, -9.499999999988844479, -191.1060308773475072 ) ) ;
#157738=ORIENTED_EDGE ( 'NONE', *, *, #225868, .F. ) ;
#157756=LINE ( 'NONE', #56002, #160981 ) ;
#157760=CIRCLE ( 'NONE', #199422, 0.09999999999999864553 ) ;
#157796=VECTOR ( 'NONE', #75418, 1000.000000000000000 ) ;
#157807=CYLINDRICAL_SURFACE ( 'NONE', #90463, 0.09999999999998898659 ) ;
#157815=ADVANCED_FACE ( 'NONE', ( #190883 ), #248259, .T. ) ;
#157821=EDGE_LOOP ( 'NONE', ( #40158, #52747, #79740, #257048 ) ) ;
#157829=FACE_OUTER_BOUND ( 'NONE', #152256, .T. ) ;
#157844=ORIENTED_EDGE ( 'NONE', *, *, #183233, .T. ) ;
#157852=FACE_OUTER_BOUND ( 'NONE', #113972, .T. ) ;
#157875=ADVANCED_FACE ( 'NONE', ( #72206 ), #231281, .F. ) ;
#157878=EDGE_CURVE ( 'NONE', #22668, #202617, #192157, .T. ) ;
#157884=CIRCLE ( 'NONE', #203795, 0.09999999999999892308 ) ;
#157905=LINE ( 'NONE', #24796, #40648 ) ;
#157916=EDGE_LOOP ( 'NONE', ( #191544, #242475, #211065, #45709, #217502 ) ) ;
#157923=ORIENTED_EDGE ( 'NONE', *, *, #177190, .T. ) ;
#157944=VERTEX_POINT ( 'NONE', #83565 ) ;
#157951=EDGE_CURVE ( 'NONE', #130077, #234784, #28816, .T. ) ;
#157971=ORIENTED_EDGE ( 'NONE', *, *, #27012, .T. ) ;
#157981=ORIENTED_EDGE ( 'NONE', *, *, #179806, .F. ) ;
#157997=DIRECTION ( 'NONE',  ( 0.000000000000000000, 0.000000000000000000, -1.000000000000000000 ) ) ;
#158046=EDGE_CURVE ( 'NONE', #177021, #174631, #222806, .T. ) ;
#158048=EDGE_CURVE ( 'NONE', #239085, #27168, #43752, .T. ) ;
#158057=ORIENTED_EDGE ( 'NONE', *, *, #113555, .F. ) ;
#158068=CARTESIAN_POINT ( 'NONE',  ( 18.49505816908824229, -9.437872553199969872, -207.7776572016708769 ) ) ;
#158171=ORIENTED_EDGE ( 'NONE', *, *, #130826, .F. ) ;
#158199=CARTESIAN_POINT ( 'NONE',  ( 21.05000000000000071, 6.257814610487280937, -167.4022097086911742 ) ) ;
#158207=CARTESIAN_POINT ( 'NONE',  ( -20.94999999999999929, -11.64999999998884483, -170.3999999999999773 ) ) ;
#158219=ORIENTED_EDGE ( 'NONE', *, *, #231307, .F. ) ;
#158297=ORIENTED_EDGE ( 'NONE', *, *, #223582, .T. ) ;
#158301=DIRECTION ( 'NONE',  ( -1.000000000000000000, 7.304098846218134667E-16, 2.111765289898285610E-31 ) ) ;
#158326=CIRCLE ( 'NONE', #91839, 0.09999999999999971412 ) ;
#158331=CARTESIAN_POINT ( 'NONE',  ( -18.51024323315077424, 10.31104185824062291, -206.5204516983105805 ) ) ;
#158381=DIRECTION ( 'NONE',  ( 0.000000000000000000, 0.000000000000000000, 1.000000000000000000 ) ) ;
#158401=DIRECTION ( 'NONE',  ( -0.000000000000000000, -0.000000000000000000, 1.000000000000000000 ) ) ;
#158405=CARTESIAN_POINT ( 'NONE',  ( 21.03675099975492202, 8.875180032795963569, -179.8255421367780400 ) ) ;
#158428=ORIENTED_EDGE ( 'NONE', *, *, #59982, .F. ) ;
#158434=CARTESIAN_POINT ( 'NONE',  ( 21.14999999999999858, 1.115600667400684642E-11, -167.4999999999999716 ) ) ;
#158443=CARTESIAN_POINT ( 'NONE',  ( 20.94999999999999929, 4.813084112160684214, -189.0584822434761634 ) ) ;
#158475=AXIS2_PLACEMENT_3D ( 'NONE', #15307, #132675, #235602 ) ;
#158487=AXIS2_PLACEMENT_3D ( 'NONE', #221458, #42851, #139358 ) ;
#158520=VECTOR ( 'NONE', #172824, 1000.000000000000000 ) ;
#158532=ADVANCED_FACE ( 'NONE', ( #11689 ), #168223, .F. ) ;
#158602=DIRECTION ( 'NONE',  ( 0.000000000000000000, 0.9915357197604973694, -0.1298341882519105928 ) ) ;
#158614=EDGE_CURVE ( 'NONE', #196929, #254440, #60858, .T. ) ;
#158619=ORIENTED_EDGE ( 'NONE', *, *, #184549, .T. ) ;
#158628=DIRECTION ( 'NONE',  ( -0.000000000000000000, -1.000000000000000000, 0.000000000000000000 ) ) ;
#158648=CARTESIAN_POINT ( 'NONE',  ( -22.39999999999999858, 11.65000000001115588, -167.4999999999999716 ) ) ;
#158668=CIRCLE ( 'NONE', #104443, 0.09999999999998898659 ) ;
#158671=CARTESIAN_POINT ( 'NONE',  ( -20.54999999999999716, 4.350000000011156054, -179.8499999999999943 ) ) ;
#158673=AXIS2_PLACEMENT_3D ( 'NONE', #208389, #170583, #145812 ) ;
#158677=EDGE_LOOP ( 'NONE', ( #153154, #200481, #128718, #50485, #166662, #117814, #226274, #83677, #180168, #17158, #78746, #139934, #172538, #140798, #56295, #150218, #76230, #212638, #135466, #221697, #193469, #119403, #217057, #131429, #64925 ) ) ;
#158678=CIRCLE ( 'NONE', #179514, 0.09999999999999949207 ) ;
#158681=CARTESIAN_POINT ( 'NONE',  ( 18.59999999999999076, 6.450000000011156587, -177.5170271704400022 ) ) ;
#158701=CARTESIAN_POINT ( 'NONE',  ( -21.05000000000000071, 1.115600667400684642E-11, -200.9999999999999432 ) ) ;
#158708=VERTEX_POINT ( 'NONE', #61055 ) ;
#158718=CIRCLE ( 'NONE', #133731, 0.09999999999998898659 ) ;
#158720=ORIENTED_EDGE ( 'NONE', *, *, #115519, .T. ) ;
#158753=CARTESIAN_POINT ( 'NONE',  ( -21.05000000000000071, 0.2561057921033771945, -167.4651035583276553 ) ) ;
#158810=CARTESIAN_POINT ( 'NONE',  ( -20.94999999999999929, 1.750000000011155743, -179.1695115579016147 ) ) ;
#158852=VERTEX_POINT ( 'NONE', #188708 ) ;
#158853=CARTESIAN_POINT ( 'NONE',  ( 20.94999999999999929, -8.663551401858002876, -177.0241011180672785 ) ) ;
#158865=ORIENTED_EDGE ( 'NONE', *, *, #22129, .F. ) ;
#158872=DIRECTION ( 'NONE',  ( 0.000000000000000000, 0.000000000000000000, -1.000000000000000000 ) ) ;
#158875=DIRECTION ( 'NONE',  ( -1.000000000000000000, -0.000000000000000000, -0.000000000000000000 ) ) ;
#158877=CARTESIAN_POINT ( 'NONE',  ( -23.25000000000000000, 4.150000000011156764, -179.8499999999999943 ) ) ;
#158895=DIRECTION ( 'NONE',  ( 1.000000000000000000, 0.000000000000000000, 0.000000000000000000 ) ) ;
#158918=DIRECTION ( 'NONE',  ( 0.000000000000000000, -0.4791956752371546169, -0.8777080977375152360 ) ) ;
#158969=ORIENTED_EDGE ( 'NONE', *, *, #170682, .F. ) ;
#158975=CARTESIAN_POINT ( 'NONE',  ( -20.94999999999999929, 1.115600667400684642E-11, -167.4999999999999716 ) ) ;
#158983=EDGE_CURVE ( 'NONE', #141200, #39669, #10979, .T. ) ;
#158984=ADVANCED_FACE ( 'NONE', ( #153494 ), #48572, .T. ) ;
#158994=DIRECTION ( 'NONE',  ( 0.000000000000000000, 0.9908441862701782288, 0.1350103645450542456 ) ) ;
#158996=CYLINDRICAL_SURFACE ( 'NONE', #232882, 0.09999999999999939493 ) ;
#159006=DIRECTION ( 'NONE',  ( 0.000000000000000000, 1.000000000000000000, 0.000000000000000000 ) ) ;
#159012=CARTESIAN_POINT ( 'NONE',  ( 20.94999999999999574, 1.162701749949165642, -175.5999999999999659 ) ) ;
#159017=FACE_OUTER_BOUND ( 'NONE', #115632, .T. ) ;
#159064=CARTESIAN_POINT ( 'NONE',  ( 20.95512820512820440, 8.876151316299271343, -176.0586289951409071 ) ) ;
#159093=VECTOR ( 'NONE', #244663, 1000.000000000000000 ) ;
#159101=ADVANCED_FACE ( 'NONE', ( #50166 ), #170179, .T. ) ;
#159114=CARTESIAN_POINT ( 'NONE',  ( 20.94999999999999929, -1.835341550213257733, -179.0551512925629538 ) ) ;
#159117=ADVANCED_FACE ( 'NONE', ( #230099 ), #127151, .F. ) ;
#159139=DIRECTION ( 'NONE',  ( 2.915501640297155269E-16, -1.000000000000000000, 0.000000000000000000 ) ) ;
#159183=EDGE_LOOP ( 'NONE', ( #44315, #131948, #165418, #9856, #229256 ) ) ;
#159197=FACE_OUTER_BOUND ( 'NONE', #78878, .T. ) ;
#159202=ORIENTED_EDGE ( 'NONE', *, *, #153434, .F. ) ;
#159218=CIRCLE ( 'NONE', #209256, 0.09999999999999439892 ) ;
#159224=ORIENTED_EDGE ( 'NONE', *, *, #250324, .T. ) ;
#159232=TOROIDAL_SURFACE ( 'NONE', #209266, 0.2000000000000000111, 0.1000000000000000056 ) ;
#159274=LINE ( 'NONE', #167000, #253004 ) ;
#159318=FACE_OUTER_BOUND ( 'NONE', #103095, .T. ) ;
#159324=DIRECTION ( 'NONE',  ( -1.000000000000000000, -0.000000000000000000, -0.000000000000000000 ) ) ;
#159359=ORIENTED_EDGE ( 'NONE', *, *, #107275, .F. ) ;
#159377=AXIS2_PLACEMENT_3D ( 'NONE', #207839, #209087, #231240 ) ;
#159397=ORIENTED_EDGE ( 'NONE', *, *, #14181, .F. ) ;
#159401=DIRECTION ( 'NONE',  ( 0.000000000000000000, -0.1568667991644863147, -0.9876197685951252359 ) ) ;
#159422=EDGE_LOOP ( 'NONE', ( #209481, #136751, #119308, #144070 ) ) ;
#159440=AXIS2_PLACEMENT_3D ( 'NONE', #66244, #221433, #41568 ) ;
#159460=EDGE_CURVE ( 'NONE', #191879, #141200, #244387, .T. ) ;
#159518=VECTOR ( 'NONE', #552, 1000.000000000000000 ) ;
#159548=EDGE_CURVE ( 'NONE', #179560, #111061, #198594, .T. ) ;
#159590=CARTESIAN_POINT ( 'NONE',  ( 23.24999999999999645, 1.115600667400684642E-11, -200.9999999999999432 ) ) ;
#159597=VECTOR ( 'NONE', #210159, 1000.000000000000000 ) ;
#159610=CARTESIAN_POINT ( 'NONE',  ( 21.17356465864818915, 0.09891124102502621418, -161.0771968737582540 ) ) ;
#159614=VERTEX_POINT ( 'NONE', #156400 ) ;
#159617=DIRECTION ( 'NONE',  ( 2.694716079187272946E-16, -1.000000000000000000, 0.000000000000000000 ) ) ;
#159621=ADVANCED_FACE ( 'NONE', ( #235887 ), #57238, .F. ) ;
#159629=DIRECTION ( 'NONE',  ( 1.000000000000000000, 0.000000000000000000, -0.000000000000000000 ) ) ;
#159636=ORIENTED_EDGE ( 'NONE', *, *, #180911, .F. ) ;
#159641=AXIS2_PLACEMENT_3D ( 'NONE', #79473, #218991, #40405 ) ;
#159647=CARTESIAN_POINT ( 'NONE',  ( -23.25000000000000000, 5.950000000011167245, -190.6942976949651438 ) ) ;
#159673=CARTESIAN_POINT ( 'NONE',  ( 21.05000000000000071, 8.776282895303632259, -179.6499999999999773 ) ) ;
#159681=CARTESIAN_POINT ( 'NONE',  ( 21.05000000000000071, 10.72371681401022592, -175.0943992358841683 ) ) ;
#159711=ORIENTED_EDGE ( 'NONE', *, *, #59561, .F. ) ;
#159739=CARTESIAN_POINT ( 'NONE',  ( 21.05000000000000071, -8.663551401858002876, -177.0241011180672785 ) ) ;
#159756=CARTESIAN_POINT ( 'NONE',  ( -21.37071067811865532, 8.070710678129811910, -188.6499999999999488 ) ) ;
#159789=EDGE_CURVE ( 'NONE', #252796, #221674, #19742, .T. ) ;
#159838=ORIENTED_EDGE ( 'NONE', *, *, #64078, .F. ) ;
#159895=ORIENTED_EDGE ( 'NONE', *, *, #98151, .F. ) ;
#159897=DIRECTION ( 'NONE',  ( 2.940209281316622495E-16, -1.000000000000000000, 2.352167425053297996E-15 ) ) ;
#159932=EDGE_LOOP ( 'NONE', ( #158171, #100441, #166019, #202038 ) ) ;
#159944=VERTEX_POINT ( 'NONE', #158648 ) ;
#159948=AXIS2_PLACEMENT_3D ( 'NONE', #43883, #244636, #26914 ) ;
#159969=ORIENTED_EDGE ( 'NONE', *, *, #93239, .F. ) ;
#159992=AXIS2_PLACEMENT_3D ( 'NONE', #5455, #2895, #122874 ) ;
#160023=CARTESIAN_POINT ( 'NONE',  ( 20.04142135623730070, 11.75000000001115907, -155.7499999999999716 ) ) ;
#160051=DIRECTION ( 'NONE',  ( 1.000000000000000000, 0.000000000000000000, 0.000000000000000000 ) ) ;
#160077=EDGE_LOOP ( 'NONE', ( #240284, #45952, #47795, #246937 ) ) ;
#160110=TOROIDAL_SURFACE ( 'NONE', #210171, 0.2000000000000000111, 0.1000000000000000056 ) ;
#160128=CARTESIAN_POINT ( 'NONE',  ( 20.94999999999999574, -1.162701749926853712, -175.5999999999999659 ) ) ;
#160131=CARTESIAN_POINT ( 'NONE',  ( 20.85000000000000142, 7.070967871809997973, -204.7465642218682547 ) ) ;
#160159=CARTESIAN_POINT ( 'NONE',  ( 20.94999999999999574, -11.48912529306490349, -170.4999999999999716 ) ) ;
#160170=LINE ( 'NONE', #200546, #125484 ) ;
#160186=CARTESIAN_POINT ( 'NONE',  ( -23.25000000000000000, 1.115600667400684642E-11, -200.9999999999999432 ) ) ;
#160190=VERTEX_POINT ( 'NONE', #30690 ) ;
#160199=DIRECTION ( 'NONE',  ( 2.952720810173289112E-16, -1.000000000000000000, 0.000000000000000000 ) ) ;
#160215=AXIS2_PLACEMENT_3D ( 'NONE', #199829, #144948, #43309 ) ;
#160260=CARTESIAN_POINT ( 'NONE',  ( 23.14999999999998437, 11.75000000001115552, -167.4999999999999716 ) ) ;
#160305=DIRECTION ( 'NONE',  ( 1.000000000000000000, 0.000000000000000000, 0.000000000000000000 ) ) ;
#160339=DIRECTION ( 'NONE',  ( -3.469446951953635015E-14, -1.000000000000000000, 0.000000000000000000 ) ) ;
#160359=DIRECTION ( 'NONE',  ( 1.000000000000000000, -0.000000000000000000, -0.000000000000000000 ) ) ;
#160380=CYLINDRICAL_SURFACE ( 'NONE', #6565, 2.000000000000001776 ) ;
#160401=LINE ( 'NONE', #239922, #84748 ) ;
#160410=DIRECTION ( 'NONE',  ( -0.000000000000000000, 0.000000000000000000, -1.000000000000000000 ) ) ;
#160412=CARTESIAN_POINT ( 'NONE',  ( 21.14999999999999503, 1.115600667400684642E-11, -161.2499999999999716 ) ) ;
#160455=DIRECTION ( 'NONE',  ( 1.000000000000000000, 0.000000000000000000, 0.000000000000000000 ) ) ;
#160457=ORIENTED_EDGE ( 'NONE', *, *, #129078, .T. ) ;
#160472=ORIENTED_EDGE ( 'NONE', *, *, #170322, .T. ) ;
#160521=AXIS2_PLACEMENT_3D ( 'NONE', #117736, #18638, #89480 ) ;
#160527=CARTESIAN_POINT ( 'NONE',  ( -18.50000000000000000, 1.115600667400684642E-11, -200.9999999999999432 ) ) ;
#160530=ORIENTED_EDGE ( 'NONE', *, *, #5773, .T. ) ;
#160532=CARTESIAN_POINT ( 'NONE',  ( -18.59999999999999787, 11.65000000001115232, -174.4148057706539987 ) ) ;
#160540=AXIS2_PLACEMENT_3D ( 'NONE', #155951, #136323, #118080 ) ;
#160579=VERTEX_POINT ( 'NONE', #91616 ) ;
#160584=EDGE_CURVE ( 'NONE', #233370, #254577, #91012, .T. ) ;
#160589=AXIS2_PLACEMENT_3D ( 'NONE', #16601, #256401, #56952 ) ;
#160605=DIRECTION ( 'NONE',  ( 1.000000000000000000, 0.000000000000000000, -0.000000000000000000 ) ) ;
#160622=AXIS2_PLACEMENT_3D ( 'NONE', #165856, #206252, #8060 ) ;
#160627=CYLINDRICAL_SURFACE ( 'NONE', #229208, 0.09999999999999939493 ) ;
#160632=ORIENTED_EDGE ( 'NONE', *, *, #219311, .F. ) ;
#160641=FACE_OUTER_BOUND ( 'NONE', #93387, .T. ) ;
#160649=CARTESIAN_POINT ( 'NONE',  ( -18.59999999999999787, -1.835859311432481045, -212.5044391687984842 ) ) ;
#160671=LINE ( 'NONE', #36881, #90069 ) ;
#160692=EDGE_CURVE ( 'NONE', #69026, #118647, #253245, .T. ) ;
#160706=DIRECTION ( 'NONE',  ( 0.000000000000000000, 0.000000000000000000, -1.000000000000000000 ) ) ;
#160726=AXIS2_PLACEMENT_3D ( 'NONE', #232998, #13936, #128749 ) ;
#160729=CARTESIAN_POINT ( 'NONE',  ( -18.59999999999999787, 9.350000000011156942, -179.8499999999999943 ) ) ;
#160730=AXIS2_PLACEMENT_3D ( 'NONE', #204889, #86211, #67959 ) ;
#160762=ORIENTED_EDGE ( 'NONE', *, *, #244680, .F. ) ;
#160767=EDGE_LOOP ( 'NONE', ( #137584, #240981, #69980 ) ) ;
#160786=EDGE_LOOP ( 'NONE', ( #224962, #241582, #230959, #78282 ) ) ;
#160791=AXIS2_PLACEMENT_3D ( 'NONE', #35216, #209976, #173467 ) ;
#160800=ORIENTED_EDGE ( 'NONE', *, *, #6977, .T. ) ;
#160804=ORIENTED_EDGE ( 'NONE', *, *, #98846, .F. ) ;
#160831=ORIENTED_EDGE ( 'NONE', *, *, #158048, .T. ) ;
#160833=VECTOR ( 'NONE', #123967, 1000.000000000000000 ) ;
#160852=DIRECTION ( 'NONE',  ( 0.000000000000000000, -0.8660254037844384856, 0.5000000000000003331 ) ) ;
#160929=CARTESIAN_POINT ( 'NONE',  ( -20.64999999999999858, 7.150000000011155876, -179.7499999999999716 ) ) ;
#160930=ORIENTED_EDGE ( 'NONE', *, *, #31028, .T. ) ;
#160944=ADVANCED_FACE ( 'NONE', ( #105709 ), #16201, .T. ) ;
#160946=VERTEX_POINT ( 'NONE', #65326 ) ;
#160964=CARTESIAN_POINT ( 'NONE',  ( 21.07964655665547582, 8.774889614989714204, -179.7219165829640417 ) ) ;
#160969=CARTESIAN_POINT ( 'NONE',  ( 21.05000000000000071, 6.540656951712400691, -167.5999999999999659 ) ) ;
#160981=VECTOR ( 'NONE', #194291, 999.9999999999998863 ) ;
#160997=ORIENTED_EDGE ( 'NONE', *, *, #134574, .T. ) ;
#161078=CARTESIAN_POINT ( 'NONE',  ( 21.14999999999999503, 11.65000000001116298, -167.4999999999999716 ) ) ;
#161082=ORIENTED_EDGE ( 'NONE', *, *, #76993, .T. ) ;
#161085=EDGE_CURVE ( 'NONE', #43467, #70620, #53475, .T. ) ;
#161131=CYLINDRICAL_SURFACE ( 'NONE', #118437, 0.09999999999998898659 ) ;
#161139=ORIENTED_EDGE ( 'NONE', *, *, #209238, .T. ) ;
#161158=ORIENTED_EDGE ( 'NONE', *, *, #67026, .T. ) ;
#161196=DIRECTION ( 'NONE',  ( 0.000000000000000000, -0.8660254037844411501, -0.4999999999999956146 ) ) ;
#161207=VECTOR ( 'NONE', #155094, 1000.000000000000000 ) ;
#161224=DIRECTION ( 'NONE',  ( 0.000000000000000000, 1.561251128379298294E-13, 1.000000000000000000 ) ) ;
#161227=DIRECTION ( 'NONE',  ( 0.000000000000000000, 0.000000000000000000, -1.000000000000000000 ) ) ;
#161228=CARTESIAN_POINT ( 'NONE',  ( 20.94999999999999929, -8.999999999988844479, -177.3939691226524076 ) ) ;
#161229=AXIS2_PLACEMENT_3D ( 'NONE', #91768, #206575, #8387 ) ;
#161238=EDGE_CURVE ( 'NONE', #54023, #72236, #57848, .T. ) ;
#161240=B_SPLINE_CURVE_WITH_KNOTS ( 'NONE', 3,
 ( #218263, #119196, #57908, #157045, #32300, #152249 ),
 .UNSPECIFIED., .F., .F.,
 ( 4, 2, 4 ),
 ( 1.138412281109779656E-18, 0.0001569047307838639517, 0.0003138094615677267650 ),
 .UNSPECIFIED. ) ;
#161249=DIRECTION ( 'NONE',  ( 0.000000000000000000, 0.000000000000000000, 1.000000000000000000 ) ) ;
#161263=DIRECTION ( 'NONE',  ( -1.000000000000000000, -0.000000000000000000, -0.000000000000000000 ) ) ;
#161268=CARTESIAN_POINT ( 'NONE',  ( 18.50000000000000711, 10.37342005529115241, -192.2657881246250042 ) ) ;
#161366=DIRECTION ( 'NONE',  ( 1.000000000000000000, -0.000000000000000000, -0.000000000000000000 ) ) ;
#161398=EDGE_CURVE ( 'NONE', #51843, #19120, #137485, .T. ) ;
#161399=DIRECTION ( 'NONE',  ( 0.000000000000000000, 0.000000000000000000, -1.000000000000000000 ) ) ;
#161416=FACE_OUTER_BOUND ( 'NONE', #13647, .T. ) ;
#161427=CIRCLE ( 'NONE', #82263, 0.09999999999998898659 ) ;
#161447=CARTESIAN_POINT ( 'NONE',  ( 18.59999999999999076, 6.450000000011156587, -177.5170271704400022 ) ) ;
#161468=CARTESIAN_POINT ( 'NONE',  ( -21.11927991906891222, 0.009083679485029434036, -161.0515068815084589 ) ) ;
#161487=EDGE_LOOP ( 'NONE', ( #224127, #8837, #160804, #124915 ) ) ;
#161488=SPHERICAL_SURFACE ( 'NONE', #208695, 0.1000000000000000056 ) ;
#161549=CARTESIAN_POINT ( 'NONE',  ( 20.94999999999999929, 1.360870587203197646, -175.5729979270909382 ) ) ;
#161562=DIRECTION ( 'NONE',  ( 1.000000000000000000, -0.000000000000000000, -0.000000000000000000 ) ) ;
#161586=ADVANCED_FACE ( 'NONE', ( #241741 ), #70560, .T. ) ;
#161593=AXIS2_PLACEMENT_3D ( 'NONE', #183476, #243436, #218721 ) ;
#161610=TOROIDAL_SURFACE ( 'NONE', #165704, 0.2000000000000000111, 0.1000000000000000056 ) ;
#161617=AXIS2_PLACEMENT_3D ( 'NONE', #256902, #168172, #224236 ) ;
#161629=EDGE_LOOP ( 'NONE', ( #166109, #222629, #213586, #119455 ) ) ;
#161661=AXIS2_PLACEMENT_3D ( 'NONE', #127133, #206675, #8484 ) ;
#161688=DIRECTION ( 'NONE',  ( 0.000000000000000000, -0.1350103645451876666, 0.9908441862701600211 ) ) ;
#161719=EDGE_CURVE ( 'NONE', #43643, #129705, #11714, .T. ) ;
#161769=ADVANCED_FACE ( 'NONE', ( #185022 ), #85889, .T. ) ;
#161779=EDGE_LOOP ( 'NONE', ( #31207, #62556, #169496, #250094 ) ) ;
#161785=EDGE_CURVE ( 'NONE', #119397, #3198, #190800, .T. ) ;
#161823=EDGE_CURVE ( 'NONE', #9380, #62433, #252682, .T. ) ;
#161831=TOROIDAL_SURFACE ( 'NONE', #82652, 0.2000000000000000111, 0.1000000000000000056 ) ;
#161842=ORIENTED_EDGE ( 'NONE', *, *, #106496, .F. ) ;
#161852=ADVANCED_FACE ( 'NONE', ( #51904 ), #28572, .T. ) ;
#161858=ORIENTED_EDGE ( 'NONE', *, *, #101570, .T. ) ;
#161880=DIRECTION ( 'NONE',  ( -1.000000000000000000, -0.000000000000000000, -0.000000000000000000 ) ) ;
#161900=EDGE_CURVE ( 'NONE', #227765, #68874, #20080, .T. ) ;
#161913=CARTESIAN_POINT ( 'NONE',  ( 20.85000000000000142, 0.1610488207298751417, -200.7158101556397582 ) ) ;
#161923=EDGE_CURVE ( 'NONE', #182666, #113374, #103258, .T. ) ;
#161941=DIRECTION ( 'NONE',  ( 0.000000000000000000, 0.8660254037844352659, -0.5000000000000058842 ) ) ;
#161951=FACE_OUTER_BOUND ( 'NONE', #108622, .T. ) ;
#161952=CARTESIAN_POINT ( 'NONE',  ( 20.94999999999999929, 8.776282895303632259, -188.7499999999999716 ) ) ;
#162002=DIRECTION ( 'NONE',  ( 1.000000000000000000, -0.000000000000000000, -0.000000000000000000 ) ) ;
#162135=DIRECTION ( 'NONE',  ( 0.000000000000000000, 0.000000000000000000, -1.000000000000000000 ) ) ;
#162169=ORIENTED_EDGE ( 'NONE', *, *, #34963, .T. ) ;
#162174=DIRECTION ( 'NONE',  ( 1.000000000000000000, 0.000000000000000000, 0.000000000000000000 ) ) ;
#162200=EDGE_CURVE ( 'NONE', #90934, #87279, #128588, .T. ) ;
#162224=CARTESIAN_POINT ( 'NONE',  ( 22.39999999999999503, 0.1000000000111554016, -159.7092204016265669 ) ) ;
#162229=ADVANCED_FACE ( 'NONE', ( #23765 ), #11912, .T. ) ;
#162243=ORIENTED_EDGE ( 'NONE', *, *, #58975, .T. ) ;
#162259=ADVANCED_FACE ( 'NONE', ( #238938 ), #74467, .F. ) ;
#162280=FILL_AREA_STYLE ('',( #85254 ) ) ;
#162302=LINE ( 'NONE', #64478, #38733 ) ;
#162425=CARTESIAN_POINT ( 'NONE',  ( -20.94999999999999929, 11.75000000001115552, -174.5148057706539930 ) ) ;
#162556=AXIS2_PLACEMENT_3D ( 'NONE', #220136, #178463, #197985 ) ;
#162557=CARTESIAN_POINT ( 'NONE',  ( 18.49999999999999289, 10.25000000001115730, -192.1499999999999773 ) ) ;
#162569=DIRECTION ( 'NONE',  ( -1.000000000000000000, -2.952720810173289112E-16, 0.000000000000000000 ) ) ;
#162570=AXIS2_PLACEMENT_3D ( 'NONE', #219256, #79728, #60181 ) ;
#162617=LINE ( 'NONE', #143015, #209881 ) ;
#162659=ADVANCED_FACE ( 'NONE', ( #61268 ), #41724, .T. ) ;
#162661=EDGE_LOOP ( 'NONE', ( #117500, #216668, #71262, #216093 ) ) ;
#162672=CARTESIAN_POINT ( 'NONE',  ( -23.25000000000000000, 1.115600667400684642E-11, -167.4999999999999716 ) ) ;
#162704=CARTESIAN_POINT ( 'NONE',  ( -20.94999999999999929, 7.031312794766356511, -204.6091509382272591 ) ) ;
#162710=CARTESIAN_POINT ( 'NONE',  ( 20.94999999999999929, -11.48912529306489994, -197.8999999999999773 ) ) ;
#162723=CARTESIAN_POINT ( 'NONE',  ( -21.05000000000000071, 11.65000000001115232, -174.2838656629781156 ) ) ;
#162728=VERTEX_POINT ( 'NONE', #2559 ) ;
#162732=ORIENTED_EDGE ( 'NONE', *, *, #196100, .F. ) ;
#162742=ORIENTED_EDGE ( 'NONE', *, *, #150030, .F. ) ;
#162754=CIRCLE ( 'NONE', #4320, 0.09999999999999939493 ) ;
#162760=CIRCLE ( 'NONE', #25210, 0.09999999999998902822 ) ;
#162762=ORIENTED_EDGE ( 'NONE', *, *, #102149, .F. ) ;
#162780=DIRECTION ( 'NONE',  ( -1.000000000000000000, 0.000000000000000000, 0.000000000000000000 ) ) ;
#162825=ORIENTED_EDGE ( 'NONE', *, *, #31721, .F. ) ;
#162833=CARTESIAN_POINT ( 'NONE',  ( -20.64999999999999858, 2.000000000011154189, -188.1753780772378946 ) ) ;
#162837=CARTESIAN_POINT ( 'NONE',  ( -22.47071067811865319, 0.09909245471376178227, -159.7799252555018938 ) ) ;
#162838=CARTESIAN_POINT ( 'NONE',  ( 23.25000000000000000, 6.550000000011156231, -179.8499999999999943 ) ) ;
#162840=CARTESIAN_POINT ( 'NONE',  ( -21.05000000000000071, 6.257814610492677510, -167.4022097086907763 ) ) ;
#162844=ORIENTED_EDGE ( 'NONE', *, *, #252795, .F. ) ;
#162894=CARTESIAN_POINT ( 'NONE',  ( 23.14999999999999503, 11.65000000001116298, -179.6499999999999773 ) ) ;
#162905=CYLINDRICAL_SURFACE ( 'NONE', #3787, 0.5000000000000004441 ) ;
#162908=ORIENTED_EDGE ( 'NONE', *, *, #30563, .T. ) ;
#162911=CARTESIAN_POINT ( 'NONE',  ( -20.85000000000000142, 1.115600667400684642E-11, -200.9999999999999432 ) ) ;
#162912=ORIENTED_EDGE ( 'NONE', *, *, #177464, .F. ) ;
#162915=ORIENTED_EDGE ( 'NONE', *, *, #49005, .F. ) ;
#162917=CARTESIAN_POINT ( 'NONE',  ( 23.14999999999999858, 5.600000000011153389, -179.9052660189130677 ) ) ;
#162918=DIRECTION ( 'NONE',  ( 0.000000000000000000, 0.000000000000000000, 1.000000000000000000 ) ) ;
#162974=DIRECTION ( 'NONE',  ( 1.000000000000000000, -0.000000000000000000, -0.000000000000000000 ) ) ;
#163011=CARTESIAN_POINT ( 'NONE',  ( -22.50000000000000000, 1.115600667400684642E-11, -155.8504291924551808 ) ) ;
#163031=FACE_OUTER_BOUND ( 'NONE', #118361, .T. ) ;
#163043=CARTESIAN_POINT ( 'NONE',  ( -21.05000000000000071, 1.115600667400684642E-11, -167.4999999999999716 ) ) ;
#163054=ORIENTED_EDGE ( 'NONE', *, *, #99604, .F. ) ;
#163088=CARTESIAN_POINT ( 'NONE',  ( -21.15000000000000213, 1.115526128501326264E-11, -160.9593430482987344 ) ) ;
#163089=VERTEX_POINT ( 'NONE', #137905 ) ;
#163140=CARTESIAN_POINT ( 'NONE',  ( 21.05000000000000071, 11.60000000001116227, -194.0717967697244717 ) ) ;
#163141=CARTESIAN_POINT ( 'NONE',  ( 21.05000000000000071, 6.450000000011156587, -177.5170271704400022 ) ) ;
#163166=AXIS2_PLACEMENT_3D ( 'NONE', #183411, #4738, #106406 ) ;
#163175=EDGE_CURVE ( 'NONE', #152513, #88951, #184737, .T. ) ;
#163254=CYLINDRICAL_SURFACE ( 'NONE', #247700, 7.899999999999990585 ) ;
#163289=AXIS2_PLACEMENT_3D ( 'NONE', #148779, #225699, #206174 ) ;
#163304=ORIENTED_EDGE ( 'NONE', *, *, #251615, .F. ) ;
#163324=CARTESIAN_POINT ( 'NONE',  ( 21.13461538461538325, 10.61458296203669249, -179.8499999999999943 ) ) ;
#163335=VECTOR ( 'NONE', #186983, 1000.000000000000000 ) ;
#163349=ORIENTED_EDGE ( 'NONE', *, *, #207150, .T. ) ;
#163380=AXIS2_PLACEMENT_3D ( 'NONE', #1227, #160359, #61225 ) ;
#163390=VERTEX_POINT ( 'NONE', #88184 ) ;
#163391=CARTESIAN_POINT ( 'NONE',  ( -20.64999999999999858, -8.999999999988844479, -191.1060308773475356 ) ) ;
#163403=CIRCLE ( 'NONE', #130638, 0.1999999999999987899 ) ;
#163443=DIRECTION ( 'NONE',  ( 0.000000000000000000, -1.000000000000000000, 0.000000000000000000 ) ) ;
#163489=VERTEX_POINT ( 'NONE', #38522 ) ;
#163522=CARTESIAN_POINT ( 'NONE',  ( 21.05000000000000426, 6.258817194692633201, -167.4663672646663599 ) ) ;
#163537=DIRECTION ( 'NONE',  ( 1.000000000000000000, 0.000000000000000000, -0.000000000000000000 ) ) ;
#163597=EDGE_CURVE ( 'NONE', #190383, #156526, #125054, .T. ) ;
#163608=( BOUNDED_SURFACE ( )  B_SPLINE_SURFACE ( 3, 2, ( 
 ( #109996, #189556, #209101 ),
 ( #86558, #65741, #246934 ),
 ( #10919, #210407, #145260 ),
 ( #206537, #48736, #166164 ) ),
 .UNSPECIFIED., .F., .F., .F. ) 
 B_SPLINE_SURFACE_WITH_KNOTS ( ( 4, 4 ),
 ( 3, 3 ),
 ( 0.04058434257139457990, 0.04256401539001584966 ),
 ( 0.000000000000000000, 1.000000000000000000 ),
 .UNSPECIFIED. ) 
 GEOMETRIC_REPRESENTATION_ITEM ( )  RATIONAL_B_SPLINE_SURFACE ( (
 ( 1.000000000000000000, 0.7103081912007809251, 1.000000000000000000),
 ( 1.000000000000000000, 0.7104998333556791223, 1.000000000000000000),
 ( 1.000000000000000000, 0.7107238315753988678, 1.000000000000000000),
 ( 1.000000000000000000, 0.7110073749539779220, 1.000000000000000000) ) ) 
 REPRESENTATION_ITEM ( '' )  SURFACE ( )  );
#163610=EDGE_LOOP ( 'NONE', ( #33774, #43415, #50442, #219980 ) ) ;
#163641=AXIS2_PLACEMENT_3D ( 'NONE', #51263, #128274, #133411 ) ;
#163654=FACE_OUTER_BOUND ( 'NONE', #76234, .T. ) ;
#163670=EDGE_CURVE ( 'NONE', #108752, #117253, #29394, .T. ) ;
#163671=FACE_OUTER_BOUND ( 'NONE', #201120, .T. ) ;
#163685=DIRECTION ( 'NONE',  ( 1.000000000000000000, 0.000000000000000000, 0.000000000000000000 ) ) ;
#163705=VERTEX_POINT ( 'NONE', #110044 ) ;
#163718=CARTESIAN_POINT ( 'NONE',  ( -18.59999999999999787, 11.65000000001115232, -174.5148057706539930 ) ) ;
#163720=CARTESIAN_POINT ( 'NONE',  ( 23.14999999999998437, 1.115600667400684642E-11, -167.4999999999999716 ) ) ;
#163736=CIRCLE ( 'NONE', #30483, 0.09999999999999939493 ) ;
#163744=DIRECTION ( 'NONE',  ( 1.000000000000000000, 0.000000000000000000, -0.000000000000000000 ) ) ;
#163795=DIRECTION ( 'NONE',  ( 1.000000000000000000, 7.304098846218134667E-16, 0.000000000000000000 ) ) ;
#163806=CARTESIAN_POINT ( 'NONE',  ( -20.94999999999999929, -1.362429037182149694, -208.8888812479211765 ) ) ;
#163826=CARTESIAN_POINT ( 'NONE',  ( 18.49999999999999289, 10.25000000263022493, -192.1871719496316473 ) ) ;
#163843=FACE_OUTER_BOUND ( 'NONE', #227535, .T. ) ;
#163859=ORIENTED_EDGE ( 'NONE', *, *, #153470, .T. ) ;
#163863=CIRCLE ( 'NONE', #209655, 0.09999999999999939493 ) ;
#163876=LINE ( 'NONE', #30479, #3330 ) ;
#163890=DIRECTION ( 'NONE',  ( 1.000000000000000000, 0.000000000000000000, 0.000000000000000000 ) ) ;
#163896=ORIENTED_EDGE ( 'NONE', *, *, #134287, .F. ) ;
#163911=DIRECTION ( 'NONE',  ( -0.000000000000000000, -0.000000000000000000, -1.000000000000000000 ) ) ;
#163912=FACE_OUTER_BOUND ( 'NONE', #237957, .T. ) ;
#163931=CARTESIAN_POINT ( 'NONE',  ( 18.49999999999999289, 6.450000000011156587, -177.5170271704400022 ) ) ;
#164001=CARTESIAN_POINT ( 'NONE',  ( -20.94999999999999929, 11.60000000001115161, -174.4282032302755283 ) ) ;
#164005=ADVANCED_FACE ( 'NONE', ( #242829 ), #139975, .T. ) ;
#164013=AXIS2_PLACEMENT_3D ( 'NONE', #173759, #17217, #18486 ) ;
#164096=EDGE_LOOP ( 'NONE', ( #129420, #209975, #186691, #220384 ) ) ;
#164101=AXIS2_PLACEMENT_3D ( 'NONE', #107952, #64965, #66264 ) ;
#164152=CYLINDRICAL_SURFACE ( 'NONE', #6426, 2.000000000000001776 ) ;
#164170=LINE ( 'NONE', #243695, #107826 ) ;
#164194=CARTESIAN_POINT ( 'NONE',  ( -20.64999999999999858, 4.350000000011156054, -188.6499999999999488 ) ) ;
#164200=FACE_OUTER_BOUND ( 'NONE', #121535, .T. ) ;
#164241=CARTESIAN_POINT ( 'NONE',  ( -23.15000000000000213, 5.950000000011163692, -190.6942976949651438 ) ) ;
#164270=ORIENTED_EDGE ( 'NONE', *, *, #200770, .T. ) ;
#164285=FACE_OUTER_BOUND ( 'NONE', #128904, .T. ) ;
#164290=CARTESIAN_POINT ( 'NONE',  ( -18.59999999999999787, 11.75000000001115197, -155.7499999999999716 ) ) ;
#164343=AXIS2_PLACEMENT_3D ( 'NONE', #169871, #129409, #208946 ) ;
#164351=ORIENTED_EDGE ( 'NONE', *, *, #61793, .T. ) ;
#164352=DIRECTION ( 'NONE',  ( 0.000000000000000000, -0.9893560106964500722, 0.1455152366551550613 ) ) ;
#164358=ORIENTED_EDGE ( 'NONE', *, *, #257148, .T. ) ;
#164403=CIRCLE ( 'NONE', #51937, 11.75000000000001066 ) ;
#164417=ORIENTED_EDGE ( 'NONE', *, *, #177624, .T. ) ;
#164430=ORIENTED_EDGE ( 'NONE', *, *, #249208, .T. ) ;
#164444=DIRECTION ( 'NONE',  ( -1.000000000000000000, -7.304098846218134667E-16, 0.000000000000000000 ) ) ;
#164447=CARTESIAN_POINT ( 'NONE',  ( 18.59999999999999432, 5.699452464332755319, -154.9577260434301422 ) ) ;
#164471=CARTESIAN_POINT ( 'NONE',  ( -18.59999999999999787, 1.750000000011155743, -179.1695115579016147 ) ) ;
#164484=CARTESIAN_POINT ( 'NONE',  ( 20.95512820512820440, 8.876151316299271343, -179.6499999999999773 ) ) ;
#164517=CARTESIAN_POINT ( 'NONE',  ( -20.64999999999999858, 4.350000000011156054, -188.6499999999999488 ) ) ;
#164571=TOROIDAL_SURFACE ( 'NONE', #235272, 11.65000000000000036, 0.1000000000000000056 ) ;
#164584=DIRECTION ( 'NONE',  ( -0.000000000000000000, -1.000000000000000000, 0.000000000000000000 ) ) ;
#164585=AXIS2_PLACEMENT_3D ( 'NONE', #78022, #121042, #239678 ) ;
#164595=CARTESIAN_POINT ( 'NONE',  ( -18.50000000000000000, -9.399999999988850163, -207.8820418481726335 ) ) ;
#164607=CARTESIAN_POINT ( 'NONE',  ( 23.14999999999999147, 4.150000000011154988, -167.4999999999999716 ) ) ;
#164614=CIRCLE ( 'NONE', #177106, 0.09999999999998898659 ) ;
#164617=ADVANCED_FACE ( 'NONE', ( #124525 ), #46275, .T. ) ;
#164654=CARTESIAN_POINT ( 'NONE',  ( -23.15000000000000213, -8.596261682231835621, -176.9501275171502641 ) ) ;
#164666=VERTEX_POINT ( 'NONE', #85352 ) ;
#164730=CARTESIAN_POINT ( 'NONE',  ( 20.94999999999999929, 5.500000000011153745, -188.5947339810868755 ) ) ;
#164739=ADVANCED_FACE ( 'NONE', ( #149238 ), #50102, .F. ) ;
#164740=VECTOR ( 'NONE', #165641, 1000.000000000000000 ) ;
#164755=EDGE_CURVE ( 'NONE', #165951, #147926, #129851, .T. ) ;
#164763=CARTESIAN_POINT ( 'NONE',  ( -23.25000000000000000, -8.999999999988846255, -177.3939691226524076 ) ) ;
#164790=CIRCLE ( 'NONE', #119014, 0.09999999999999939493 ) ;
#164792=CARTESIAN_POINT ( 'NONE',  ( -20.94999999999999929, 1.162701749949165642, -175.3999999999999773 ) ) ;
#164802=CARTESIAN_POINT ( 'NONE',  ( 21.14250536705908345, 6.518172176891879666, -167.4999999999999716 ) ) ;
#164813=EDGE_CURVE ( 'NONE', #180362, #199601, #233918, .T. ) ;
#164818=CARTESIAN_POINT ( 'NONE',  ( 21.05000000000000071, 10.72371710471867701, -179.6611902941274082 ) ) ;
#164838=SURFACE_SIDE_STYLE ('',( #241794 ) ) ;
#164870=EDGE_CURVE ( 'NONE', #32118, #96541, #167306, .T. ) ;
#164882=ADVANCED_FACE ( 'NONE', ( #67949 ), #23724, .T. ) ;
#164906=FACE_OUTER_BOUND ( 'NONE', #235768, .T. ) ;
#164912=CARTESIAN_POINT ( 'NONE',  ( -21.05000000000000071, 6.400000000011158541, -177.4304246300615375 ) ) ;
#164931=EDGE_CURVE ( 'NONE', #152772, #55017, #254717, .T. ) ;
#164956=ORIENTED_EDGE ( 'NONE', *, *, #153470, .F. ) ;
#164958=ORIENTED_EDGE ( 'NONE', *, *, #206618, .F. ) ;
#164960=AXIS2_PLACEMENT_3D ( 'NONE', #71106, #172801, #208050 ) ;
#165021=AXIS2_PLACEMENT_3D ( 'NONE', #226206, #127150, #227523 ) ;
#165040=CARTESIAN_POINT ( 'NONE',  ( -20.64999999999999858, 4.250000000011156409, -188.6499999999999488 ) ) ;
#165055=EDGE_CURVE ( 'NONE', #52860, #154991, #54790, .T. ) ;
#165064=DIRECTION ( 'NONE',  ( -3.265361837132813093E-16, 1.000000000000000000, 0.000000000000000000 ) ) ;
#165066=LINE ( 'NONE', #82926, #26028 ) ;
#165069=CARTESIAN_POINT ( 'NONE',  ( 21.05000000000000071, -1.360870587180885716, -175.5729979270909382 ) ) ;
#165092=ADVANCED_FACE ( 'NONE', ( #156515 ), #100323, .T. ) ;
#165107=AXIS2_PLACEMENT_3D ( 'NONE', #58163, #118164, #79003 ) ;
#165125=ADVANCED_FACE ( 'NONE', ( #58635 ), #150891, .T. ) ;
#165131=ORIENTED_EDGE ( 'NONE', *, *, #125972, .T. ) ;
#165157=CARTESIAN_POINT ( 'NONE',  ( -20.85000000000000497, 11.75000000001115019, -194.0808527540412456 ) ) ;
#165176=DIRECTION ( 'NONE',  ( 0.000000000000000000, 0.8700118002898321601, -0.4930308989875230030 ) ) ;
#165180=DIRECTION ( 'NONE',  ( 0.000000000000000000, 0.000000000000000000, -1.000000000000000000 ) ) ;
#165181=AXIS2_PLACEMENT_3D ( 'NONE', #182921, #222002, #122941 ) ;
#165208=CARTESIAN_POINT ( 'NONE',  ( 20.51284917709620359, 10.31088662285602275, -175.1724731855919686 ) ) ;
#165219=VECTOR ( 'NONE', #74692, 1000.000000000000000 ) ;
#165254=ADVANCED_FACE ( 'NONE', ( #215316 ), #30122, .T. ) ;
#165277=VECTOR ( 'NONE', #115428, 1000.000000000000000 ) ;
#165307=DIRECTION ( 'NONE',  ( -1.000000000000000000, 0.000000000000000000, -0.000000000000000000 ) ) ;
#165309=AXIS2_PLACEMENT_3D ( 'NONE', #128721, #169159, #109134 ) ;
#165354=DIRECTION ( 'NONE',  ( 1.000000000000000000, 3.265361837132813093E-16, -0.000000000000000000 ) ) ;
#165359=VECTOR ( 'NONE', #227526, 1000.000000000000000 ) ;
#165361=CYLINDRICAL_SURFACE ( 'NONE', #127592, 0.5000000000000004441 ) ;
#165396=ORIENTED_EDGE ( 'NONE', *, *, #213163, .T. ) ;
#165409=LINE ( 'NONE', #208400, #128143 ) ;
#165418=ORIENTED_EDGE ( 'NONE', *, *, #108168, .F. ) ;
#165423=DIRECTION ( 'NONE',  ( 1.000000000000000000, 2.952720810173289112E-16, -0.000000000000000000 ) ) ;
#165430=VECTOR ( 'NONE', #117308, 1000.000000000000000 ) ;
#165457=FACE_OUTER_BOUND ( 'NONE', #71637, .T. ) ;
#165459=DIRECTION ( 'NONE',  ( 1.000000000000000000, -0.000000000000000000, -0.000000000000000000 ) ) ;
#165482=CARTESIAN_POINT ( 'NONE',  ( -23.25000000000000000, 1.115600667400684642E-11, -208.8999999999999488 ) ) ;
#165498=CARTESIAN_POINT ( 'NONE',  ( 18.57071067811864040, 10.17928932189250091, -188.7499999999999716 ) ) ;
#165500=AXIS2_PLACEMENT_3D ( 'NONE', #20453, #63393, #157416 ) ;
#165511=AXIS2_PLACEMENT_3D ( 'NONE', #254149, #75558, #195506 ) ;
#165550=PLANE ( 'NONE',  #17559 ) ;
#165580=EDGE_CURVE ( 'NONE', #86132, #77947, #230187, .T. ) ;
#165596=DIRECTION ( 'NONE',  ( 0.000000000000000000, 0.000000000000000000, 1.000000000000000000 ) ) ;
#165621=VERTEX_POINT ( 'NONE', #211162 ) ;
#165637=CARTESIAN_POINT ( 'NONE',  ( 20.94999999999999574, 1.115600667400684642E-11, -167.4999999999999716 ) ) ;
#165641=DIRECTION ( 'NONE',  ( 1.000000000000000000, -0.000000000000000000, -0.000000000000000000 ) ) ;
#165651=CARTESIAN_POINT ( 'NONE',  ( 20.94999999999999929, 6.846123162363745074, -204.7377262668498190 ) ) ;
#165661=ORIENTED_EDGE ( 'NONE', *, *, #247347, .T. ) ;
#165667=CARTESIAN_POINT ( 'NONE',  ( 21.05000000000000071, -9.399999999988844834, -191.1060308773475072 ) ) ;
#165675=AXIS2_PLACEMENT_3D ( 'NONE', #148521, #26010, #185070 ) ;
#165678=ORIENTED_EDGE ( 'NONE', *, *, #101379, .T. ) ;
#165689=FACE_OUTER_BOUND ( 'NONE', #56121, .T. ) ;
#165704=AXIS2_PLACEMENT_3D ( 'NONE', #77401, #156986, #137381 ) ;
#165713=AXIS2_PLACEMENT_3D ( 'NONE', #10029, #132549, #153440 ) ;
#165741=CARTESIAN_POINT ( 'NONE',  ( -21.00448002041607864, 11.75000000001115552, -174.3483408623104935 ) ) ;
#165742=DIRECTION ( 'NONE',  ( 1.000000000000000000, -0.000000000000000000, -0.000000000000000000 ) ) ;
#165754=CARTESIAN_POINT ( 'NONE',  ( 23.15000000000000213, -8.999999999988844479, -177.3939691226524076 ) ) ;
#165783=DIRECTION ( 'NONE',  ( 0.7071067811865388020, -0.7071067811865561215, 0.000000000000000000 ) ) ;
#165798=EDGE_CURVE ( 'NONE', #27481, #493, #5304, .T. ) ;
#165801=AXIS2_PLACEMENT_3D ( 'NONE', #175581, #236809, #38626 ) ;
#165829=CARTESIAN_POINT ( 'NONE',  ( 20.94999999999999929, 10.72371710471868056, -179.6499999999999773 ) ) ;
#165856=CARTESIAN_POINT ( 'NONE',  ( 18.59999999999999076, 6.450000000011156587, -177.5170271704400022 ) ) ;
#165886=AXIS2_PLACEMENT_3D ( 'NONE', #137078, #216610, #217871 ) ;
#165896=ORIENTED_EDGE ( 'NONE', *, *, #67359, .F. ) ;
#165907=CARTESIAN_POINT ( 'NONE',  ( 22.49999999999999645, 11.64957080755595520, -167.3999999999999773 ) ) ;
#165951=VERTEX_POINT ( 'NONE', #94423 ) ;
#165976=VERTEX_POINT ( 'NONE', #193547 ) ;
#165985=ORIENTED_EDGE ( 'NONE', *, *, #228314, .T. ) ;
#165995=CARTESIAN_POINT ( 'NONE',  ( -18.50000000000000000, 7.120270961708746960, -204.6595630418393057 ) ) ;
#166015=VERTEX_POINT ( 'NONE', #72321 ) ;
#166019=ORIENTED_EDGE ( 'NONE', *, *, #212160, .F. ) ;
#166029=DIRECTION ( 'NONE',  ( 0.000000000000000000, 0.000000000000000000, 1.000000000000000000 ) ) ;
#166034=AXIS2_PLACEMENT_3D ( 'NONE', #24571, #4948, #104056 ) ;
#166075=CARTESIAN_POINT ( 'NONE',  ( 22.39999999999999503, 11.65000000001116298, -167.5999999999999659 ) ) ;
#166077=AXIS2_PLACEMENT_3D ( 'NONE', #143634, #244013, #245319 ) ;
#166097=EDGE_CURVE ( 'NONE', #210872, #227765, #23318, .T. ) ;
#166104=VECTOR ( 'NONE', #106819, 1000.000000000000000 ) ;
#166106=DIRECTION ( 'NONE',  ( 0.000000000000000000, 0.000000000000000000, -1.000000000000000000 ) ) ;
#166109=ORIENTED_EDGE ( 'NONE', *, *, #98846, .T. ) ;
#166120=CARTESIAN_POINT ( 'NONE',  ( 21.08884785362045378, 6.357193367436396514, -167.4502169049331144 ) ) ;
#166126=DIRECTION ( 'NONE',  ( 0.000000000000000000, 0.000000000000000000, 1.000000000000000000 ) ) ;
#166154=SPHERICAL_SURFACE ( 'NONE', #49724, 0.1000000000000000056 ) ;
#166164=CARTESIAN_POINT ( 'NONE',  ( -21.07094088545304089, 6.320167221927643020, -167.4011062974477682 ) ) ;
#166173=CARTESIAN_POINT ( 'NONE',  ( 20.94999999999999929, 1.115600667400684642E-11, -200.9999999999999432 ) ) ;
#166191=ORIENTED_EDGE ( 'NONE', *, *, #238430, .F. ) ;
#166210=DIRECTION ( 'NONE',  ( -1.000000000000000000, 0.000000000000000000, 0.000000000000000000 ) ) ;
#166211=CARTESIAN_POINT ( 'NONE',  ( 23.14999999999999503, 6.550000000011156231, -188.6499999999999488 ) ) ;
#166220=VERTEX_POINT ( 'NONE', #165995 ) ;
#166222=CARTESIAN_POINT ( 'NONE',  ( -22.50000000000000000, 1.115600667400684642E-11, -161.2499999999999716 ) ) ;
#166228=DIRECTION ( 'NONE',  ( 0.000000000000000000, 0.000000000000000000, -1.000000000000000000 ) ) ;
#166270=ORIENTED_EDGE ( 'NONE', *, *, #104444, .F. ) ;
#166278=CARTESIAN_POINT ( 'NONE',  ( -23.25000000000000000, 1.115600667400684642E-11, -167.4999999999999716 ) ) ;
#166285=ORIENTED_EDGE ( 'NONE', *, *, #127673, .F. ) ;
#166298=DIRECTION ( 'NONE',  ( 0.000000000000000000, 0.000000000000000000, -1.000000000000000000 ) ) ;
#166301=EDGE_CURVE ( 'NONE', #100439, #76299, #232379, .T. ) ;
#166302=EDGE_CURVE ( 'NONE', #16283, #175979, #12049, .T. ) ;
#166305=FACE_OUTER_BOUND ( 'NONE', #27100, .T. ) ;
#166309=EDGE_LOOP ( 'NONE', ( #189639, #65601, #113382, #136697, #238061 ) ) ;
#166334=CARTESIAN_POINT ( 'NONE',  ( -22.39999999999999858, 11.75000000001115552, -167.5999999999999659 ) ) ;
#166400=DIRECTION ( 'NONE',  ( 0.000000000000000000, 0.000000000000000000, 1.000000000000000000 ) ) ;
#166496=DIRECTION ( 'NONE',  ( 1.000000000000000000, -0.000000000000000000, -0.000000000000000000 ) ) ;
#166497=ORIENTED_EDGE ( 'NONE', *, *, #202681, .T. ) ;
#166509=DIRECTION ( 'NONE',  ( -6.938893903907224433E-15, 1.000000000000000000, 0.000000000000000000 ) ) ;
#166519=ORIENTED_EDGE ( 'NONE', *, *, #22907, .T. ) ;
#166552=ADVANCED_FACE ( 'NONE', ( #100511 ), #50893, .T. ) ;
#166567=DIRECTION ( 'NONE',  ( -0.000000000000000000, -0.000000000000000000, -1.000000000000000000 ) ) ;
#166587=CARTESIAN_POINT ( 'NONE',  ( 21.14999999999999858, 6.550000000011156231, -179.6499999999999773 ) ) ;
#166598=VECTOR ( 'NONE', #142058, 1000.000000000000114 ) ;
#166616=DIRECTION ( 'NONE',  ( 1.000000000000000000, -0.000000000000000000, -0.000000000000000000 ) ) ;
#166619=LINE ( 'NONE', #24534, #152919 ) ;
#166620=CARTESIAN_POINT ( 'NONE',  ( 21.05000000000000071, 1.115625160336667635E-11, -198.9999999999999432 ) ) ;
#166660=DIRECTION ( 'NONE',  ( 1.000000000000000000, 0.000000000000000000, 0.000000000000000000 ) ) ;
#166662=ORIENTED_EDGE ( 'NONE', *, *, #189210, .T. ) ;
#166672=DIRECTION ( 'NONE',  ( 0.000000000000000000, 0.000000000000000000, -1.000000000000000000 ) ) ;
#166721=ORIENTED_EDGE ( 'NONE', *, *, #207253, .T. ) ;
#166737=CARTESIAN_POINT ( 'NONE',  ( 21.14999999999999858, -11.64999999998883595, -167.4999999999999432 ) ) ;
#166762=CARTESIAN_POINT ( 'NONE',  ( 22.49806830649814060, 11.64988965485023620, -167.4225356836744538 ) ) ;
#166806=AXIS2_PLACEMENT_3D ( 'NONE', #109359, #127670, #106800 ) ;
#166811=CARTESIAN_POINT ( 'NONE',  ( -21.05000000000000071, 11.65000000001115588, -193.9851942293460070 ) ) ;
#166836=ORIENTED_EDGE ( 'NONE', *, *, #224514, .T. ) ;
#166908=DIRECTION ( 'NONE',  ( 0.000000000000000000, -1.000000000000000000, 0.000000000000000000 ) ) ;
#166924=CARTESIAN_POINT ( 'NONE',  ( -22.50000000000094147, 0.1000000000110504439, -155.8504291924551524 ) ) ;
#166942=FACE_OUTER_BOUND ( 'NONE', #74245, .T. ) ;
#166943=ORIENTED_EDGE ( 'NONE', *, *, #91634, .T. ) ;
#167000=CARTESIAN_POINT ( 'NONE',  ( -23.25000000000000000, 1.115600667400684642E-11, -171.5499999999999829 ) ) ;
#167007=CIRCLE ( 'NONE', #200281, 0.09999999999998898659 ) ;
#167039=FACE_OUTER_BOUND ( 'NONE', #222952, .T. ) ;
#167049=DIRECTION ( 'NONE',  ( -1.000000000000000000, -3.265361837132813093E-16, 0.000000000000000000 ) ) ;
#167065=LINE ( 'NONE', #164471, #242489 ) ;
#167085=CARTESIAN_POINT ( 'NONE',  ( 18.59999999999998721, 6.846123162363745074, -204.7377262668498190 ) ) ;
#167103=ORIENTED_EDGE ( 'NONE', *, *, #202893, .T. ) ;
#167110=DIRECTION ( 'NONE',  ( -0.000000000000000000, -0.2605042016806452532, -0.9654727137038777718 ) ) ;
#167111=CARTESIAN_POINT ( 'NONE',  ( -20.94999999999999929, 1.115600667400684642E-11, -200.9999999999999432 ) ) ;
#167124=DIRECTION ( 'NONE',  ( -0.000000000000000000, 0.1350103645451626311, 0.9908441862701635738 ) ) ;
#167130=CARTESIAN_POINT ( 'NONE',  ( -21.04999999999999716, -0.08574093702224822033, -161.0861737111870013 ) ) ;
#167142=EDGE_CURVE ( 'NONE', #22985, #43643, #15284, .T. ) ;
#167149=CARTESIAN_POINT ( 'NONE',  ( -18.59999999999999787, -1.835859311432484375, -212.5044391687984842 ) ) ;
#167152=CIRCLE ( 'NONE', #171428, 0.2000000000000057288 ) ;
#167158=FACE_OUTER_BOUND ( 'NONE', #9394, .T. ) ;
#167176=EDGE_CURVE ( 'NONE', #140280, #225193, #35240, .T. ) ;
#167190=CARTESIAN_POINT ( 'NONE',  ( -18.33981767444319289, -9.569575789792956755, -207.8191618437251407 ) ) ;
#167201=CARTESIAN_POINT ( 'NONE',  ( 21.03670563405603033, 10.62482368933940258, -179.8255468862091959 ) ) ;
#167246=VERTEX_POINT ( 'NONE', #195216 ) ;
#167306=CIRCLE ( 'NONE', #25813, 0.09999999999999363565 ) ;
#167352=ORIENTED_EDGE ( 'NONE', *, *, #4415, .T. ) ;
#167373=ORIENTED_EDGE ( 'NONE', *, *, #200702, .T. ) ;
#167387=CARTESIAN_POINT ( 'NONE',  ( 21.05000000000000071, -8.999999999988842703, -191.1060308773475072 ) ) ;
#167391=CARTESIAN_POINT ( 'NONE',  ( 21.08134388332232234, 6.334680580529113314, -167.4241810824929360 ) ) ;
#167416=CYLINDRICAL_SURFACE ( 'NONE', #163641, 4.049999999999998046 ) ;
#167424=( BOUNDED_CURVE ( )  B_SPLINE_CURVE ( 3, ( #17258, #96747, #14710, #75940 ),
 .UNSPECIFIED., .F., .F. ) 
 B_SPLINE_CURVE_WITH_KNOTS ( ( 4, 4 ),
 ( 1.570796326794896558, 3.141592653589793116 ),
 .UNSPECIFIED. ) 
 CURVE ( )  GEOMETRIC_REPRESENTATION_ITEM ( )  RATIONAL_B_SPLINE_CURVE ( ( 1.000000000000000000, 0.8047378541243649375, 0.8047378541243649375, 1.000000000000000000 ) ) 
 REPRESENTATION_ITEM ( '' )  );
#167429=DIRECTION ( 'NONE',  ( 1.000000000000000000, 0.000000000000000000, 0.000000000000000000 ) ) ;
#167445=CARTESIAN_POINT ( 'NONE',  ( -23.25000000000000000, -11.74999999998884448, -200.9999999999999432 ) ) ;
#167475=EDGE_LOOP ( 'NONE', ( #178443, #175928, #3034, #178393 ) ) ;
#167517=ADVANCED_FACE ( 'NONE', ( #189743 ), #208040, .F. ) ;
#167546=ORIENTED_EDGE ( 'NONE', *, *, #215678, .F. ) ;
#167558=EDGE_LOOP ( 'NONE', ( #131011, #104255, #49302, #156380 ) ) ;
#167599=CARTESIAN_POINT ( 'NONE',  ( 21.05000000000000071, -9.499999999988844479, -191.1060308773475072 ) ) ;
#167604=CARTESIAN_POINT ( 'NONE',  ( 20.85882249326303040, 10.33248238083634796, -206.5948465439131496 ) ) ;
#167628=CARTESIAN_POINT ( 'NONE',  ( 21.06086055315971350, 8.774707514967413857, -179.7023221551538938 ) ) ;
#167669=CARTESIAN_POINT ( 'NONE',  ( -20.94999999999999929, 1.115600667400684642E-11, -200.9999999999999432 ) ) ;
#167689=DIRECTION ( 'NONE',  ( -1.836970198721029934E-16, 1.000000000000000000, 0.000000000000000000 ) ) ;
#167726=CARTESIAN_POINT ( 'NONE',  ( -20.64999999999999858, -9.499999999988848032, -177.3939691226524076 ) ) ;
#167752=CARTESIAN_POINT ( 'NONE',  ( -18.50000000000000000, 9.150000000011157653, -179.8499999999999943 ) ) ;
#167780=DIRECTION ( 'NONE',  ( 0.000000000000000000, 1.224646799142185182E-16, 1.000000000000000000 ) ) ;
#167825=DIRECTION ( 'NONE',  ( 1.000000000000000000, 2.952720810173289112E-16, -0.000000000000000000 ) ) ;
#167837=EDGE_LOOP ( 'NONE', ( #201921, #218351, #114450, #154981 ) ) ;
#167861=ORIENTED_EDGE ( 'NONE', *, *, #227057, .T. ) ;
#167925=ORIENTED_EDGE ( 'NONE', *, *, #147689, .F. ) ;
#167930=SPHERICAL_SURFACE ( 'NONE', #232358, 0.1000000000000000056 ) ;
#167950=AXIS2_PLACEMENT_3D ( 'NONE', #234759, #19575, #117383 ) ;
#167951=DIRECTION ( 'NONE',  ( 1.000000000000000000, 0.000000000000000000, 0.000000000000000000 ) ) ;
#167961=ADVANCED_FACE ( 'NONE', ( #71759 ), #60032, .T. ) ;
#167964=DIRECTION ( 'NONE',  ( -1.000000000000000000, 0.000000000000000000, 0.000000000000000000 ) ) ;
#167984=CARTESIAN_POINT ( 'NONE',  ( 21.14999999999999858, 1.115488181425289271E-11, -160.9593430482987344 ) ) ;
#167985=CARTESIAN_POINT ( 'NONE',  ( 20.94999999999999929, -11.29603075032412995, -170.5478991596638423 ) ) ;
#168047=ORIENTED_EDGE ( 'NONE', *, *, #231577, .F. ) ;
#168057=VERTEX_POINT ( 'NONE', #201964 ) ;
#168062=DIRECTION ( 'NONE',  ( -1.000000000000000000, 0.000000000000000000, 0.000000000000000000 ) ) ;
#168066=CARTESIAN_POINT ( 'NONE',  ( -20.54999999999999716, 1.115600667400684642E-11, -198.9999999999999432 ) ) ;
#168086=CARTESIAN_POINT ( 'NONE',  ( 22.49436431346199683, 0.06690352973341695542, -155.8500490523465203 ) ) ;
#168121=DIRECTION ( 'NONE',  ( 1.000000000000000000, 0.000000000000000000, 0.000000000000000000 ) ) ;
#168132=DIRECTION ( 'NONE',  ( -3.265361837132813093E-16, 1.000000000000000000, -0.000000000000000000 ) ) ;
#168140=FACE_OUTER_BOUND ( 'NONE', #234885, .T. ) ;
#168145=ORIENTED_EDGE ( 'NONE', *, *, #195454, .T. ) ;
#168171=ORIENTED_EDGE ( 'NONE', *, *, #123794, .T. ) ;
#168172=DIRECTION ( 'NONE',  ( -1.000000000000000000, -0.000000000000000000, -0.000000000000000000 ) ) ;
#168176=LINE ( 'NONE', #164290, #114376 ) ;
#168223=PLANE ( 'NONE',  #177432 ) ;
#168237=EDGE_CURVE ( 'NONE', #59716, #130077, #886, .T. ) ;
#168245=CIRCLE ( 'NONE', #84960, 7.800000000000000711 ) ;
#168291=FACE_OUTER_BOUND ( 'NONE', #182632, .T. ) ;
#168322=ORIENTED_EDGE ( 'NONE', *, *, #106647, .F. ) ;
#168334=DIRECTION ( 'NONE',  ( 1.000000000000000000, 0.000000000000000000, -0.000000000000000000 ) ) ;
#168342=ORIENTED_EDGE ( 'NONE', *, *, #19807, .F. ) ;
#168343=AXIS2_PLACEMENT_3D ( 'NONE', #38827, #120950, #62233 ) ;
#168346=EDGE_CURVE ( 'NONE', #36747, #179090, #88374, .T. ) ;
#168377=DIRECTION ( 'NONE',  ( 0.000000000000000000, 0.000000000000000000, 1.000000000000000000 ) ) ;
#168410=DIRECTION ( 'NONE',  ( 0.000000000000000000, 0.000000000000000000, -1.000000000000000000 ) ) ;
#168436=EDGE_CURVE ( 'NONE', #62638, #225193, #171639, .T. ) ;
#168474=EDGE_CURVE ( 'NONE', #218583, #103201, #42794, .T. ) ;
#168480=AXIS2_PLACEMENT_3D ( 'NONE', #234939, #195832, #58831 ) ;
#168494=DIRECTION ( 'NONE',  ( -0.000000000000000000, 0.1350103645451876666, 0.9908441862701600211 ) ) ;
#168507=ORIENTED_EDGE ( 'NONE', *, *, #248886, .F. ) ;
#168508=CARTESIAN_POINT ( 'NONE',  ( 23.14999999999999503, 11.75000000001116263, -188.8499999999999659 ) ) ;
#168673=PLANE ( 'NONE',  #216965 ) ;
#168681=CARTESIAN_POINT ( 'NONE',  ( -21.14999999999999858, 11.65000000001115588, -167.5999999999999659 ) ) ;
#168699=ADVANCED_FACE ( 'NONE', ( #63405, #223758 ), #48984, .F. ) ;
#168708=EDGE_CURVE ( 'NONE', #31369, #6262, #113532, .T. ) ;
#168737=DIRECTION ( 'NONE',  ( 0.000000000000000000, 0.000000000000000000, -1.000000000000000000 ) ) ;
#168760=DIRECTION ( 'NONE',  ( 0.000000000000000000, 1.734723475976997999E-14, 1.000000000000000000 ) ) ;
#168761=ORIENTED_EDGE ( 'NONE', *, *, #71904, .F. ) ;
#168774=ORIENTED_EDGE ( 'NONE', *, *, #238430, .T. ) ;
#168800=VECTOR ( 'NONE', #251959, 1000.000000000000000 ) ;
#168825=EDGE_CURVE ( 'NONE', #132399, #163489, #191096, .T. ) ;
#168872=EDGE_CURVE ( 'NONE', #201908, #133, #219602, .T. ) ;
#168912=ADVANCED_FACE ( 'NONE', ( #95794 ), #230234, .T. ) ;
#168927=B_SPLINE_CURVE_WITH_KNOTS ( 'NONE', 3,
 ( #42731, #175850, #41476, #197945, #80543, #140533, #2301, #200523, #57135, #117144 ),
 .UNSPECIFIED., .F., .F.,
 ( 4, 3, 3, 4 ),
 ( 0.000000000000000000, 0.0002000000000002785953, 0.001000000000045107385, 0.001967863649472122601 ),
 .UNSPECIFIED. ) ;
#168947=ORIENTED_EDGE ( 'NONE', *, *, #13214, .F. ) ;
#168949=CYLINDRICAL_SURFACE ( 'NONE', #164960, 0.5000000000000004441 ) ;
#168968=DIRECTION ( 'NONE',  ( 0.000000000000000000, 2.891205793294679805E-16, -1.000000000000000000 ) ) ;
#168999=VERTEX_POINT ( 'NONE', #190318 ) ;
#169000=AXIS2_PLACEMENT_3D ( 'NONE', #193430, #137277, #73497 ) ;
#169015=DIRECTION ( 'NONE',  ( 1.000000000000000000, 0.000000000000000000, 0.000000000000000000 ) ) ;
#169041=EDGE_CURVE ( 'NONE', #129423, #46904, #71659, .T. ) ;
#169070=FACE_OUTER_BOUND ( 'NONE', #70663, .T. ) ;
#169119=CARTESIAN_POINT ( 'NONE',  ( -20.94999999999999929, 1.261786168576181755, -175.5864989635454378 ) ) ;
#169154=VERTEX_POINT ( 'NONE', #80592 ) ;
#169156=LINE ( 'NONE', #247363, #201509 ) ;
#169159=DIRECTION ( 'NONE',  ( 1.000000000000000000, 2.952720810173289112E-16, -0.000000000000000000 ) ) ;
#169170=AXIS2_PLACEMENT_3D ( 'NONE', #32656, #91309, #133009 ) ;
#169203=ADVANCED_FACE ( 'NONE', ( #87009 ), #127452, .T. ) ;
#169221=DIRECTION ( 'NONE',  ( 4.239556034732056743E-17, -0.1298341882520022694, -0.9915357197604852679 ) ) ;
#169241=CIRCLE ( 'NONE', #56731, 11.75000000000001066 ) ;
#169263=ORIENTED_EDGE ( 'NONE', *, *, #168237, .F. ) ;
#169269=DIRECTION ( 'NONE',  ( -1.000000000000000000, 0.000000000000000000, 0.000000000000000000 ) ) ;
#169270=CARTESIAN_POINT ( 'NONE',  ( 20.94999999999999574, 5.900000000011102586, -177.7190997646563915 ) ) ;
#169274=DIRECTION ( 'NONE',  ( -1.000000000000000000, -0.000000000000000000, -0.000000000000000000 ) ) ;
#169310=AXIS2_PLACEMENT_3D ( 'NONE', #163718, #63312, #5900 ) ;
#169398=DIRECTION ( 'NONE',  ( 0.000000000000000000, -1.000000000000000000, 0.000000000000000000 ) ) ;
#169402=CARTESIAN_POINT ( 'NONE',  ( -18.59999999999999787, 11.75000000001115552, -188.7499999999999716 ) ) ;
#169454=ORIENTED_EDGE ( 'NONE', *, *, #209531, .F. ) ;
#169476=ORIENTED_EDGE ( 'NONE', *, *, #34963, .F. ) ;
#169477=CARTESIAN_POINT ( 'NONE',  ( 22.39999999999999503, 1.115600667400684642E-11, -155.8504291924551808 ) ) ;
#169482=DIRECTION ( 'NONE',  ( -1.000000000000000000, -0.000000000000000000, 0.000000000000000000 ) ) ;
#169487=VERTEX_POINT ( 'NONE', #191310 ) ;
#169496=ORIENTED_EDGE ( 'NONE', *, *, #118348, .F. ) ;
#169498=AXIS2_PLACEMENT_3D ( 'NONE', #200213, #25436, #179381 ) ;
#169505=AXIS2_PLACEMENT_3D ( 'NONE', #133940, #31040, #169269 ) ;
#169528=AXIS2_PLACEMENT_3D ( 'NONE', #10253, #92339, #91061 ) ;
#169562=ORIENTED_EDGE ( 'NONE', *, *, #17567, .T. ) ;
#169565=CARTESIAN_POINT ( 'NONE',  ( -18.59999999999999787, -1.261786168553869603, -175.5864989635454378 ) ) ;
#169576=CARTESIAN_POINT ( 'NONE',  ( -23.25000000000000000, 1.115651490242849210E-11, -163.3499999999999943 ) ) ;
#169588=EDGE_LOOP ( 'NONE', ( #76543, #107913, #257527, #54632 ) ) ;
#169604=DIRECTION ( 'NONE',  ( 1.000000000000000000, 0.000000000000000000, -0.000000000000000000 ) ) ;
#169609=DIRECTION ( 'NONE',  ( -1.000000000000000000, 0.000000000000000000, 0.000000000000000000 ) ) ;
#169619=CARTESIAN_POINT ( 'NONE',  ( -20.95613430942402644, 11.75000000001115552, -174.3571626482202817 ) ) ;
#169629=EDGE_CURVE ( 'NONE', #185332, #96541, #255494, .T. ) ;
#169663=CARTESIAN_POINT ( 'NONE',  ( 20.94999999999999574, 8.926614585098251453, -175.9716830192230930 ) ) ;
#169665=EDGE_LOOP ( 'NONE', ( #57417, #177203, #216767, #128276 ) ) ;
#169670=AXIS2_PLACEMENT_3D ( 'NONE', #43178, #247788, #148707 ) ;
#169730=DIRECTION ( 'NONE',  ( 1.000000000000000000, 0.000000000000000000, 0.000000000000000000 ) ) ;
#169751=ORIENTED_EDGE ( 'NONE', *, *, #57073, .F. ) ;
#169760=CARTESIAN_POINT ( 'NONE',  ( -23.25000000000000000, 11.75000000001115552, -188.8499999999999659 ) ) ;
#169774=TOROIDAL_SURFACE ( 'NONE', #227997, 7.800000000000000711, 0.1000000000000000056 ) ;
#169791=CIRCLE ( 'NONE', #69815, 3.899999999999999467 ) ;
#169801=CIRCLE ( 'NONE', #57312, 0.1000000000000043493 ) ;
#169809=ORIENTED_EDGE ( 'NONE', *, *, #220011, .F. ) ;
#169832=DIRECTION ( 'NONE',  ( 1.000000000000000000, 0.000000000000000000, 0.000000000000000000 ) ) ;
#169867=CARTESIAN_POINT ( 'NONE',  ( -18.50000000000000000, 6.846123162363745074, -204.7377262668498190 ) ) ;
#169868=DIRECTION ( 'NONE',  ( 0.1538461538461510236, 0.9880948137434718559, 0.000000000000000000 ) ) ;
#169869=ORIENTED_EDGE ( 'NONE', *, *, #62410, .T. ) ;
#169871=CARTESIAN_POINT ( 'NONE',  ( 23.14999999999999858, 4.775700934590584090, -179.3487681040459165 ) ) ;
#169886=VERTEX_POINT ( 'NONE', #96962 ) ;
#169929=VERTEX_POINT ( 'NONE', #137401 ) ;
#169949=CYLINDRICAL_SURFACE ( 'NONE', #112000, 4.049999999999998046 ) ;
#169961=AXIS2_PLACEMENT_3D ( 'NONE', #178560, #35208, #258010 ) ;
#169998=DIRECTION ( 'NONE',  ( 1.000000000000000000, 3.469446951953704435E-14, -2.003086131649669752E-14 ) ) ;
#170001=EDGE_CURVE ( 'NONE', #82909, #218080, #116572, .T. ) ;
#170016=CIRCLE ( 'NONE', #65727, 0.09999999999999939493 ) ;
#170017=ORIENTED_EDGE ( 'NONE', *, *, #14700, .F. ) ;
#170029=EDGE_LOOP ( 'NONE', ( #100898, #218631, #249216, #132772 ) ) ;
#170087=CARTESIAN_POINT ( 'NONE',  ( 18.49999999999998934, 11.65000000001115943, -192.2499999999999716 ) ) ;
#170128=DIRECTION ( 'NONE',  ( 0.000000000000000000, 0.8660254037844411501, 0.4999999999999956701 ) ) ;
#170130=DIRECTION ( 'NONE',  ( 0.000000000000000000, 1.265107689135680095E-16, -1.000000000000000000 ) ) ;
#170160=EDGE_CURVE ( 'NONE', #222295, #111061, #235082, .T. ) ;
#170179=SPHERICAL_SURFACE ( 'NONE', #223350, 0.1000000000000000056 ) ;
#170193=ORIENTED_EDGE ( 'NONE', *, *, #56379, .F. ) ;
#170204=PRODUCT ( 'Injection Molded Chain Links 6', 'Injection Molded Chain Links 6', '', ( #93915 ) ) ;
#170207=AXIS2_PLACEMENT_3D ( 'NONE', #81528, #41181, #221061 ) ;
#170233=FACE_OUTER_BOUND ( 'NONE', #5841, .T. ) ;
#170241=EDGE_CURVE ( 'NONE', #44391, #84620, #176816, .T. ) ;
#170258=DIRECTION ( 'NONE',  ( 0.000000000000000000, 1.000000000000000000, 0.000000000000000000 ) ) ;
#170266=CARTESIAN_POINT ( 'NONE',  ( -18.43599941264894326, -9.519327428583080675, -174.4729767895220220 ) ) ;
#170271=CARTESIAN_POINT ( 'NONE',  ( 23.15000000000000213, -11.64999999998883595, -197.8999999999999773 ) ) ;
#170287=EDGE_LOOP ( 'NONE', ( #176401, #95507, #157923, #215265 ) ) ;
#170309=CARTESIAN_POINT ( 'NONE',  ( 21.14999999999999858, 6.540656951712402467, -167.4999999999999716 ) ) ;
#170311=DIRECTION ( 'NONE',  ( 0.000000000000000000, 0.9274965247785529332, -0.3738317757009255171 ) ) ;
#170313=EDGE_LOOP ( 'NONE', ( #124341, #86421, #185228, #190417 ) ) ;
#170322=EDGE_CURVE ( 'NONE', #190824, #16272, #64376, .T. ) ;
#170329=ORIENTED_EDGE ( 'NONE', *, *, #200622, .T. ) ;
#170332=CARTESIAN_POINT ( 'NONE',  ( -20.94999999999999929, 1.115600667400684642E-11, -200.9999999999999432 ) ) ;
#170346=CYLINDRICAL_SURFACE ( 'NONE', #251979, 0.09999999999999939493 ) ;
#170347=AXIS2_PLACEMENT_3D ( 'NONE', #33185, #35738, #133523 ) ;
#170354=DIRECTION ( 'NONE',  ( 1.000000000000000000, -0.000000000000000000, -0.000000000000000000 ) ) ;
#170358=CARTESIAN_POINT ( 'NONE',  ( 21.05000000000000071, 11.65000000001115943, -167.5999999999999659 ) ) ;
#170377=EDGE_CURVE ( 'NONE', #202760, #214529, #247542, .T. ) ;
#170390=EDGE_LOOP ( 'NONE', ( #198965, #184658, #91494 ) ) ;
#170409=EDGE_LOOP ( 'NONE', ( #171397, #42087, #159895 ) ) ;
#170411=VECTOR ( 'NONE', #186336, 1000.000000000000227 ) ;
#170429=EDGE_CURVE ( 'NONE', #96910, #238407, #47776, .T. ) ;
#170440=FACE_OUTER_BOUND ( 'NONE', #128616, .T. ) ;
#170447=ORIENTED_EDGE ( 'NONE', *, *, #252726, .F. ) ;
#170453=CARTESIAN_POINT ( 'NONE',  ( -18.59999999999999787, 1.736257131608553550, -179.0686523290174819 ) ) ;
#170473=AXIS2_PLACEMENT_3D ( 'NONE', #109001, #188550, #69918 ) ;
#170479=VECTOR ( 'NONE', #195902, 1000.000000000000000 ) ;
#170490=TOROIDAL_SURFACE ( 'NONE', #233194, 12.77499999999999858, 0.1000000000000000056 ) ;
#170503=ORIENTED_EDGE ( 'NONE', *, *, #26461, .T. ) ;
#170507=ORIENTED_EDGE ( 'NONE', *, *, #187504, .F. ) ;
#170536=DIRECTION ( 'NONE',  ( -2.978066053179067751E-16, 1.000000000000000000, 2.382452842543254201E-15 ) ) ;
#170570=CARTESIAN_POINT ( 'NONE',  ( -18.59999999999999787, 1.115600667400684642E-11, -167.4999999999999716 ) ) ;
#170583=DIRECTION ( 'NONE',  ( 0.000000000000000000, 0.000000000000000000, -1.000000000000000000 ) ) ;
#170609=AXIS2_PLACEMENT_3D ( 'NONE', #126593, #27535, #107011 ) ;
#170628=PLANE ( 'NONE',  #71634 ) ;
#170640=EDGE_CURVE ( 'NONE', #48880, #242139, #81111, .T. ) ;
#170676=AXIS2_PLACEMENT_3D ( 'NONE', #68901, #108013, #148431 ) ;
#170681=VECTOR ( 'NONE', #226963, 1000.000000000000000 ) ;
#170682=EDGE_CURVE ( 'NONE', #196712, #178378, #79527, .T. ) ;
#170734=CARTESIAN_POINT ( 'NONE',  ( -22.39999999999999858, 0.1000000000111554016, -159.7092204016265384 ) ) ;
#170752=DIRECTION ( 'NONE',  ( 7.304098846218134667E-16, -1.000000000000000000, 0.000000000000000000 ) ) ;
#170771=DIRECTION ( 'NONE',  ( 0.000000000000000000, 0.000000000000000000, -1.000000000000000000 ) ) ;
#170792=ORIENTED_EDGE ( 'NONE', *, *, #45079, .F. ) ;
#170829=LINE ( 'NONE', #54666, #161207 ) ;
#170838=ADVANCED_FACE ( 'NONE', ( #144159 ), #7222, .F. ) ;
#170861=CARTESIAN_POINT ( 'NONE',  ( -18.46856557590792391, -9.474215907775342060, -174.6019862408821837 ) ) ;
#170869=LINE ( 'NONE', #147394, #48485 ) ;
#170879=VERTEX_POINT ( 'NONE', #241994 ) ;
#170895=CARTESIAN_POINT ( 'NONE',  ( 22.50046968638161360, 0.04516984715162254693, -155.7499548455311924 ) ) ;
#170903=DIRECTION ( 'NONE',  ( 0.000000000000000000, 0.000000000000000000, -1.000000000000000000 ) ) ;
#170908=CARTESIAN_POINT ( 'NONE',  ( -21.55000000000000071, 7.150000000011155876, -188.7499999999999716 ) ) ;
#170909=CARTESIAN_POINT ( 'NONE',  ( -20.85000000000000142, 7.021664781911246322, -204.8335654018972605 ) ) ;
#170912=DIRECTION ( 'NONE',  ( 0.000000000000000000, 0.000000000000000000, 1.000000000000000000 ) ) ;
#170951=CARTESIAN_POINT ( 'NONE',  ( 18.57071067811864040, 10.17928932189250091, -188.8499999999999659 ) ) ;
#170952=CARTESIAN_POINT ( 'NONE',  ( 20.95346350065193519, 8.887177249185651107, -176.0117319470353721 ) ) ;
#170966=CARTESIAN_POINT ( 'NONE',  ( 23.15000000000000213, -11.48912529306489994, -197.8999999999999773 ) ) ;
#170968=ORIENTED_EDGE ( 'NONE', *, *, #177174, .F. ) ;
#170969=CIRCLE ( 'NONE', #58455, 0.09999999999998898659 ) ;
#170989=AXIS2_PLACEMENT_3D ( 'NONE', #165754, #65341, #144868 ) ;
#171004=AXIS2_PLACEMENT_3D ( 'NONE', #120785, #123333, #202853 ) ;
#171010=ORIENTED_EDGE ( 'NONE', *, *, #51067, .F. ) ;
#171025=DIRECTION ( 'NONE',  ( 0.000000000000000000, 0.000000000000000000, -1.000000000000000000 ) ) ;
#171052=CARTESIAN_POINT ( 'NONE',  ( 21.05000000000000071, -11.74999999998883560, -198.0999999999999659 ) ) ;
#171063=CARTESIAN_POINT ( 'NONE',  ( -20.64999999999999858, 1.115600667400684642E-11, -198.9999999999999432 ) ) ;
#171089=EDGE_LOOP ( 'NONE', ( #22757, #41492, #160632, #232559 ) ) ;
#171116=ORIENTED_EDGE ( 'NONE', *, *, #128, .T. ) ;
#171162=CYLINDRICAL_SURFACE ( 'NONE', #99394, 11.75000000000001066 ) ;
#171166=DIRECTION ( 'NONE',  ( 7.589415207398576792E-15, -1.000000000000000000, -0.000000000000000000 ) ) ;
#171217=CARTESIAN_POINT ( 'NONE',  ( -21.98333005346336577, 1.115600667400684642E-11, -160.1259246709432773 ) ) ;
#171222=ORIENTED_EDGE ( 'NONE', *, *, #26142, .F. ) ;
#171225=EDGE_CURVE ( 'NONE', #88951, #103901, #220834, .T. ) ;
#171230=CYLINDRICAL_SURFACE ( 'NONE', #53492, 0.09999999999998898659 ) ;
#171233=DIRECTION ( 'NONE',  ( -1.000000000000000000, -0.000000000000000000, 0.000000000000000000 ) ) ;
#171236=VERTEX_POINT ( 'NONE', #43500 ) ;
#171238=CARTESIAN_POINT ( 'NONE',  ( 19.99999999738042789, 11.75000000001116263, -192.1871719496316473 ) ) ;
#171259=ADVANCED_FACE ( 'NONE', ( #244243 ), #46050, .F. ) ;
#171267=CARTESIAN_POINT ( 'NONE',  ( -23.15000000000000213, 11.75000000001115552, -188.8499999999999659 ) ) ;
#171279=CARTESIAN_POINT ( 'NONE',  ( -20.94999999999999929, -11.48912529306489994, -197.8999999999999773 ) ) ;
#171285=CARTESIAN_POINT ( 'NONE',  ( -23.15000000000000213, -8.999999999988844479, -191.7060308773475299 ) ) ;
#171302=ORIENTED_EDGE ( 'NONE', *, *, #3784, .F. ) ;
#171319=ORIENTED_EDGE ( 'NONE', *, *, #137839, .F. ) ;
#171336=DIRECTION ( 'NONE',  ( 0.000000000000000000, 0.000000000000000000, 1.000000000000000000 ) ) ;
#171348=DIRECTION ( 'NONE',  ( 0.000000000000000000, 0.000000000000000000, -1.000000000000000000 ) ) ;
#171349=FACE_OUTER_BOUND ( 'NONE', #203241, .T. ) ;
#171388=CARTESIAN_POINT ( 'NONE',  ( 18.50000000000000000, -9.499999999988842703, -155.7499999999999716 ) ) ;
#171394=CARTESIAN_POINT ( 'NONE',  ( -23.15000000000000213, 2.500000000011154633, -187.7753780772378889 ) ) ;
#171397=ORIENTED_EDGE ( 'NONE', *, *, #122583, .T. ) ;
#171403=ORIENTED_EDGE ( 'NONE', *, *, #88663, .F. ) ;
#171428=AXIS2_PLACEMENT_3D ( 'NONE', #50598, #231846, #28540 ) ;
#171451=DIRECTION ( 'NONE',  ( 0.000000000000000000, 0.000000000000000000, 1.000000000000000000 ) ) ;
#171455=CYLINDRICAL_SURFACE ( 'NONE', #232202, 0.09999999999998898659 ) ;
#171495=DIRECTION ( 'NONE',  ( 0.000000000000000000, 0.000000000000000000, -1.000000000000000000 ) ) ;
#171529=DIRECTION ( 'NONE',  ( -1.000000000000000000, 0.000000000000000000, 0.000000000000000000 ) ) ;
#171535=VECTOR ( 'NONE', #226702, 1000.000000000000000 ) ;
#171544=CARTESIAN_POINT ( 'NONE',  ( 20.94999999999999929, 5.000000000011153745, -179.9052660189130677 ) ) ;
#171563=CARTESIAN_POINT ( 'NONE',  ( 21.05000000000000071, -9.499999999988844479, -191.1060308773475072 ) ) ;
#171577=CARTESIAN_POINT ( 'NONE',  ( 21.05000000000000071, 6.540656951712403355, -167.5999999999999659 ) ) ;
#171581=DIRECTION ( 'NONE',  ( -1.000000000000000000, 0.000000000000000000, 0.000000000000000000 ) ) ;
#171586=DIRECTION ( 'NONE',  ( 0.000000000000000000, -3.552713678800542739E-15, 1.000000000000000000 ) ) ;
#171611=VERTEX_POINT ( 'NONE', #199724 ) ;
#171619=EDGE_CURVE ( 'NONE', #190986, #236967, #173311, .T. ) ;
#171639=CIRCLE ( 'NONE', #59140, 0.09999999999998898659 ) ;
#171641=ADVANCED_FACE ( 'NONE', ( #202273 ), #114993, .F. ) ;
#171647=ADVANCED_FACE ( 'NONE', ( #185277 ), #240120, .F. ) ;
#171648=DIRECTION ( 'NONE',  ( 1.000000000000000000, -0.000000000000000000, 0.000000000000000000 ) ) ;
#171672=CYLINDRICAL_SURFACE ( 'NONE', #160540, 0.09999999999999939493 ) ;
#171679=ORIENTED_EDGE ( 'NONE', *, *, #144056, .T. ) ;
#171692=VECTOR ( 'NONE', #7646, 1000.000000000000000 ) ;
#171722=CARTESIAN_POINT ( 'NONE',  ( 20.94999999999999929, -11.48912529306489994, -197.8999999999999773 ) ) ;
#171744=EDGE_CURVE ( 'NONE', #252820, #42259, #156727, .T. ) ;
#171765=ORIENTED_EDGE ( 'NONE', *, *, #36169, .T. ) ;
#171782=VECTOR ( 'NONE', #225486, 1000.000000000000000 ) ;
#171846=ORIENTED_EDGE ( 'NONE', *, *, #207253, .F. ) ;
#171847=ORIENTED_EDGE ( 'NONE', *, *, #245953, .F. ) ;
#171848=FACE_OUTER_BOUND ( 'NONE', #32917, .T. ) ;
#171851=ADVANCED_FACE ( 'NONE', ( #226968 ), #187864, .F. ) ;
#171875=CIRCLE ( 'NONE', #134217, 11.75000000000001066 ) ;
#171886=ORIENTED_EDGE ( 'NONE', *, *, #198514, .F. ) ;
#171905=DIRECTION ( 'NONE',  ( -1.000000000000000000, -0.000000000000000000, -0.000000000000000000 ) ) ;
#171916=ORIENTED_EDGE ( 'NONE', *, *, #41030, .T. ) ;
#171919=CARTESIAN_POINT ( 'NONE',  ( 21.14999999999999858, 11.65000000001115943, -167.5999999999999659 ) ) ;
#171938=CARTESIAN_POINT ( 'NONE',  ( 18.50000000000000000, -10.35479209691423996, -194.7565409830737337 ) ) ;
#171941=EDGE_CURVE ( 'NONE', #250193, #21068, #157756, .T. ) ;
#172011=CARTESIAN_POINT ( 'NONE',  ( -18.46154800491014569, -9.480206274230836172, -207.6574508383814361 ) ) ;
#172024=VECTOR ( 'NONE', #216269, 1000.000000000000000 ) ;
#172038=CARTESIAN_POINT ( 'NONE',  ( -23.15000000000000213, -11.64999999998884483, -167.4999999999999432 ) ) ;
#172049=CARTESIAN_POINT ( 'NONE',  ( 23.14999999999999858, 1.115600667400684642E-11, -167.4999999999999716 ) ) ;
#172057=ORIENTED_EDGE ( 'NONE', *, *, #139444, .T. ) ;
#172060=ADVANCED_FACE ( 'NONE', ( #159017 ), #141979, .F. ) ;
#172063=ORIENTED_EDGE ( 'NONE', *, *, #153945, .T. ) ;
#172078=CARTESIAN_POINT ( 'NONE',  ( -20.94999999999999929, 1.115600667400684642E-11, -196.9999999999999432 ) ) ;
#172108=DIRECTION ( 'NONE',  ( 1.000000000000000000, 0.000000000000000000, 0.000000000000000000 ) ) ;
#172158=VECTOR ( 'NONE', #20513, 999.9999999999998863 ) ;
#172179=CYLINDRICAL_SURFACE ( 'NONE', #207067, 0.09999999999998898659 ) ;
#172222=DIRECTION ( 'NONE',  ( 1.000000000000000000, 0.000000000000000000, 0.000000000000000000 ) ) ;
#172245=FACE_OUTER_BOUND ( 'NONE', #196707, .T. ) ;
#172270=EDGE_CURVE ( 'NONE', #116826, #185664, #231905, .T. ) ;
#172274=VERTEX_POINT ( 'NONE', #88404 ) ;
#172278=AXIS2_PLACEMENT_3D ( 'NONE', #130060, #186204, #167951 ) ;
#172323=EDGE_CURVE ( 'NONE', #199385, #34439, #251345, .T. ) ;
#172325=CIRCLE ( 'NONE', #39022, 0.09999999999998898659 ) ;
#172330=VERTEX_POINT ( 'NONE', #36182 ) ;
#172364=ORIENTED_EDGE ( 'NONE', *, *, #113359, .F. ) ;
#172366=CIRCLE ( 'NONE', #205611, 1.900000000000012790 ) ;
#172377=DIRECTION ( 'NONE',  ( 0.000000000000000000, -0.8700118002898359348, 0.4930308989875165082 ) ) ;
#172385=EDGE_LOOP ( 'NONE', ( #113952, #226325, #183930, #13272, #231283, #205450, #22290, #206003, #151842, #215005, #10987 ) ) ;
#172392=DIRECTION ( 'NONE',  ( 2.952720810173289112E-16, -1.000000000000000000, 0.000000000000000000 ) ) ;
#172398=LINE ( 'NONE', #173691, #208963 ) ;
#172406=CARTESIAN_POINT ( 'NONE',  ( -23.15000000000000213, 11.65000000001115588, -193.9851942293460070 ) ) ;
#172408=ORIENTED_EDGE ( 'NONE', *, *, #138632, .F. ) ;
#172434=CARTESIAN_POINT ( 'NONE',  ( 21.30000000000002558, 1.115600667400684642E-11, -167.4999999999999716 ) ) ;
#172446=VECTOR ( 'NONE', #11293, 1000.000000000000000 ) ;
#172478=LINE ( 'NONE', #192014, #168800 ) ;
#172485=AXIS2_PLACEMENT_3D ( 'NONE', #246648, #88845, #129285 ) ;
#172504=ADVANCED_FACE ( 'NONE', ( #47371 ), #41324, .F. ) ;
#172523=DIRECTION ( 'NONE',  ( 0.000000000000000000, -0.9915357197604971473, 0.1298341882519111479 ) ) ;
#172525=ORIENTED_EDGE ( 'NONE', *, *, #15667, .F. ) ;
#172531=VECTOR ( 'NONE', #194992, 1000.000000000000000 ) ;
#172538=ORIENTED_EDGE ( 'NONE', *, *, #254464, .F. ) ;
#172544=CARTESIAN_POINT ( 'NONE',  ( -18.59999999999999787, 11.65000000001115232, -174.5148057706539930 ) ) ;
#172547=ORIENTED_EDGE ( 'NONE', *, *, #46742, .F. ) ;
#172591=ORIENTED_EDGE ( 'NONE', *, *, #18668, .F. ) ;
#172607=DIRECTION ( 'NONE',  ( 0.000000000000000000, -1.000000000000000000, 0.000000000000000000 ) ) ;
#172645=CARTESIAN_POINT ( 'NONE',  ( 22.39999999999999503, 11.75000000001115552, -167.3999999999999773 ) ) ;
#172688=VERTEX_POINT ( 'NONE', #57642 ) ;
#172694=TOROIDAL_SURFACE ( 'NONE', #31223, 11.90000000000000391, 0.1000000000000000056 ) ;
#172741=ORIENTED_EDGE ( 'NONE', *, *, #1400, .F. ) ;
#172745=EDGE_CURVE ( 'NONE', #116862, #57200, #35560, .T. ) ;
#172747=DIRECTION ( 'NONE',  ( 0.000000000000000000, 1.000000000000000000, -1.224646799147353207E-16 ) ) ;
#172750=DIRECTION ( 'NONE',  ( 0.000000000000000000, 1.000000000000000000, 0.000000000000000000 ) ) ;
#172798=ORIENTED_EDGE ( 'NONE', *, *, #170377, .F. ) ;
#172801=DIRECTION ( 'NONE',  ( 1.000000000000000000, -0.000000000000000000, -0.000000000000000000 ) ) ;
#172824=DIRECTION ( 'NONE',  ( -2.952720810173289112E-16, 1.000000000000000000, 0.000000000000000000 ) ) ;
#172880=DIRECTION ( 'NONE',  ( 0.000000000000000000, 1.000000000000000000, 0.000000000000000000 ) ) ;
#172892=AXIS2_PLACEMENT_3D ( 'NONE', #125178, #204685, #165596 ) ;
#172941=DIRECTION ( 'NONE',  ( -3.265361837132813586E-16, 1.000000000000000000, 0.000000000000000000 ) ) ;
#172987=DIRECTION ( 'NONE',  ( 0.7071067811865475727, -0.7071067811865475727, 0.000000000000000000 ) ) ;
#173026=EDGE_CURVE ( 'NONE', #41250, #86050, #148490, .T. ) ;
#173046=CARTESIAN_POINT ( 'NONE',  ( -22.50000000000000000, 0.09263750062063520752, -155.8503027929592122 ) ) ;
#173050=CARTESIAN_POINT ( 'NONE',  ( 21.05000000000000071, 5.000000000011153745, -188.9947339810868812 ) ) ;
#173051=DIRECTION ( 'NONE',  ( 0.000000000000000000, -1.000000000000000000, 0.000000000000000000 ) ) ;
#173089=CARTESIAN_POINT ( 'NONE',  ( 21.00023020733438273, 6.390869245278871347, -167.4999999999999432 ) ) ;
#173107=ADVANCED_FACE ( 'NONE', ( #123685 ), #13589, .T. ) ;
#173163=DIRECTION ( 'NONE',  ( 1.000000000000000000, 0.000000000000000000, 0.000000000000000000 ) ) ;
#173179=CARTESIAN_POINT ( 'NONE',  ( -18.59999999999999787, 11.65000000001115232, -179.6499999999999773 ) ) ;
#173195=ORIENTED_EDGE ( 'NONE', *, *, #235833, .T. ) ;
#173235=EDGE_CURVE ( 'NONE', #12612, #117026, #106774, .T. ) ;
#173266=DIRECTION ( 'NONE',  ( -1.000000000000000000, -7.304098846218134667E-16, 0.000000000000000000 ) ) ;
#173277=DIRECTION ( 'NONE',  ( 0.000000000000000000, -1.000000000000000000, -0.000000000000000000 ) ) ;
#173283=CARTESIAN_POINT ( 'NONE',  ( -18.50000000000000000, 1.340746217944851715, -157.2271374945787841 ) ) ;
#173288=DIRECTION ( 'NONE',  ( -1.000000000000000000, -0.000000000000000000, 0.000000000000000000 ) ) ;
#173303=CARTESIAN_POINT ( 'NONE',  ( -18.41809261886920623, -9.682403314745256395, -207.6568435500914234 ) ) ;
#173304=EDGE_CURVE ( 'NONE', #236886, #2978, #152617, .T. ) ;
#173311=CIRCLE ( 'NONE', #139913, 0.09999999999999892308 ) ;
#173347=DIRECTION ( 'NONE',  ( -1.000000000000000000, -2.952720810173289112E-16, 0.000000000000000000 ) ) ;
#173362=ADVANCED_FACE ( 'NONE', ( #180777 ), #81630, .F. ) ;
#173384=DIRECTION ( 'NONE',  ( 1.000000000000000000, 0.000000000000000000, 0.000000000000000000 ) ) ;
#173395=ORIENTED_EDGE ( 'NONE', *, *, #87458, .T. ) ;
#173444=TOROIDAL_SURFACE ( 'NONE', #60936, 0.2000000000000000111, 0.1000000000000000056 ) ;
#173448=EDGE_CURVE ( 'NONE', #1689, #90736, #61181, .T. ) ;
#173467=DIRECTION ( 'NONE',  ( 1.000000000000000000, 0.000000000000000000, 0.000000000000000000 ) ) ;
#173506=VECTOR ( 'NONE', #200479, 1000.000000000000000 ) ;
#173579=DIRECTION ( 'NONE',  ( 0.000000000000000000, -0.8777080977375715243, 0.4791956752370512551 ) ) ;
#173591=FACE_OUTER_BOUND ( 'NONE', #148704, .T. ) ;
#173643=EDGE_CURVE ( 'NONE', #21068, #17724, #57047, .T. ) ;
#173691=CARTESIAN_POINT ( 'NONE',  ( -20.94999999999999929, 11.60000000001115517, -194.0717967697244717 ) ) ;
#173694=CARTESIAN_POINT ( 'NONE',  ( -20.54999999999999716, 2.000000000011154189, -180.7246219227620543 ) ) ;
#173745=ORIENTED_EDGE ( 'NONE', *, *, #14181, .T. ) ;
#173753=DIRECTION ( 'NONE',  ( 1.000000000000000000, 0.000000000000000000, 0.000000000000000000 ) ) ;
#173756=ORIENTED_EDGE ( 'NONE', *, *, #219693, .T. ) ;
#173759=CARTESIAN_POINT ( 'NONE',  ( -18.39999999999999858, -9.599999999988849453, -207.6001893912220169 ) ) ;
#173782=DIRECTION ( 'NONE',  ( -2.827886303505249259E-16, 0.8660254037844412611, 0.4999999999999956701 ) ) ;
#173798=ORIENTED_EDGE ( 'NONE', *, *, #227585, .F. ) ;
#173805=ORIENTED_EDGE ( 'NONE', *, *, #42375, .T. ) ;
#173826=DIRECTION ( 'NONE',  ( 1.000000000000000000, -3.965082230804126670E-15, 0.000000000000000000 ) ) ;
#173839=CARTESIAN_POINT ( 'NONE',  ( 21.07971444708685738, 6.329792081637700463, -167.4121765636820669 ) ) ;
#173869=AXIS2_PLACEMENT_3D ( 'NONE', #237715, #42103, #176475 ) ;
#173946=AXIS2_PLACEMENT_3D ( 'NONE', #60535, #235325, #176665 ) ;
#173967=EDGE_CURVE ( 'NONE', #253024, #22668, #39072, .T. ) ;
#174045=CARTESIAN_POINT ( 'NONE',  ( 20.94999999999999929, 10.29288807859936838, -206.4580020160121592 ) ) ;
#174058=EDGE_CURVE ( 'NONE', #61597, #182833, #61357, .T. ) ;
#174071=DIRECTION ( 'NONE',  ( 0.000000000000000000, 0.000000000000000000, 1.000000000000000000 ) ) ;
#174090=DIRECTION ( 'NONE',  ( 0.000000000000000000, -0.4999999999999348299, 0.8660254037844762331 ) ) ;
#174098=DIRECTION ( 'NONE',  ( 0.000000000000000000, 0.000000000000000000, 1.000000000000000000 ) ) ;
#174106=CARTESIAN_POINT ( 'NONE',  ( 20.94999999999999929, 5.850000000011105428, -177.6324972242779268 ) ) ;
#174119=AXIS2_PLACEMENT_3D ( 'NONE', #255952, #77349, #78633 ) ;
#174162=FACE_OUTER_BOUND ( 'NONE', #82699, .T. ) ;
#174175=CARTESIAN_POINT ( 'NONE',  ( -20.07928932188135107, 9.220710678129810489, -188.7499999999999716 ) ) ;
#174200=CYLINDRICAL_SURFACE ( 'NONE', #152129, 0.09999999999998898659 ) ;
#174215=FACE_OUTER_BOUND ( 'NONE', #72191, .T. ) ;
#174280=PLANE ( 'NONE',  #130458 ) ;
#174283=CIRCLE ( 'NONE', #53438, 0.09999999999999939493 ) ;
#174334=CARTESIAN_POINT ( 'NONE',  ( -22.49072729836729678, 0.05648193274477467801, -155.8499917508450210 ) ) ;
#174360=ORIENTED_EDGE ( 'NONE', *, *, #124966, .F. ) ;
#174382=AXIS2_PLACEMENT_3D ( 'NONE', #254289, #135634, #112251 ) ;
#174406=AXIS2_PLACEMENT_3D ( 'NONE', #180920, #161366, #240895 ) ;
#174433=AXIS2_PLACEMENT_3D ( 'NONE', #217561, #119792, #199316 ) ;
#174446=CARTESIAN_POINT ( 'NONE',  ( -18.58735405345342784, -9.566478620325430171, -207.8227146462658652 ) ) ;
#174458=CARTESIAN_POINT ( 'NONE',  ( 21.04999999999999716, -0.08561306079281304215, -161.0862402661896624 ) ) ;
#174487=DIRECTION ( 'NONE',  ( 0.000000000000000000, -2.498001805406600196E-13, -1.000000000000000000 ) ) ;
#174532=AXIS2_PLACEMENT_3D ( 'NONE', #145866, #45495, #25944 ) ;
#174579=EDGE_LOOP ( 'NONE', ( #245752, #208914, #231660, #6237 ) ) ;
#174631=VERTEX_POINT ( 'NONE', #91975 ) ;
#174662=LINE ( 'NONE', #172078, #229011 ) ;
#174668=FACE_OUTER_BOUND ( 'NONE', #228537, .T. ) ;
#174673=FACE_OUTER_BOUND ( 'NONE', #166309, .T. ) ;
#174685=CARTESIAN_POINT ( 'NONE',  ( -22.39999999999999503, 7.790779598384560245, -167.3999999999999773 ) ) ;
#174706=ORIENTED_EDGE ( 'NONE', *, *, #146497, .F. ) ;
#174709=FACE_OUTER_BOUND ( 'NONE', #238017, .T. ) ;
#174760=AXIS2_PLACEMENT_3D ( 'NONE', #216364, #40346, #195551 ) ;
#174773=AXIS2_PLACEMENT_3D ( 'NONE', #246993, #48797, #35377 ) ;
#174774=ADVANCED_FACE ( 'NONE', ( #234053 ), #117957, .T. ) ;
#174783=DIRECTION ( 'NONE',  ( -1.000000000000000000, 0.000000000000000000, 0.000000000000000000 ) ) ;
#174801=PLANE ( 'NONE',  #186747 ) ;
#174810=DIRECTION ( 'NONE',  ( 0.000000000000000000, 0.000000000000000000, -1.000000000000000000 ) ) ;
#174824=DIRECTION ( 'NONE',  ( 0.000000000000000000, 0.000000000000000000, -1.000000000000000000 ) ) ;
#174884=PLANE ( 'NONE',  #60311 ) ;
#174994=DIRECTION ( 'NONE',  ( -6.938893903907222856E-15, 1.000000000000000000, 2.891205793294679805E-16 ) ) ;
#175001=VECTOR ( 'NONE', #185624, 999.9999999999998863 ) ;
#175017=CARTESIAN_POINT ( 'NONE',  ( 20.94999999999999929, 6.550000000011156231, -179.7499999999999716 ) ) ;
#175036=CARTESIAN_POINT ( 'NONE',  ( 18.49999999999998934, 10.25000000001115552, -192.1499999999999488 ) ) ;
#175042=DIRECTION ( 'NONE',  ( -1.000000000000000000, 0.000000000000000000, 0.000000000000000000 ) ) ;
#175045=EDGE_LOOP ( 'NONE', ( #140120, #89729, #64248, #13657, #34138, #78140, #113957, #41927, #124640, #95636, #212002 ) ) ;
#175063=CIRCLE ( 'NONE', #91797, 0.09999999999999839573 ) ;
#175087=EDGE_LOOP ( 'NONE', ( #50923, #221130, #219432, #97940 ) ) ;
#175095=DIRECTION ( 'NONE',  ( 1.000000000000000000, -0.000000000000000000, -0.000000000000000000 ) ) ;
#175137=DIRECTION ( 'NONE',  ( 0.000000000000000000, 0.000000000000000000, -1.000000000000000000 ) ) ;
#175138=CARTESIAN_POINT ( 'NONE',  ( 23.14999999999999858, 11.65000000001116298, -193.9851942293460070 ) ) ;
#175152=CARTESIAN_POINT ( 'NONE',  ( -21.12642695952773764, 6.375659922046319927, -167.4010967168105708 ) ) ;
#175164=ORIENTED_EDGE ( 'NONE', *, *, #209051, .T. ) ;
#175213=ORIENTED_EDGE ( 'NONE', *, *, #54810, .F. ) ;
#175222=CIRCLE ( 'NONE', #29465, 0.09999999999999939493 ) ;
#175241=ORIENTED_EDGE ( 'NONE', *, *, #190670, .T. ) ;
#175248=AXIS2_PLACEMENT_3D ( 'NONE', #43157, #63994, #44448 ) ;
#175255=CARTESIAN_POINT ( 'NONE',  ( -21.44999999999999929, 7.150000000011155876, -188.7499999999999716 ) ) ;
#175269=DIRECTION ( 'NONE',  ( 4.336808689942128177E-15, 0.8660254037844330455, -0.5000000000000096589 ) ) ;
#175299=LINE ( 'NONE', #177852, #231872 ) ;
#175301=DIRECTION ( 'NONE',  ( 0.000000000000000000, 1.224646799142185182E-16, 1.000000000000000000 ) ) ;
#175325=CIRCLE ( 'NONE', #216967, 11.80000000000000426 ) ;
#175340=CARTESIAN_POINT ( 'NONE',  ( -20.00857864376270001, 9.150000000011157653, -188.7499999999999716 ) ) ;
#175351=EDGE_LOOP ( 'NONE', ( #26171, #71705, #50811 ) ) ;
#175358=AXIS2_PLACEMENT_3D ( 'NONE', #62615, #142138, #183836 ) ;
#175361=AXIS2_PLACEMENT_3D ( 'NONE', #210625, #91957, #166400 ) ;
#175377=LINE ( 'NONE', #13698, #40224 ) ;
#175383=ADVANCED_FACE ( 'NONE', ( #255198 ), #107070, .F. ) ;
#175396=VERTEX_POINT ( 'NONE', #221244 ) ;
#175405=CIRCLE ( 'NONE', #62945, 0.09999999999999817368 ) ;
#175416=EDGE_CURVE ( 'NONE', #107466, #191501, #81711, .T. ) ;
#175440=DIRECTION ( 'NONE',  ( 1.000000000000000000, -0.000000000000000000, -0.000000000000000000 ) ) ;
#175459=AXIS2_PLACEMENT_3D ( 'NONE', #182117, #42600, #222492 ) ;
#175481=CARTESIAN_POINT ( 'NONE',  ( -20.54999999999999716, 9.350000000011156942, -188.7499999999999716 ) ) ;
#175505=VECTOR ( 'NONE', #80735, 1000.000000000000000 ) ;
#175565=ORIENTED_EDGE ( 'NONE', *, *, #80246, .T. ) ;
#175571=CARTESIAN_POINT ( 'NONE',  ( -20.85000000106584750, 11.75000000001115197, -194.1555046564733971 ) ) ;
#175581=CARTESIAN_POINT ( 'NONE',  ( -20.64999999999999858, 7.150000000011155876, -179.8499999999999943 ) ) ;
#175599=ADVANCED_FACE ( 'NONE', ( #128584 ), #29517, .T. ) ;
#175606=CARTESIAN_POINT ( 'NONE',  ( 23.14999999999999858, 1.115600667400684642E-11, -200.9999999999999432 ) ) ;
#175611=ORIENTED_EDGE ( 'NONE', *, *, #105266, .F. ) ;
#175641=DIRECTION ( 'NONE',  ( 0.000000000000000000, -0.9908441862701782288, 0.1350103645450542456 ) ) ;
#175691=DIRECTION ( 'NONE',  ( 0.000000000000000000, 0.000000000000000000, -1.000000000000000000 ) ) ;
#175692=CARTESIAN_POINT ( 'NONE',  ( -1.820710678118657944, -9.929289321870186313, -192.2499999999999716 ) ) ;
#175698=ORIENTED_EDGE ( 'NONE', *, *, #250324, .F. ) ;
#175703=CARTESIAN_POINT ( 'NONE',  ( 18.59999999999999076, 6.650000000011155876, -188.8499999999999659 ) ) ;
#175721=CARTESIAN_POINT ( 'NONE',  ( -23.15000000000000213, 1.115600667400684642E-11, -167.4999999999999716 ) ) ;
#175732=AXIS2_PLACEMENT_3D ( 'NONE', #128849, #243647, #248796 ) ;
#175770=FACE_OUTER_BOUND ( 'NONE', #241493, .T. ) ;
#175799=EDGE_LOOP ( 'NONE', ( #198559, #32570, #41210, #46124 ) ) ;
#175805=ORIENTED_EDGE ( 'NONE', *, *, #106766, .F. ) ;
#175808=FACE_OUTER_BOUND ( 'NONE', #187509, .T. ) ;
#175839=DIRECTION ( 'NONE',  ( -0.000000000000000000, -0.000000000000000000, 1.000000000000000000 ) ) ;
#175850=CARTESIAN_POINT ( 'NONE',  ( -22.42357213249529480, 0.09908696401271366305, -159.8270676136400539 ) ) ;
#175859=VECTOR ( 'NONE', #132713, 1000.000000000000000 ) ;
#175865=DIRECTION ( 'NONE',  ( -1.000000000000000000, 0.000000000000000000, 0.000000000000000000 ) ) ;
#175867=CARTESIAN_POINT ( 'NONE',  ( 20.85000000000000142, -1.749999999988843813, -212.6189500386222164 ) ) ;
#175871=EDGE_LOOP ( 'NONE', ( #180209, #87101, #44060, #179664 ) ) ;
#175916=ORIENTED_EDGE ( 'NONE', *, *, #115887, .T. ) ;
#175922=EDGE_CURVE ( 'NONE', #154503, #202001, #49796, .T. ) ;
#175928=ORIENTED_EDGE ( 'NONE', *, *, #106158, .T. ) ;
#175931=AXIS2_PLACEMENT_3D ( 'NONE', #250367, #93853, #133003 ) ;
#175932=ORIENTED_EDGE ( 'NONE', *, *, #138832, .T. ) ;
#175979=VERTEX_POINT ( 'NONE', #150432 ) ;
#175989=ADVANCED_FACE ( 'NONE', ( #30481 ), #195580, .F. ) ;
#176000=CARTESIAN_POINT ( 'NONE',  ( 22.59999999999999432, 0.1008583691098678403, -155.7504328765105868 ) ) ;
#176002=VERTEX_POINT ( 'NONE', #14783 ) ;
#176027=VERTEX_POINT ( 'NONE', #94279 ) ;
#176034=EDGE_CURVE ( 'NONE', #82856, #147015, #52582, .T. ) ;
#176094=CARTESIAN_POINT ( 'NONE',  ( 18.59999999999998366, 1.115600667400684642E-11, -200.9999999999999432 ) ) ;
#176125=DIRECTION ( 'NONE',  ( 0.000000000000000000, 0.000000000000000000, -1.000000000000000000 ) ) ;
#176134=LINE ( 'NONE', #139533, #35289 ) ;
#176154=SPHERICAL_SURFACE ( 'NONE', #174773, 0.1000000000000000056 ) ;
#176167=ORIENTED_EDGE ( 'NONE', *, *, #190249, .T. ) ;
#176226=CARTESIAN_POINT ( 'NONE',  ( 22.47071067811864964, 0.09909245471376178227, -159.7799252555019223 ) ) ;
#176259=AXIS2_PLACEMENT_3D ( 'NONE', #133368, #77223, #218004 ) ;
#176276=DIRECTION ( 'NONE',  ( 0.000000000000000000, 0.000000000000000000, -1.000000000000000000 ) ) ;
#176308=DIRECTION ( 'NONE',  ( 0.000000000000000000, 0.000000000000000000, -1.000000000000000000 ) ) ;
#176340=EDGE_CURVE ( 'NONE', #27168, #58719, #218411, .T. ) ;
#176341=LINE ( 'NONE', #257086, #170479 ) ;
#176345=DIRECTION ( 'NONE',  ( 0.000000000000000000, 0.000000000000000000, 1.000000000000000000 ) ) ;
#176361=DIRECTION ( 'NONE',  ( -0.000000000000000000, 0.000000000000000000, -1.000000000000000000 ) ) ;
#176401=ORIENTED_EDGE ( 'NONE', *, *, #15574, .T. ) ;
#176413=FACE_OUTER_BOUND ( 'NONE', #17268, .T. ) ;
#176417=AXIS2_PLACEMENT_3D ( 'NONE', #164194, #143326, #80769 ) ;
#176460=EDGE_LOOP ( 'NONE', ( #146224, #94380, #191962, #210797 ) ) ;
#176475=DIRECTION ( 'NONE',  ( 0.000000000000000000, 0.000000000000000000, -1.000000000000000000 ) ) ;
#176493=CARTESIAN_POINT ( 'NONE',  ( -21.14999999999999858, -11.64999999998884483, -170.3999999999999773 ) ) ;
#176507=AXIS2_PLACEMENT_3D ( 'NONE', #50056, #93038, #171348 ) ;
#176529=ORIENTED_EDGE ( 'NONE', *, *, #247347, .F. ) ;
#176537=DIRECTION ( 'NONE',  ( 0.000000000000000000, -0.000000000000000000, -1.000000000000000000 ) ) ;
#176549=CYLINDRICAL_SURFACE ( 'NONE', #239605, 11.75000000000001066 ) ;
#176572=EDGE_CURVE ( 'NONE', #131693, #169929, #192293, .T. ) ;
#176585=VERTEX_POINT ( 'NONE', #15943 ) ;
#176601=EDGE_LOOP ( 'NONE', ( #197258, #116828, #172591, #213434 ) ) ;
#176649=CYLINDRICAL_SURFACE ( 'NONE', #154271, 0.09999999999999939493 ) ;
#176665=DIRECTION ( 'NONE',  ( 0.000000000000000000, 0.000000000000000000, -1.000000000000000000 ) ) ;
#176706=DIRECTION ( 'NONE',  ( 1.000000000000000000, -0.000000000000000000, -0.000000000000000000 ) ) ;
#176734=ORIENTED_EDGE ( 'NONE', *, *, #92283, .T. ) ;
#176784=CYLINDRICAL_SURFACE ( 'NONE', #67713, 0.09999999999998898659 ) ;
#176790=CARTESIAN_POINT ( 'NONE',  ( -20.64999999999999858, 1.115625160336667635E-11, -202.9999999999999716 ) ) ;
#176801=AXIS2_PLACEMENT_3D ( 'NONE', #210385, #227364, #250778 ) ;
#176805=ORIENTED_EDGE ( 'NONE', *, *, #247632, .F. ) ;
#176816=CIRCLE ( 'NONE', #110156, 11.80000000000000426 ) ;
#176834=DIRECTION ( 'NONE',  ( 0.000000000000000000, -0.000000000000000000, -1.000000000000000000 ) ) ;
#176846=EDGE_CURVE ( 'NONE', #182323, #235498, #104941, .T. ) ;
#176863=AXIS2_PLACEMENT_3D ( 'NONE', #60830, #196495, #137796 ) ;
#176881=TOROIDAL_SURFACE ( 'NONE', #218522, 11.65000000000000036, 0.1000000000000000056 ) ;
#176911=CIRCLE ( 'NONE', #135362, 0.09999999999998898659 ) ;
#176916=DIRECTION ( 'NONE',  ( 0.000000000000000000, 0.1568667991644863147, 0.9876197685951252359 ) ) ;
#176918=AXIS2_PLACEMENT_3D ( 'NONE', #134467, #57499, #233603 ) ;
#176940=EDGE_CURVE ( 'NONE', #247867, #172688, #5186, .T. ) ;
#176954=ORIENTED_EDGE ( 'NONE', *, *, #125220, .F. ) ;
#176965=CARTESIAN_POINT ( 'NONE',  ( -23.25000000000000000, 11.75000000001115552, -167.4999999999999716 ) ) ;
#176974=CARTESIAN_POINT ( 'NONE',  ( -18.59999999999999787, 6.982009704867601307, -204.6961521182562649 ) ) ;
#177021=VERTEX_POINT ( 'NONE', #218927 ) ;
#177027=DIRECTION ( 'NONE',  ( -1.000000000000000000, 0.000000000000000000, 0.000000000000000000 ) ) ;
#177052=CARTESIAN_POINT ( 'NONE',  ( 18.58222699835054570, 10.33200063080772324, -206.5931674956642610 ) ) ;
#177053=AXIS2_PLACEMENT_3D ( 'NONE', #153728, #173288, #134093 ) ;
#177055=CIRCLE ( 'NONE', #156211, 0.09999999999998898659 ) ;
#177070=ORIENTED_EDGE ( 'NONE', *, *, #12196, .F. ) ;
#177071=VECTOR ( 'NONE', #21919, 1000.000000000000000 ) ;
#177073=CIRCLE ( 'NONE', #89550, 0.09999999999998898659 ) ;
#177081=CIRCLE ( 'NONE', #127169, 0.4000000000000114575 ) ;
#177082=AXIS2_PLACEMENT_3D ( 'NONE', #43346, #240268, #202407 ) ;
#177089=FACE_OUTER_BOUND ( 'NONE', #123607, .T. ) ;
#177099=CARTESIAN_POINT ( 'NONE',  ( 20.53930447207977039, 8.977148687535430938, -175.9425071415753621 ) ) ;
#177106=AXIS2_PLACEMENT_3D ( 'NONE', #126021, #184714, #222545 ) ;
#177110=EDGE_CURVE ( 'NONE', #232095, #34141, #80003, .T. ) ;
#177129=DIRECTION ( 'NONE',  ( 0.000000000000000000, 1.000000000000000000, 0.000000000000000000 ) ) ;
#177138=ORIENTED_EDGE ( 'NONE', *, *, #34975, .T. ) ;
#177139=DIRECTION ( 'NONE',  ( 1.000000000000000000, 0.000000000000000000, 0.000000000000000000 ) ) ;
#177148=EDGE_CURVE ( 'NONE', #220110, #63695, #225336, .T. ) ;
#177155=DIRECTION ( 'NONE',  ( 0.000000000000000000, 0.000000000000000000, -1.000000000000000000 ) ) ;
#177172=DIRECTION ( 'NONE',  ( -0.000000000000000000, -0.000000000000000000, -1.000000000000000000 ) ) ;
#177174=EDGE_CURVE ( 'NONE', #72109, #254577, #30182, .T. ) ;
#177179=EDGE_CURVE ( 'NONE', #85475, #27168, #124987, .T. ) ;
#177190=EDGE_CURVE ( 'NONE', #45677, #38476, #184093, .T. ) ;
#177203=ORIENTED_EDGE ( 'NONE', *, *, #186846, .T. ) ;
#177213=ORIENTED_EDGE ( 'NONE', *, *, #189302, .F. ) ;
#177250=EDGE_CURVE ( 'NONE', #132941, #147015, #11463, .T. ) ;
#177277=DIRECTION ( 'NONE',  ( 0.000000000000000000, -1.000000000000000000, 0.000000000000000000 ) ) ;
#177278=CARTESIAN_POINT ( 'NONE',  ( -21.45000000000000284, 7.708578643773852157, -179.7499999999999716 ) ) ;
#177310=ADVANCED_FACE ( 'NONE', ( #255133 ), #140514, .T. ) ;
#177314=B_SPLINE_CURVE_WITH_KNOTS ( 'NONE', 3,
 ( #141648, #99926, #823, #101194 ),
 .UNSPECIFIED., .F., .F.,
 ( 4, 4 ),
 ( 0.000000000000000000, 0.0001048066582182725291 ),
 .UNSPECIFIED. ) ;
#177324=AXIS2_PLACEMENT_3D ( 'NONE', #189285, #92726, #229691 ) ;
#177364=DIRECTION ( 'NONE',  ( 0.000000000000000000, 1.000000000000000000, 0.000000000000000000 ) ) ;
#177374=VECTOR ( 'NONE', #75947, 1000.000000000000000 ) ;
#177376=CARTESIAN_POINT ( 'NONE',  ( 21.05000000000000071, 1.115600667400684642E-11, -163.1999999999999602 ) ) ;
#177394=EDGE_CURVE ( 'NONE', #118040, #178378, #36523, .T. ) ;
#177419=EDGE_CURVE ( 'NONE', #158708, #134756, #44686, .T. ) ;
#177425=DIRECTION ( 'NONE',  ( -1.000000000000000000, -0.000000000000000000, -0.000000000000000000 ) ) ;
#177432=AXIS2_PLACEMENT_3D ( 'NONE', #72964, #148633, #49520 ) ;
#177464=EDGE_CURVE ( 'NONE', #22716, #107478, #123389, .T. ) ;
#177487=VERTEX_POINT ( 'NONE', #163806 ) ;
#177488=CYLINDRICAL_SURFACE ( 'NONE', #125313, 11.80000000000000426 ) ;
#177547=CARTESIAN_POINT ( 'NONE',  ( 23.14999999999998437, 1.115600667400684642E-11, -167.4999999999999716 ) ) ;
#177551=VERTEX_POINT ( 'NONE', #133649 ) ;
#177559=CIRCLE ( 'NONE', #10941, 11.89999999999999858 ) ;
#177578=TOROIDAL_SURFACE ( 'NONE', #181643, 3.899999999999999467, 0.1000000000000000056 ) ;
#177579=EDGE_CURVE ( 'NONE', #138331, #201908, #169801, .T. ) ;
#177583=ORIENTED_EDGE ( 'NONE', *, *, #75736, .T. ) ;
#177596=DIRECTION ( 'NONE',  ( 0.000000000000000000, 0.000000000000000000, -1.000000000000000000 ) ) ;
#177611=EDGE_CURVE ( 'NONE', #7452, #197017, #194929, .T. ) ;
#177624=EDGE_CURVE ( 'NONE', #75581, #86050, #175377, .T. ) ;
#177626=CARTESIAN_POINT ( 'NONE',  ( -18.58693740092132884, -9.406432150241801793, -174.6248164565013496 ) ) ;
#177628=LINE ( 'NONE', #216714, #133589 ) ;
#177630=VERTEX_POINT ( 'NONE', #251006 ) ;
#177633=DIRECTION ( 'NONE',  ( 1.000000000000000000, 0.000000000000000000, -0.000000000000000000 ) ) ;
#177640=CARTESIAN_POINT ( 'NONE',  ( 20.85000000000000142, 11.75000000001115907, -200.9999999999999432 ) ) ;
#177677=ORIENTED_EDGE ( 'NONE', *, *, #45405, .T. ) ;
#177681=ORIENTED_EDGE ( 'NONE', *, *, #185943, .T. ) ;
#177682=FACE_OUTER_BOUND ( 'NONE', #111159, .T. ) ;
#177683=DIRECTION ( 'NONE',  ( -1.000000000000000000, 0.000000000000000000, 0.000000000000000000 ) ) ;
#177716=ORIENTED_EDGE ( 'NONE', *, *, #192182, .F. ) ;
#177784=DIRECTION ( 'NONE',  ( 0.000000000000000000, 0.000000000000000000, -1.000000000000000000 ) ) ;
#177850=DIRECTION ( 'NONE',  ( 0.000000000000000000, 0.000000000000000000, 1.000000000000000000 ) ) ;
#177852=CARTESIAN_POINT ( 'NONE',  ( -20.54999999999999716, -9.399999999988846611, -191.1060308773475356 ) ) ;
#177876=DIRECTION ( 'NONE',  ( 0.000000000000000000, -1.000000000000000000, 0.000000000000000000 ) ) ;
#177881=EDGE_LOOP ( 'NONE', ( #78183, #93402 ) ) ;
#177895=CARTESIAN_POINT ( 'NONE',  ( 22.24259225415828922, 0.09906588346399246292, -160.0080621294345633 ) ) ;
#177909=ORIENTED_EDGE ( 'NONE', *, *, #230815, .F. ) ;
#177913=EDGE_CURVE ( 'NONE', #195513, #42095, #219252, .T. ) ;
#177917=DIRECTION ( 'NONE',  ( 1.000000000000000000, -0.000000000000000000, -0.000000000000000000 ) ) ;
#177934=DIRECTION ( 'NONE',  ( 0.000000000000000000, -0.8660254037844384856, 0.5000000000000002220 ) ) ;
#177964=CARTESIAN_POINT ( 'NONE',  ( 21.04999999999914806, 10.54375127550720137, -175.0563878086650504 ) ) ;
#177967=CARTESIAN_POINT ( 'NONE',  ( -20.85000000000000142, 7.021664781911246322, -204.6335654018972434 ) ) ;
#177992=CARTESIAN_POINT ( 'NONE',  ( 20.95017935633852346, 10.47548927963648246, -175.0774397973904399 ) ) ;
#177998=AXIS2_PLACEMENT_3D ( 'NONE', #115983, #33918, #192945 ) ;
#178077=CARTESIAN_POINT ( 'NONE',  ( 18.49999999999999289, 10.49142135624846439, -192.3499999999999659 ) ) ;
#178107=FACE_OUTER_BOUND ( 'NONE', #106656, .T. ) ;
#178150=ORIENTED_EDGE ( 'NONE', *, *, #189145, .T. ) ;
#178159=DIRECTION ( 'NONE',  ( 1.000000000000000000, 7.304098846218134667E-16, -0.000000000000000000 ) ) ;
#178171=AXIS2_PLACEMENT_3D ( 'NONE', #184893, #7542, #126196 ) ;
#178199=CARTESIAN_POINT ( 'NONE',  ( -21.14999999999999858, -11.64999999998884483, -167.4999999999999716 ) ) ;
#178203=ORIENTED_EDGE ( 'NONE', *, *, #29896, .T. ) ;
#178239=EDGE_CURVE ( 'NONE', #96541, #244617, #148443, .T. ) ;
#178240=CARTESIAN_POINT ( 'NONE',  ( 21.30000000000002558, 1.115650265596050101E-11, -171.5499999999999829 ) ) ;
#178255=VERTEX_POINT ( 'NONE', #128880 ) ;
#178276=DIRECTION ( 'NONE',  ( 1.000000000000000000, 0.000000000000000000, -0.000000000000000000 ) ) ;
#178298=EDGE_CURVE ( 'NONE', #135423, #228990, #14072, .T. ) ;
#178318=AXIS2_PLACEMENT_3D ( 'NONE', #224139, #123774, #162918 ) ;
#178327=CARTESIAN_POINT ( 'NONE',  ( -20.94999999999999929, -11.29603075032412640, -197.9521008403361009 ) ) ;
#178337=DIRECTION ( 'NONE',  ( -1.000000000000000000, -0.000000000000000000, 0.000000000000000000 ) ) ;
#178371=DIRECTION ( 'NONE',  ( -7.304098846218201720E-16, 1.000000000000000000, 0.000000000000000000 ) ) ;
#178378=VERTEX_POINT ( 'NONE', #133994 ) ;
#178391=AXIS2_PLACEMENT_3D ( 'NONE', #85156, #4361, #8242 ) ;
#178393=ORIENTED_EDGE ( 'NONE', *, *, #44129, .T. ) ;
#178404=ADVANCED_FACE ( 'NONE', ( #214814 ), #111308, .T. ) ;
#178406=DIRECTION ( 'NONE',  ( 0.000000000000000000, -8.881784197000871698E-16, -1.000000000000000000 ) ) ;
#178412=DIRECTION ( 'NONE',  ( -1.000000000000000000, 0.000000000000000000, 0.000000000000000000 ) ) ;
#178421=LINE ( 'NONE', #158853, #57510 ) ;
#178425=ADVANCED_FACE ( 'NONE', ( #56998 ), #72781, .F. ) ;
#178441=CYLINDRICAL_SURFACE ( 'NONE', #136836, 0.09999999999998898659 ) ;
#178443=ORIENTED_EDGE ( 'NONE', *, *, #76171, .F. ) ;
#178444=CARTESIAN_POINT ( 'NONE',  ( -23.25000000000000000, -11.74999999998884448, -167.4999999999999432 ) ) ;
#178463=DIRECTION ( 'NONE',  ( 1.000000000000000000, 0.000000000000000000, 0.000000000000000000 ) ) ;
#178489=ORIENTED_EDGE ( 'NONE', *, *, #219388, .T. ) ;
#178529=VERTEX_POINT ( 'NONE', #103835 ) ;
#178560=CARTESIAN_POINT ( 'NONE',  ( -20.64999999999999858, -8.730841121484171907, -177.0980747189843214 ) ) ;
#178629=CARTESIAN_POINT ( 'NONE',  ( 23.15000000000000213, -9.599999999988845900, -177.3939691226524076 ) ) ;
#178681=ORIENTED_EDGE ( 'NONE', *, *, #18326, .T. ) ;
#178695=AXIS2_PLACEMENT_3D ( 'NONE', #20690, #158918, #238432 ) ;
#178705=ORIENTED_EDGE ( 'NONE', *, *, #250878, .T. ) ;
#178736=CARTESIAN_POINT ( 'NONE',  ( 23.14999999999999858, -11.74999999998883560, -155.7499999999999716 ) ) ;
#178785=ORIENTED_EDGE ( 'NONE', *, *, #95466, .T. ) ;
#178787=CYLINDRICAL_SURFACE ( 'NONE', #41757, 0.09999999999998898659 ) ;
#178806=CARTESIAN_POINT ( 'NONE',  ( 21.95218792049437795, 7.201507561257818324, -167.4009715602000483 ) ) ;
#178819=ORIENTED_EDGE ( 'NONE', *, *, #158046, .F. ) ;
#178837=AXIS2_PLACEMENT_3D ( 'NONE', #163141, #242648, #44475 ) ;
#178848=ORIENTED_EDGE ( 'NONE', *, *, #98856, .T. ) ;
#178866=VERTEX_POINT ( 'NONE', #121846 ) ;
#178867=VERTEX_POINT ( 'NONE', #198793 ) ;
#178891=VECTOR ( 'NONE', #35516, 1000.000000000000000 ) ;
#178941=STYLED_ITEM ( 'NONE', ( #123143 ), #110572 ) ;
#178951=AXIS2_PLACEMENT_3D ( 'NONE', #255951, #148230, #194771 ) ;
#178968=ORIENTED_EDGE ( 'NONE', *, *, #69926, .T. ) ;
#179056=DIRECTION ( 'NONE',  ( 1.000000000000000000, -0.000000000000000000, -0.000000000000000000 ) ) ;
#179088=CIRCLE ( 'NONE', #137336, 0.09999999999998898659 ) ;
#179090=VERTEX_POINT ( 'NONE', #189528 ) ;
#179097=EDGE_LOOP ( 'NONE', ( #181315, #52020, #125246, #232551, #179402 ) ) ;
#179126=CARTESIAN_POINT ( 'NONE',  ( -21.05000000000000071, 5.900000000011162093, -190.7809002353436085 ) ) ;
#179140=EDGE_CURVE ( 'NONE', #15539, #199092, #112559, .T. ) ;
#179177=DIRECTION ( 'NONE',  ( -1.000000000000000000, -0.000000000000000000, 0.000000000000000000 ) ) ;
#179238=AXIS2_PLACEMENT_3D ( 'NONE', #12763, #92261, #184305 ) ;
#179262=ORIENTED_EDGE ( 'NONE', *, *, #98804, .F. ) ;
#179327=ORIENTED_EDGE ( 'NONE', *, *, #200770, .F. ) ;
#179350=CARTESIAN_POINT ( 'NONE',  ( -21.04999999999999716, 6.307425219576570541, -167.5168198683856247 ) ) ;
#179381=DIRECTION ( 'NONE',  ( 0.000000000000000000, 0.000000000000000000, -1.000000000000000000 ) ) ;
#179388=ORIENTED_EDGE ( 'NONE', *, *, #99475, .T. ) ;
#179402=ORIENTED_EDGE ( 'NONE', *, *, #73390, .F. ) ;
#179466=EDGE_CURVE ( 'NONE', #165951, #5557, #223185, .T. ) ;
#179474=FACE_OUTER_BOUND ( 'NONE', #45364, .T. ) ;
#179479=CARTESIAN_POINT ( 'NONE',  ( 20.12500000000000000, 9.750000000011153745, -175.6117712821142618 ) ) ;
#179495=ORIENTED_EDGE ( 'NONE', *, *, #57533, .T. ) ;
#179514=AXIS2_PLACEMENT_3D ( 'NONE', #108562, #90259, #169868 ) ;
#179519=DIRECTION ( 'NONE',  ( -0.000000000000000000, 0.8660254037844411501, 0.4999999999999956701 ) ) ;
#179552=AXIS2_PLACEMENT_3D ( 'NONE', #128341, #44942, #4511 ) ;
#179560=VERTEX_POINT ( 'NONE', #30155 ) ;
#179581=( BOUNDED_SURFACE ( )  B_SPLINE_SURFACE ( 3, 2, ( 
 ( #51557, #32061, #131128 ),
 ( #191136, #91998, #253627 ),
 ( #50291, #248509, #129837 ),
 ( #209382, #110275, #189829 ),
 ( #11189, #90711, #33359 ),
 ( #170309, #71180, #171577 ) ),
 .UNSPECIFIED., .F., .F., .F. ) 
 B_SPLINE_SURFACE_WITH_KNOTS ( ( 4, 2, 4 ),
 ( 3, 3 ),
 ( 0.0001792624049599819626, 0.0003686986002124877700, 0.0005581347954649935232 ),
 ( 0.000000000000000000, 1.000000000000000000 ),
 .UNSPECIFIED. ) 
 GEOMETRIC_REPRESENTATION_ITEM ( )  RATIONAL_B_SPLINE_SURFACE ( (
 ( 1.000000000000000000, 0.9238795325112830747, 1.000000000000000000),
 ( 1.000000000000000000, 0.9229318695232786585, 1.000000000000000000),
 ( 1.000000000000000000, 0.8926288119238298124, 1.000000000000000000),
 ( 1.000000000000000000, 0.8123777807263558026, 1.000000000000000000),
 ( 1.000000000000000000, 0.7629087100937371746, 1.000000000000000000),
 ( 1.000000000000000000, 0.7071067811865475727, 1.000000000000000000) ) ) 
 REPRESENTATION_ITEM ( '' )  SURFACE ( )  );
#179587=EDGE_CURVE ( 'NONE', #63066, #8158, #106623, .T. ) ;
#179590=CARTESIAN_POINT ( 'NONE',  ( 23.15000000000000213, -8.663551401857999323, -191.4758988819326646 ) ) ;
#179597=EDGE_CURVE ( 'NONE', #253941, #153829, #143197, .T. ) ;
#179664=ORIENTED_EDGE ( 'NONE', *, *, #164755, .T. ) ;
#179665=DIRECTION ( 'NONE',  ( -1.000000000000000000, 9.012599976028471648E-15, 6.882867235861662930E-14 ) ) ;
#179678=EDGE_CURVE ( 'NONE', #52856, #66806, #149461, .T. ) ;
#179680=DIRECTION ( 'NONE',  ( 0.000000000000000000, 0.000000000000000000, -1.000000000000000000 ) ) ;
#179686=ADVANCED_FACE ( 'NONE', ( #25839 ), #84468, .F. ) ;
#179691=CIRCLE ( 'NONE', #117322, 0.09999999999998898659 ) ;
#179698=EDGE_CURVE ( 'NONE', #61007, #8158, #82757, .T. ) ;
#179711=DIRECTION ( 'NONE',  ( 1.000000000000000000, -0.000000000000000000, -0.000000000000000000 ) ) ;
#179712=EDGE_LOOP ( 'NONE', ( #47131, #15611, #47528, #115940 ) ) ;
#179753=FACE_OUTER_BOUND ( 'NONE', #35825, .T. ) ;
#179759=EDGE_CURVE ( 'NONE', #143316, #83250, #133904, .T. ) ;
#179767=AXIS2_PLACEMENT_3D ( 'NONE', #202322, #126639, #242723 ) ;
#179791=AXIS2_PLACEMENT_3D ( 'NONE', #60964, #154971, #57096 ) ;
#179806=EDGE_CURVE ( 'NONE', #145808, #138726, #154789, .T. ) ;
#179807=DIRECTION ( 'NONE',  ( -1.000000000000000000, -0.000000000000000000, -0.000000000000000000 ) ) ;
#179837=CARTESIAN_POINT ( 'NONE',  ( 21.14999999999999503, 1.115600667400684642E-11, -167.4999999999999716 ) ) ;
#179846=DIRECTION ( 'NONE',  ( 1.000000000000000000, 0.000000000000000000, 0.000000000000000000 ) ) ;
#179848=ORIENTED_EDGE ( 'NONE', *, *, #66108, .T. ) ;
#179871=CARTESIAN_POINT ( 'NONE',  ( -20.54999999999999716, 2.000000000011154189, -187.7753780772378889 ) ) ;
#179885=CARTESIAN_POINT ( 'NONE',  ( 18.50000000000000000, -9.399999999988843058, -174.7972597596632625 ) ) ;
#179915=AXIS2_PLACEMENT_3D ( 'NONE', #54142, #213210, #157129 ) ;
#179931=ORIENTED_EDGE ( 'NONE', *, *, #218081, .F. ) ;
#179964=CYLINDRICAL_SURFACE ( 'NONE', #239060, 0.09999999999998898659 ) ;
#179987=AXIS2_PLACEMENT_3D ( 'NONE', #102211, #239193, #145215 ) ;
#180005=ORIENTED_EDGE ( 'NONE', *, *, #136879, .F. ) ;
#180016=CARTESIAN_POINT ( 'NONE',  ( -22.16821283564876666, 7.558973340791935058, -167.4999999999999716 ) ) ;
#180039=DIRECTION ( 'NONE',  ( 0.000000000000000000, 0.000000000000000000, 1.000000000000000000 ) ) ;
#180069=CIRCLE ( 'NONE', #121814, 0.1000000000000000472 ) ;
#180115=CARTESIAN_POINT ( 'NONE',  ( 18.59999999999999076, 6.650000000011155876, -188.6499999999999488 ) ) ;
#180125=ORIENTED_EDGE ( 'NONE', *, *, #189917, .F. ) ;
#180140=CIRCLE ( 'NONE', #67692, 0.09999999999998898659 ) ;
#180151=DIRECTION ( 'NONE',  ( 0.000000000000000000, -0.000000000000000000, 1.000000000000000000 ) ) ;
#180157=TOROIDAL_SURFACE ( 'NONE', #5135, 11.70000000000000107, 0.1000000000000000056 ) ;
#180168=ORIENTED_EDGE ( 'NONE', *, *, #224264, .T. ) ;
#180180=ORIENTED_EDGE ( 'NONE', *, *, #96331, .F. ) ;
#180209=ORIENTED_EDGE ( 'NONE', *, *, #236285, .T. ) ;
#180223=CARTESIAN_POINT ( 'NONE',  ( 20.85000000000000142, 11.65000000001115943, -200.9999999999999432 ) ) ;
#180264=CARTESIAN_POINT ( 'NONE',  ( -18.59999999999999787, 11.65000000001115232, -174.5148057706539930 ) ) ;
#180269=DIRECTION ( 'NONE',  ( 0.000000000000000000, 1.000000000000000000, 0.000000000000000000 ) ) ;
#180275=CARTESIAN_POINT ( 'NONE',  ( 18.51997666896878059, -9.392332131507652448, -174.6434061874831514 ) ) ;
#180328=ORIENTED_EDGE ( 'NONE', *, *, #224312, .T. ) ;
#180344=ORIENTED_EDGE ( 'NONE', *, *, #115519, .F. ) ;
#180362=VERTEX_POINT ( 'NONE', #108591 ) ;
#180367=EDGE_CURVE ( 'NONE', #54023, #213186, #188132, .T. ) ;
#180396=EDGE_CURVE ( 'NONE', #70888, #3673, #40661, .T. ) ;
#180405=CARTESIAN_POINT ( 'NONE',  ( -20.54999999999999716, 2.500000000011154633, -187.7753780772378889 ) ) ;
#180415=EDGE_LOOP ( 'NONE', ( #64930, #90631, #54976 ) ) ;
#180419=EDGE_CURVE ( 'NONE', #38476, #128403, #12275, .T. ) ;
#180430=DIRECTION ( 'NONE',  ( 0.000000000000000000, -1.000000000000000000, 0.000000000000000000 ) ) ;
#180501=AXIS2_PLACEMENT_3D ( 'NONE', #176493, #177784, #21283 ) ;
#180508=EDGE_CURVE ( 'NONE', #6622, #236967, #37393, .T. ) ;
#180520=CARTESIAN_POINT ( 'NONE',  ( 21.05995757104869170, 8.775389244732430427, -179.6949051229912016 ) ) ;
#180564=DIRECTION ( 'NONE',  ( 0.000000000000000000, 1.000000000000000000, 0.000000000000000000 ) ) ;
#180582=ORIENTED_EDGE ( 'NONE', *, *, #79596, .F. ) ;
#180588=ORIENTED_EDGE ( 'NONE', *, *, #203998, .T. ) ;
#180615=VERTEX_POINT ( 'NONE', #243942 ) ;
#180634=ORIENTED_EDGE ( 'NONE', *, *, #43279, .F. ) ;
#180668=CIRCLE ( 'NONE', #197403, 0.09999999999998898659 ) ;
#180714=ADVANCED_FACE ( 'NONE', ( #87430 ), #75008, .F. ) ;
#180751=DIRECTION ( 'NONE',  ( -1.000000000000000000, 0.000000000000000000, 0.000000000000000000 ) ) ;
#180755=EDGE_CURVE ( 'NONE', #122594, #17724, #225263, .T. ) ;
#180768=VECTOR ( 'NONE', #154805, 1000.000000000000000 ) ;
#180777=FACE_OUTER_BOUND ( 'NONE', #167558, .T. ) ;
#180787=FACE_OUTER_BOUND ( 'NONE', #245436, .T. ) ;
#180799=DIRECTION ( 'NONE',  ( -2.342056488767301376E-15, -0.1350103645451904977, 0.9908441862701596881 ) ) ;
#180809=DIRECTION ( 'NONE',  ( -1.000000000000000000, 0.000000000000000000, 0.000000000000000000 ) ) ;
#180814=ORIENTED_EDGE ( 'NONE', *, *, #6709, .F. ) ;
#180896=ORIENTED_EDGE ( 'NONE', *, *, #168346, .F. ) ;
#180911=EDGE_CURVE ( 'NONE', #43643, #20715, #116666, .T. ) ;
#180920=CARTESIAN_POINT ( 'NONE',  ( -18.59999999999999787, 1.835341550235567887, -179.0551512925629538 ) ) ;
#180940=ORIENTED_EDGE ( 'NONE', *, *, #174, .F. ) ;
#180956=DIRECTION ( 'NONE',  ( -1.000000000000000000, 0.000000000000000000, 0.000000000000000000 ) ) ;
#180965=DIRECTION ( 'NONE',  ( -1.000000000000000000, 0.000000000000000000, 0.000000000000000000 ) ) ;
#181003=ADVANCED_FACE ( 'NONE', ( #8890 ), #224969, .F. ) ;
#181037=CARTESIAN_POINT ( 'NONE',  ( 23.14999999999999503, 11.65000000001116298, -194.0851942293460013 ) ) ;
#181072=DIRECTION ( 'NONE',  ( -1.000000000000000000, -2.952720810173289112E-16, 0.000000000000000000 ) ) ;
#181083=DIRECTION ( 'NONE',  ( 0.000000000000000000, 0.000000000000000000, -1.000000000000000000 ) ) ;
#181086=ORIENTED_EDGE ( 'NONE', *, *, #104444, .T. ) ;
#181087=DIRECTION ( 'NONE',  ( -1.000000000000000000, 0.000000000000000000, 0.000000000000000000 ) ) ;
#181123=DIRECTION ( 'NONE',  ( 1.000000000000000000, 0.000000000000000000, 0.000000000000000000 ) ) ;
#181125=DIRECTION ( 'NONE',  ( 0.000000000000000000, -0.9915357197604971473, 0.1298341882519111479 ) ) ;
#181158=CARTESIAN_POINT ( 'NONE',  ( -18.59999999999999787, 1.162701749949165642, -175.5999999999999659 ) ) ;
#181167=ORIENTED_EDGE ( 'NONE', *, *, #84670, .F. ) ;
#181179=TOROIDAL_SURFACE ( 'NONE', #177082, 2.100000000000002309, 0.1000000000000000056 ) ;
#181185=DIRECTION ( 'NONE',  ( 0.000000000000000000, 0.000000000000000000, -1.000000000000000000 ) ) ;
#181204=CARTESIAN_POINT ( 'NONE',  ( 22.47110162079220785, 0.02879741281384913879, -155.8500640633156422 ) ) ;
#181207=ORIENTED_EDGE ( 'NONE', *, *, #191076, .T. ) ;
#181215=DIRECTION ( 'NONE',  ( -1.000000000000000000, -2.952720810173289112E-16, 0.000000000000000000 ) ) ;
#181233=EDGE_CURVE ( 'NONE', #60251, #166220, #58575, .T. ) ;
#181281=CARTESIAN_POINT ( 'NONE',  ( 21.09793522318412684, 10.72462451022393282, -179.7392908709771007 ) ) ;
#181287=LINE ( 'NONE', #62608, #93339 ) ;
#181315=ORIENTED_EDGE ( 'NONE', *, *, #156571, .T. ) ;
#181333=ORIENTED_EDGE ( 'NONE', *, *, #133226, .F. ) ;
#181381=VERTEX_POINT ( 'NONE', #250702 ) ;
#181387=LINE ( 'NONE', #204759, #160833 ) ;
#181397=ORIENTED_EDGE ( 'NONE', *, *, #136757, .T. ) ;
#181435=ORIENTED_EDGE ( 'NONE', *, *, #34064, .F. ) ;
#181439=CARTESIAN_POINT ( 'NONE',  ( 22.60000000000000142, 1.115600667400684642E-11, -167.4999999999999716 ) ) ;
#181465=EDGE_CURVE ( 'NONE', #182323, #31369, #177628, .T. ) ;
#181494=ORIENTED_EDGE ( 'NONE', *, *, #27016, .F. ) ;
#181499=CARTESIAN_POINT ( 'NONE',  ( 18.59999999999999076, -1.249999999988843369, -175.4999999999999716 ) ) ;
#181517=DIRECTION ( 'NONE',  ( 0.000000000000000000, 0.000000000000000000, -1.000000000000000000 ) ) ;
#181541=EDGE_CURVE ( 'NONE', #114385, #119397, #58898, .T. ) ;
#181560=ORIENTED_EDGE ( 'NONE', *, *, #8297, .F. ) ;
#181568=FACE_OUTER_BOUND ( 'NONE', #118829, .T. ) ;
#181608=AXIS2_PLACEMENT_3D ( 'NONE', #150378, #52533, #116384 ) ;
#181615=ORIENTED_EDGE ( 'NONE', *, *, #129836, .F. ) ;
#181616=DIRECTION ( 'NONE',  ( 0.000000000000000000, 0.000000000000000000, -1.000000000000000000 ) ) ;
#181620=EDGE_LOOP ( 'NONE', ( #229801, #172525, #80607, #38271, #225550 ) ) ;
#181622=AXIS2_PLACEMENT_3D ( 'NONE', #96073, #115660, #19121 ) ;
#181626=EDGE_CURVE ( 'NONE', #213687, #246745, #175325, .T. ) ;
#181643=AXIS2_PLACEMENT_3D ( 'NONE', #83579, #44505, #245271 ) ;
#181657=ORIENTED_EDGE ( 'NONE', *, *, #214552, .T. ) ;
#181680=ADVANCED_FACE ( 'NONE', ( #212581 ), #191755, .F. ) ;
#181706=DIRECTION ( 'NONE',  ( 1.000000000000000000, 3.265361837132813093E-16, -0.000000000000000000 ) ) ;
#181719=CARTESIAN_POINT ( 'NONE',  ( -18.59999999999999787, -1.835859311432481045, -212.6044391687984785 ) ) ;
#181734=CYLINDRICAL_SURFACE ( 'NONE', #178391, 0.09999999999999939493 ) ;
#181739=VERTEX_POINT ( 'NONE', #228290 ) ;
#181759=DIRECTION ( 'NONE',  ( -1.000000000000000000, -2.952720810173289112E-16, 0.000000000000000000 ) ) ;
#181777=AXIS2_PLACEMENT_3D ( 'NONE', #35581, #233766, #198471 ) ;
#181787=ORIENTED_EDGE ( 'NONE', *, *, #164870, .T. ) ;
#181824=CARTESIAN_POINT ( 'NONE',  ( -20.54999999999999716, 2.500000000011156409, -180.7246219227620543 ) ) ;
#181831=CARTESIAN_POINT ( 'NONE',  ( 20.95539060131842746, 10.62386215766680131, -175.1537338136561743 ) ) ;
#181844=ORIENTED_EDGE ( 'NONE', *, *, #111898, .T. ) ;
#181876=CIRCLE ( 'NONE', #131805, 2.000000000000002665 ) ;
#181885=CARTESIAN_POINT ( 'NONE',  ( 23.14999999999999858, 2.100000000011158274, -200.9999999999999432 ) ) ;
#181901=ORIENTED_EDGE ( 'NONE', *, *, #28063, .T. ) ;
#181933=CYLINDRICAL_SURFACE ( 'NONE', #169498, 7.899999999999990585 ) ;
#181971=ORIENTED_EDGE ( 'NONE', *, *, #107275, .T. ) ;
#182007=EDGE_CURVE ( 'NONE', #241874, #253941, #122465, .T. ) ;
#182054=ORIENTED_EDGE ( 'NONE', *, *, #249728, .F. ) ;
#182075=CARTESIAN_POINT ( 'NONE',  ( 20.85000000000000142, 11.75000000001115907, -194.2161343370218560 ) ) ;
#182105=AXIS2_PLACEMENT_3D ( 'NONE', #62741, #143547, #142264 ) ;
#182108=EDGE_CURVE ( 'NONE', #107466, #256132, #167152, .T. ) ;
#182111=ORIENTED_EDGE ( 'NONE', *, *, #80246, .F. ) ;
#182115=FACE_OUTER_BOUND ( 'NONE', #189040, .T. ) ;
#182117=CARTESIAN_POINT ( 'NONE',  ( -21.14999999999999858, 11.65000000001115588, -167.5999999999999659 ) ) ;
#182126=CIRCLE ( 'NONE', #207263, 11.75000000000001066 ) ;
#182141=ADVANCED_FACE ( 'NONE', ( #31099 ), #128886, .F. ) ;
#182142=ADVANCED_FACE ( 'NONE', ( #110589 ), #170628, .F. ) ;
#182189=VECTOR ( 'NONE', #237007, 1000.000000000000000 ) ;
#182192=ORIENTED_EDGE ( 'NONE', *, *, #138001, .T. ) ;
#182228=EDGE_CURVE ( 'NONE', #154602, #243191, #113128, .T. ) ;
#182318=CIRCLE ( 'NONE', #244830, 11.79999999999999893 ) ;
#182323=VERTEX_POINT ( 'NONE', #114446 ) ;
#182339=VERTEX_POINT ( 'NONE', #36214 ) ;
#182355=VERTEX_POINT ( 'NONE', #19194 ) ;
#182388=LINE ( 'NONE', #205781, #150729 ) ;
#182395=CARTESIAN_POINT ( 'NONE',  ( -21.07954640115348610, 6.329287696035510891, -167.4339922928603528 ) ) ;
#182405=CIRCLE ( 'NONE', #20076, 0.09999999999999971412 ) ;
#182457=FACE_OUTER_BOUND ( 'NONE', #71692, .T. ) ;
#182481=VECTOR ( 'NONE', #167964, 1000.000000000000000 ) ;
#182506=VECTOR ( 'NONE', #50258, 1000.000000000000000 ) ;
#182561=CARTESIAN_POINT ( 'NONE',  ( 21.06089410995830491, 10.72529553213474429, -179.7023807310431494 ) ) ;
#182588=ORIENTED_EDGE ( 'NONE', *, *, #177464, .T. ) ;
#182590=CIRCLE ( 'NONE', #241018, 0.1999999999999996503 ) ;
#182624=ORIENTED_EDGE ( 'NONE', *, *, #170001, .F. ) ;
#182632=EDGE_LOOP ( 'NONE', ( #92472, #203289, #115075 ) ) ;
#182634=DIRECTION ( 'NONE',  ( 0.000000000000000000, 0.000000000000000000, -1.000000000000000000 ) ) ;
#182636=ORIENTED_EDGE ( 'NONE', *, *, #103815, .F. ) ;
#182638=LINE ( 'NONE', #86049, #164740 ) ;
#182656=CARTESIAN_POINT ( 'NONE',  ( -21.55000000000000426, 7.708578643773852157, -188.7499999999999716 ) ) ;
#182663=CIRCLE ( 'NONE', #91062, 0.09999999999998898659 ) ;
#182666=VERTEX_POINT ( 'NONE', #236639 ) ;
#182671=TOROIDAL_SURFACE ( 'NONE', #140975, 0.2000000000000000111, 0.1000000000000000056 ) ;
#182681=CIRCLE ( 'NONE', #169670, 0.2000000000000057288 ) ;
#182703=CARTESIAN_POINT ( 'NONE',  ( -21.05000000000000071, 1.115600667400684642E-11, -200.9999999999999432 ) ) ;
#182721=EDGE_CURVE ( 'NONE', #49571, #183971, #4397, .T. ) ;
#182727=LINE ( 'NONE', #62763, #244408 ) ;
#182796=ADVANCED_FACE ( 'NONE', ( #63130 ), #239216, .T. ) ;
#182817=ORIENTED_EDGE ( 'NONE', *, *, #180755, .F. ) ;
#182833=VERTEX_POINT ( 'NONE', #59248 ) ;
#182852=CARTESIAN_POINT ( 'NONE',  ( -20.64999999999999858, 4.350000000011156054, -179.8499999999999943 ) ) ;
#182859=AXIS2_PLACEMENT_3D ( 'NONE', #117312, #74371, #14389 ) ;
#182899=FACE_OUTER_BOUND ( 'NONE', #172385, .T. ) ;
#182911=ORIENTED_EDGE ( 'NONE', *, *, #32652, .F. ) ;
#182921=CARTESIAN_POINT ( 'NONE',  ( -18.59999999999999787, 1.115600667400684642E-11, -167.4999999999999716 ) ) ;
#182936=ADVANCED_FACE ( 'NONE', ( #172245 ), #147838, .T. ) ;
#182959=DIRECTION ( 'NONE',  ( 1.000000000000000000, -0.000000000000000000, -0.000000000000000000 ) ) ;
#182980=CIRCLE ( 'NONE', #216089, 0.09999999999999939493 ) ;
#183087=ADVANCED_FACE ( 'NONE', ( #99051 ), #234738, .T. ) ;
#183099=CARTESIAN_POINT ( 'NONE',  ( 21.04999999999999716, 6.304455821958825368, -167.5210354765400780 ) ) ;
#183165=DIRECTION ( 'NONE',  ( 0.000000000000000000, -0.1350103645451876944, 0.9908441862701601321 ) ) ;
#183184=DIRECTION ( 'NONE',  ( -0.000000000000000000, 0.000000000000000000, -1.000000000000000000 ) ) ;
#183211=EDGE_LOOP ( 'NONE', ( #111066, #24181, #170507, #191821 ) ) ;
#183215=ADVANCED_FACE ( 'NONE', ( #164200 ), #126340, .F. ) ;
#183233=EDGE_CURVE ( 'NONE', #236853, #128410, #65808, .T. ) ;
#183313=DIRECTION ( 'NONE',  ( 0.000000000000000000, 1.000000000000000000, 0.000000000000000000 ) ) ;
#183315=DIRECTION ( 'NONE',  ( -0.000000000000000000, -0.000000000000000000, -1.000000000000000000 ) ) ;
#183344=AXIS2_PLACEMENT_3D ( 'NONE', #225454, #8997, #88505 ) ;
#183347=CIRCLE ( 'NONE', #249979, 2.000000000000001776 ) ;
#183352=ORIENTED_EDGE ( 'NONE', *, *, #160692, .F. ) ;
#183377=EDGE_LOOP ( 'NONE', ( #61706, #170193, #51607, #226434, #99712 ) ) ;
#183386=AXIS2_PLACEMENT_3D ( 'NONE', #138585, #1662, #181616 ) ;
#183404=DIRECTION ( 'NONE',  ( 1.000000000000000000, 0.000000000000000000, 0.000000000000000000 ) ) ;
#183411=CARTESIAN_POINT ( 'NONE',  ( -20.94999999999999929, 7.021664781911246322, -204.8335654018972605 ) ) ;
#183414=CIRCLE ( 'NONE', #158487, 0.09999999999999864553 ) ;
#183420=CARTESIAN_POINT ( 'NONE',  ( -21.04999999999999716, -9.599999999988844124, -174.5320693966996259 ) ) ;
#183440=DIRECTION ( 'NONE',  ( -2.827886303505248766E-16, 0.8660254037844411501, 0.4999999999999956146 ) ) ;
#183461=DIRECTION ( 'NONE',  ( 0.000000000000000000, 1.000000000000000000, -6.308085367188393199E-16 ) ) ;
#183476=CARTESIAN_POINT ( 'NONE',  ( 20.94999999999999929, 5.000000000011153745, -188.5947339810868755 ) ) ;
#183494=CARTESIAN_POINT ( 'NONE',  ( 20.77766267348356166, 10.44904239062959839, -175.0927089158778074 ) ) ;
#183514=CYLINDRICAL_SURFACE ( 'NONE', #220611, 4.049999999999998046 ) ;
#183540=ORIENTED_EDGE ( 'NONE', *, *, #61729, .F. ) ;
#183561=ORIENTED_EDGE ( 'NONE', *, *, #122929, .F. ) ;
#183571=CARTESIAN_POINT ( 'NONE',  ( -23.15000000000000213, 1.115625160336667635E-11, -202.9999999999999716 ) ) ;
#183604=EDGE_CURVE ( 'NONE', #90327, #56940, #172398, .T. ) ;
#183607=FACE_OUTER_BOUND ( 'NONE', #45404, .T. ) ;
#183631=CONICAL_SURFACE ( 'NONE', #200380, 6.250000000000005329, 0.7853981633974431720 ) ;
#183661=CARTESIAN_POINT ( 'NONE',  ( 18.48413544395662100, -9.664304033616598844, -207.6831049930382562 ) ) ;
#183673=CARTESIAN_POINT ( 'NONE',  ( -22.00411653889214136, 0.09903810579743195508, -160.2465571323594986 ) ) ;
#183676=CARTESIAN_POINT ( 'NONE',  ( -21.05000000000000071, 6.478078221105875834, -167.5999999353044529 ) ) ;
#183720=DIRECTION ( 'NONE',  ( 1.000000000000000000, -0.000000000000000000, -0.000000000000000000 ) ) ;
#183729=CARTESIAN_POINT ( 'NONE',  ( 22.49231231312462853, 11.64998490368843953, -167.4389471123986084 ) ) ;
#183750=FACE_OUTER_BOUND ( 'NONE', #188041, .T. ) ;
#183761=CARTESIAN_POINT ( 'NONE',  ( 21.14999999999999503, -11.74999999998883560, -170.3999999999999773 ) ) ;
#183770=ADVANCED_FACE ( 'NONE', ( #187770 ), #104865, .T. ) ;
#183774=EDGE_CURVE ( 'NONE', #117379, #226840, #130014, .T. ) ;
#183780=ORIENTED_EDGE ( 'NONE', *, *, #99000, .T. ) ;
#183794=CARTESIAN_POINT ( 'NONE',  ( -21.59142135623730852, 7.850000000011158718, -179.8499999999999943 ) ) ;
#183811=ORIENTED_EDGE ( 'NONE', *, *, #114358, .T. ) ;
#183822=CARTESIAN_POINT ( 'NONE',  ( 21.11344571971254069, 10.61787902352924817, -179.7460208924021856 ) ) ;
#183836=DIRECTION ( 'NONE',  ( 0.000000000000000000, 0.000000000000000000, -1.000000000000000000 ) ) ;
#183844=EDGE_CURVE ( 'NONE', #232247, #115618, #9123, .T. ) ;
#183860=CARTESIAN_POINT ( 'NONE',  ( -23.15000000000000213, 4.350000000011156054, -179.7499999999999716 ) ) ;
#183867=DIRECTION ( 'NONE',  ( 0.000000000000000000, 0.000000000000000000, -1.000000000000000000 ) ) ;
#183870=DIRECTION ( 'NONE',  ( 1.000000000000000000, 2.952720810173289112E-16, -0.000000000000000000 ) ) ;
#183880=CARTESIAN_POINT ( 'NONE',  ( -20.54999999999999716, -8.999999999988844479, -191.1060308773475356 ) ) ;
#183886=VERTEX_POINT ( 'NONE', #213731 ) ;
#183895=AXIS2_PLACEMENT_3D ( 'NONE', #23103, #160051, #141735 ) ;
#183930=ORIENTED_EDGE ( 'NONE', *, *, #22304, .T. ) ;
#183943=ORIENTED_EDGE ( 'NONE', *, *, #7888, .T. ) ;
#183957=CIRCLE ( 'NONE', #21479, 11.64999999999999325 ) ;
#183962=VERTEX_POINT ( 'NONE', #249030 ) ;
#183971=VERTEX_POINT ( 'NONE', #218851 ) ;
#183988=ORIENTED_EDGE ( 'NONE', *, *, #35283, .F. ) ;
#184004=AXIS2_PLACEMENT_3D ( 'NONE', #222522, #64749, #223813 ) ;
#184030=AXIS2_PLACEMENT_3D ( 'NONE', #171388, #151805, #128375 ) ;
#184057=DIRECTION ( 'NONE',  ( 0.000000000000000000, 0.000000000000000000, -1.000000000000000000 ) ) ;
#184058=DIRECTION ( 'NONE',  ( -2.602085213965226419E-14, -0.000000000000000000, -1.000000000000000000 ) ) ;
#184071=ORIENTED_EDGE ( 'NONE', *, *, #14498, .T. ) ;
#184075=AXIS2_PLACEMENT_3D ( 'NONE', #4496, #103586, #124475 ) ;
#184093=CIRCLE ( 'NONE', #59151, 0.09999999999999939493 ) ;
#184112=ADVANCED_FACE ( 'NONE', ( #199318 ), #254873, .F. ) ;
#184151=EDGE_CURVE ( 'NONE', #32139, #191879, #250998, .T. ) ;
#184185=EDGE_LOOP ( 'NONE', ( #156065, #111541, #158969, #162169 ) ) ;
#184199=ORIENTED_EDGE ( 'NONE', *, *, #188763, .F. ) ;
#184210=AXIS2_PLACEMENT_3D ( 'NONE', #194111, #134098, #231955 ) ;
#184227=CIRCLE ( 'NONE', #109207, 0.09999999999998898659 ) ;
#184252=CIRCLE ( 'NONE', #254922, 11.75000000000001066 ) ;
#184272=DIRECTION ( 'NONE',  ( -0.000000000000000000, 1.000000000000000000, 0.000000000000000000 ) ) ;
#184305=DIRECTION ( 'NONE',  ( 0.000000000000000000, -0.4930308989874653269, -0.8700118002898649117 ) ) ;
#184314=CARTESIAN_POINT ( 'NONE',  ( -18.50000000000000000, 11.75000000001115552, -179.6499999999999773 ) ) ;
#184333=DIRECTION ( 'NONE',  ( -1.000000000000000000, -0.000000000000000000, -0.000000000000000000 ) ) ;
#184350=DIRECTION ( 'NONE',  ( -1.000000000000000000, 0.000000000000000000, 0.000000000000000000 ) ) ;
#184360=CYLINDRICAL_SURFACE ( 'NONE', #63178, 0.09999999999999939493 ) ;
#184361=CARTESIAN_POINT ( 'NONE',  ( 21.14261333020286671, 10.71569264926606202, -179.7500000000001990 ) ) ;
#184370=CARTESIAN_POINT ( 'NONE',  ( 22.57320508075687115, 11.75000000001115552, -167.4999999999999716 ) ) ;
#184380=CIRCLE ( 'NONE', #71972, 0.09999999999998898659 ) ;
#184392=LINE ( 'NONE', #83964, #182189 ) ;
#184448=EDGE_CURVE ( 'NONE', #145757, #230164, #184380, .T. ) ;
#184463=EDGE_LOOP ( 'NONE', ( #225839, #239305, #127820, #135775 ) ) ;
#184499=CARTESIAN_POINT ( 'NONE',  ( 23.15000000000000213, -11.64999999998883595, -197.8999999999999773 ) ) ;
#184501=DIRECTION ( 'NONE',  ( 3.265361837132813093E-16, -1.000000000000000000, -0.000000000000000000 ) ) ;
#184524=DIRECTION ( 'NONE',  ( -1.000000000000000000, 7.304098846218134667E-16, 4.217023435051625732E-16 ) ) ;
#184538=DIRECTION ( 'NONE',  ( -0.000000000000000000, 0.000000000000000000, -1.000000000000000000 ) ) ;
#184549=EDGE_CURVE ( 'NONE', #232784, #209275, #130402, .T. ) ;
#184654=CARTESIAN_POINT ( 'NONE',  ( 18.49999999999999289, 10.20857864377384416, -192.1499999999999488 ) ) ;
#184658=ORIENTED_EDGE ( 'NONE', *, *, #187807, .F. ) ;
#184660=CIRCLE ( 'NONE', #164013, 0.09999999999998898659 ) ;
#184685=EDGE_CURVE ( 'NONE', #131341, #190027, #1208, .T. ) ;
#184714=DIRECTION ( 'NONE',  ( 1.000000000000000000, -0.000000000000000000, -0.000000000000000000 ) ) ;
#184737=LINE ( 'NONE', #23134, #112397 ) ;
#184740=CARTESIAN_POINT ( 'NONE',  ( 21.05000000000000071, 1.115600667400684642E-11, -167.4999999999999716 ) ) ;
#184779=DIRECTION ( 'NONE',  ( 0.000000000000000000, -1.000000000000000000, 0.000000000000000000 ) ) ;
#184786=ADVANCED_FACE ( 'NONE', ( #155436 ), #42932, .T. ) ;
#184791=VERTEX_POINT ( 'NONE', #216645 ) ;
#184851=DIRECTION ( 'NONE',  ( 0.000000000000000000, 0.000000000000000000, -1.000000000000000000 ) ) ;
#184884=EDGE_LOOP ( 'NONE', ( #208131, #123956, #158057, #66059 ) ) ;
#184891=DIRECTION ( 'NONE',  ( 1.000000000000000000, -0.000000000000000000, -0.000000000000000000 ) ) ;
#184893=CARTESIAN_POINT ( 'NONE',  ( -18.59999999999999787, -26.43935341558978891, -185.6415086075074328 ) ) ;
#184906=CARTESIAN_POINT ( 'NONE',  ( 20.94999999999999574, 1.115600667400684642E-11, -167.4999999999999716 ) ) ;
#184932=VERTEX_POINT ( 'NONE', #156712 ) ;
#184945=ORIENTED_EDGE ( 'NONE', *, *, #91763, .T. ) ;
#184948=DIRECTION ( 'NONE',  ( 0.000000000000000000, 0.000000000000000000, -1.000000000000000000 ) ) ;
#185004=VERTEX_POINT ( 'NONE', #203512 ) ;
#185009=EDGE_CURVE ( 'NONE', #219222, #5557, #238738, .T. ) ;
#185010=DIRECTION ( 'NONE',  ( 1.000000000000000000, 0.000000000000000000, 0.000000000000000000 ) ) ;
#185013=DIRECTION ( 'NONE',  ( -0.7071067811865474617, -0.7071067811865474617, -2.044391222244499837E-16 ) ) ;
#185022=FACE_OUTER_BOUND ( 'NONE', #149622, .T. ) ;
#185038=AXIS2_PLACEMENT_3D ( 'NONE', #122422, #62448, #201959 ) ;
#185070=DIRECTION ( 'NONE',  ( -1.000000000000000000, 0.000000000000000000, 0.000000000000000000 ) ) ;
#185075=CIRCLE ( 'NONE', #189365, 0.09999999999999939493 ) ;
#185085=VECTOR ( 'NONE', #78954, 1000.000000000000227 ) ;
#185132=LINE ( 'NONE', #6483, #11204 ) ;
#185154=EDGE_CURVE ( 'NONE', #228990, #114385, #108740, .T. ) ;
#185228=ORIENTED_EDGE ( 'NONE', *, *, #224044, .F. ) ;
#185232=CARTESIAN_POINT ( 'NONE',  ( -20.94999999999999929, -1.162701749926853712, -175.5999999999999659 ) ) ;
#185242=EDGE_CURVE ( 'NONE', #115342, #238407, #68233, .T. ) ;
#185244=ORIENTED_EDGE ( 'NONE', *, *, #227193, .T. ) ;
#185277=FACE_OUTER_BOUND ( 'NONE', #129379, .T. ) ;
#185292=ORIENTED_EDGE ( 'NONE', *, *, #152011, .F. ) ;
#185300=DIRECTION ( 'NONE',  ( 0.000000000000000000, 0.000000000000000000, -1.000000000000000000 ) ) ;
#185332=VERTEX_POINT ( 'NONE', #96377 ) ;
#185408=ADVANCED_FACE ( 'NONE', ( #102785 ), #143212, .T. ) ;
#185441=EDGE_CURVE ( 'NONE', #209575, #234902, #43300, .T. ) ;
#185444=VECTOR ( 'NONE', #3533, 1000.000000000000000 ) ;
#185463=VERTEX_POINT ( 'NONE', #14000 ) ;
#185493=CARTESIAN_POINT ( 'NONE',  ( -18.59999999999999787, -1.736705739456431807, -212.5174225876236846 ) ) ;
#185510=EDGE_LOOP ( 'NONE', ( #235182, #181971, #189248, #194178, #65449 ) ) ;
#185525=CIRCLE ( 'NONE', #210472, 0.09999999999999939493 ) ;
#185549=ORIENTED_EDGE ( 'NONE', *, *, #164755, .F. ) ;
#185551=CARTESIAN_POINT ( 'NONE',  ( -20.85000000000000142, -11.74999999998884448, -198.0999999999999659 ) ) ;
#185570=CARTESIAN_POINT ( 'NONE',  ( -22.50000000000000000, 11.64957080755595520, -167.3999999999999773 ) ) ;
#185593=DIRECTION ( 'NONE',  ( 0.000000000000000000, 0.000000000000000000, -1.000000000000000000 ) ) ;
#185595=ORIENTED_EDGE ( 'NONE', *, *, #33114, .T. ) ;
#185624=DIRECTION ( 'NONE',  ( 2.827886303505249259E-16, -0.8660254037844411501, -0.4999999999999956701 ) ) ;
#185627=VERTEX_POINT ( 'NONE', #150935 ) ;
#185629=FACE_OUTER_BOUND ( 'NONE', #131167, .T. ) ;
#185640=CIRCLE ( 'NONE', #35811, 0.5000000000000004441 ) ;
#185647=CARTESIAN_POINT ( 'NONE',  ( 21.09813707148777340, 6.385062105747654648, -167.4686485004704650 ) ) ;
#185661=CARTESIAN_POINT ( 'NONE',  ( 21.06490991615909181, 10.72489134759826790, -179.7037113535330946 ) ) ;
#185664=VERTEX_POINT ( 'NONE', #17823 ) ;
#185675=DIRECTION ( 'NONE',  ( 0.000000000000000000, -1.265107689135680095E-16, 1.000000000000000000 ) ) ;
#185682=CARTESIAN_POINT ( 'NONE',  ( 20.04142135623730070, 11.65000000001115943, -188.8499999999999659 ) ) ;
#185685=AXIS2_PLACEMENT_3D ( 'NONE', #236902, #252607, #58254 ) ;
#185697=VERTEX_POINT ( 'NONE', #216021 ) ;
#185724=CARTESIAN_POINT ( 'NONE',  ( 20.94999999999999574, 1.250000000011155299, -175.4999999999999716 ) ) ;
#185735=ADVANCED_FACE ( 'NONE', ( #806 ), #157386, .F. ) ;
#185797=DIRECTION ( 'NONE',  ( -1.000000000000000000, -0.000000000000000000, -0.000000000000000000 ) ) ;
#185807=DIRECTION ( 'NONE',  ( 2.715809747126116508E-16, -1.000000000000000000, 0.000000000000000000 ) ) ;
#185885=EDGE_LOOP ( 'NONE', ( #76717, #37227, #92524, #23190 ) ) ;
#185902=VECTOR ( 'NONE', #249268, 1000.000000000000000 ) ;
#185924=DIRECTION ( 'NONE',  ( 0.000000000000000000, -1.000000000000000000, 0.000000000000000000 ) ) ;
#185930=FACE_OUTER_BOUND ( 'NONE', #189594, .T. ) ;
#185943=EDGE_CURVE ( 'NONE', #120605, #238407, #135015, .T. ) ;
#185951=AXIS2_PLACEMENT_3D ( 'NONE', #71176, #76276, #32058 ) ;
#185952=AXIS2_PLACEMENT_3D ( 'NONE', #173050, #213396, #215960 ) ;
#185955=MECHANICAL_DESIGN_GEOMETRIC_PRESENTATION_REPRESENTATION('',(#10981),#106834);
#185969=ADVANCED_FACE ( 'NONE', ( #236253 ), #68525, .F. ) ;
#186010=CARTESIAN_POINT ( 'NONE',  ( 20.95429402530550433, 8.876194151113340425, -176.0230866979378561 ) ) ;
#186035=CARTESIAN_POINT ( 'NONE',  ( -20.85000000000000142, 11.75000000001115552, -200.9999999999999432 ) ) ;
#186052=ORIENTED_EDGE ( 'NONE', *, *, #214473, .T. ) ;
#186071=AXIS2_PLACEMENT_3D ( 'NONE', #55059, #13404, #31704 ) ;
#186139=ADVANCED_FACE ( 'NONE', ( #142285 ), #127039, .T. ) ;
#186151=CARTESIAN_POINT ( 'NONE',  ( -21.45000000000000284, 7.708578643773852157, -179.8499999999999943 ) ) ;
#186178=ORIENTED_EDGE ( 'NONE', *, *, #99450, .F. ) ;
#186200=CIRCLE ( 'NONE', #119579, 3.999999999999999112 ) ;
#186204=DIRECTION ( 'NONE',  ( -0.000000000000000000, 0.000000000000000000, 1.000000000000000000 ) ) ;
#186224=CARTESIAN_POINT ( 'NONE',  ( 18.39999999999999858, -9.499999999988844479, -207.6001893912220169 ) ) ;
#186234=CARTESIAN_POINT ( 'NONE',  ( 21.05000000000000071, 5.400000000011154988, -188.5947339810868755 ) ) ;
#186240=CARTESIAN_POINT ( 'NONE',  ( -21.04999999999998295, 6.440770893673168018, -167.5175971870085050 ) ) ;
#186276=AXIS2_PLACEMENT_3D ( 'NONE', #236423, #198576, #213009 ) ;
#186289=CARTESIAN_POINT ( 'NONE',  ( -20.94999999999999929, -11.39257802169451317, -197.9260504201680249 ) ) ;
#186317=CARTESIAN_POINT ( 'NONE',  ( -1.739115166359751801E-14, 11.65000000001114699, -188.8499999999999659 ) ) ;
#186318=CARTESIAN_POINT ( 'NONE',  ( 21.14999999999999858, 11.65000000001116298, -179.7499999999999716 ) ) ;
#186321=CARTESIAN_POINT ( 'NONE',  ( -20.64999999999999858, 4.350000000011156054, -188.6499999999999488 ) ) ;
#186336=DIRECTION ( 'NONE',  ( 2.840903330521631775E-16, -0.8700118002898321601, 0.4930308989875230585 ) ) ;
#186407=CYLINDRICAL_SURFACE ( 'NONE', #6533, 0.1000000000000098310 ) ;
#186412=TOROIDAL_SURFACE ( 'NONE', #190523, 11.70000000000000462, 0.1000000000000000056 ) ;
#186455=CYLINDRICAL_SURFACE ( 'NONE', #241464, 0.5000000000000004441 ) ;
#186456=ORIENTED_EDGE ( 'NONE', *, *, #199516, .F. ) ;
#186457=CARTESIAN_POINT ( 'NONE',  ( -22.50875500270928598, -0.1008579137641491541, -155.7504328726020617 ) ) ;
#186489=CARTESIAN_POINT ( 'NONE',  ( -21.11833042828112994, 0.007100509070636552671, -161.0543553061450837 ) ) ;
#186582=CARTESIAN_POINT ( 'NONE',  ( -21.03922262424684675, 11.62390063401601381, -174.3592080428932434 ) ) ;
#186609=DIRECTION ( 'NONE',  ( 0.000000000000000000, -1.000000000000000000, 0.000000000000000000 ) ) ;
#186619=LINE ( 'NONE', #228308, #248182 ) ;
#186620=CARTESIAN_POINT ( 'NONE',  ( 20.94999999999999929, 6.550000000011156231, -177.5170271704400022 ) ) ;
#186632=CARTESIAN_POINT ( 'NONE',  ( -21.05000000000000071, -11.41227409413852989, -170.4999999999999716 ) ) ;
#186661=CARTESIAN_POINT ( 'NONE',  ( 23.24999999999999289, -4.149999999988843058, -167.4999999999999716 ) ) ;
#186691=ORIENTED_EDGE ( 'NONE', *, *, #223452, .F. ) ;
#186694=CARTESIAN_POINT ( 'NONE',  ( 20.94999999999999929, 6.650000000011155876, -188.7499999999999716 ) ) ;
#186701=CARTESIAN_POINT ( 'NONE',  ( 18.42595409746875745, -9.499999812553152623, -174.4993623517493404 ) ) ;
#186708=AXIS2_PLACEMENT_3D ( 'NONE', #207896, #149201, #166210 ) ;
#186726=DIRECTION ( 'NONE',  ( -1.000000000000000000, 0.000000000000000000, 0.000000000000000000 ) ) ;
#186736=CARTESIAN_POINT ( 'NONE',  ( -18.50000000000000000, -9.421290279512176014, -207.8238821790266115 ) ) ;
#186747=AXIS2_PLACEMENT_3D ( 'NONE', #217703, #155223, #97746 ) ;
#186757=CIRCLE ( 'NONE', #116028, 0.5999999999999894307 ) ;
#186786=DIRECTION ( 'NONE',  ( -0.000000000000000000, -1.000000000000000000, 6.308085367188393199E-16 ) ) ;
#186787=ORIENTED_EDGE ( 'NONE', *, *, #61184, .F. ) ;
#186805=CARTESIAN_POINT ( 'NONE',  ( 21.05000000000000071, 14.05000000001115623, -195.4863049292390542 ) ) ;
#186846=EDGE_CURVE ( 'NONE', #199945, #68874, #7074, .T. ) ;
#186883=ADVANCED_FACE ( 'NONE', ( #40043 ), #152862, .F. ) ;
#186910=SHAPE_REPRESENTATION_RELATIONSHIP ( 'NONE' , 'NONE' ,  #196772, #88633 ) ;
#186912=ORIENTED_EDGE ( 'NONE', *, *, #189145, .F. ) ;
#186915=TOROIDAL_SURFACE ( 'NONE', #145175, 4.099999999999999645, 0.1000000000000000056 ) ;
#186930=VECTOR ( 'NONE', #6894, 1000.000000000000000 ) ;
#186973=CARTESIAN_POINT ( 'NONE',  ( 21.09696443733127325, 10.72400988392963228, -179.7347775270482089 ) ) ;
#186980=AXIS2_PLACEMENT_3D ( 'NONE', #139429, #221526, #238548 ) ;
#186983=DIRECTION ( 'NONE',  ( -1.000000000000000000, -0.000000000000000000, -0.000000000000000000 ) ) ;
#186989=SURFACE_STYLE_USAGE ( .BOTH. , #164838 ) ;
#187015=ORIENTED_EDGE ( 'NONE', *, *, #238893, .T. ) ;
#187042=EDGE_LOOP ( 'NONE', ( #246145, #51683, #1708, #145914 ) ) ;
#187048=CARTESIAN_POINT ( 'NONE',  ( 18.59999999999999787, 1.115600667400684642E-11, -167.4999999999999716 ) ) ;
#187086=VERTEX_POINT ( 'NONE', #78669 ) ;
#187091=ORIENTED_EDGE ( 'NONE', *, *, #148750, .T. ) ;
#187139=DIRECTION ( 'NONE',  ( 1.000000000000000000, -0.000000000000000000, 0.000000000000000000 ) ) ;
#187153=CARTESIAN_POINT ( 'NONE',  ( -20.85000000000000142, -11.64999999998884483, -200.9999999999999432 ) ) ;
#187213=AXIS2_PLACEMENT_3D ( 'NONE', #146416, #225941, #129448 ) ;
#187242=ORIENTED_EDGE ( 'NONE', *, *, #14809, .F. ) ;
#187285=DIRECTION ( 'NONE',  ( 0.000000000000000000, 1.000000000000000000, 0.000000000000000000 ) ) ;
#187298=DIRECTION ( 'NONE',  ( 0.000000000000000000, 2.168404344970946942E-15, 1.000000000000000000 ) ) ;
#187307=AXIS2_PLACEMENT_3D ( 'NONE', #126879, #189427, #225938 ) ;
#187319=ORIENTED_EDGE ( 'NONE', *, *, #106192, .T. ) ;
#187331=CIRCLE ( 'NONE', #212281, 0.09999999999998898659 ) ;
#187335=CARTESIAN_POINT ( 'NONE',  ( -23.15000000000000213, 1.115600667400684642E-11, -180.3749999999999716 ) ) ;
#187351=AXIS2_PLACEMENT_3D ( 'NONE', #172645, #214290, #151771 ) ;
#187353=ORIENTED_EDGE ( 'NONE', *, *, #214696, .T. ) ;
#187382=CIRCLE ( 'NONE', #37543, 0.09999999999998898659 ) ;
#187504=EDGE_CURVE ( 'NONE', #155258, #13363, #134635, .T. ) ;
#187509=EDGE_LOOP ( 'NONE', ( #87710, #126323, #125590, #187554 ) ) ;
#187520=DIRECTION ( 'NONE',  ( 0.000000000000000000, -1.243449787580175010E-14, -1.000000000000000000 ) ) ;
#187523=CARTESIAN_POINT ( 'NONE',  ( 18.46932045258651200, -9.670685200254535374, -207.6738603729966712 ) ) ;
#187537=EDGE_CURVE ( 'NONE', #131693, #229311, #56590, .T. ) ;
#187538=CARTESIAN_POINT ( 'NONE',  ( 19.75857864376268935, 11.65000000001115943, -192.3499999999999659 ) ) ;
#187543=ADVANCED_FACE ( 'NONE', ( #161951 ), #22443, .T. ) ;
#187554=ORIENTED_EDGE ( 'NONE', *, *, #10788, .T. ) ;
#187559=CARTESIAN_POINT ( 'NONE',  ( -20.64999999999999858, 7.150000000011155876, -188.6499999999999488 ) ) ;
#187568=LINE ( 'NONE', #127572, #245932 ) ;
#187589=DIRECTION ( 'NONE',  ( 0.000000000000000000, -0.8700118002898321601, 0.4930308989875230030 ) ) ;
#187617=DIRECTION ( 'NONE',  ( -7.304098846218134667E-16, 1.000000000000000000, -0.000000000000000000 ) ) ;
#187639=EDGE_CURVE ( 'NONE', #108752, #39612, #164790, .T. ) ;
#187707=CARTESIAN_POINT ( 'NONE',  ( 23.14999999999999503, 6.650000000011155876, -188.6499999999999488 ) ) ;
#187712=EDGE_CURVE ( 'NONE', #116826, #43467, #98280, .T. ) ;
#187724=DIRECTION ( 'NONE',  ( 0.000000000000000000, 0.000000000000000000, 1.000000000000000000 ) ) ;
#187770=FACE_OUTER_BOUND ( 'NONE', #66238, .T. ) ;
#187785=DIRECTION ( 'NONE',  ( -3.469446951953677298E-14, -0.9908441862701782288, -0.1350103645450542456 ) ) ;
#187803=EDGE_CURVE ( 'NONE', #135750, #115507, #14951, .T. ) ;
#187807=EDGE_CURVE ( 'NONE', #239082, #165621, #248175, .T. ) ;
#187864=PLANE ( 'NONE',  #98374 ) ;
#187878=VECTOR ( 'NONE', #24292, 1000.000000000000000 ) ;
#187925=CARTESIAN_POINT ( 'NONE',  ( 23.15000000000000213, -11.64999999998883595, -197.8999999999999773 ) ) ;
#187937=ORIENTED_EDGE ( 'NONE', *, *, #160584, .F. ) ;
#187938=EDGE_CURVE ( 'NONE', #50174, #94619, #198284, .T. ) ;
#187959=EDGE_LOOP ( 'NONE', ( #104636, #238181, #124236, #212167 ) ) ;
#187978=CARTESIAN_POINT ( 'NONE',  ( 18.48536876927993333, -9.463527249856051426, -174.5486182650826095 ) ) ;
#187991=VECTOR ( 'NONE', #183184, 1000.000000000000000 ) ;
#188024=CARTESIAN_POINT ( 'NONE',  ( 20.95512820512820795, 10.62384868372303615, -179.7001620194243969 ) ) ;
#188041=EDGE_LOOP ( 'NONE', ( #17373, #242783, #142234 ) ) ;
#188054=LINE ( 'NONE', #88926, #97751 ) ;
#188082=ORIENTED_EDGE ( 'NONE', *, *, #113805, .T. ) ;
#188132=LINE ( 'NONE', #9482, #70730 ) ;
#188166=AXIS2_PLACEMENT_3D ( 'NONE', #141689, #122145, #23065 ) ;
#188168=CARTESIAN_POINT ( 'NONE',  ( -21.56666275994540172, 1.115600667400684642E-11, -160.5426315931066483 ) ) ;
#188179=AXIS2_PLACEMENT_3D ( 'NONE', #111911, #171905, #205856 ) ;
#188181=AXIS2_PLACEMENT_3D ( 'NONE', #89161, #244381, #145276 ) ;
#188193=ORIENTED_EDGE ( 'NONE', *, *, #221940, .T. ) ;
#188225=CARTESIAN_POINT ( 'NONE',  ( 21.05000000000000071, 11.75000000001115907, -194.1583993101029080 ) ) ;
#188288=EDGE_CURVE ( 'NONE', #185332, #145757, #78858, .T. ) ;
#188291=CARTESIAN_POINT ( 'NONE',  ( -18.52139480978222252, -9.481358845055746443, -174.5245565671190491 ) ) ;
#188313=EDGE_CURVE ( 'NONE', #120605, #115342, #144455, .T. ) ;
#188328=CIRCLE ( 'NONE', #117606, 0.09999999999998898659 ) ;
#188371=ORIENTED_EDGE ( 'NONE', *, *, #59561, .T. ) ;
#188381=ORIENTED_EDGE ( 'NONE', *, *, #250878, .F. ) ;
#188391=TOROIDAL_SURFACE ( 'NONE', #75975, 0.2000000000000000111, 0.1000000000000000056 ) ;
#188404=DIRECTION ( 'NONE',  ( 0.000000000000000000, -0.000000000000000000, 1.000000000000000000 ) ) ;
#188407=TOROIDAL_SURFACE ( 'NONE', #92546, 0.2000000000000000111, 0.1000000000000000056 ) ;
#188441=AXIS2_PLACEMENT_3D ( 'NONE', #176094, #136211, #39147 ) ;
#188444=CARTESIAN_POINT ( 'NONE',  ( -21.05000000000000071, -11.74999999998884448, -198.0999999999999659 ) ) ;
#188499=CIRCLE ( 'NONE', #21917, 0.1000000000000043493 ) ;
#188501=VERTEX_POINT ( 'NONE', #125709 ) ;
#188505=DIRECTION ( 'NONE',  ( -1.000000000000000000, -0.000000000000000000, -0.000000000000000000 ) ) ;
#188506=CARTESIAN_POINT ( 'NONE',  ( -20.94999999999999929, 10.29270135741298731, -206.4573618871519045 ) ) ;
#188508=AXIS2_PLACEMENT_3D ( 'NONE', #56631, #94502, #174098 ) ;
#188534=ADVANCED_FACE ( 'NONE', ( #129576 ), #163608, .F. ) ;
#188539=CARTESIAN_POINT ( 'NONE',  ( 18.59999999999999432, 1.162701749949165642, -175.5999999999999659 ) ) ;
#188544=DIRECTION ( 'NONE',  ( 0.000000000000000000, 0.000000000000000000, -1.000000000000000000 ) ) ;
#188550=DIRECTION ( 'NONE',  ( 1.000000000000000000, -0.000000000000000000, -0.000000000000000000 ) ) ;
#188556=ORIENTED_EDGE ( 'NONE', *, *, #187504, .T. ) ;
#188569=CARTESIAN_POINT ( 'NONE',  ( -22.50000000000000000, 11.64957080755595520, -167.3999999999999773 ) ) ;
#188594=DIRECTION ( 'NONE',  ( 0.000000000000000000, 0.1568667991644863147, -0.9876197685951252359 ) ) ;
#188623=AXIS2_PLACEMENT_3D ( 'NONE', #30242, #191900, #189308 ) ;
#188626=AXIS2_PLACEMENT_3D ( 'NONE', #49236, #188746, #251278 ) ;
#188661=AXIS2_PLACEMENT_3D ( 'NONE', #109831, #105965, #223357 ) ;
#188687=ORIENTED_EDGE ( 'NONE', *, *, #142185, .F. ) ;
#188688=AXIS2_PLACEMENT_3D ( 'NONE', #83474, #226865, #225559 ) ;
#188706=CARTESIAN_POINT ( 'NONE',  ( -22.46246831459151494, 0.02191216695058596786, -155.8501354387900051 ) ) ;
#188708=CARTESIAN_POINT ( 'NONE',  ( 23.14999999999999858, 1.115649653272650466E-11, -196.9999999999999432 ) ) ;
#188731=ORIENTED_EDGE ( 'NONE', *, *, #72732, .T. ) ;
#188746=DIRECTION ( 'NONE',  ( 0.000000000000000000, 0.000000000000000000, 1.000000000000000000 ) ) ;
#188759=CYLINDRICAL_SURFACE ( 'NONE', #172278, 0.09999999999999939493 ) ;
#188763=EDGE_CURVE ( 'NONE', #82856, #429, #62870, .T. ) ;
#188773=ORIENTED_EDGE ( 'NONE', *, *, #118940, .F. ) ;
#188774=AXIS2_PLACEMENT_3D ( 'NONE', #198500, #60267, #254918 ) ;
#188811=DIRECTION ( 'NONE',  ( 1.000000000000000000, 0.000000000000000000, 0.000000000000000000 ) ) ;
#188827=FACE_OUTER_BOUND ( 'NONE', #240292, .T. ) ;
#188859=LINE ( 'NONE', #149760, #80477 ) ;
#188881=FACE_OUTER_BOUND ( 'NONE', #192074, .T. ) ;
#188961=DIRECTION ( 'NONE',  ( -1.000000000000000000, 0.000000000000000000, 0.000000000000000000 ) ) ;
#188981=AXIS2_PLACEMENT_3D ( 'NONE', #172049, #173347, #252817 ) ;
#188982=DIRECTION ( 'NONE',  ( 0.000000000000000000, 0.000000000000000000, -1.000000000000000000 ) ) ;
#188986=DIRECTION ( 'NONE',  ( 0.000000000000000000, 6.308085367183347448E-16, 1.000000000000000000 ) ) ;
#188990=ADVANCED_FACE ( 'NONE', ( #76985 ), #232239, .T. ) ;
#188996=ORIENTED_EDGE ( 'NONE', *, *, #194355, .F. ) ;
#188999=CARTESIAN_POINT ( 'NONE',  ( -23.25000000000000000, -11.64999999998884483, -197.8999999999999773 ) ) ;
#189009=VECTOR ( 'NONE', #126325, 1000.000000000000000 ) ;
#189040=EDGE_LOOP ( 'NONE', ( #178681, #182636, #17863, #236172 ) ) ;
#189114=DIRECTION ( 'NONE',  ( 0.000000000000000000, 0.000000000000000000, -1.000000000000000000 ) ) ;
#189122=ORIENTED_EDGE ( 'NONE', *, *, #101597, .T. ) ;
#189134=CARTESIAN_POINT ( 'NONE',  ( -21.12844524849339223, 11.75000000001115197, -174.4044134708423996 ) ) ;
#189145=EDGE_CURVE ( 'NONE', #232784, #204695, #71876, .T. ) ;
#189164=CARTESIAN_POINT ( 'NONE',  ( -21.05000000000000071, 1.115600667400684642E-11, -200.9999999999999432 ) ) ;
#189169=ORIENTED_EDGE ( 'NONE', *, *, #168708, .T. ) ;
#189186=AXIS2_PLACEMENT_3D ( 'NONE', #79283, #218800, #177155 ) ;
#189209=DIRECTION ( 'NONE',  ( -1.000000000000000000, -2.952720810173289112E-16, 0.000000000000000000 ) ) ;
#189210=EDGE_CURVE ( 'NONE', #158708, #182323, #61282, .T. ) ;
#189212=CARTESIAN_POINT ( 'NONE',  ( 23.24999999999999645, 2.100000000011158274, -200.9999999999999432 ) ) ;
#189219=CIRCLE ( 'NONE', #89232, 12.87499999999999822 ) ;
#189222=CARTESIAN_POINT ( 'NONE',  ( -23.15000000000000213, 1.115600667400684642E-11, -200.9999999999999432 ) ) ;
#189237=EDGE_CURVE ( 'NONE', #172274, #167246, #140822, .T. ) ;
#189244=DIRECTION ( 'NONE',  ( 1.000000000000000000, 0.000000000000000000, -0.000000000000000000 ) ) ;
#189248=ORIENTED_EDGE ( 'NONE', *, *, #251302, .F. ) ;
#189262=CARTESIAN_POINT ( 'NONE',  ( 18.43473516226061548, -9.494942282747109275, -174.5458986833494919 ) ) ;
#189271=CIRCLE ( 'NONE', #85163, 0.1000000000000001860 ) ;
#189283=ORIENTED_EDGE ( 'NONE', *, *, #176034, .F. ) ;
#189285=CARTESIAN_POINT ( 'NONE',  ( -23.15000000000000213, 1.115600667400684642E-11, -167.4999999999999716 ) ) ;
#189288=CARTESIAN_POINT ( 'NONE',  ( -20.94999999999999929, -11.74999999998884448, -170.5999999999999659 ) ) ;
#189302=EDGE_CURVE ( 'NONE', #103641, #108161, #6434, .T. ) ;
#189308=DIRECTION ( 'NONE',  ( 0.000000000000000000, 0.000000000000000000, -1.000000000000000000 ) ) ;
#189322=AXIS2_PLACEMENT_3D ( 'NONE', #59844, #159006, #181123 ) ;
#189337=FACE_OUTER_BOUND ( 'NONE', #170390, .T. ) ;
#189342=DIRECTION ( 'NONE',  ( -3.469446951953995998E-14, 0.000000000000000000, 1.000000000000000000 ) ) ;
#189348=ORIENTED_EDGE ( 'NONE', *, *, #106158, .F. ) ;
#189359=DIRECTION ( 'NONE',  ( 0.000000000000000000, 1.000000000000000000, 0.000000000000000000 ) ) ;
#189361=CIRCLE ( 'NONE', #68732, 0.09999999999999939493 ) ;
#189362=ORIENTED_EDGE ( 'NONE', *, *, #98861, .F. ) ;
#189365=AXIS2_PLACEMENT_3D ( 'NONE', #208862, #69367, #151481 ) ;
#189398=CARTESIAN_POINT ( 'NONE',  ( -23.15000000000000213, -11.48912529306489994, -197.8999999999999773 ) ) ;
#189401=ORIENTED_EDGE ( 'NONE', *, *, #253933, .T. ) ;
#189427=DIRECTION ( 'NONE',  ( 0.000000000000000000, 0.000000000000000000, -1.000000000000000000 ) ) ;
#189440=CARTESIAN_POINT ( 'NONE',  ( -20.94999999999999929, 1.835341550235567887, -179.1551512925629197 ) ) ;
#189444=DIRECTION ( 'NONE',  ( 0.000000000000000000, -0.4999999999999348299, 0.8660254037844762331 ) ) ;
#189512=VECTOR ( 'NONE', #66612, 999.9999999999998863 ) ;
#189521=CARTESIAN_POINT ( 'NONE',  ( 20.94560253601876809, 11.75000000001115907, -194.0100835125150240 ) ) ;
#189528=CARTESIAN_POINT ( 'NONE',  ( 23.14999999999999858, -1.999999999988846699, -200.9999999999999432 ) ) ;
#189535=ORIENTED_EDGE ( 'NONE', *, *, #195282, .T. ) ;
#189543=PLANE ( 'NONE',  #47542 ) ;
#189556=CARTESIAN_POINT ( 'NONE',  ( -22.47007471830799830, 7.720710651937626068, -167.4999999999999432 ) ) ;
#189564=CARTESIAN_POINT ( 'NONE',  ( -21.05000000000000071, -11.48912529306489994, -197.8999999999999773 ) ) ;
#189588=VECTOR ( 'NONE', #164584, 1000.000000000000000 ) ;
#189594=EDGE_LOOP ( 'NONE', ( #210277, #243489, #16831, #75497, #115947 ) ) ;
#189603=DIRECTION ( 'NONE',  ( -1.000000000000000000, -3.265361837132813093E-16, 0.000000000000000000 ) ) ;
#189616=LINE ( 'NONE', #190920, #240346 ) ;
#189622=DIRECTION ( 'NONE',  ( -1.000000000000000000, -0.000000000000000000, -0.000000000000000000 ) ) ;
#189627=TOROIDAL_SURFACE ( 'NONE', #222927, 0.9750000000000019762, 0.1000000000000000056 ) ;
#189639=ORIENTED_EDGE ( 'NONE', *, *, #162200, .T. ) ;
#189653=CARTESIAN_POINT ( 'NONE',  ( 20.94999999999999574, 1.849084418638171856, -179.1560105214470866 ) ) ;
#189691=CARTESIAN_POINT ( 'NONE',  ( 23.14999999999999503, 11.65000000001116298, -179.6499999999999773 ) ) ;
#189713=ORIENTED_EDGE ( 'NONE', *, *, #31519, .T. ) ;
#189727=ORIENTED_EDGE ( 'NONE', *, *, #109360, .T. ) ;
#189735=CARTESIAN_POINT ( 'NONE',  ( 20.94999999999999929, 1.115600667400684642E-11, -208.7999999999999545 ) ) ;
#189739=CARTESIAN_POINT ( 'NONE',  ( 21.15000000000000213, 8.786607556611267356, -179.7500000000000000 ) ) ;
#189742=CARTESIAN_POINT ( 'NONE',  ( -20.64999999999999858, 4.350000000011156054, -179.7499999999999716 ) ) ;
#189743=FACE_OUTER_BOUND ( 'NONE', #191437, .T. ) ;
#189744=ORIENTED_EDGE ( 'NONE', *, *, #18038, .F. ) ;
#189747=DIRECTION ( 'NONE',  ( -6.938893903907209445E-14, -0.9999176327611370985, -0.01283462868040260302 ) ) ;
#189764=ADVANCED_FACE ( 'NONE', ( #229989 ), #51321, .T. ) ;
#189788=DIRECTION ( 'NONE',  ( -1.000000000000000000, -1.836970198721029934E-16, 0.000000000000000000 ) ) ;
#189798=CARTESIAN_POINT ( 'NONE',  ( -20.86777300164944648, 10.33200063080771969, -206.5931674956642610 ) ) ;
#189819=ORIENTED_EDGE ( 'NONE', *, *, #191076, .F. ) ;
#189825=DIRECTION ( 'NONE',  ( 0.000000000000000000, 0.000000000000000000, -1.000000000000000000 ) ) ;
#189829=CARTESIAN_POINT ( 'NONE',  ( 21.05000000000000071, 6.413978881499349249, -167.5857991162739609 ) ) ;
#189836=CYLINDRICAL_SURFACE ( 'NONE', #149913, 0.09999999999999939493 ) ;
#189887=DIRECTION ( 'NONE',  ( 0.000000000000000000, 0.000000000000000000, -1.000000000000000000 ) ) ;
#189892=CARTESIAN_POINT ( 'NONE',  ( 18.59999999999999787, 1.115600667400684642E-11, -167.4999999999999716 ) ) ;
#189917=EDGE_CURVE ( 'NONE', #191282, #165976, #231981, .T. ) ;
#189947=FACE_OUTER_BOUND ( 'NONE', #245840, .T. ) ;
#190027=VERTEX_POINT ( 'NONE', #189288 ) ;
#190033=CARTESIAN_POINT ( 'NONE',  ( -23.25000000000000000, -9.682403433465239573, -207.6568433774127413 ) ) ;
#190036=EDGE_CURVE ( 'NONE', #9569, #122995, #244410, .T. ) ;
#190091=DIRECTION ( 'NONE',  ( 0.000000000000000000, 0.000000000000000000, -1.000000000000000000 ) ) ;
#190092=ADVANCED_FACE ( 'NONE', ( #9344 ), #252976, .T. ) ;
#190094=ORIENTED_EDGE ( 'NONE', *, *, #42559, .T. ) ;
#190198=EDGE_LOOP ( 'NONE', ( #38509, #15878, #105869, #27134 ) ) ;
#190201=TOROIDAL_SURFACE ( 'NONE', #19514, 7.800000000000000711, 0.1000000000000000056 ) ;
#190249=EDGE_CURVE ( 'NONE', #80509, #220110, #157905, .T. ) ;
#190274=CIRCLE ( 'NONE', #248698, 0.2000000000000057288 ) ;
#190292=LINE ( 'NONE', #10373, #206171 ) ;
#190294=CYLINDRICAL_SURFACE ( 'NONE', #42680, 0.09999999999999939493 ) ;
#190318=CARTESIAN_POINT ( 'NONE',  ( 18.39999999999999858, -9.519327731081283162, -174.4729763765593020 ) ) ;
#190329=CARTESIAN_POINT ( 'NONE',  ( -23.25000000000000000, 11.75000000001115552, -193.9851942293460070 ) ) ;
#190383=VERTEX_POINT ( 'NONE', #6473 ) ;
#190388=CARTESIAN_POINT ( 'NONE',  ( -18.47653818581420282, -9.465280387751809243, -174.6259608161397807 ) ) ;
#190396=EDGE_CURVE ( 'NONE', #99286, #202617, #40813, .T. ) ;
#190412=LINE ( 'NONE', #74335, #120387 ) ;
#190417=ORIENTED_EDGE ( 'NONE', *, *, #257212, .F. ) ;
#190418=DIRECTION ( 'NONE',  ( -1.000000000000000000, -0.000000000000000000, -0.000000000000000000 ) ) ;
#190502=DIRECTION ( 'NONE',  ( 0.000000000000000000, 0.8660254037844383745, -0.5000000000000003331 ) ) ;
#190522=CIRCLE ( 'NONE', #48452, 0.4000000000000114575 ) ;
#190523=AXIS2_PLACEMENT_3D ( 'NONE', #241109, #179846, #80706 ) ;
#190537=CARTESIAN_POINT ( 'NONE',  ( -21.05000000000000426, -0.09999999998884340213, -161.0229329788752182 ) ) ;
#190551=DIRECTION ( 'NONE',  ( 0.000000000000000000, 0.000000000000000000, -1.000000000000000000 ) ) ;
#190554=ORIENTED_EDGE ( 'NONE', *, *, #36871, .T. ) ;
#190565=EDGE_LOOP ( 'NONE', ( #244172, #57881, #123968, #233277 ) ) ;
#190613=CIRCLE ( 'NONE', #115570, 0.2000000000000057288 ) ;
#190629=DIRECTION ( 'NONE',  ( -7.304098846218134667E-16, -1.000000000000000000, 0.000000000000000000 ) ) ;
#190654=ORIENTED_EDGE ( 'NONE', *, *, #144352, .T. ) ;
#190656=DIRECTION ( 'NONE',  ( 0.000000000000000000, 0.000000000000000000, -1.000000000000000000 ) ) ;
#190670=EDGE_CURVE ( 'NONE', #246179, #152513, #170016, .T. ) ;
#190710=EDGE_CURVE ( 'NONE', #234902, #178867, #178421, .T. ) ;
#190753=CARTESIAN_POINT ( 'NONE',  ( -18.50000000000000000, 11.75000000001115197, -188.8499999999999659 ) ) ;
#190755=AXIS2_PLACEMENT_3D ( 'NONE', #104772, #184333, #166106 ) ;
#190775=ORIENTED_EDGE ( 'NONE', *, *, #127659, .T. ) ;
#190796=AXIS2_PLACEMENT_3D ( 'NONE', #147083, #90972, #12752 ) ;
#190800=CIRCLE ( 'NONE', #49294, 11.64999999999999325 ) ;
#190824=VERTEX_POINT ( 'NONE', #85663 ) ;
#190846=ORIENTED_EDGE ( 'NONE', *, *, #140278, .F. ) ;
#190848=CARTESIAN_POINT ( 'NONE',  ( -21.05000000000000071, 1.115600667400684642E-11, -167.4999999999999716 ) ) ;
#190860=VERTEX_POINT ( 'NONE', #29615 ) ;
#190883=FACE_OUTER_BOUND ( 'NONE', #183211, .T. ) ;
#190886=EDGE_LOOP ( 'NONE', ( #88265, #69124, #5578, #62496 ) ) ;
#190896=ADVANCED_FACE ( 'NONE', ( #189947 ), #230342, .F. ) ;
#190903=CARTESIAN_POINT ( 'NONE',  ( -18.39999999999999858, -9.519327731081281385, -174.4729763765593020 ) ) ;
#190920=CARTESIAN_POINT ( 'NONE',  ( -21.05000000000000071, 1.115600667400684642E-11, -171.7999999999999545 ) ) ;
#190928=AXIS2_PLACEMENT_3D ( 'NONE', #189691, #12361, #171451 ) ;
#190933=ORIENTED_EDGE ( 'NONE', *, *, #131491, .T. ) ;
#190973=AXIS2_PLACEMENT_3D ( 'NONE', #144750, #127789, #225566 ) ;
#190986=VERTEX_POINT ( 'NONE', #104785 ) ;
#190987=VECTOR ( 'NONE', #117601, 1000.000000000000000 ) ;
#190991=CARTESIAN_POINT ( 'NONE',  ( -20.85000000000000142, -11.74999999998884448, -200.9999999999999432 ) ) ;
#191017=CYLINDRICAL_SURFACE ( 'NONE', #152701, 0.09999999999999881206 ) ;
#191022=CARTESIAN_POINT ( 'NONE',  ( 20.93302460841142931, 10.31565961587945424, -206.5364194119177625 ) ) ;
#191036=CARTESIAN_POINT ( 'NONE',  ( 23.24999999999999289, 11.65000000001116298, -155.7499999999999716 ) ) ;
#191046=CARTESIAN_POINT ( 'NONE',  ( 21.08804582317324616, 8.878166167103060502, -179.8499998294057036 ) ) ;
#191076=EDGE_CURVE ( 'NONE', #58719, #69026, #136945, .T. ) ;
#191080=DIRECTION ( 'NONE',  ( 0.000000000000000000, -0.4999999999999348299, 0.8660254037844762331 ) ) ;
#191087=CARTESIAN_POINT ( 'NONE',  ( -18.49346865148320518, -9.443073798513781369, -174.6851962553152759 ) ) ;
#191088=AXIS2_PLACEMENT_3D ( 'NONE', #217438, #41416, #220032 ) ;
#191091=ORIENTED_EDGE ( 'NONE', *, *, #164870, .F. ) ;
#191096=LINE ( 'NONE', #13711, #201019 ) ;
#191100=FACE_OUTER_BOUND ( 'NONE', #99935, .T. ) ;
#191122=ADVANCED_FACE ( 'NONE', ( #118844 ), #95406, .T. ) ;
#191132=CIRCLE ( 'NONE', #224409, 0.1000000000000094008 ) ;
#191136=CARTESIAN_POINT ( 'NONE',  ( 21.07954763557432543, 6.329290990048807686, -167.4341240813815546 ) ) ;
#191150=DIRECTION ( 'NONE',  ( 0.000000000000000000, -0.000000000000000000, 1.000000000000000000 ) ) ;
#191165=ADVANCED_FACE ( 'NONE', ( #199668 ), #236195, .F. ) ;
#191167=FACE_OUTER_BOUND ( 'NONE', #116, .T. ) ;
#191208=DIRECTION ( 'NONE',  ( -1.000000000000000000, 0.000000000000000000, 0.000000000000000000 ) ) ;
#191213=DIRECTION ( 'NONE',  ( 0.000000000000000000, 0.000000000000000000, -1.000000000000000000 ) ) ;
#191220=CARTESIAN_POINT ( 'NONE',  ( 20.95512820512820440, 10.62384868372303615, -175.1649135690875880 ) ) ;
#191239=CARTESIAN_POINT ( 'NONE',  ( -20.94999999999999929, 1.360870587203197646, -175.5729979270909382 ) ) ;
#191282=VERTEX_POINT ( 'NONE', #27476 ) ;
#191310=CARTESIAN_POINT ( 'NONE',  ( -23.15000000000000213, -8.999999999988844479, -191.6060308773475356 ) ) ;
#191315=CARTESIAN_POINT ( 'NONE',  ( -22.42253884134832020, 0.001932351146464877023, -155.8503943026515515 ) ) ;
#191328=CARTESIAN_POINT ( 'NONE',  ( 20.94999999999999929, 10.38178547073510316, -206.5078453638841438 ) ) ;
#191335=CARTESIAN_POINT ( 'NONE',  ( -20.94999999999999929, 1.851028230152016674, -179.1539132694224463 ) ) ;
#191378=CIRCLE ( 'NONE', #24785, 0.09999999999998898659 ) ;
#191397=DIRECTION ( 'NONE',  ( 0.000000000000000000, 0.9654727137038715545, 0.2605042016806676242 ) ) ;
#191437=EDGE_LOOP ( 'NONE', ( #200386, #46162, #18071, #54265 ) ) ;
#191446=CARTESIAN_POINT ( 'NONE',  ( -18.39999999999999858, -9.499999999988849808, -174.4992856778388273 ) ) ;
#191501=VERTEX_POINT ( 'NONE', #135492 ) ;
#191517=DIRECTION ( 'NONE',  ( 0.000000000000000000, -0.000000000000000000, -1.000000000000000000 ) ) ;
#191536=EDGE_CURVE ( 'NONE', #169154, #246179, #16866, .T. ) ;
#191539=CARTESIAN_POINT ( 'NONE',  ( 21.14999999999999503, -0.09999999998884338825, -155.8504291924551808 ) ) ;
#191540=DIRECTION ( 'NONE',  ( 1.000000000000000000, 0.000000000000000000, 0.000000000000000000 ) ) ;
#191544=ORIENTED_EDGE ( 'NONE', *, *, #59141, .F. ) ;
#191558=CARTESIAN_POINT ( 'NONE',  ( -18.43459694179555797, -9.494210124986887323, -207.6170052026610620 ) ) ;
#191592=CARTESIAN_POINT ( 'NONE',  ( 23.14999999999999503, 11.65000000001116298, -188.7499999999999716 ) ) ;
#191697=CARTESIAN_POINT ( 'NONE',  ( 18.39999999999999858, -9.499999999988842703, -174.5320693966996259 ) ) ;
#191715=CARTESIAN_POINT ( 'NONE',  ( -20.64999999999999858, -8.663551401858004652, -177.0241011180672785 ) ) ;
#191736=EDGE_CURVE ( 'NONE', #77400, #152331, #113075, .T. ) ;
#191749=EDGE_CURVE ( 'NONE', #139380, #232784, #128826, .T. ) ;
#191755=PLANE ( 'NONE',  #46111 ) ;
#191774=CARTESIAN_POINT ( 'NONE',  ( 23.14999999999999858, 4.000000000011155521, -200.9999999999999432 ) ) ;
#191778=DIRECTION ( 'NONE',  ( -0.000000000000000000, -0.000000000000000000, 1.000000000000000000 ) ) ;
#191786=FACE_OUTER_BOUND ( 'NONE', #175045, .T. ) ;
#191790=CARTESIAN_POINT ( 'NONE',  ( -20.94999999999999929, 14.05000000001115623, -195.4863049292390542 ) ) ;
#191810=AXIS2_PLACEMENT_3D ( 'NONE', #234936, #112425, #38037 ) ;
#191821=ORIENTED_EDGE ( 'NONE', *, *, #126280, .F. ) ;
#191861=EDGE_LOOP ( 'NONE', ( #80971, #37496, #108887, #250796 ) ) ;
#191879=VERTEX_POINT ( 'NONE', #216002 ) ;
#191881=CARTESIAN_POINT ( 'NONE',  ( -20.54999999999999716, 1.115600667400684642E-11, -200.9999999999999432 ) ) ;
#191893=DIRECTION ( 'NONE',  ( 0.000000000000000000, 0.000000000000000000, 1.000000000000000000 ) ) ;
#191900=DIRECTION ( 'NONE',  ( 1.000000000000000000, 0.000000000000000000, 0.000000000000000000 ) ) ;
#191906=DIRECTION ( 'NONE',  ( 0.000000000000000000, 0.000000000000000000, -1.000000000000000000 ) ) ;
#191924=ORIENTED_EDGE ( 'NONE', *, *, #3589, .F. ) ;
#191962=ORIENTED_EDGE ( 'NONE', *, *, #205901, .F. ) ;
#191984=LINE ( 'NONE', #150276, #90295 ) ;
#192014=CARTESIAN_POINT ( 'NONE',  ( 21.05000000000000071, 11.65000000001116298, -167.4999999999999716 ) ) ;
#192054=CARTESIAN_POINT ( 'NONE',  ( 20.85000000000000142, -1.362429037182151470, -208.8888812479211765 ) ) ;
#192074=EDGE_LOOP ( 'NONE', ( #54272, #94735, #211605, #33641 ) ) ;
#192077=CARTESIAN_POINT ( 'NONE',  ( -21.14999999999999858, -0.09999999998884338825, -155.8504291924551808 ) ) ;
#192096=AXIS2_PLACEMENT_3D ( 'NONE', #139440, #100310, #160339 ) ;
#192128=CARTESIAN_POINT ( 'NONE',  ( -20.64999999999999858, 2.000000000011154189, -180.7246219227620543 ) ) ;
#192143=ORIENTED_EDGE ( 'NONE', *, *, #241072, .F. ) ;
#192153=DIRECTION ( 'NONE',  ( -1.000000000000000000, 0.000000000000000000, 0.000000000000000000 ) ) ;
#192157=LINE ( 'NONE', #108743, #10445 ) ;
#192163=EDGE_CURVE ( 'NONE', #67428, #6622, #35813, .T. ) ;
#192164=SPHERICAL_SURFACE ( 'NONE', #176507, 0.1000000000000000056 ) ;
#192182=EDGE_CURVE ( 'NONE', #157060, #138430, #254783, .T. ) ;
#192263=CIRCLE ( 'NONE', #100630, 0.09999999999999939493 ) ;
#192277=LINE ( 'NONE', #31930, #120120 ) ;
#192284=VECTOR ( 'NONE', #226390, 1000.000000000000114 ) ;
#192293=CIRCLE ( 'NONE', #71513, 0.09999999999998902822 ) ;
#192329=EDGE_CURVE ( 'NONE', #26762, #199945, #96336, .T. ) ;
#192346=DIRECTION ( 'NONE',  ( 0.000000000000000000, 0.008583690987124100932, -0.9999631594459055250 ) ) ;
#192348=CARTESIAN_POINT ( 'NONE',  ( -18.50000000000000355, -9.399999999988818189, -174.7972597596632625 ) ) ;
#192355=CARTESIAN_POINT ( 'NONE',  ( -23.15000000000000213, -11.48912529306489816, -197.8999999999999773 ) ) ;
#192380=LINE ( 'NONE', #11180, #25499 ) ;
#192408=DIRECTION ( 'NONE',  ( -1.000000000000000000, -0.000000000000000000, 0.000000000000000000 ) ) ;
#192446=DIRECTION ( 'NONE',  ( 0.000000000000000000, 0.000000000000000000, -1.000000000000000000 ) ) ;
#192516=ORIENTED_EDGE ( 'NONE', *, *, #72612, .F. ) ;
#192517=AXIS2_PLACEMENT_3D ( 'NONE', #195689, #19604, #237360 ) ;
#192536=DIRECTION ( 'NONE',  ( -1.000000000000000000, 0.000000000000000000, 0.000000000000000000 ) ) ;
#192556=DIRECTION ( 'NONE',  ( 1.000000000000000000, -0.000000000000000000, -0.000000000000000000 ) ) ;
#192663=DIRECTION ( 'NONE',  ( 1.000000000000000000, 0.000000000000000000, 0.000000000000000000 ) ) ;
#192685=CARTESIAN_POINT ( 'NONE',  ( -21.45000000000000284, 7.708578643773852157, -188.6499999999999488 ) ) ;
#192748=CIRCLE ( 'NONE', #59411, 0.09999999999998898659 ) ;
#192756=CARTESIAN_POINT ( 'NONE',  ( -21.05000000000000071, 1.736257131608553550, -179.0686523290174819 ) ) ;
#192825=CARTESIAN_POINT ( 'NONE',  ( -18.48408745364673678, -9.664322258651997899, -207.6830785333282563 ) ) ;
#192856=CARTESIAN_POINT ( 'NONE',  ( 23.25000000000000000, -9.599999999988849453, -155.7499999999999716 ) ) ;
#192858=CARTESIAN_POINT ( 'NONE',  ( -21.05000000000000071, 6.257814610487270279, -167.4022097086911742 ) ) ;
#192876=VERTEX_POINT ( 'NONE', #133953 ) ;
#192938=CARTESIAN_POINT ( 'NONE',  ( 23.14999999999999147, 1.115600667400684642E-11, -167.4999999999999716 ) ) ;
#192945=DIRECTION ( 'NONE',  ( 0.000000000000000000, 0.000000000000000000, 1.000000000000000000 ) ) ;
#192969=CIRCLE ( 'NONE', #159641, 0.2000000000000057288 ) ;
#192982=CARTESIAN_POINT ( 'NONE',  ( 22.40000000000010516, 1.020945751984553285E-11, -155.8504291924548397 ) ) ;
#193024=CARTESIAN_POINT ( 'NONE',  ( -20.64999999999999858, 4.250000000011156409, -179.7499999999999716 ) ) ;
#193042=EDGE_CURVE ( 'NONE', #156856, #157570, #74846, .T. ) ;
#193066=CIRCLE ( 'NONE', #105527, 0.09999999999999939493 ) ;
#193070=ORIENTED_EDGE ( 'NONE', *, *, #121948, .T. ) ;
#193079=ORIENTED_EDGE ( 'NONE', *, *, #248094, .T. ) ;
#193084=CIRCLE ( 'NONE', #222253, 0.09999999999998898659 ) ;
#193113=ORIENTED_EDGE ( 'NONE', *, *, #215932, .T. ) ;
#193117=CIRCLE ( 'NONE', #80649, 0.2000000000000057288 ) ;
#193134=DIRECTION ( 'NONE',  ( 0.000000000000000000, 0.9915357197604973694, -0.1298341882519105928 ) ) ;
#193166=ORIENTED_EDGE ( 'NONE', *, *, #225730, .F. ) ;
#193167=ADVANCED_FACE ( 'NONE', ( #73711 ), #241964, .F. ) ;
#193168=VECTOR ( 'NONE', #222656, 1000.000000000000000 ) ;
#193188=ORIENTED_EDGE ( 'NONE', *, *, #205926, .T. ) ;
#193196=ORIENTED_EDGE ( 'NONE', *, *, #195282, .F. ) ;
#193216=FACE_OUTER_BOUND ( 'NONE', #127483, .T. ) ;
#193221=ORIENTED_EDGE ( 'NONE', *, *, #245728, .T. ) ;
#193227=EDGE_LOOP ( 'NONE', ( #78898, #99418, #229520, #63362 ) ) ;
#193260=CIRCLE ( 'NONE', #234763, 0.09999999999999817368 ) ;
#193268=SPHERICAL_SURFACE ( 'NONE', #90829, 0.1000000000000000056 ) ;
#193323=EDGE_CURVE ( 'NONE', #185627, #210872, #21438, .T. ) ;
#193330=CARTESIAN_POINT ( 'NONE',  ( 19.75857864376269291, 11.65000000001116476, -192.2499999999999716 ) ) ;
#193386=DIRECTION ( 'NONE',  ( 0.000000000000000000, -1.000000000000000000, 0.000000000000000000 ) ) ;
#193402=CARTESIAN_POINT ( 'NONE',  ( -21.17356465864818205, 6.422803126252873973, -167.4010887589861056 ) ) ;
#193425=CYLINDRICAL_SURFACE ( 'NONE', #68728, 0.09999999999998898659 ) ;
#193430=CARTESIAN_POINT ( 'NONE',  ( 21.05000000000000071, 1.115600667400684642E-11, -200.9999999999999432 ) ) ;
#193437=AXIS2_PLACEMENT_3D ( 'NONE', #216055, #233094, #94831 ) ;
#193440=ORIENTED_EDGE ( 'NONE', *, *, #96220, .F. ) ;
#193469=ORIENTED_EDGE ( 'NONE', *, *, #213959, .T. ) ;
#193501=ORIENTED_EDGE ( 'NONE', *, *, #99646, .F. ) ;
#193503=EDGE_CURVE ( 'NONE', #69705, #148316, #228616, .T. ) ;
#193519=TOROIDAL_SURFACE ( 'NONE', #72743, 6.258578643762700899, 0.1000000000000000056 ) ;
#193547=CARTESIAN_POINT ( 'NONE',  ( -21.05000000000000071, -11.39257802169451139, -197.9260504201680249 ) ) ;
#193556=CARTESIAN_POINT ( 'NONE',  ( 20.85000000000000142, -1.736705739456431807, -212.5174225876236846 ) ) ;
#193561=AXIS2_PLACEMENT_3D ( 'NONE', #43160, #41892, #240075 ) ;
#193570=ORIENTED_EDGE ( 'NONE', *, *, #62476, .T. ) ;
#193618=CYLINDRICAL_SURFACE ( 'NONE', #34591, 0.09999999999999939493 ) ;
#193667=ADVANCED_FACE ( 'NONE', ( #14718 ), #253284, .T. ) ;
#193671=DIRECTION ( 'NONE',  ( 0.000000000000000000, -1.000000000000000000, 0.000000000000000000 ) ) ;
#193682=CIRCLE ( 'NONE', #143774, 0.09999999999999939493 ) ;
#193696=CARTESIAN_POINT ( 'NONE',  ( 18.59999999999999432, -1.637172712959223952, -179.0821533654719815 ) ) ;
#193739=LINE ( 'NONE', #49079, #139251 ) ;
#193743=LINE ( 'NONE', #175481, #249067 ) ;
#193746=DIRECTION ( 'NONE',  ( -1.000000000000000000, 0.000000000000000000, 0.000000000000000000 ) ) ;
#193801=ORIENTED_EDGE ( 'NONE', *, *, #75537, .T. ) ;
#193829=CARTESIAN_POINT ( 'NONE',  ( -20.94999999999999929, -11.74999999998884448, -197.8999999999999773 ) ) ;
#193839=ORIENTED_EDGE ( 'NONE', *, *, #53519, .T. ) ;
#193841=DIRECTION ( 'NONE',  ( 1.000000000000000000, -0.000000000000000000, -0.000000000000000000 ) ) ;
#193851=ORIENTED_EDGE ( 'NONE', *, *, #112417, .F. ) ;
#193867=DIRECTION ( 'NONE',  ( -2.952720810173288619E-16, 1.000000000000000000, 0.000000000000000000 ) ) ;
#193893=ORIENTED_EDGE ( 'NONE', *, *, #200889, .F. ) ;
#193908=ORIENTED_EDGE ( 'NONE', *, *, #30576, .F. ) ;
#193942=FACE_OUTER_BOUND ( 'NONE', #212780, .T. ) ;
#193977=VECTOR ( 'NONE', #192446, 1000.000000000000000 ) ;
#193984=EDGE_CURVE ( 'NONE', #95434, #117714, #225173, .T. ) ;
#194056=TOROIDAL_SURFACE ( 'NONE', #73266, 0.2000000000000000111, 0.1000000000000000056 ) ;
#194091=CARTESIAN_POINT ( 'NONE',  ( 20.30466543256828160, 9.304236939266628426, -175.7536626513919771 ) ) ;
#194094=AXIS2_PLACEMENT_3D ( 'NONE', #124897, #50455, #184851 ) ;
#194106=AXIS2_PLACEMENT_3D ( 'NONE', #139532, #40488, #220381 ) ;
#194111=CARTESIAN_POINT ( 'NONE',  ( -20.64999999999999858, 2.000000000011154189, -180.7246219227620543 ) ) ;
#194118=CARTESIAN_POINT ( 'NONE',  ( -18.37151313414815945, -9.571014125766627245, -207.8166629092395112 ) ) ;
#194122=DIRECTION ( 'NONE',  ( 1.000000000000000000, 0.000000000000000000, 0.000000000000000000 ) ) ;
#194146=ORIENTED_EDGE ( 'NONE', *, *, #226223, .F. ) ;
#194178=ORIENTED_EDGE ( 'NONE', *, *, #146602, .F. ) ;
#194184=EDGE_CURVE ( 'NONE', #133882, #9380, #8724, .T. ) ;
#194254=AXIS2_PLACEMENT_3D ( 'NONE', #153425, #118104, #232943 ) ;
#194291=DIRECTION ( 'NONE',  ( 0.000000000000000000, -0.8660254037844411501, -0.4999999999999956701 ) ) ;
#194298=CARTESIAN_POINT ( 'NONE',  ( -20.94999999999999929, -11.64999999998884306, -197.8999999999999773 ) ) ;
#194333=CARTESIAN_POINT ( 'NONE',  ( -20.94999999999999929, -1.835859311432479268, -212.5044391687984842 ) ) ;
#194351=CARTESIAN_POINT ( 'NONE',  ( 20.94999999999999929, 7.021664781911246322, -204.8335654018972605 ) ) ;
#194355=EDGE_CURVE ( 'NONE', #252063, #48880, #200448, .T. ) ;
#194356=PLANE ( 'NONE',  #198422 ) ;
#194391=DIRECTION ( 'NONE',  ( 1.000000000000000000, 0.000000000000000000, 0.000000000000000000 ) ) ;
#194400=AXIS2_PLACEMENT_3D ( 'NONE', #16215, #257306, #198672 ) ;
#194416=ORIENTED_EDGE ( 'NONE', *, *, #179759, .T. ) ;
#194424=DIRECTION ( 'NONE',  ( -1.000000000000000000, -0.000000000000000000, 0.000000000000000000 ) ) ;
#194454=DIRECTION ( 'NONE',  ( 0.000000000000000000, -6.938893903907222067E-15, -1.000000000000000000 ) ) ;
#194468=VERTEX_POINT ( 'NONE', #98371 ) ;
#194481=ORIENTED_EDGE ( 'NONE', *, *, #108168, .T. ) ;
#194492=CIRCLE ( 'NONE', #7028, 0.09999999999998898659 ) ;
#194498=ADVANCED_FACE ( 'NONE', ( #233647 ), #70738, .F. ) ;
#194509=CARTESIAN_POINT ( 'NONE',  ( 20.94999999999999929, 10.29270135741298731, -206.4573618871519045 ) ) ;
#194518=ORIENTED_EDGE ( 'NONE', *, *, #86425, .T. ) ;
#194576=DIRECTION ( 'NONE',  ( 0.000000000000000000, 0.000000000000000000, -1.000000000000000000 ) ) ;
#194639=AXIS2_PLACEMENT_3D ( 'NONE', #229499, #225604, #245213 ) ;
#194665=VECTOR ( 'NONE', #45454, 1000.000000000000000 ) ;
#194679=DIRECTION ( 'NONE',  ( 0.000000000000000000, 0.000000000000000000, -1.000000000000000000 ) ) ;
#194728=VERTEX_POINT ( 'NONE', #148442 ) ;
#194752=ORIENTED_EDGE ( 'NONE', *, *, #257809, .F. ) ;
#194757=DIRECTION ( 'NONE',  ( 1.000000000000000000, 0.000000000000000000, 0.000000000000000000 ) ) ;
#194764=CIRCLE ( 'NONE', #78206, 1.900000000000012790 ) ;
#194771=DIRECTION ( 'NONE',  ( 0.000000000000000000, 0.000000000000000000, 1.000000000000000000 ) ) ;
#194777=VECTOR ( 'NONE', #61857, 1000.000000000000000 ) ;
#194792=CARTESIAN_POINT ( 'NONE',  ( -21.05000000000000071, 1.750000000011155743, -179.1695115579016147 ) ) ;
#194805=EDGE_CURVE ( 'NONE', #93167, #85372, #129875, .T. ) ;
#194846=ADVANCED_FACE ( 'NONE', ( #200395 ), #138252, .T. ) ;
#194856=DIRECTION ( 'NONE',  ( -0.7070776581709311559, 0.000000000000000000, 0.7071359030027479786 ) ) ;
#194858=EDGE_CURVE ( 'NONE', #213687, #20901, #200636, .T. ) ;
#194876=LINE ( 'NONE', #16246, #138058 ) ;
#194925=ORIENTED_EDGE ( 'NONE', *, *, #163175, .F. ) ;
#194929=LINE ( 'NONE', #32009, #123984 ) ;
#194937=EDGE_CURVE ( 'NONE', #181381, #26762, #42404, .T. ) ;
#194954=CARTESIAN_POINT ( 'NONE',  ( 22.16821283564876666, 7.558973340791918183, -167.4999999999999716 ) ) ;
#194957=CARTESIAN_POINT ( 'NONE',  ( -18.42637059832565427, -9.496945461878542716, -207.6090773097997726 ) ) ;
#194985=DIRECTION ( 'NONE',  ( 1.000000000000000000, 0.000000000000000000, 0.000000000000000000 ) ) ;
#194992=DIRECTION ( 'NONE',  ( -0.000000000000000000, -0.000000000000000000, 1.000000000000000000 ) ) ;
#195007=DIRECTION ( 'NONE',  ( 0.000000000000000000, 0.000000000000000000, -1.000000000000000000 ) ) ;
#195108=AXIS2_PLACEMENT_3D ( 'NONE', #152874, #54992, #74627 ) ;
#195122=CARTESIAN_POINT ( 'NONE',  ( -20.85000000000000142, -11.64999999998884306, -200.9999999999999432 ) ) ;
#195129=ORIENTED_EDGE ( 'NONE', *, *, #172745, .F. ) ;
#195130=EDGE_CURVE ( 'NONE', #3673, #57200, #130066, .T. ) ;
#195163=AXIS2_PLACEMENT_3D ( 'NONE', #43713, #218473, #123247 ) ;
#195199=FACE_OUTER_BOUND ( 'NONE', #231730, .T. ) ;
#195216=CARTESIAN_POINT ( 'NONE',  ( 21.14999999999999858, 1.115600667400684642E-11, -155.8504291924551808 ) ) ;
#195221=DIRECTION ( 'NONE',  ( -2.812466655313719426E-14, 0.1350103645451904977, 0.9908441862701596881 ) ) ;
#195243=DIRECTION ( 'NONE',  ( -1.000000000000000000, -2.952720810173289112E-16, 0.000000000000000000 ) ) ;
#195260=CARTESIAN_POINT ( 'NONE',  ( -20.94999999999999929, -1.162701749926853712, -175.5999999999999659 ) ) ;
#195282=EDGE_CURVE ( 'NONE', #199182, #89904, #125971, .T. ) ;
#195285=AXIS2_PLACEMENT_3D ( 'NONE', #237846, #213144, #17506 ) ;
#195293=DIRECTION ( 'NONE',  ( -0.000000000000000000, 1.000000000000000000, -1.224646799147352961E-16 ) ) ;
#195298=AXIS2_PLACEMENT_3D ( 'NONE', #57359, #216445, #177364 ) ;
#195368=ORIENTED_EDGE ( 'NONE', *, *, #41453, .F. ) ;
#195376=CARTESIAN_POINT ( 'NONE',  ( 20.58091095332318332, 9.018470153363605135, -175.9186501821585296 ) ) ;
#195403=EDGE_LOOP ( 'NONE', ( #41832, #167373, #144176, #50754 ) ) ;
#195454=EDGE_CURVE ( 'NONE', #200909, #11610, #246768, .T. ) ;
#195457=EDGE_CURVE ( 'NONE', #58178, #166015, #117781, .T. ) ;
#195477=CIRCLE ( 'NONE', #195298, 0.2000000000000005107 ) ;
#195494=DIRECTION ( 'NONE',  ( 0.000000000000000000, 0.000000000000000000, 1.000000000000000000 ) ) ;
#195506=DIRECTION ( 'NONE',  ( 0.000000000000000000, 1.000000000000000000, 0.000000000000000000 ) ) ;
#195513=VERTEX_POINT ( 'NONE', #206505 ) ;
#195521=VECTOR ( 'NONE', #118906, 1000.000000000000000 ) ;
#195524=VERTEX_POINT ( 'NONE', #29206 ) ;
#195551=DIRECTION ( 'NONE',  ( 0.000000000000000000, 0.000000000000000000, 1.000000000000000000 ) ) ;
#195576=AXIS2_PLACEMENT_3D ( 'NONE', #257464, #136263, #17612 ) ;
#195580=TOROIDAL_SURFACE ( 'NONE', #83071, 0.4000000000000017431, 0.1000000000000000056 ) ;
#195675=DIRECTION ( 'NONE',  ( 0.000000000000000000, 0.000000000000000000, 1.000000000000000000 ) ) ;
#195679=SPHERICAL_SURFACE ( 'NONE', #62549, 0.1000000000000000056 ) ;
#195689=CARTESIAN_POINT ( 'NONE',  ( -23.25000000000000000, 1.115600667400684642E-11, -167.4999999999999716 ) ) ;
#195751=CARTESIAN_POINT ( 'NONE',  ( -20.64999999999999858, 1.115600667400684642E-11, -167.4999999999999716 ) ) ;
#195753=ORIENTED_EDGE ( 'NONE', *, *, #182, .F. ) ;
#195765=ORIENTED_EDGE ( 'NONE', *, *, #161085, .T. ) ;
#195773=ORIENTED_EDGE ( 'NONE', *, *, #244331, .T. ) ;
#195826=VECTOR ( 'NONE', #46098, 1000.000000000000000 ) ;
#195828=ADVANCED_FACE ( 'NONE', ( #122833 ), #151321, .F. ) ;
#195832=DIRECTION ( 'NONE',  ( 1.000000000000000000, 0.000000000000000000, 0.000000000000000000 ) ) ;
#195833=EDGE_LOOP ( 'NONE', ( #150096, #204813, #224365, #63351 ) ) ;
#195867=DIRECTION ( 'NONE',  ( 1.000000000000000000, 0.000000000000000000, -0.000000000000000000 ) ) ;
#195871=ORIENTED_EDGE ( 'NONE', *, *, #246538, .F. ) ;
#195881=CARTESIAN_POINT ( 'NONE',  ( -23.15000000000000213, 11.75000000001115907, -194.1583993101029364 ) ) ;
#195902=DIRECTION ( 'NONE',  ( 0.000000000000000000, -1.000000000000000000, -0.000000000000000000 ) ) ;
#195904=EDGE_LOOP ( 'NONE', ( #160930, #143810, #174360, #10437 ) ) ;
#195913=DIRECTION ( 'NONE',  ( 0.000000000000000000, 0.000000000000000000, -1.000000000000000000 ) ) ;
#195936=DIRECTION ( 'NONE',  ( 1.000000000000000000, 0.000000000000000000, 0.000000000000000000 ) ) ;
#195941=DIRECTION ( 'NONE',  ( 0.000000000000000000, 1.000000000000000000, -6.308085367188393199E-16 ) ) ;
#195970=EDGE_CURVE ( 'NONE', #220454, #82222, #80517, .T. ) ;
#195997=DIRECTION ( 'NONE',  ( 0.000000000000000000, 0.000000000000000000, -1.000000000000000000 ) ) ;
#196039=AXIS2_PLACEMENT_3D ( 'NONE', #86015, #183870, #166908 ) ;
#196088=EDGE_LOOP ( 'NONE', ( #163054, #97030, #209186, #123445 ) ) ;
#196100=EDGE_CURVE ( 'NONE', #62075, #147404, #176911, .T. ) ;
#196112=EDGE_CURVE ( 'NONE', #138993, #429, #28858, .T. ) ;
#196129=AXIS2_PLACEMENT_3D ( 'NONE', #227354, #48712, #251734 ) ;
#196157=CIRCLE ( 'NONE', #200256, 0.09999999999999939493 ) ;
#196191=FACE_OUTER_BOUND ( 'NONE', #190886, .T. ) ;
#196233=DIRECTION ( 'NONE',  ( -1.000000000000000000, 0.000000000000000000, 0.000000000000000000 ) ) ;
#196242=DIRECTION ( 'NONE',  ( -0.000000000000000000, -0.000000000000000000, 1.000000000000000000 ) ) ;
#196256=ORIENTED_EDGE ( 'NONE', *, *, #120672, .T. ) ;
#196271=EDGE_LOOP ( 'NONE', ( #50862, #140245, #124148, #250608 ) ) ;
#196293=VERTEX_POINT ( 'NONE', #32086 ) ;
#196317=FACE_OUTER_BOUND ( 'NONE', #130150, .T. ) ;
#196347=CARTESIAN_POINT ( 'NONE',  ( 21.30000000000002558, 1.115600667400684642E-11, -167.4999999999999716 ) ) ;
#196389=CARTESIAN_POINT ( 'NONE',  ( -21.05000000000000071, 11.75000000001115197, -193.9851942293460070 ) ) ;
#196417=DIRECTION ( 'NONE',  ( 1.000000000000000000, 0.000000000000000000, 0.000000000000000000 ) ) ;
#196430=VERTEX_POINT ( 'NONE', #155890 ) ;
#196431=ORIENTED_EDGE ( 'NONE', *, *, #163670, .F. ) ;
#196495=DIRECTION ( 'NONE',  ( 0.000000000000000000, 0.4999999999999956701, -0.8660254037844411501 ) ) ;
#196498=AXIS2_PLACEMENT_3D ( 'NONE', #223157, #227016, #105763 ) ;
#196504=ADVANCED_FACE ( 'NONE', ( #55439 ), #219676, .T. ) ;
#196530=DIRECTION ( 'NONE',  ( 0.000000000000000000, -1.000000000000000000, 0.000000000000000000 ) ) ;
#196549=LINE ( 'NONE', #17907, #201356 ) ;
#196556=ORIENTED_EDGE ( 'NONE', *, *, #175922, .T. ) ;
#196568=EDGE_CURVE ( 'NONE', #117253, #128029, #162302, .T. ) ;
#196578=CARTESIAN_POINT ( 'NONE',  ( 18.49999999999999289, 10.29270135741298731, -206.4573618871519045 ) ) ;
#196589=DIRECTION ( 'NONE',  ( 1.000000000000000000, -0.000000000000000000, -0.000000000000000000 ) ) ;
#196599=AXIS2_PLACEMENT_3D ( 'NONE', #180264, #99415, #117710 ) ;
#196656=EDGE_LOOP ( 'NONE', ( #144751, #172547, #68646, #180125 ) ) ;
#196662=AXIS2_PLACEMENT_3D ( 'NONE', #140976, #41884, #121431 ) ;
#196707=EDGE_LOOP ( 'NONE', ( #49527, #83750, #99819, #146580, #177677 ) ) ;
#196712=VERTEX_POINT ( 'NONE', #129586 ) ;
#196714=CARTESIAN_POINT ( 'NONE',  ( -21.09813707148783735, 0.03135149954058748939, -161.1149378942632779 ) ) ;
#196732=EDGE_LOOP ( 'NONE', ( #256194, #13833, #77825, #80203 ) ) ;
#196739=DIRECTION ( 'NONE',  ( 0.000000000000000000, 0.000000000000000000, 1.000000000000000000 ) ) ;
#196740=VECTOR ( 'NONE', #130100, 1000.000000000000000 ) ;
#196749=CARTESIAN_POINT ( 'NONE',  ( -18.59999999999999787, 1.835341550235567887, -179.0551512925629538 ) ) ;
#196760=DIRECTION ( 'NONE',  ( 0.000000000000000000, -0.1298341882520022694, -0.9915357197604853789 ) ) ;
#196772=SHAPE_REPRESENTATION ( 'Injection Molded Chain Links 6', ( #2425 ), #252581 ) ;
#196805=CIRCLE ( 'NONE', #5239, 0.09999999999999939493 ) ;
#196811=VECTOR ( 'NONE', #225485, 1000.000000000000114 ) ;
#196827=AXIS2_PLACEMENT_3D ( 'NONE', #3689, #62392, #45389 ) ;
#196852=AXIS2_PLACEMENT_3D ( 'NONE', #7175, #104967, #110143 ) ;
#196857=AXIS2_PLACEMENT_3D ( 'NONE', #119573, #240788, #141672 ) ;
#196895=DIRECTION ( 'NONE',  ( -1.000000000000000000, 0.000000000000000000, 0.000000000000000000 ) ) ;
#196901=ADVANCED_FACE ( 'NONE', ( #181568 ), #146257, .T. ) ;
#196903=ORIENTED_EDGE ( 'NONE', *, *, #127389, .T. ) ;
#196929=VERTEX_POINT ( 'NONE', #82412 ) ;
#197015=CIRCLE ( 'NONE', #251169, 0.1000000000000094008 ) ;
#197017=VERTEX_POINT ( 'NONE', #129277 ) ;
#197023=AXIS2_PLACEMENT_3D ( 'NONE', #29346, #163685, #245788 ) ;
#197040=CARTESIAN_POINT ( 'NONE',  ( -21.07928932188134397, 0.09889514566555075714, -161.1714833436066385 ) ) ;
#197120=CARTESIAN_POINT ( 'NONE',  ( -23.25000000000000000, 1.115600667400684642E-11, -200.9999999999999432 ) ) ;
#197145=DIRECTION ( 'NONE',  ( 0.000000000000000000, 0.000000000000000000, -1.000000000000000000 ) ) ;
#197149=CIRCLE ( 'NONE', #113946, 0.09999999999999939493 ) ;
#197184=DIRECTION ( 'NONE',  ( 0.000000000000000000, 0.000000000000000000, -1.000000000000000000 ) ) ;
#197225=CARTESIAN_POINT ( 'NONE',  ( -21.22070241538126112, 6.469946272880768845, -167.4010809694649424 ) ) ;
#197258=ORIENTED_EDGE ( 'NONE', *, *, #49664, .T. ) ;
#197284=DIRECTION ( 'NONE',  ( -1.000000000000000000, 0.000000000000000000, 0.000000000000000000 ) ) ;
#197310=ORIENTED_EDGE ( 'NONE', *, *, #77872, .T. ) ;
#197371=EDGE_CURVE ( 'NONE', #63249, #68443, #22536, .T. ) ;
#197400=AXIS2_PLACEMENT_3D ( 'NONE', #227665, #208137, #46454 ) ;
#197403=AXIS2_PLACEMENT_3D ( 'NONE', #100349, #127496, #90925 ) ;
#197446=B_SPLINE_CURVE_WITH_KNOTS ( 'NONE', 3,
 ( #235333, #134927, #194957, #231512, #234054, #151990, #213199, #55383, #94537, #254846 ),
 .UNSPECIFIED., .F., .F.,
 ( 4, 2, 2, 2, 4 ),
 ( 0.000000000000000000, 4.221631689683615497E-05, 8.443263379367230994E-05, 0.0001688652675874169633, 0.0003377305351749844138 ),
 .UNSPECIFIED. ) ;
#197469=ORIENTED_EDGE ( 'NONE', *, *, #247949, .F. ) ;
#197526=CARTESIAN_POINT ( 'NONE',  ( 20.95545211741311320, 10.58641331155510379, -175.0861468595882684 ) ) ;
#197528=AXIS2_PLACEMENT_3D ( 'NONE', #65765, #67058, #64490 ) ;
#197551=VECTOR ( 'NONE', #206543, 1000.000000000000000 ) ;
#197594=AXIS2_PLACEMENT_3D ( 'NONE', #175340, #253549, #213147 ) ;
#197631=ORIENTED_EDGE ( 'NONE', *, *, #14647, .T. ) ;
#197687=DIRECTION ( 'NONE',  ( -1.000000000000000000, -0.000000000000000000, -0.000000000000000000 ) ) ;
#197706=AXIS2_PLACEMENT_3D ( 'NONE', #217432, #16706, #237027 ) ;
#197734=ORIENTED_EDGE ( 'NONE', *, *, #244331, .F. ) ;
#197753=DIRECTION ( 'NONE',  ( 0.000000000000000000, -0.1298341882520022694, -0.9915357197604853789 ) ) ;
#197834=ORIENTED_EDGE ( 'NONE', *, *, #42559, .F. ) ;
#197843=CIRCLE ( 'NONE', #151903, 0.4000000000000114575 ) ;
#197878=DIRECTION ( 'NONE',  ( 0.000000000000000000, -1.000000000000000000, 0.000000000000000000 ) ) ;
#197908=CARTESIAN_POINT ( 'NONE',  ( 20.85000000000000142, -1.164121893230052995, -208.9148480855715775 ) ) ;
#197923=DIRECTION ( 'NONE',  ( 0.000000000000000000, 0.000000000000000000, -1.000000000000000000 ) ) ;
#197926=CARTESIAN_POINT ( 'NONE',  ( 18.47149038651512143, -9.671457157995547504, -207.6727863347383618 ) ) ;
#197932=DIRECTION ( 'NONE',  ( 0.000000000000000000, 0.000000000000000000, -1.000000000000000000 ) ) ;
#197945=CARTESIAN_POINT ( 'NONE',  ( -22.32929514600008503, 0.09907567812507747651, -159.9213524346234578 ) ) ;
#197985=DIRECTION ( 'NONE',  ( 0.000000000000000000, 0.000000000000000000, -1.000000000000000000 ) ) ;
#198053=FACE_OUTER_BOUND ( 'NONE', #72797, .T. ) ;
#198062=ORIENTED_EDGE ( 'NONE', *, *, #211565, .F. ) ;
#198103=VECTOR ( 'NONE', #195941, 1000.000000000000000 ) ;
#198106=ORIENTED_EDGE ( 'NONE', *, *, #146902, .T. ) ;
#198114=CARTESIAN_POINT ( 'NONE',  ( 21.05000000000000071, -8.999999999988842703, -191.5060308773475128 ) ) ;
#198119=EDGE_CURVE ( 'NONE', #36105, #72109, #197843, .T. ) ;
#198136=SPHERICAL_SURFACE ( 'NONE', #101543, 0.1000000000000000056 ) ;
#198159=ORIENTED_EDGE ( 'NONE', *, *, #6385, .T. ) ;
#198176=CIRCLE ( 'NONE', #169170, 4.049999999999998046 ) ;
#198234=CARTESIAN_POINT ( 'NONE',  ( 21.13461538461538325, 10.61458296203669249, -179.8499999999999943 ) ) ;
#198237=EDGE_CURVE ( 'NONE', #247867, #117217, #10613, .T. ) ;
#198251=LINE ( 'NONE', #178736, #45727 ) ;
#198283=EDGE_LOOP ( 'NONE', ( #188193, #126473, #25732, #41138 ) ) ;
#198284=CIRCLE ( 'NONE', #6752, 0.1999999999999996503 ) ;
#198325=CIRCLE ( 'NONE', #127608, 0.1999999999999987899 ) ;
#198326=ORIENTED_EDGE ( 'NONE', *, *, #173643, .T. ) ;
#198383=EDGE_CURVE ( 'NONE', #182323, #146255, #139570, .T. ) ;
#198407=CARTESIAN_POINT ( 'NONE',  ( 18.59999999999998366, 7.021664781911246322, -204.8335654018972605 ) ) ;
#198422=AXIS2_PLACEMENT_3D ( 'NONE', #191790, #153967, #190502 ) ;
#198471=DIRECTION ( 'NONE',  ( 1.000000000000000000, 7.304098846218134667E-16, 0.000000000000000000 ) ) ;
#198477=DIRECTION ( 'NONE',  ( 0.000000000000000000, 0.000000000000000000, -1.000000000000000000 ) ) ;
#198500=CARTESIAN_POINT ( 'NONE',  ( -21.05000000000000071, 1.115600667400684642E-11, -167.4999999999999716 ) ) ;
#198509=ORIENTED_EDGE ( 'NONE', *, *, #105144, .F. ) ;
#198512=CARTESIAN_POINT ( 'NONE',  ( -23.25000000000000000, 1.115649040949250830E-11, -197.0999999999999659 ) ) ;
#198514=EDGE_CURVE ( 'NONE', #176027, #135423, #106247, .T. ) ;
#198556=EDGE_CURVE ( 'NONE', #143156, #44391, #203271, .T. ) ;
#198559=ORIENTED_EDGE ( 'NONE', *, *, #23779, .T. ) ;
#198567=DIRECTION ( 'NONE',  ( 0.000000000000000000, 0.000000000000000000, -1.000000000000000000 ) ) ;
#198576=DIRECTION ( 'NONE',  ( 1.000000000000000000, 0.000000000000000000, 0.000000000000000000 ) ) ;
#198594=CIRCLE ( 'NONE', #23847, 0.5000000000000013323 ) ;
#198606=ORIENTED_EDGE ( 'NONE', *, *, #201806, .F. ) ;
#198618=ORIENTED_EDGE ( 'NONE', *, *, #192182, .T. ) ;
#198622=AXIS2_PLACEMENT_3D ( 'NONE', #171052, #27678, #186726 ) ;
#198650=ORIENTED_EDGE ( 'NONE', *, *, #13943, .T. ) ;
#198654=EDGE_LOOP ( 'NONE', ( #249077, #156952, #225962, #151475 ) ) ;
#198672=DIRECTION ( 'NONE',  ( 0.000000000000000000, 0.000000000000000000, -1.000000000000000000 ) ) ;
#198702=CARTESIAN_POINT ( 'NONE',  ( -18.50211644919735576, 10.30207779525983192, -206.4895520716782187 ) ) ;
#198706=DIRECTION ( 'NONE',  ( 0.000000000000000000, 1.000000000000000000, 0.000000000000000000 ) ) ;
#198716=DIRECTION ( 'NONE',  ( 0.000000000000000000, 0.000000000000000000, 1.000000000000000000 ) ) ;
#198750=CARTESIAN_POINT ( 'NONE',  ( 23.15000000000000213, -11.74999999998883560, -179.6499999999999773 ) ) ;
#198774=VECTOR ( 'NONE', #132831, 1000.000000000000114 ) ;
#198790=ORIENTED_EDGE ( 'NONE', *, *, #53468, .T. ) ;
#198793=CARTESIAN_POINT ( 'NONE',  ( 23.15000000000000213, -8.663551401858002876, -177.0241011180672785 ) ) ;
#198803=FACE_OUTER_BOUND ( 'NONE', #163610, .T. ) ;
#198805=ORIENTED_EDGE ( 'NONE', *, *, #11707, .T. ) ;
#198865=ORIENTED_EDGE ( 'NONE', *, *, #215007, .T. ) ;
#198887=CARTESIAN_POINT ( 'NONE',  ( -21.05000000000000071, 6.258316057343182415, -167.4342983896778776 ) ) ;
#198912=ORIENTED_EDGE ( 'NONE', *, *, #203998, .F. ) ;
#198965=ORIENTED_EDGE ( 'NONE', *, *, #96331, .T. ) ;
#198966=ORIENTED_EDGE ( 'NONE', *, *, #107064, .F. ) ;
#198973=APPLICATION_CONTEXT ( 'automotive_design' ) ;
#199067=DIRECTION ( 'NONE',  ( 0.000000000000000000, 2.891205793294679805E-16, -1.000000000000000000 ) ) ;
#199092=VERTEX_POINT ( 'NONE', #79793 ) ;
#199106=CARTESIAN_POINT ( 'NONE',  ( -20.54999999999999361, 11.65000000001115232, -188.8499999999999659 ) ) ;
#199111=ORIENTED_EDGE ( 'NONE', *, *, #121948, .F. ) ;
#199127=DIRECTION ( 'NONE',  ( 0.000000000000000000, 0.000000000000000000, 1.000000000000000000 ) ) ;
#199136=CIRCLE ( 'NONE', #169961, 0.09999999999999062417 ) ;
#199137=VECTOR ( 'NONE', #59080, 1000.000000000000000 ) ;
#199182=VERTEX_POINT ( 'NONE', #87503 ) ;
#199185=EDGE_CURVE ( 'NONE', #202583, #239004, #1995, .T. ) ;
#199210=CARTESIAN_POINT ( 'NONE',  ( 20.87631937322887410, 10.47149503677486138, -175.0797458745818176 ) ) ;
#199216=DIRECTION ( 'NONE',  ( 1.000000000000000000, -0.000000000000000000, -0.000000000000000000 ) ) ;
#199316=DIRECTION ( 'NONE',  ( 0.000000000000000000, 0.000000000000000000, 1.000000000000000000 ) ) ;
#199318=FACE_OUTER_BOUND ( 'NONE', #121382, .T. ) ;
#199339=ORIENTED_EDGE ( 'NONE', *, *, #9320, .T. ) ;
#199385=VERTEX_POINT ( 'NONE', #62523 ) ;
#199394=DIRECTION ( 'NONE',  ( 0.000000000000000000, 0.1350103645451904977, -0.9908441862701596881 ) ) ;
#199400=DIRECTION ( 'NONE',  ( 0.000000000000000000, 1.000000000000000000, 0.000000000000000000 ) ) ;
#199405=CYLINDRICAL_SURFACE ( 'NONE', #212645, 0.09999999999998898659 ) ;
#199422=AXIS2_PLACEMENT_3D ( 'NONE', #110892, #151326, #46082 ) ;
#199436=ORIENTED_EDGE ( 'NONE', *, *, #40110, .F. ) ;
#199477=FACE_OUTER_BOUND ( 'NONE', #32809, .T. ) ;
#199513=ORIENTED_EDGE ( 'NONE', *, *, #106766, .T. ) ;
#199516=EDGE_CURVE ( 'NONE', #199385, #103641, #89671, .T. ) ;
#199549=DIRECTION ( 'NONE',  ( 0.000000000000000000, 0.000000000000000000, -1.000000000000000000 ) ) ;
#199556=VECTOR ( 'NONE', #21179, 1000.000000000000000 ) ;
#199567=AXIS2_PLACEMENT_3D ( 'NONE', #164447, #2772, #103155 ) ;
#199590=EDGE_CURVE ( 'NONE', #200909, #7750, #245005, .T. ) ;
#199601=VERTEX_POINT ( 'NONE', #11548 ) ;
#199622=EDGE_CURVE ( 'NONE', #46891, #493, #16684, .T. ) ;
#199624=VECTOR ( 'NONE', #199127, 1000.000000000000000 ) ;
#199627=ORIENTED_EDGE ( 'NONE', *, *, #192163, .T. ) ;
#199628=CIRCLE ( 'NONE', #212084, 4.049999999999998046 ) ;
#199635=ORIENTED_EDGE ( 'NONE', *, *, #10872, .T. ) ;
#199637=CARTESIAN_POINT ( 'NONE',  ( 23.14999999999999503, 11.75000000001116263, -155.7499999999999716 ) ) ;
#199651=ORIENTED_EDGE ( 'NONE', *, *, #154041, .F. ) ;
#199668=FACE_OUTER_BOUND ( 'NONE', #29349, .T. ) ;
#199678=FACE_OUTER_BOUND ( 'NONE', #148937, .T. ) ;
#199684=CARTESIAN_POINT ( 'NONE',  ( 18.59999999999997655, 1.115600667400684642E-11, -200.9999999999999432 ) ) ;
#199697=CARTESIAN_POINT ( 'NONE',  ( -23.25000000000000000, 1.115600667400684642E-11, -171.5499999999999829 ) ) ;
#199709=CARTESIAN_POINT ( 'NONE',  ( -21.05000000000000071, -0.2561057920810652089, -167.4651035583276553 ) ) ;
#199724=CARTESIAN_POINT ( 'NONE',  ( 21.05000000000000071, -11.64999999998883595, -197.9999999999999432 ) ) ;
#199733=CARTESIAN_POINT ( 'NONE',  ( -21.14999999999999858, 11.75000000001115552, -167.5999999999999659 ) ) ;
#199734=DIRECTION ( 'NONE',  ( 0.000000000000000000, 0.000000000000000000, 1.000000000000000000 ) ) ;
#199777=DIRECTION ( 'NONE',  ( -1.000000000000000000, -0.000000000000000000, -0.000000000000000000 ) ) ;
#199785=LINE ( 'NONE', #181499, #206705 ) ;
#199791=DIRECTION ( 'NONE',  ( -1.000000000000000000, -0.000000000000000000, -0.000000000000000000 ) ) ;
#199809=ORIENTED_EDGE ( 'NONE', *, *, #227585, .T. ) ;
#199821=CARTESIAN_POINT ( 'NONE',  ( 20.95512820512820440, 8.876151316299271343, -176.0586289951409071 ) ) ;
#199829=CARTESIAN_POINT ( 'NONE',  ( -18.59999999999999787, 11.65000000001115232, -188.8499999999999659 ) ) ;
#199945=VERTEX_POINT ( 'NONE', #188569 ) ;
#200062=CYLINDRICAL_SURFACE ( 'NONE', #132596, 0.09999999999999939493 ) ;
#200078=EDGE_LOOP ( 'NONE', ( #102589, #101350, #75817 ) ) ;
#200110=CARTESIAN_POINT ( 'NONE',  ( 20.95566103547454517, 10.61824765095822087, -175.1318401929805475 ) ) ;
#200178=ORIENTED_EDGE ( 'NONE', *, *, #101645, .F. ) ;
#200180=TOROIDAL_SURFACE ( 'NONE', #87722, 1.900000000000002576, 0.1000000000000000056 ) ;
#200188=CARTESIAN_POINT ( 'NONE',  ( 20.94999999999999574, 10.62357026049396680, -174.9919452032305287 ) ) ;
#200197=ORIENTED_EDGE ( 'NONE', *, *, #73520, .T. ) ;
#200213=CARTESIAN_POINT ( 'NONE',  ( -23.25000000000000000, 1.115600667400684642E-11, -200.9999999999999432 ) ) ;
#200219=CARTESIAN_POINT ( 'NONE',  ( -23.15000000000000213, 2.000000000011154189, -187.7753780772378889 ) ) ;
#200251=FACE_OUTER_BOUND ( 'NONE', #49742, .T. ) ;
#200256=AXIS2_PLACEMENT_3D ( 'NONE', #212697, #73204, #34087 ) ;
#200263=CIRCLE ( 'NONE', #254402, 0.09999999999999864553 ) ;
#200277=AXIS2_PLACEMENT_3D ( 'NONE', #125979, #107702, #144242 ) ;
#200281=AXIS2_PLACEMENT_3D ( 'NONE', #42899, #85836, #222795 ) ;
#200283=ORIENTED_EDGE ( 'NONE', *, *, #30559, .F. ) ;
#200340=ORIENTED_EDGE ( 'NONE', *, *, #62476, .F. ) ;
#200354=ORIENTED_EDGE ( 'NONE', *, *, #115781, .F. ) ;
#200377=ORIENTED_EDGE ( 'NONE', *, *, #92837, .F. ) ;
#200380=AXIS2_PLACEMENT_3D ( 'NONE', #129897, #209440, #189887 ) ;
#200383=DIRECTION ( 'NONE',  ( 0.000000000000000000, 0.000000000000000000, 1.000000000000000000 ) ) ;
#200386=ORIENTED_EDGE ( 'NONE', *, *, #71235, .F. ) ;
#200387=FACE_OUTER_BOUND ( 'NONE', #161779, .T. ) ;
#200395=FACE_OUTER_BOUND ( 'NONE', #212488, .T. ) ;
#200430=CARTESIAN_POINT ( 'NONE',  ( 18.52928932188133970, 10.27928932189249878, -192.2085786437626211 ) ) ;
#200448=CIRCLE ( 'NONE', #63061, 0.5000000000000004441 ) ;
#200456=DIRECTION ( 'NONE',  ( -0.000000000000000000, -1.000000000000000000, -5.421010862427649374E-16 ) ) ;
#200467=ADVANCED_FACE ( 'NONE', ( #129593 ), #132153, .F. ) ;
#200471=DIRECTION ( 'NONE',  ( 1.000000000000000000, 1.836970198721029934E-16, 3.186635328391151676E-31 ) ) ;
#200479=DIRECTION ( 'NONE',  ( -0.000000000000000000, -0.1350103645451876666, 0.9908441862701600211 ) ) ;
#200481=ORIENTED_EDGE ( 'NONE', *, *, #130826, .T. ) ;
#200515=ORIENTED_EDGE ( 'NONE', *, *, #98861, .T. ) ;
#200520=CYLINDRICAL_SURFACE ( 'NONE', #59704, 11.75000000000001066 ) ;
#200522=AXIS2_PLACEMENT_3D ( 'NONE', #145133, #87726, #241683 ) ;
#200523=CARTESIAN_POINT ( 'NONE',  ( -21.53551880898957904, 0.09896973458281840830, -160.7152022385836574 ) ) ;
#200530=UNCERTAINTY_MEASURE_WITH_UNIT (LENGTH_MEASURE( 1.000000000000000082E-05 ), #205219, 'distance_accuracy_value', 'NONE');
#200546=CARTESIAN_POINT ( 'NONE',  ( -18.59999999999999787, 9.250000000011157297, -188.7499999999999716 ) ) ;
#200603=ORIENTED_EDGE ( 'NONE', *, *, #179140, .T. ) ;
#200622=EDGE_CURVE ( 'NONE', #212963, #232095, #115184, .T. ) ;
#200627=B_SPLINE_CURVE_WITH_KNOTS ( 'NONE', 3,
 ( #119199, #57910, #159610, #154499, #233990, #55325, #117895, #137451, #177895, #20100 ),
 .UNSPECIFIED., .F., .F.,
 ( 4, 3, 3, 4 ),
 ( 3.103167691559091397E-17, 0.0002000000000008536833, 0.001000000000082982687, 0.001967863649483335420 ),
 .UNSPECIFIED. ) ;
#200632=DIRECTION ( 'NONE',  ( 0.7071067811865474617, 0.7071067811865474617, 2.044391222244499837E-16 ) ) ;
#200636=CIRCLE ( 'NONE', #125781, 0.09999999999998898659 ) ;
#200642=DIRECTION ( 'NONE',  ( 1.000000000000000000, 0.000000000000000000, 0.000000000000000000 ) ) ;
#200645=DIRECTION ( 'NONE',  ( 0.000000000000000000, 0.000000000000000000, 1.000000000000000000 ) ) ;
#200651=CIRCLE ( 'NONE', #88177, 11.65000000000000036 ) ;
#200670=ORIENTED_EDGE ( 'NONE', *, *, #240222, .T. ) ;
#200673=SPHERICAL_SURFACE ( 'NONE', #189322, 0.1000000000000000056 ) ;
#200701=EDGE_LOOP ( 'NONE', ( #209884, #148878, #4106, #97925 ) ) ;
#200702=EDGE_CURVE ( 'NONE', #252199, #62638, #90213, .T. ) ;
#200706=DIRECTION ( 'NONE',  ( -1.000000000000000000, -0.000000000000000000, -0.000000000000000000 ) ) ;
#200723=CARTESIAN_POINT ( 'NONE',  ( 20.94999999999999929, -9.399999999988846611, -177.3939691226524076 ) ) ;
#200742=DIRECTION ( 'NONE',  ( -1.000000000000000000, 0.000000000000000000, 0.000000000000000000 ) ) ;
#200743=CIRCLE ( 'NONE', #9208, 0.09999999999999158173 ) ;
#200750=CARTESIAN_POINT ( 'NONE',  ( 22.46250603428203618, 0.02114417614996233138, -155.8501369026598979 ) ) ;
#200752=ORIENTED_EDGE ( 'NONE', *, *, #159460, .F. ) ;
#200768=VECTOR ( 'NONE', #112420, 1000.000000000000000 ) ;
#200769=ADVANCED_FACE ( 'NONE', ( #177089 ), #111972, .T. ) ;
#200770=EDGE_CURVE ( 'NONE', #47818, #147926, #240892, .T. ) ;
#200784=DIRECTION ( 'NONE',  ( 1.000000000000000000, 0.000000000000000000, 0.000000000000000000 ) ) ;
#200795=CARTESIAN_POINT ( 'NONE',  ( -18.50000000000000000, -1.687074390080403941, -154.6854270334582964 ) ) ;
#200819=CARTESIAN_POINT ( 'NONE',  ( -20.54999999999999716, 7.250000000011155521, -188.7499999999999716 ) ) ;
#200885=CIRCLE ( 'NONE', #155141, 0.09999999999998898659 ) ;
#200889=EDGE_CURVE ( 'NONE', #90736, #182355, #115354, .T. ) ;
#200890=DIRECTION ( 'NONE',  ( -1.000000000000000000, 0.000000000000000000, 0.000000000000000000 ) ) ;
#200894=ORIENTED_EDGE ( 'NONE', *, *, #240487, .T. ) ;
#200902=TOROIDAL_SURFACE ( 'NONE', #84311, 0.4000000000000012990, 0.1000000000000000056 ) ;
#200909=VERTEX_POINT ( 'NONE', #109063 ) ;
#200941=DIRECTION ( 'NONE',  ( -4.391705002472929091E-16, 1.000000000000000000, 0.000000000000000000 ) ) ;
#200962=EDGE_CURVE ( 'NONE', #196929, #235213, #82010, .T. ) ;
#201006=ORIENTED_EDGE ( 'NONE', *, *, #180367, .F. ) ;
#201014=DIRECTION ( 'NONE',  ( 1.000000000000000000, 0.000000000000000000, 0.000000000000000000 ) ) ;
#201019=VECTOR ( 'NONE', #131090, 1000.000000000000000 ) ;
#201020=DIRECTION ( 'NONE',  ( -0.000000000000000000, -0.000000000000000000, 1.000000000000000000 ) ) ;
#201022=DIRECTION ( 'NONE',  ( 0.000000000000000000, -0.8700118002898322711, 0.4930308989875231140 ) ) ;
#201037=LINE ( 'NONE', #44543, #103388 ) ;
#201081=DIRECTION ( 'NONE',  ( 0.000000000000000000, 0.4999999999999413247, -0.8660254037844724584 ) ) ;
#201082=ORIENTED_EDGE ( 'NONE', *, *, #93755, .T. ) ;
#201120=EDGE_LOOP ( 'NONE', ( #219832, #160530, #17637, #195368 ) ) ;
#201156=DIRECTION ( 'NONE',  ( 1.000000000000000000, -0.000000000000000000, 0.000000000000000000 ) ) ;
#201161=VECTOR ( 'NONE', #3241, 1000.000000000000000 ) ;
#201162=DIRECTION ( 'NONE',  ( 0.000000000000000000, 0.000000000000000000, -1.000000000000000000 ) ) ;
#201175=DIRECTION ( 'NONE',  ( 1.000000000000000000, 0.000000000000000000, 0.000000000000000000 ) ) ;
#201209=ORIENTED_EDGE ( 'NONE', *, *, #241818, .F. ) ;
#201226=AXIS2_PLACEMENT_3D ( 'NONE', #226129, #139220, #178406 ) ;
#201251=CARTESIAN_POINT ( 'NONE',  ( 18.59999999999999076, -1.164121893230052995, -208.9148480855715775 ) ) ;
#201272=DIRECTION ( 'NONE',  ( 4.377807931758638789E-15, 0.2605042016806672911, 0.9654727137038716656 ) ) ;
#201286=CARTESIAN_POINT ( 'NONE',  ( 20.85000000000000142, 1.115600667400684642E-11, -208.8999999999999488 ) ) ;
#201354=CARTESIAN_POINT ( 'NONE',  ( 21.07199075132371746, 8.774944999127242795, -179.7135321616128465 ) ) ;
#201356=VECTOR ( 'NONE', #177027, 1000.000000000000000 ) ;
#201384=CARTESIAN_POINT ( 'NONE',  ( 20.95576188350343116, 10.60898054497455512, -175.1112337227542639 ) ) ;
#201395=ORIENTED_EDGE ( 'NONE', *, *, #158048, .F. ) ;
#201400=FACE_OUTER_BOUND ( 'NONE', #146645, .T. ) ;
#201413=AXIS2_PLACEMENT_3D ( 'NONE', #22986, #137746, #255088 ) ;
#201434=EDGE_CURVE ( 'NONE', #98329, #91307, #94686, .T. ) ;
#201446=ORIENTED_EDGE ( 'NONE', *, *, #209531, .T. ) ;
#201449=ORIENTED_EDGE ( 'NONE', *, *, #187712, .F. ) ;
#201454=DIRECTION ( 'NONE',  ( -0.000000000000000000, 0.8660254037844411501, 0.4999999999999956701 ) ) ;
#201465=EDGE_CURVE ( 'NONE', #134756, #16193, #207142, .T. ) ;
#201489=CARTESIAN_POINT ( 'NONE',  ( -23.25000000000000000, 4.350000000011156054, -188.8499999999999659 ) ) ;
#201495=DIRECTION ( 'NONE',  ( -0.000000000000000000, 1.000000000000000000, 0.000000000000000000 ) ) ;
#201500=AXIS2_PLACEMENT_3D ( 'NONE', #228008, #187617, #226708 ) ;
#201509=VECTOR ( 'NONE', #45322, 1000.000000000000000 ) ;
#201564=ORIENTED_EDGE ( 'NONE', *, *, #37975, .F. ) ;
#201643=ORIENTED_EDGE ( 'NONE', *, *, #222397, .F. ) ;
#201702=ORIENTED_EDGE ( 'NONE', *, *, #63785, .F. ) ;
#201721=AXIS2_PLACEMENT_3D ( 'NONE', #98888, #57203, #19395 ) ;
#201751=ORIENTED_EDGE ( 'NONE', *, *, #94653, .T. ) ;
#201759=CARTESIAN_POINT ( 'NONE',  ( 20.50589344625199217, 10.48318793148705197, -175.0729949786710051 ) ) ;
#201769=AXIS2_PLACEMENT_3D ( 'NONE', #132888, #169482, #251530 ) ;
#201805=DIRECTION ( 'NONE',  ( 0.000000000000000000, 1.224646799142185182E-16, 1.000000000000000000 ) ) ;
#201806=EDGE_CURVE ( 'NONE', #7200, #250279, #91255, .T. ) ;
#201816=EDGE_LOOP ( 'NONE', ( #74970, #211317, #188773, #42830 ) ) ;
#201827=LINE ( 'NONE', #102698, #193168 ) ;
#201850=ORIENTED_EDGE ( 'NONE', *, *, #108550, .F. ) ;
#201854=DIRECTION ( 'NONE',  ( 0.000000000000000000, 0.000000000000000000, -1.000000000000000000 ) ) ;
#201881=CIRCLE ( 'NONE', #172892, 0.09999999999998898659 ) ;
#201893=CARTESIAN_POINT ( 'NONE',  ( 18.49999999999999645, 5.699452464332751767, -154.9577260434301422 ) ) ;
#201901=FACE_OUTER_BOUND ( 'NONE', #256591, .T. ) ;
#201908=VERTEX_POINT ( 'NONE', #16859 ) ;
#201921=ORIENTED_EDGE ( 'NONE', *, *, #34749, .T. ) ;
#201932=CARTESIAN_POINT ( 'NONE',  ( 18.52326479938690795, -9.642364444904243825, -207.7147574134057493 ) ) ;
#201939=ORIENTED_EDGE ( 'NONE', *, *, #225424, .T. ) ;
#201952=CARTESIAN_POINT ( 'NONE',  ( -21.13435531349817964, 6.493721063603158150, -167.4999999999999716 ) ) ;
#201959=DIRECTION ( 'NONE',  ( -1.000000000000000000, 0.000000000000000000, 0.000000000000000000 ) ) ;
#201964=CARTESIAN_POINT ( 'NONE',  ( -20.94999999999999929, 1.115600667400684642E-11, -196.8999999999999773 ) ) ;
#201968=EDGE_LOOP ( 'NONE', ( #219273, #168047, #47796, #64480 ) ) ;
#202001=VERTEX_POINT ( 'NONE', #66241 ) ;
#202029=CARTESIAN_POINT ( 'NONE',  ( 23.15000000000000213, -12.41227409413852811, -197.8999999999999773 ) ) ;
#202038=ORIENTED_EDGE ( 'NONE', *, *, #12906, .F. ) ;
#202091=AXIS2_PLACEMENT_3D ( 'NONE', #113955, #149262, #94392 ) ;
#202120=EDGE_LOOP ( 'NONE', ( #221580, #245168, #85975, #151514 ) ) ;
#202128=VECTOR ( 'NONE', #115765, 1000.000000000000000 ) ;
#202137=ADVANCED_FACE ( 'NONE', ( #203173 ), #104051, .T. ) ;
#202158=ADVANCED_FACE ( 'NONE', ( #248729 ), #257209, .F. ) ;
#202185=VERTEX_POINT ( 'NONE', #110489 ) ;
#202206=CARTESIAN_POINT ( 'NONE',  ( 18.59999999999999787, -1.851028230129704522, -179.1539132694224463 ) ) ;
#202240=DIRECTION ( 'NONE',  ( 1.000000000000000000, -0.000000000000000000, -0.000000000000000000 ) ) ;
#202258=EDGE_CURVE ( 'NONE', #121293, #73463, #66024, .T. ) ;
#202265=CARTESIAN_POINT ( 'NONE',  ( -20.00857864376270001, 9.150000000011157653, -188.6499999999999488 ) ) ;
#202273=FACE_OUTER_BOUND ( 'NONE', #98199, .T. ) ;
#202281=CARTESIAN_POINT ( 'NONE',  ( 23.14999999999999858, 1.115625160336667635E-11, -198.9999999999999432 ) ) ;
#202285=CARTESIAN_POINT ( 'NONE',  ( 20.94999999999999929, 6.450000000011156587, -177.5170271704400022 ) ) ;
#202287=AXIS2_PLACEMENT_3D ( 'NONE', #125647, #6981, #86490 ) ;
#202307=ORIENTED_EDGE ( 'NONE', *, *, #228617, .F. ) ;
#202322=CARTESIAN_POINT ( 'NONE',  ( -18.59999999999999787, 11.65000000001115232, -188.8499999999999659 ) ) ;
#202350=CARTESIAN_POINT ( 'NONE',  ( 21.05000000000000071, 5.000000000011153745, -188.5947339810868755 ) ) ;
#202407=DIRECTION ( 'NONE',  ( 0.000000000000000000, 0.000000000000000000, -1.000000000000000000 ) ) ;
#202437=DIRECTION ( 'NONE',  ( 0.000000000000000000, -1.000000000000000000, 0.000000000000000000 ) ) ;
#202454=CARTESIAN_POINT ( 'NONE',  ( -18.50000000000000000, -1.362429037182155023, -208.8888812479211765 ) ) ;
#202513=ORIENTED_EDGE ( 'NONE', *, *, #168474, .T. ) ;
#202527=CARTESIAN_POINT ( 'NONE',  ( 20.94999999999999929, -1.835859311432481045, -212.5044391687984842 ) ) ;
#202583=VERTEX_POINT ( 'NONE', #116603 ) ;
#202617=VERTEX_POINT ( 'NONE', #114020 ) ;
#202641=ADVANCED_FACE ( 'NONE', ( #38359 ), #218247, .F. ) ;
#202645=DIRECTION ( 'NONE',  ( -0.000000000000000000, 0.9876197685951276783, 0.1568667991644721316 ) ) ;
#202650=FACE_OUTER_BOUND ( 'NONE', #49116, .T. ) ;
#202659=FACE_OUTER_BOUND ( 'NONE', #159422, .T. ) ;
#202667=CARTESIAN_POINT ( 'NONE',  ( 20.85000000000000142, 1.115600667400684642E-11, -200.9999999999999432 ) ) ;
#202668=EDGE_LOOP ( 'NONE', ( #138656, #178705, #21697, #72568 ) ) ;
#202674=LINE ( 'NONE', #157499, #48895 ) ;
#202678=ORIENTED_EDGE ( 'NONE', *, *, #34749, .F. ) ;
#202681=EDGE_CURVE ( 'NONE', #41100, #145487, #211973, .T. ) ;
#202682=DIRECTION ( 'NONE',  ( 0.000000000000000000, 0.000000000000000000, -1.000000000000000000 ) ) ;
#202712=ADVANCED_FACE ( 'NONE', ( #42213 ), #123033, .T. ) ;
#202719=DIRECTION ( 'NONE',  ( 3.616040088954497272E-32, -1.224646799147352961E-16, 1.000000000000000000 ) ) ;
#202721=CARTESIAN_POINT ( 'NONE',  ( 21.00000000000000000, 9.750000000011153745, -179.7499999999999716 ) ) ;
#202734=CARTESIAN_POINT ( 'NONE',  ( -23.15000000000000213, -9.599999999988845900, -191.1060308773475356 ) ) ;
#202760=VERTEX_POINT ( 'NONE', #181719 ) ;
#202761=LINE ( 'NONE', #679, #85990 ) ;
#202770=CIRCLE ( 'NONE', #61129, 0.09999999999998898659 ) ;
#202773=DIRECTION ( 'NONE',  ( 0.000000000000000000, -0.4930308989874653269, -0.8700118002898649117 ) ) ;
#202785=CIRCLE ( 'NONE', #157023, 7.899999999999990585 ) ;
#202853=DIRECTION ( 'NONE',  ( 1.000000000000000000, 0.000000000000000000, 0.000000000000000000 ) ) ;
#202870=ORIENTED_EDGE ( 'NONE', *, *, #3784, .T. ) ;
#202893=EDGE_CURVE ( 'NONE', #215603, #14186, #228727, .T. ) ;
#202939=CARTESIAN_POINT ( 'NONE',  ( 18.56308993302939925, 10.38069115533503961, -192.2392226389382301 ) ) ;
#202949=AXIS2_PLACEMENT_3D ( 'NONE', #205015, #227167, #26424 ) ;
#202979=ORIENTED_EDGE ( 'NONE', *, *, #198119, .F. ) ;
#202989=CARTESIAN_POINT ( 'NONE',  ( 18.59999999999999076, 10.49142135624846439, -192.2499999999999716 ) ) ;
#203001=CARTESIAN_POINT ( 'NONE',  ( 20.95512820512820440, 8.876151316299273120, -176.0586289951409071 ) ) ;
#203019=VERTEX_POINT ( 'NONE', #73358 ) ;
#203055=AXIS2_PLACEMENT_3D ( 'NONE', #122377, #106630, #2400 ) ;
#203066=FACE_OUTER_BOUND ( 'NONE', #114184, .T. ) ;
#203067=ORIENTED_EDGE ( 'NONE', *, *, #47040, .F. ) ;
#203069=ORIENTED_EDGE ( 'NONE', *, *, #59714, .T. ) ;
#203133=ORIENTED_EDGE ( 'NONE', *, *, #34121, .T. ) ;
#203142=DIRECTION ( 'NONE',  ( -0.000000000000000000, 0.01283462868039629209, -0.9999176327611372095 ) ) ;
#203149=ORIENTED_EDGE ( 'NONE', *, *, #94403, .T. ) ;
#203173=FACE_OUTER_BOUND ( 'NONE', #198654, .T. ) ;
#203185=CIRCLE ( 'NONE', #190755, 2.000000000000001776 ) ;
#203192=EDGE_CURVE ( 'NONE', #242283, #91307, #74809, .T. ) ;
#203223=EDGE_LOOP ( 'NONE', ( #79538, #89302, #190654, #167861 ) ) ;
#203234=AXIS2_PLACEMENT_3D ( 'NONE', #130646, #85068, #45975 ) ;
#203239=( BOUNDED_SURFACE ( )  B_SPLINE_SURFACE ( 3, 2, ( 
 ( #245143, #106896, #66507 ),
 ( #91203, #207314, #186457 ),
 ( #7824, #88605, #129048 ),
 ( #166924, #28707, #147315 ) ),
 .UNSPECIFIED., .F., .F., .F. ) 
 B_SPLINE_SURFACE_WITH_KNOTS ( ( 4, 4 ),
 ( 3, 3 ),
 ( 1.355252715606880543E-20, 0.0003124336117481269631 ),
 ( 0.000000000000000000, 1.000000000000000000 ),
 .UNSPECIFIED. ) 
 GEOMETRIC_REPRESENTATION_ITEM ( )  RATIONAL_B_SPLINE_SURFACE ( (
 ( 1.000000000000000000, 0.7040654476015975050, 1.000000000000000000),
 ( 1.000000000000000000, 0.7039193538781914894, 1.000000000000000000),
 ( 1.000000000000000000, 0.7089171279145413118, 1.000000000000000000),
 ( 1.000000000000000000, 0.7071067811865506814, 1.000000000000000000) ) ) 
 REPRESENTATION_ITEM ( '' )  SURFACE ( )  );
#203241=EDGE_LOOP ( 'NONE', ( #250698, #131756, #119241 ) ) ;
#203262=EDGE_CURVE ( 'NONE', #242287, #429, #24912, .T. ) ;
#203271=LINE ( 'NONE', #126294, #126740 ) ;
#203289=ORIENTED_EDGE ( 'NONE', *, *, #247018, .T. ) ;
#203304=EDGE_CURVE ( 'NONE', #219222, #252182, #204814, .T. ) ;
#203350=CARTESIAN_POINT ( 'NONE',  ( -20.85000000000000142, -1.362429037182151470, -208.8888812479211765 ) ) ;
#203384=FACE_OUTER_BOUND ( 'NONE', #12647, .T. ) ;
#203388=DIRECTION ( 'NONE',  ( 0.000000000000000000, 0.000000000000000000, 1.000000000000000000 ) ) ;
#203396=CARTESIAN_POINT ( 'NONE',  ( 21.04999999999999716, 10.62872031401550466, -179.6499999999999488 ) ) ;
#203403=ADVANCED_FACE ( 'NONE', ( #20447 ), #108097, .F. ) ;
#203410=ORIENTED_EDGE ( 'NONE', *, *, #129078, .F. ) ;
#203431=DIRECTION ( 'NONE',  ( 0.000000000000000000, -1.000000000000000000, 0.000000000000000000 ) ) ;
#203442=AXIS2_PLACEMENT_3D ( 'NONE', #9500, #129461, #51171 ) ;
#203445=EDGE_LOOP ( 'NONE', ( #168761, #51982, #188082, #236496, #27170 ) ) ;
#203448=ORIENTED_EDGE ( 'NONE', *, *, #110922, .F. ) ;
#203449=FACE_OUTER_BOUND ( 'NONE', #171089, .T. ) ;
#203512=CARTESIAN_POINT ( 'NONE',  ( -20.00857864376270001, 9.350000000011156942, -179.7499999999999716 ) ) ;
#203514=ORIENTED_EDGE ( 'NONE', *, *, #109471, .T. ) ;
#203531=ORIENTED_EDGE ( 'NONE', *, *, #49750, .F. ) ;
#203553=CARTESIAN_POINT ( 'NONE',  ( -20.15000000000000568, 9.291421356248463326, -188.6499999999999488 ) ) ;
#203577=ORIENTED_EDGE ( 'NONE', *, *, #14809, .T. ) ;
#203586=ORIENTED_EDGE ( 'NONE', *, *, #171619, .T. ) ;
#203686=CIRCLE ( 'NONE', #107811, 0.2000000000000057288 ) ;
#203700=TOROIDAL_SURFACE ( 'NONE', #174532, 12.77499999999999858, 0.1000000000000000056 ) ;
#203757=CIRCLE ( 'NONE', #137126, 0.5999999999999894307 ) ;
#203795=AXIS2_PLACEMENT_3D ( 'NONE', #130819, #16040, #31758 ) ;
#203835=EDGE_CURVE ( 'NONE', #83655, #208426, #3097, .T. ) ;
#203840=DIRECTION ( 'NONE',  ( 1.000000000000000000, -0.000000000000000000, -0.000000000000000000 ) ) ;
#203853=FACE_OUTER_BOUND ( 'NONE', #60145, .T. ) ;
#203858=ORIENTED_EDGE ( 'NONE', *, *, #184549, .F. ) ;
#203860=ORIENTED_EDGE ( 'NONE', *, *, #161085, .F. ) ;
#203868=( NAMED_UNIT ( * ) SI_UNIT ( $, .STERADIAN. ) SOLID_ANGLE_UNIT ( ) );
#203876=DIRECTION ( 'NONE',  ( 0.000000000000000000, 0.000000000000000000, -1.000000000000000000 ) ) ;
#203935=ADVANCED_FACE ( 'NONE', ( #147780 ), #169949, .F. ) ;
#203952=CARTESIAN_POINT ( 'NONE',  ( 18.54116936837187879, -9.463564198361289925, -174.5485424908883090 ) ) ;
#203953=ORIENTED_EDGE ( 'NONE', *, *, #33022, .T. ) ;
#203998=EDGE_CURVE ( 'NONE', #95676, #234784, #120393, .T. ) ;
#204003=DIRECTION ( 'NONE',  ( -0.000000000000000000, 0.000000000000000000, -1.000000000000000000 ) ) ;
#204018=DIRECTION ( 'NONE',  ( 1.000000000000000000, 0.000000000000000000, 0.000000000000000000 ) ) ;
#204019=ORIENTED_EDGE ( 'NONE', *, *, #251302, .T. ) ;
#204028=EDGE_CURVE ( 'NONE', #127614, #36019, #176341, .T. ) ;
#204029=CIRCLE ( 'NONE', #204214, 0.09999999999998898659 ) ;
#204048=CIRCLE ( 'NONE', #241490, 11.80000000000000426 ) ;
#204050=ORIENTED_EDGE ( 'NONE', *, *, #57283, .F. ) ;
#204067=CARTESIAN_POINT ( 'NONE',  ( 18.59999999999999076, 6.550000000011156231, -188.7499999999999716 ) ) ;
#204068=AXIS2_PLACEMENT_3D ( 'NONE', #44632, #21244, #254937 ) ;
#204075=ORIENTED_EDGE ( 'NONE', *, *, #81200, .T. ) ;
#204103=EDGE_CURVE ( 'NONE', #103641, #194468, #167424, .T. ) ;
#204112=FACE_OUTER_BOUND ( 'NONE', #221446, .T. ) ;
#204170=AXIS2_PLACEMENT_3D ( 'NONE', #112187, #109584, #70508 ) ;
#204173=CIRCLE ( 'NONE', #254244, 0.09999999999998898659 ) ;
#204182=CARTESIAN_POINT ( 'NONE',  ( 20.93284271247462414, 11.75000000001116085, -193.9851942293460354 ) ) ;
#204214=AXIS2_PLACEMENT_3D ( 'NONE', #228451, #68075, #227142 ) ;
#204219=CARTESIAN_POINT ( 'NONE',  ( 18.49999999999999289, 10.34378108836433263, -192.3284452778769662 ) ) ;
#204233=DIRECTION ( 'NONE',  ( 2.952720810173289112E-16, -1.000000000000000000, 0.000000000000000000 ) ) ;
#204242=AXIS2_PLACEMENT_3D ( 'NONE', #245278, #167049, #224407 ) ;
#204246=DIRECTION ( 'NONE',  ( 0.000000000000000000, -1.000000000000000000, 0.000000000000000000 ) ) ;
#204315=AXIS2_PLACEMENT_3D ( 'NONE', #181885, #202719, #65783 ) ;
#204406=EDGE_CURVE ( 'NONE', #163089, #8860, #249722, .T. ) ;
#204407=DIRECTION ( 'NONE',  ( 0.000000000000000000, 3.552713678800413366E-15, -1.000000000000000000 ) ) ;
#204451=VERTEX_POINT ( 'NONE', #95196 ) ;
#204480=CARTESIAN_POINT ( 'NONE',  ( 18.43466021071414218, -9.494190690445382330, -207.6170615601278371 ) ) ;
#204495=CARTESIAN_POINT ( 'NONE',  ( -21.14999999999999858, 6.540656951712399803, -167.4999999999999716 ) ) ;
#204533=VECTOR ( 'NONE', #74501, 1000.000000000000000 ) ;
#204562=ORIENTED_EDGE ( 'NONE', *, *, #220343, .T. ) ;
#204563=CARTESIAN_POINT ( 'NONE',  ( 23.14999999999999858, 5.600000000011153389, -188.5947339810868755 ) ) ;
#204622=VERTEX_POINT ( 'NONE', #40398 ) ;
#204633=DIRECTION ( 'NONE',  ( 1.000000000000000000, 0.000000000000000000, -0.000000000000000000 ) ) ;
#204648=CARTESIAN_POINT ( 'NONE',  ( 23.14999999999999503, 14.05000000001115623, -195.4863049292390542 ) ) ;
#204665=EDGE_LOOP ( 'NONE', ( #169263, #21963, #226396 ) ) ;
#204666=LINE ( 'NONE', #163011, #142010 ) ;
#204685=DIRECTION ( 'NONE',  ( 0.000000000000000000, 1.000000000000000000, 0.000000000000000000 ) ) ;
#204695=VERTEX_POINT ( 'NONE', #179885 ) ;
#204735=( BOUNDED_CURVE ( )  B_SPLINE_CURVE ( 3, ( #126048, #66091, #145614, #102620 ),
 .UNSPECIFIED., .F., .T. ) 
 B_SPLINE_CURVE_WITH_KNOTS ( ( 4, 4 ),
 ( 3.141592653589793116, 4.712388980384689674 ),
 .UNSPECIFIED. ) 
 CURVE ( )  GEOMETRIC_REPRESENTATION_ITEM ( )  RATIONAL_B_SPLINE_CURVE ( ( 1.000000000000000000, 0.8047378541243649375, 0.8047378541243649375, 1.000000000000000000 ) ) 
 REPRESENTATION_ITEM ( '' )  );
#204743=CARTESIAN_POINT ( 'NONE',  ( -21.05000000000000071, 1.115873073196521464E-11, -160.9593430482987344 ) ) ;
#204759=CARTESIAN_POINT ( 'NONE',  ( 21.05000000000000071, -11.64999999998883595, -167.4999999999999716 ) ) ;
#204767=( BOUNDED_SURFACE ( )  B_SPLINE_SURFACE ( 3, 2, ( 
 ( #32097, #71218, #227692 ),
 ( #208161, #49060, #128611 ),
 ( #248547, #150738, #29538 ),
 ( #109025, #9941, #69939 ) ),
 .UNSPECIFIED., .F., .F., .T. ) 
 B_SPLINE_SURFACE_WITH_KNOTS ( ( 4, 4 ),
 ( 3, 3 ),
 ( 0.0006461284895273765793, 0.0007503702773986197947 ),
 ( 0.000000000000000000, 1.000000000000000000 ),
 .UNSPECIFIED. ) 
 GEOMETRIC_REPRESENTATION_ITEM ( )  RATIONAL_B_SPLINE_SURFACE ( (
 ( 1.000000000000000000, 0.7071067811865475727, 1.000000000000000000),
 ( 1.000000000000000000, 0.7076476444649250075, 1.000000000000000000),
 ( 1.000000000000000000, 0.7075727925191404033, 1.000000000000000000),
 ( 1.000000000000000000, 0.7071067811865581199, 1.000000000000000000) ) ) 
 REPRESENTATION_ITEM ( '' )  SURFACE ( )  );
#204775=CARTESIAN_POINT ( 'NONE',  ( -21.09610168723072832, 6.378955715235936630, -167.4664104931084410 ) ) ;
#204777=DIRECTION ( 'NONE',  ( 1.000000000000000000, 0.000000000000000000, 0.000000000000000000 ) ) ;
#204802=CARTESIAN_POINT ( 'NONE',  ( -18.59999999999999787, -9.399999999988787991, -174.7972597596632625 ) ) ;
#204813=ORIENTED_EDGE ( 'NONE', *, *, #168474, .F. ) ;
#204814=LINE ( 'NONE', #108307, #170681 ) ;
#204889=CARTESIAN_POINT ( 'NONE',  ( 21.14999999999999858, 6.650000000011155876, -179.8499999999999943 ) ) ;
#204894=CARTESIAN_POINT ( 'NONE',  ( 21.05000000000000071, 5.000000000011153745, -188.5947339810868755 ) ) ;
#204973=ORIENTED_EDGE ( 'NONE', *, *, #89160, .T. ) ;
#205015=CARTESIAN_POINT ( 'NONE',  ( 22.50000000000000000, 1.115600667400684642E-11, -167.4999999999999716 ) ) ;
#205059=CIRCLE ( 'NONE', #84221, 0.09999999999998898659 ) ;
#205070=DIRECTION ( 'NONE',  ( 0.000000000000000000, -0.01283462868042125823, -0.9999176327611367654 ) ) ;
#205102=CARTESIAN_POINT ( 'NONE',  ( -18.59999999999999787, 1.115600667400684642E-11, -200.9999999999999432 ) ) ;
#205109=CARTESIAN_POINT ( 'NONE',  ( -21.05000000000000071, -11.29603075032412463, -197.9521008403361009 ) ) ;
#205110=CARTESIAN_POINT ( 'NONE',  ( -20.64999999999999858, 2.400000000011155432, -187.7753780772378889 ) ) ;
#205153=CYLINDRICAL_SURFACE ( 'NONE', #88341, 0.09999999999999939493 ) ;
#205159=ORIENTED_EDGE ( 'NONE', *, *, #182007, .F. ) ;
#205163=EDGE_LOOP ( 'NONE', ( #763, #257292, #65485, #200197 ) ) ;
#205175=ADVANCED_FACE ( 'NONE', ( #108687 ), #50845, .T. ) ;
#205193=ORIENTED_EDGE ( 'NONE', *, *, #39770, .F. ) ;
#205219=( LENGTH_UNIT ( ) NAMED_UNIT ( * ) SI_UNIT ( .MILLI., .METRE. ) );
#205283=CARTESIAN_POINT ( 'NONE',  ( -23.25000000000000000, 4.150000000011156764, -188.7499999999999716 ) ) ;
#205292=VERTEX_POINT ( 'NONE', #228941 ) ;
#205298=CARTESIAN_POINT ( 'NONE',  ( 22.50000000000000000, 11.64957080755595520, -167.3999999999999773 ) ) ;
#205349=ADVANCED_FACE ( 'NONE', ( #78821 ), #155838, .T. ) ;
#205371=DIRECTION ( 'NONE',  ( 1.000000000000000000, 0.000000000000000000, 0.000000000000000000 ) ) ;
#205414=ORIENTED_EDGE ( 'NONE', *, *, #171941, .F. ) ;
#205432=DIRECTION ( 'NONE',  ( -0.000000000000000000, -0.000000000000000000, 1.000000000000000000 ) ) ;
#205450=ORIENTED_EDGE ( 'NONE', *, *, #57751, .T. ) ;
#205479=EDGE_LOOP ( 'NONE', ( #37589, #153551, #24125, #137842 ) ) ;
#205519=AXIS2_PLACEMENT_3D ( 'NONE', #226101, #183165, #25385 ) ;
#205555=CARTESIAN_POINT ( 'NONE',  ( 20.85000000000000142, -1.835859311432481045, -212.5044391687984842 ) ) ;
#205567=DIRECTION ( 'NONE',  ( 1.000000000000000000, -0.000000000000000000, -0.000000000000000000 ) ) ;
#205569=TOROIDAL_SURFACE ( 'NONE', #59820, 0.2000000000000000111, 0.1000000000000000056 ) ;
#205575=AXIS2_PLACEMENT_3D ( 'NONE', #185232, #28775, #245215 ) ;
#205595=DIRECTION ( 'NONE',  ( 0.000000000000000000, 0.000000000000000000, 1.000000000000000000 ) ) ;
#205611=AXIS2_PLACEMENT_3D ( 'NONE', #249978, #128757, #13944 ) ;
#205706=EDGE_LOOP ( 'NONE', ( #18428, #178785, #133504, #172741 ) ) ;
#205725=ORIENTED_EDGE ( 'NONE', *, *, #231016, .F. ) ;
#205740=CIRCLE ( 'NONE', #93311, 7.899999999999990585 ) ;
#205770=CARTESIAN_POINT ( 'NONE',  ( 18.59999996954842771, -9.523204137847535833, -207.8830417119165759 ) ) ;
#205781=CARTESIAN_POINT ( 'NONE',  ( -20.54999999999999716, -8.663551401858004652, -177.0241011180672785 ) ) ;
#205788=CARTESIAN_POINT ( 'NONE',  ( -21.09107601085566586, 6.363877975370981765, -167.4606928352826003 ) ) ;
#205856=DIRECTION ( 'NONE',  ( 0.000000000000000000, -2.168404344970946706E-14, -1.000000000000000000 ) ) ;
#205866=DIRECTION ( 'NONE',  ( 0.000000000000000000, 0.000000000000000000, -1.000000000000000000 ) ) ;
#205872=CARTESIAN_POINT ( 'NONE',  ( 22.42196299218230493, 0.002441673998456600492, -155.8503882973504915 ) ) ;
#205876=CIRCLE ( 'NONE', #89167, 4.099999999999992539 ) ;
#205901=EDGE_CURVE ( 'NONE', #88951, #39669, #67765, .T. ) ;
#205902=ORIENTED_EDGE ( 'NONE', *, *, #243834, .T. ) ;
#205904=FACE_OUTER_BOUND ( 'NONE', #139901, .T. ) ;
#205919=ORIENTED_EDGE ( 'NONE', *, *, #9143, .F. ) ;
#205926=EDGE_CURVE ( 'NONE', #81259, #87080, #117649, .T. ) ;
#205967=ORIENTED_EDGE ( 'NONE', *, *, #257792, .F. ) ;
#205977=CARTESIAN_POINT ( 'NONE',  ( -20.85000000000000142, 7.070967871809997973, -204.7465642218682547 ) ) ;
#205985=AXIS2_PLACEMENT_3D ( 'NONE', #73788, #18606, #120315 ) ;
#205989=DIRECTION ( 'NONE',  ( -1.000000000000000000, -1.836970198721029934E-16, -3.186635328391151676E-31 ) ) ;
#205992=VERTEX_POINT ( 'NONE', #23741 ) ;
#205995=CARTESIAN_POINT ( 'NONE',  ( 20.94999999999999574, -11.39257802169451672, -170.5739495798319183 ) ) ;
#206003=ORIENTED_EDGE ( 'NONE', *, *, #152011, .T. ) ;
#206049=ORIENTED_EDGE ( 'NONE', *, *, #240929, .F. ) ;
#206106=DIRECTION ( 'NONE',  ( 0.000000000000000000, -0.000000000000000000, 1.000000000000000000 ) ) ;
#206132=DIRECTION ( 'NONE',  ( -1.000000000000000000, 0.000000000000000000, 0.000000000000000000 ) ) ;
#206158=CARTESIAN_POINT ( 'NONE',  ( 23.14999999999999858, 1.115600667400684642E-11, -200.9999999999999432 ) ) ;
#206171=VECTOR ( 'NONE', #212423, 1000.000000000000000 ) ;
#206174=DIRECTION ( 'NONE',  ( 0.000000000000000000, 0.000000000000000000, -1.000000000000000000 ) ) ;
#206252=DIRECTION ( 'NONE',  ( 0.000000000000000000, 1.000000000000000000, 0.000000000000000000 ) ) ;
#206257=VECTOR ( 'NONE', #50690, 1000.000000000000000 ) ;
#206269=CARTESIAN_POINT ( 'NONE',  ( 21.05000000000000071, 11.65000000001116298, -179.6499999999999773 ) ) ;
#206298=AXIS2_PLACEMENT_3D ( 'NONE', #189653, #252177, #11013 ) ;
#206302=FACE_OUTER_BOUND ( 'NONE', #122562, .T. ) ;
#206345=LINE ( 'NONE', #27740, #51631 ) ;
#206366=VERTEX_POINT ( 'NONE', #85907 ) ;
#206380=ORIENTED_EDGE ( 'NONE', *, *, #176940, .F. ) ;
#206433=DIRECTION ( 'NONE',  ( -0.000000000000000000, 0.8660254037844411501, 0.4999999999999956701 ) ) ;
#206466=DIRECTION ( 'NONE',  ( -0.7071067811865474617, 0.7071067811865474617, 0.000000000000000000 ) ) ;
#206480=LINE ( 'NONE', #27878, #153348 ) ;
#206505=CARTESIAN_POINT ( 'NONE',  ( 21.05000000000000071, -11.39257802169451139, -197.9260504201680249 ) ) ;
#206522=DIRECTION ( 'NONE',  ( 1.000000000000000000, 0.000000000000000000, 0.000000000000000000 ) ) ;
#206537=CARTESIAN_POINT ( 'NONE',  ( -21.00023020733438273, 6.390869245278866018, -167.4999999999999432 ) ) ;
#206543=DIRECTION ( 'NONE',  ( 1.000000000000000000, -0.000000000000000000, -0.000000000000000000 ) ) ;
#206548=CARTESIAN_POINT ( 'NONE',  ( -23.15000000000000213, 2.000000000011154189, -180.2246219227620543 ) ) ;
#206575=DIRECTION ( 'NONE',  ( 0.000000000000000000, 0.8700118002898322711, -0.4930308989875231140 ) ) ;
#206583=CARTESIAN_POINT ( 'NONE',  ( -23.15000000000000213, 1.115600667400684642E-11, -167.4999999999999716 ) ) ;
#206594=EDGE_CURVE ( 'NONE', #163705, #138726, #225445, .T. ) ;
#206618=EDGE_CURVE ( 'NONE', #183886, #140937, #30052, .T. ) ;
#206654=ORIENTED_EDGE ( 'NONE', *, *, #185441, .T. ) ;
#206670=LINE ( 'NONE', #106258, #147971 ) ;
#206672=ORIENTED_EDGE ( 'NONE', *, *, #249621, .T. ) ;
#206674=TOROIDAL_SURFACE ( 'NONE', #244643, 0.2000000000000000111, 0.1000000000000000056 ) ;
#206675=DIRECTION ( 'NONE',  ( -0.000000000000000000, 0.000000000000000000, -1.000000000000000000 ) ) ;
#206705=VECTOR ( 'NONE', #103204, 1000.000000000000000 ) ;
#206728=CARTESIAN_POINT ( 'NONE',  ( 20.97462148592277842, 8.874737576461731337, -179.7546443317309866 ) ) ;
#206729=CARTESIAN_POINT ( 'NONE',  ( -23.15000000000000213, 4.350000000011156054, -179.8499999999999943 ) ) ;
#206735=AXIS2_PLACEMENT_3D ( 'NONE', #54400, #75281, #11447 ) ;
#206751=AXIS2_PLACEMENT_3D ( 'NONE', #220259, #59856, #258036 ) ;
#206759=FACE_OUTER_BOUND ( 'NONE', #155529, .T. ) ;
#206785=ORIENTED_EDGE ( 'NONE', *, *, #225438, .T. ) ;
#206791=CARTESIAN_POINT ( 'NONE',  ( -20.94999999999999929, 10.29288807859936661, -206.4580020160121592 ) ) ;
#206798=CARTESIAN_POINT ( 'NONE',  ( 18.59999999999999076, 10.49142135624846617, -192.2499999999999716 ) ) ;
#206809=CYLINDRICAL_SURFACE ( 'NONE', #159948, 0.09999999999998898659 ) ;
#206829=LINE ( 'NONE', #24363, #122416 ) ;
#206835=EDGE_CURVE ( 'NONE', #130308, #149929, #225622, .T. ) ;
#206858=CARTESIAN_POINT ( 'NONE',  ( 21.05000000000000071, 8.876614585098257848, -175.8850804788446567 ) ) ;
#206864=ADVANCED_FACE ( 'NONE', ( #16080 ), #84119, .T. ) ;
#206951=EDGE_CURVE ( 'NONE', #87151, #20839, #200885, .T. ) ;
#206955=EDGE_CURVE ( 'NONE', #7750, #3198, #159218, .T. ) ;
#206972=CARTESIAN_POINT ( 'NONE',  ( -23.15000000000000213, 1.115650265596050101E-11, -163.4499999999999886 ) ) ;
#206981=VECTOR ( 'NONE', #105650, 999.9999999999998863 ) ;
#206990=AXIS2_PLACEMENT_3D ( 'NONE', #77839, #37461, #175691 ) ;
#207000=TOROIDAL_SURFACE ( 'NONE', #77991, 11.65000000000000036, 0.1000000000000000056 ) ;
#207012=CARTESIAN_POINT ( 'NONE',  ( 23.14999999999999503, 11.65000000001116298, -188.8499999999999659 ) ) ;
#207067=AXIS2_PLACEMENT_3D ( 'NONE', #71766, #131717, #148727 ) ;
#207089=DIRECTION ( 'NONE',  ( -0.000000000000000000, -0.000000000000000000, -1.000000000000000000 ) ) ;
#207142=CIRCLE ( 'NONE', #240446, 0.09999999999998898659 ) ;
#207150=EDGE_CURVE ( 'NONE', #89904, #152124, #213343, .T. ) ;
#207157=LINE ( 'NONE', #168066, #25430 ) ;
#207214=DIRECTION ( 'NONE',  ( 0.000000000000000000, -1.000000000000000000, 0.000000000000000000 ) ) ;
#207229=CARTESIAN_POINT ( 'NONE',  ( 20.94999999999999574, -1.835341550213255957, -179.1551512925629197 ) ) ;
#207240=EDGE_CURVE ( 'NONE', #138184, #183886, #117689, .T. ) ;
#207253=EDGE_CURVE ( 'NONE', #82701, #71184, #42663, .T. ) ;
#207263=AXIS2_PLACEMENT_3D ( 'NONE', #59512, #41301, #161227 ) ;
#207314=CARTESIAN_POINT ( 'NONE',  ( -22.45354308602431814, 2.198887230422068235E-07, -155.7495671095381624 ) ) ;
#207342=CARTESIAN_POINT ( 'NONE',  ( -21.05000000000000071, -0.09999996528895159498, -161.0224478175061904 ) ) ;
#207343=AXIS2_PLACEMENT_3D ( 'NONE', #115006, #257037, #194576 ) ;
#207356=CARTESIAN_POINT ( 'NONE',  ( 19.75857864376268935, 11.65000000001115943, -192.2499999999999716 ) ) ;
#207373=EDGE_CURVE ( 'NONE', #202760, #3198, #125856, .T. ) ;
#207386=FACE_OUTER_BOUND ( 'NONE', #61147, .T. ) ;
#207392=VECTOR ( 'NONE', #241630, 1000.000000000000114 ) ;
#207404=CARTESIAN_POINT ( 'NONE',  ( -18.59999999999999787, 1.115600667400684642E-11, -200.9999999999999432 ) ) ;
#207488=AXIS2_PLACEMENT_3D ( 'NONE', #10853, #149092, #47384 ) ;
#207509=ADVANCED_FACE ( 'NONE', ( #175808 ), #94957, .T. ) ;
#207515=VERTEX_POINT ( 'NONE', #157554 ) ;
#207546=FACE_OUTER_BOUND ( 'NONE', #16154, .T. ) ;
#207554=CIRCLE ( 'NONE', #211644, 11.80000000000000426 ) ;
#207612=ADVANCED_FACE ( 'NONE', ( #234464 ), #87420, .T. ) ;
#207624=VERTEX_POINT ( 'NONE', #163931 ) ;
#207629=CARTESIAN_POINT ( 'NONE',  ( -23.15000000000000213, 1.115600667400684642E-11, -200.9999999999999432 ) ) ;
#207707=AXIS2_PLACEMENT_3D ( 'NONE', #55659, #195243, #136497 ) ;
#207759=CIRCLE ( 'NONE', #166077, 12.97499999999998721 ) ;
#207765=CARTESIAN_POINT ( 'NONE',  ( -23.15000000000000213, 1.115600667400684642E-11, -200.9999999999999432 ) ) ;
#207766=DIRECTION ( 'NONE',  ( 0.000000000000000000, 0.000000000000000000, -1.000000000000000000 ) ) ;
#207775=CARTESIAN_POINT ( 'NONE',  ( -22.39999999999999858, -0.1008583690875579364, -155.7504328765105868 ) ) ;
#207797=DIRECTION ( 'NONE',  ( -0.000000000000000000, 0.1298341882520022694, 0.9915357197604853789 ) ) ;
#207837=CARTESIAN_POINT ( 'NONE',  ( -23.15000000000000213, 1.910280373842930812, -188.3686321448010403 ) ) ;
#207839=CARTESIAN_POINT ( 'NONE',  ( 18.59999999999999076, 10.20857864377385127, -192.2499999999999716 ) ) ;
#207869=CIRCLE ( 'NONE', #141198, 0.09999999999999062417 ) ;
#207886=AXIS2_PLACEMENT_3D ( 'NONE', #135565, #75632, #114739 ) ;
#207892=CARTESIAN_POINT ( 'NONE',  ( -18.54118089899632693, -9.463537631836951292, -174.5485775978680749 ) ) ;
#207896=CARTESIAN_POINT ( 'NONE',  ( -20.64999999999999858, 7.150000000011155876, -179.8499999999999943 ) ) ;
#207993=CARTESIAN_POINT ( 'NONE',  ( 18.59999999999999076, 10.20857864377385127, -188.8499999999999659 ) ) ;
#207999=DIRECTION ( 'NONE',  ( 0.000000000000000000, 0.000000000000000000, 1.000000000000000000 ) ) ;
#208036=FACE_OUTER_BOUND ( 'NONE', #105925, .T. ) ;
#208040=CYLINDRICAL_SURFACE ( 'NONE', #234343, 0.09999999999998898659 ) ;
#208050=DIRECTION ( 'NONE',  ( 0.000000000000000000, 0.000000000000000000, -1.000000000000000000 ) ) ;
#208067=EDGE_CURVE ( 'NONE', #239085, #21068, #55226, .T. ) ;
#208078=CARTESIAN_POINT ( 'NONE',  ( -21.05000000000000071, 1.115600667400684642E-11, -196.8999999999999773 ) ) ;
#208116=DIRECTION ( 'NONE',  ( 0.000000000000000000, 0.000000000000000000, 1.000000000000000000 ) ) ;
#208127=DIRECTION ( 'NONE',  ( 0.000000000000000000, 0.000000000000000000, 1.000000000000000000 ) ) ;
#208131=ORIENTED_EDGE ( 'NONE', *, *, #14498, .F. ) ;
#208137=DIRECTION ( 'NONE',  ( 0.000000000000000000, 0.000000000000000000, 1.000000000000000000 ) ) ;
#208161=CARTESIAN_POINT ( 'NONE',  ( -22.50000000000000000, 11.64987090377452361, -167.4174801091270126 ) ) ;
#208198=CARTESIAN_POINT ( 'NONE',  ( -23.15000000000000213, 11.65000000001115588, -188.8499999999999659 ) ) ;
#208212=ORIENTED_EDGE ( 'NONE', *, *, #78798, .T. ) ;
#208227=( BOUNDED_SURFACE ( )  B_SPLINE_SURFACE ( 3, 2, ( 
 ( #6805, #86310, #165907 ),
 ( #245432, #66784, #233574 ),
 ( #77043, #56185, #133181 ),
 ( #254379, #92752, #156632 ) ),
 .UNSPECIFIED., .F., .F., .F. ) 
 B_SPLINE_SURFACE_WITH_KNOTS ( ( 4, 4 ),
 ( 3, 3 ),
 ( 0.0006461284895273780972, 0.0007503702773985887866 ),
 ( 0.000000000000000000, 1.000000000000000000 ),
 .UNSPECIFIED. ) 
 GEOMETRIC_REPRESENTATION_ITEM ( )  RATIONAL_B_SPLINE_SURFACE ( (
 ( 1.000000000000000000, 0.7071067811865475727, 1.000000000000000000),
 ( 1.000000000000000000, 0.7076476444649502096, 1.000000000000000000),
 ( 1.000000000000000000, 0.7075727925191112044, 1.000000000000000000),
 ( 1.000000000000000000, 0.7071067811865475727, 1.000000000000000000) ) ) 
 REPRESENTATION_ITEM ( '' )  SURFACE ( )  );
#208262=ORIENTED_EDGE ( 'NONE', *, *, #238893, .F. ) ;
#208280=EDGE_CURVE ( 'NONE', #7516, #64282, #131876, .T. ) ;
#208281=CARTESIAN_POINT ( 'NONE',  ( 23.14999999999998437, 1.115600667400684642E-11, -167.4999999999999716 ) ) ;
#208292=CARTESIAN_POINT ( 'NONE',  ( -23.25000000000000000, -11.74999999998884448, -167.4999999999999432 ) ) ;
#208301=CARTESIAN_POINT ( 'NONE',  ( 20.94999999999999574, -1.835341550213255957, -179.0551512925629538 ) ) ;
#208315=CARTESIAN_POINT ( 'NONE',  ( -20.64999999999999858, 7.150000000011155876, -188.6499999999999488 ) ) ;
#208332=DIRECTION ( 'NONE',  ( 1.000000000000000000, 0.000000000000000000, 0.000000000000000000 ) ) ;
#208347=AXIS2_PLACEMENT_3D ( 'NONE', #79311, #158895, #238406 ) ;
#208367=AXIS2_PLACEMENT_3D ( 'NONE', #96027, #196417, #116891 ) ;
#208373=ORIENTED_EDGE ( 'NONE', *, *, #74477, .F. ) ;
#208389=CARTESIAN_POINT ( 'NONE',  ( -23.15000000000000213, -9.599999999988847676, -177.3939691226524076 ) ) ;
#208400=CARTESIAN_POINT ( 'NONE',  ( -23.25000000000000000, -1.851617760457748618, -212.6031897196036198 ) ) ;
#208426=VERTEX_POINT ( 'NONE', #54453 ) ;
#208435=DIRECTION ( 'NONE',  ( 1.000000000000000000, 6.938893903907222067E-15, 0.000000000000000000 ) ) ;
#208491=ORIENTED_EDGE ( 'NONE', *, *, #92891, .F. ) ;
#208496=TOROIDAL_SURFACE ( 'NONE', #150229, 0.2000000000000000111, 0.1000000000000000056 ) ;
#208508=LINE ( 'NONE', #169402, #8369 ) ;
#208521=DIRECTION ( 'NONE',  ( 0.000000000000000000, 0.000000000000000000, 1.000000000000000000 ) ) ;
#208540=DIRECTION ( 'NONE',  ( 0.000000000000000000, 0.4999999999999478195, -0.8660254037844686836 ) ) ;
#208545=AXIS2_PLACEMENT_3D ( 'NONE', #2719, #118851, #220513 ) ;
#208562=ADVANCED_FACE ( 'NONE', ( #870 ), #60864, .T. ) ;
#208563=CARTESIAN_POINT ( 'NONE',  ( -20.64999999999999858, 1.115600667400684642E-11, -200.9999999999999432 ) ) ;
#208609=CARTESIAN_POINT ( 'NONE',  ( 18.49999999999998934, 6.650000000011155876, -179.8499999999999943 ) ) ;
#208622=ADVANCED_FACE ( 'NONE', ( #182115 ), #206809, .T. ) ;
#208631=EDGE_CURVE ( 'NONE', #143070, #182666, #24338, .T. ) ;
#208655=AXIS2_PLACEMENT_3D ( 'NONE', #211722, #35668, #134712 ) ;
#208695=AXIS2_PLACEMENT_3D ( 'NONE', #156368, #241012, #78068 ) ;
#208717=CARTESIAN_POINT ( 'NONE',  ( -21.14999999893415250, 11.75000000001115197, -174.3444953435266598 ) ) ;
#208743=ORIENTED_EDGE ( 'NONE', *, *, #226223, .T. ) ;
#208792=CYLINDRICAL_SURFACE ( 'NONE', #64976, 0.09999999999998898659 ) ;
#208819=CARTESIAN_POINT ( 'NONE',  ( 18.46082813848010673, -9.480749650896242997, -174.5843701027156385 ) ) ;
#208825=VECTOR ( 'NONE', #96262, 1000.000000000000000 ) ;
#208841=AXIS2_PLACEMENT_3D ( 'NONE', #35275, #114773, #95208 ) ;
#208842=VERTEX_POINT ( 'NONE', #92521 ) ;
#208859=LINE ( 'NONE', #90170, #215473 ) ;
#208860=ORIENTED_EDGE ( 'NONE', *, *, #113805, .F. ) ;
#208862=CARTESIAN_POINT ( 'NONE',  ( 18.59999999999999076, 6.450000000011156587, -188.6499999999999488 ) ) ;
#208864=ORIENTED_EDGE ( 'NONE', *, *, #41030, .F. ) ;
#208868=FACE_OUTER_BOUND ( 'NONE', #226765, .T. ) ;
#208878=EDGE_LOOP ( 'NONE', ( #84071, #45619, #14650, #162844 ) ) ;
#208902=VERTEX_POINT ( 'NONE', #218880 ) ;
#208914=ORIENTED_EDGE ( 'NONE', *, *, #93755, .F. ) ;
#208934=ORIENTED_EDGE ( 'NONE', *, *, #37561, .F. ) ;
#208946=DIRECTION ( 'NONE',  ( 0.000000000000000000, -0.3738317757009718689, 0.9274965247785342815 ) ) ;
#208963=VECTOR ( 'NONE', #74575, 1000.000000000000000 ) ;
#209008=ADVANCED_FACE ( 'NONE', ( #45393 ), #143537, .F. ) ;
#209051=EDGE_CURVE ( 'NONE', #133509, #185627, #164403, .T. ) ;
#209053=CARTESIAN_POINT ( 'NONE',  ( -20.85000000000000142, -1.249999999988843369, -208.8004807544150481 ) ) ;
#209069=DIRECTION ( 'NONE',  ( 0.000000000000000000, 0.000000000000000000, 1.000000000000000000 ) ) ;
#209072=CARTESIAN_POINT ( 'NONE',  ( 20.94999999999999929, 11.63687328911501773, -194.1782407866753886 ) ) ;
#209087=DIRECTION ( 'NONE',  ( 0.000000000000000000, 0.000000000000000000, 1.000000000000000000 ) ) ;
#209101=CARTESIAN_POINT ( 'NONE',  ( -22.47071067811865674, 7.720074744509219045, -167.4009075452973434 ) ) ;
#209108=ORIENTED_EDGE ( 'NONE', *, *, #95944, .F. ) ;
#209153=AXIS2_PLACEMENT_3D ( 'NONE', #51068, #113647, #172392 ) ;
#209154=AXIS2_PLACEMENT_3D ( 'NONE', #163391, #29051, #31608 ) ;
#209167=LINE ( 'NONE', #164912, #231565 ) ;
#209185=ADVANCED_FACE ( 'NONE', ( #39982 ), #176881, .T. ) ;
#209186=ORIENTED_EDGE ( 'NONE', *, *, #14294, .T. ) ;
#209211=ORIENTED_EDGE ( 'NONE', *, *, #49664, .F. ) ;
#209212=AXIS2_PLACEMENT_3D ( 'NONE', #53453, #211241, #213806 ) ;
#209235=ORIENTED_EDGE ( 'NONE', *, *, #56358, .F. ) ;
#209238=EDGE_CURVE ( 'NONE', #143070, #135750, #255536, .T. ) ;
#209256=AXIS2_PLACEMENT_3D ( 'NONE', #167149, #125429, #144964 ) ;
#209257=ORIENTED_EDGE ( 'NONE', *, *, #225868, .T. ) ;
#209266=AXIS2_PLACEMENT_3D ( 'NONE', #76736, #139258, #18050 ) ;
#209269=CARTESIAN_POINT ( 'NONE',  ( 20.90851465518105812, 10.32532329027886320, -206.5699343018359002 ) ) ;
#209275=VERTEX_POINT ( 'NONE', #217278 ) ;
#209333=ORIENTED_EDGE ( 'NONE', *, *, #234152, .T. ) ;
#209343=TOROIDAL_SURFACE ( 'NONE', #96880, 12.97499999999999787, 0.1000000000000000056 ) ;
#209349=AXIS2_PLACEMENT_3D ( 'NONE', #141343, #181759, #22708 ) ;
#209382=CARTESIAN_POINT ( 'NONE',  ( 21.11833042828123652, 6.445644693866282360, -167.4928994909405731 ) ) ;
#209383=VECTOR ( 'NONE', #114886, 1000.000000000000000 ) ;
#209416=EDGE_CURVE ( 'NONE', #207624, #205292, #67213, .T. ) ;
#209418=ORIENTED_EDGE ( 'NONE', *, *, #172323, .F. ) ;
#209440=DIRECTION ( 'NONE',  ( 1.000000000000000000, 0.000000000000000000, 0.000000000000000000 ) ) ;
#209442=ORIENTED_EDGE ( 'NONE', *, *, #117042, .F. ) ;
#209447=CARTESIAN_POINT ( 'NONE',  ( -21.05000000000000071, 1.250000000011155299, -175.4999999999999716 ) ) ;
#209460=CARTESIAN_POINT ( 'NONE',  ( -20.64999999999999858, 2.500000000011154633, -187.7753780772378889 ) ) ;
#209467=AXIS2_PLACEMENT_3D ( 'NONE', #24586, #70138, #166672 ) ;
#209469=EDGE_CURVE ( 'NONE', #114401, #176027, #184660, .T. ) ;
#209475=AXIS2_PLACEMENT_3D ( 'NONE', #35316, #54819, #19573 ) ;
#209481=ORIENTED_EDGE ( 'NONE', *, *, #119519, .T. ) ;
#209493=VECTOR ( 'NONE', #176706, 1000.000000000000000 ) ;
#209506=EDGE_CURVE ( 'NONE', #112737, #196929, #216680, .T. ) ;
#209531=EDGE_CURVE ( 'NONE', #207515, #183971, #193066, .T. ) ;
#209575=VERTEX_POINT ( 'NONE', #117582 ) ;
#209583=DIRECTION ( 'NONE',  ( -0.000000000000000000, -1.000000000000000000, 6.308085367188393199E-16 ) ) ;
#209600=DIRECTION ( 'NONE',  ( 0.000000000000000000, -1.265107689135680095E-16, 1.000000000000000000 ) ) ;
#209655=AXIS2_PLACEMENT_3D ( 'NONE', #253471, #176537, #134795 ) ;
#209665=DIRECTION ( 'NONE',  ( -0.000000000000000000, -0.000000000000000000, -1.000000000000000000 ) ) ;
#209669=CARTESIAN_POINT ( 'NONE',  ( -18.54270223418608410, -9.624105502871737272, -207.7409350504073586 ) ) ;
#209678=DIRECTION ( 'NONE',  ( 0.000000000000000000, 1.000000000000000000, -6.308085367188393199E-16 ) ) ;
#209684=DIRECTION ( 'NONE',  ( 0.000000000000000000, 0.000000000000000000, -1.000000000000000000 ) ) ;
#209717=CARTESIAN_POINT ( 'NONE',  ( -18.50000000000000000, 1.835341550235567887, -179.0551512925629538 ) ) ;
#209727=CARTESIAN_POINT ( 'NONE',  ( -18.50000000000000000, 1.115600667400684642E-11, -200.9999999999999432 ) ) ;
#209746=DIRECTION ( 'NONE',  ( 0.000000000000000000, -0.000000000000000000, -1.000000000000000000 ) ) ;
#209765=EDGE_CURVE ( 'NONE', #67305, #20901, #24926, .T. ) ;
#209766=ORIENTED_EDGE ( 'NONE', *, *, #209765, .F. ) ;
#209800=ORIENTED_EDGE ( 'NONE', *, *, #88043, .F. ) ;
#209852=DIRECTION ( 'NONE',  ( 0.000000000000000000, 1.000000000000000000, 0.000000000000000000 ) ) ;
#209860=DIRECTION ( 'NONE',  ( 1.000000000000000000, 0.000000000000000000, 0.000000000000000000 ) ) ;
#209881=VECTOR ( 'NONE', #183461, 1000.000000000000000 ) ;
#209884=ORIENTED_EDGE ( 'NONE', *, *, #88180, .T. ) ;
#209894=EDGE_LOOP ( 'NONE', ( #227518, #46949, #105122, #89612 ) ) ;
#209899=ORIENTED_EDGE ( 'NONE', *, *, #138632, .T. ) ;
#209910=VECTOR ( 'NONE', #202240, 1000.000000000000000 ) ;
#209935=EDGE_LOOP ( 'NONE', ( #85348, #209418, #131749, #75832 ) ) ;
#209946=VERTEX_POINT ( 'NONE', #191715 ) ;
#209969=ORIENTED_EDGE ( 'NONE', *, *, #233973, .T. ) ;
#209975=ORIENTED_EDGE ( 'NONE', *, *, #184151, .F. ) ;
#209976=DIRECTION ( 'NONE',  ( 0.000000000000000000, 1.000000000000000000, 0.000000000000000000 ) ) ;
#210014=AXIS2_PLACEMENT_3D ( 'NONE', #27700, #86313, #66787 ) ;
#210043=CARTESIAN_POINT ( 'NONE',  ( -21.05000000000000071, 1.115600667400684642E-11, -200.9999999999999432 ) ) ;
#210059=CARTESIAN_POINT ( 'NONE',  ( -23.15000000000000213, 1.115600667400684642E-11, -200.9999999999999432 ) ) ;
#210073=DIRECTION ( 'NONE',  ( 0.000000000000000000, 0.000000000000000000, -1.000000000000000000 ) ) ;
#210077=ADVANCED_FACE ( 'NONE', ( #20767 ), #200673, .T. ) ;
#210091=ADVANCED_FACE ( 'NONE', ( #3748 ), #123708, .T. ) ;
#210122=AXIS2_PLACEMENT_3D ( 'NONE', #207012, #28414, #32248 ) ;
#210152=DIRECTION ( 'NONE',  ( 0.000000000000000000, -1.000000000000000000, -0.000000000000000000 ) ) ;
#210159=DIRECTION ( 'NONE',  ( 1.000000000000000000, -7.304098846218135653E-16, -2.111765289898286048E-31 ) ) ;
#210171=AXIS2_PLACEMENT_3D ( 'NONE', #103983, #239680, #41495 ) ;
#210237=ORIENTED_EDGE ( 'NONE', *, *, #29430, .T. ) ;
#210259=ORIENTED_EDGE ( 'NONE', *, *, #42406, .F. ) ;
#210277=ORIENTED_EDGE ( 'NONE', *, *, #13793, .T. ) ;
#210310=EDGE_CURVE ( 'NONE', #215160, #96910, #222603, .T. ) ;
#210313=EDGE_LOOP ( 'NONE', ( #52245, #226972, #235553, #26060 ) ) ;
#210317=CARTESIAN_POINT ( 'NONE',  ( 23.24999999999999289, 11.65000000001116298, -188.8499999999999659 ) ) ;
#210324=DIRECTION ( 'NONE',  ( 1.000000000000000000, -0.000000000000000000, -0.000000000000000000 ) ) ;
#210346=EDGE_CURVE ( 'NONE', #235498, #146255, #1844, .T. ) ;
#210348=SPHERICAL_SURFACE ( 'NONE', #181608, 0.1000000000000000056 ) ;
#210364=FACE_OUTER_BOUND ( 'NONE', #200701, .T. ) ;
#210367=CARTESIAN_POINT ( 'NONE',  ( 21.02374657821588855, 11.60000000083178406, -194.0717967701982616 ) ) ;
#210385=CARTESIAN_POINT ( 'NONE',  ( -23.25000000000000000, -1.835859311432481045, -212.5044391687984842 ) ) ;
#210394=AXIS2_PLACEMENT_3D ( 'NONE', #6092, #247272, #167780 ) ;
#210398=ADVANCED_FACE ( 'NONE', ( #256409 ), #20457, .F. ) ;
#210407=CARTESIAN_POINT ( 'NONE',  ( -21.53699400381685436, 6.787711793192194420, -167.4999999999999432 ) ) ;
#210409=VECTOR ( 'NONE', #245484, 1000.000000000000000 ) ;
#210415=CARTESIAN_POINT ( 'NONE',  ( -20.95000000000000284, 11.65000000001115232, -193.9851942293460070 ) ) ;
#210438=FACE_OUTER_BOUND ( 'NONE', #160767, .T. ) ;
#210449=CARTESIAN_POINT ( 'NONE',  ( -18.59999999999999787, -9.321008403350132809, -174.7359382490778614 ) ) ;
#210472=AXIS2_PLACEMENT_3D ( 'NONE', #122714, #125264, #204777 ) ;
#210536=EDGE_CURVE ( 'NONE', #218583, #168057, #177055, .T. ) ;
#210541=FACE_OUTER_BOUND ( 'NONE', #71855, .T. ) ;
#210587=CARTESIAN_POINT ( 'NONE',  ( -18.59999999999999787, 1.115600667400684642E-11, -200.9999999999999432 ) ) ;
#210597=AXIS2_PLACEMENT_3D ( 'NONE', #139552, #234822, #217798 ) ;
#210603=AXIS2_PLACEMENT_3D ( 'NONE', #160128, #80530, #179680 ) ;
#210605=EDGE_LOOP ( 'NONE', ( #257900, #62379, #224710, #84934 ) ) ;
#210625=CARTESIAN_POINT ( 'NONE',  ( 20.94999999999999574, 1.835341550235567887, -179.0551512925629538 ) ) ;
#210691=DIRECTION ( 'NONE',  ( 0.000000000000000000, 0.000000000000000000, 1.000000000000000000 ) ) ;
#210735=ORIENTED_EDGE ( 'NONE', *, *, #245952, .F. ) ;
#210797=ORIENTED_EDGE ( 'NONE', *, *, #255539, .T. ) ;
#210842=EDGE_LOOP ( 'NONE', ( #200670, #209333, #88368, #818 ) ) ;
#210853=AXIS2_PLACEMENT_3D ( 'NONE', #23664, #180151, #160605 ) ;
#210855=ORIENTED_EDGE ( 'NONE', *, *, #102262, .F. ) ;
#210872=VERTEX_POINT ( 'NONE', #207775 ) ;
#210893=TOROIDAL_SURFACE ( 'NONE', #256623, 12.97499999999999787, 0.1000000000000000056 ) ;
#210907=EDGE_CURVE ( 'NONE', #177021, #121663, #52289, .T. ) ;
#210915=VECTOR ( 'NONE', #207797, 999.9999999999998863 ) ;
#210958=CARTESIAN_POINT ( 'NONE',  ( -18.52328366898032996, -9.642321089030088999, -207.7148193375699918 ) ) ;
#210969=CARTESIAN_POINT ( 'NONE',  ( 21.05000000000000071, -0.09999999998884510910, -161.0229536182100958 ) ) ;
#210979=ORIENTED_EDGE ( 'NONE', *, *, #808, .T. ) ;
#210987=VECTOR ( 'NONE', #193841, 1000.000000000000000 ) ;
#211051=EDGE_CURVE ( 'NONE', #85452, #158852, #63756, .T. ) ;
#211063=ORIENTED_EDGE ( 'NONE', *, *, #189917, .T. ) ;
#211065=ORIENTED_EDGE ( 'NONE', *, *, #89183, .T. ) ;
#211094=CARTESIAN_POINT ( 'NONE',  ( -18.52309608778520911, -9.642476320044041316, -207.7145963411695959 ) ) ;
#211104=ORIENTED_EDGE ( 'NONE', *, *, #72564, .F. ) ;
#211149=DIRECTION ( 'NONE',  ( 1.000000000000000000, 0.000000000000000000, -0.000000000000000000 ) ) ;
#211152=AXIS2_PLACEMENT_3D ( 'NONE', #156750, #154199, #237544 ) ;
#211162=CARTESIAN_POINT ( 'NONE',  ( 21.14999999999999858, 11.75000000001116263, -179.6499999999999773 ) ) ;
#211209=DIRECTION ( 'NONE',  ( 0.000000000000000000, -1.000000000000000000, 0.000000000000000000 ) ) ;
#211212=CARTESIAN_POINT ( 'NONE',  ( -18.44362607810620602, -9.490496158073669974, -174.5579538668471855 ) ) ;
#211219=DIRECTION ( 'NONE',  ( 1.000000000000000000, 0.000000000000000000, 0.000000000000000000 ) ) ;
#211220=CARTESIAN_POINT ( 'NONE',  ( 18.45068634130096186, -9.486506073331606004, -174.5687784311680844 ) ) ;
#211237=FACE_OUTER_BOUND ( 'NONE', #213137, .T. ) ;
#211241=DIRECTION ( 'NONE',  ( -0.000000000000000000, -1.000000000000000000, -0.000000000000000000 ) ) ;
#211254=DIRECTION ( 'NONE',  ( 0.000000000000000000, 0.1568667991644863147, -0.9876197685951252359 ) ) ;
#211264=CARTESIAN_POINT ( 'NONE',  ( -21.05000000000000071, -0.09999999998884338825, -155.8504291924551808 ) ) ;
#211303=SHAPE_DEFINITION_REPRESENTATION ( #88892, #196772 ) ;
#211317=ORIENTED_EDGE ( 'NONE', *, *, #3230, .F. ) ;
#211323=DIRECTION ( 'NONE',  ( -0.4999999999999799050, 0.000000000000000000, -0.8660254037844502539 ) ) ;
#211324=TOROIDAL_SURFACE ( 'NONE', #132206, 7.800000000000000711, 0.1000000000000000056 ) ;
#211334=FACE_OUTER_BOUND ( 'NONE', #128014, .T. ) ;
#211346=CIRCLE ( 'NONE', #202949, 7.791421356237310469 ) ;
#211361=FACE_OUTER_BOUND ( 'NONE', #3802, .T. ) ;
#211368=AXIS2_PLACEMENT_3D ( 'NONE', #166173, #145271, #223520 ) ;
#211441=AXIS2_PLACEMENT_3D ( 'NONE', #164241, #105497, #83372 ) ;
#211455=DIRECTION ( 'NONE',  ( 0.000000000000000000, -0.4930308989874653269, -0.8700118002898649117 ) ) ;
#211456=EDGE_LOOP ( 'NONE', ( #168171, #216640, #120899, #11966 ) ) ;
#211461=DIRECTION ( 'NONE',  ( 0.000000000000000000, 1.000000000000000000, 0.000000000000000000 ) ) ;
#211463=EDGE_LOOP ( 'NONE', ( #74236, #144246, #108361, #177681 ) ) ;
#211478=EDGE_LOOP ( 'NONE', ( #190554, #95701, #208373, #81402, #138456, #150206 ) ) ;
#211493=EDGE_LOOP ( 'NONE', ( #6771, #33931, #137776, #170017 ) ) ;
#211500=ORIENTED_EDGE ( 'NONE', *, *, #239391, .F. ) ;
#211565=EDGE_CURVE ( 'NONE', #185463, #247867, #40057, .T. ) ;
#211568=ORIENTED_EDGE ( 'NONE', *, *, #103401, .F. ) ;
#211585=CARTESIAN_POINT ( 'NONE',  ( -21.52071067811865746, 7.779289321892505882, -188.6499999999999488 ) ) ;
#211605=ORIENTED_EDGE ( 'NONE', *, *, #149528, .F. ) ;
#211614=EDGE_CURVE ( 'NONE', #77719, #163390, #169241, .T. ) ;
#211644=AXIS2_PLACEMENT_3D ( 'NONE', #187048, #189603, #104868 ) ;
#211648=ADVANCED_FACE ( 'NONE', ( #163843 ), #210893, .F. ) ;
#211673=ADVANCED_FACE ( 'NONE', ( #232820 ), #34619, .T. ) ;
#211684=ORIENTED_EDGE ( 'NONE', *, *, #254464, .T. ) ;
#211718=ORIENTED_EDGE ( 'NONE', *, *, #100696, .F. ) ;
#211720=DIRECTION ( 'NONE',  ( -1.000000000000000000, 0.000000000000000000, 0.000000000000000000 ) ) ;
#211722=CARTESIAN_POINT ( 'NONE',  ( 21.00000000000000000, 9.750000000011153745, -188.7499999999999716 ) ) ;
#211810=ORIENTED_EDGE ( 'NONE', *, *, #2473, .F. ) ;
#211863=VECTOR ( 'NONE', #184501, 1000.000000000000000 ) ;
#211887=CIRCLE ( 'NONE', #41020, 0.1000000000000043493 ) ;
#211924=CARTESIAN_POINT ( 'NONE',  ( -18.40000000000000213, -9.519327731081286714, -174.4729763765592736 ) ) ;
#211939=ADVANCED_FACE ( 'NONE', ( #202650 ), #246910, .T. ) ;
#211953=DIRECTION ( 'NONE',  ( 0.000000000000000000, 2.891205793294679805E-16, -1.000000000000000000 ) ) ;
#211973=CIRCLE ( 'NONE', #74445, 12.77500000000000924 ) ;
#211992=ORIENTED_EDGE ( 'NONE', *, *, #257212, .T. ) ;
#211997=ORIENTED_EDGE ( 'NONE', *, *, #190710, .T. ) ;
#212002=ORIENTED_EDGE ( 'NONE', *, *, #57283, .T. ) ;
#212019=DIRECTION ( 'NONE',  ( 0.000000000000000000, -0.000000000000000000, -1.000000000000000000 ) ) ;
#212029=VECTOR ( 'NONE', #12717, 1000.000000000000000 ) ;
#212030=CARTESIAN_POINT ( 'NONE',  ( 20.12500000000000000, 9.750000000011153745, -188.6499999999999488 ) ) ;
#212032=CARTESIAN_POINT ( 'NONE',  ( -20.94999999999999929, 1.736257131608553550, -179.0686523290174819 ) ) ;
#212033=CIRCLE ( 'NONE', #141289, 0.1000000000000002554 ) ;
#212064=EDGE_LOOP ( 'NONE', ( #103344, #61983 ) ) ;
#212084=AXIS2_PLACEMENT_3D ( 'NONE', #62677, #67799, #146043 ) ;
#212087=ORIENTED_EDGE ( 'NONE', *, *, #61729, .T. ) ;
#212133=CARTESIAN_POINT ( 'NONE',  ( 20.94999999999999929, 1.115600667400684642E-11, -200.9999999999999432 ) ) ;
#212160=EDGE_CURVE ( 'NONE', #84620, #5997, #243898, .T. ) ;
#212167=ORIENTED_EDGE ( 'NONE', *, *, #25208, .F. ) ;
#212180=CARTESIAN_POINT ( 'NONE',  ( 21.07016717456945187, 6.320940838111420490, -167.4999999999999432 ) ) ;
#212189=ADVANCED_FACE ( 'NONE', ( #66560 ), #223529, .T. ) ;
#212254=LINE ( 'NONE', #33650, #175859 ) ;
#212281=AXIS2_PLACEMENT_3D ( 'NONE', #78089, #21997, #20718 ) ;
#212324=B_SPLINE_CURVE_WITH_KNOTS ( 'NONE', 3,
 ( #169663, #70546, #150076, #229595, #91372, #170952, #118652, #153956, #93924, #159064 ),
 .UNSPECIFIED., .F., .F.,
 ( 4, 3, 3, 4 ),
 ( 0.000000000000000000, 3.394313611811197040E-05, 6.779740500701634262E-05, 0.0001049857339142623287 ),
 .UNSPECIFIED. ) ;
#212329=CARTESIAN_POINT ( 'NONE',  ( -20.54999999999999716, 2.400000000011155432, -191.1060308773475356 ) ) ;
#212335=EDGE_CURVE ( 'NONE', #31369, #87279, #93691, .T. ) ;
#212392=CARTESIAN_POINT ( 'NONE',  ( -18.33682934331473291, -9.511185591082572444, -207.9056547686734575 ) ) ;
#212399=ORIENTED_EDGE ( 'NONE', *, *, #61779, .T. ) ;
#212423=DIRECTION ( 'NONE',  ( 0.000000000000000000, -0.1350103645451876666, -0.9908441862701600211 ) ) ;
#212435=ORIENTED_EDGE ( 'NONE', *, *, #126774, .F. ) ;
#212466=CARTESIAN_POINT ( 'NONE',  ( -18.59999999999999787, -1.736257131586239844, -179.0686523290174819 ) ) ;
#212480=ORIENTED_EDGE ( 'NONE', *, *, #119070, .F. ) ;
#212488=EDGE_LOOP ( 'NONE', ( #139981, #99207, #85728, #48129, #63097 ) ) ;
#212517=ORIENTED_EDGE ( 'NONE', *, *, #179597, .F. ) ;
#212541=CARTESIAN_POINT ( 'NONE',  ( 20.94999999999999929, -11.64999999998883595, -200.9999999999999432 ) ) ;
#212581=FACE_OUTER_BOUND ( 'NONE', #202668, .T. ) ;
#212589=TOROIDAL_SURFACE ( 'NONE', #62552, 11.65000000000000036, 0.1000000000000000056 ) ;
#212608=DIRECTION ( 'NONE',  ( 0.000000000000000000, 0.000000000000000000, -1.000000000000000000 ) ) ;
#212634=CARTESIAN_POINT ( 'NONE',  ( -20.94999999999999929, 11.65000000001115232, -194.2161343370218560 ) ) ;
#212638=ORIENTED_EDGE ( 'NONE', *, *, #2199, .T. ) ;
#212645=AXIS2_PLACEMENT_3D ( 'NONE', #42878, #141966, #20766 ) ;
#212661=ORIENTED_EDGE ( 'NONE', *, *, #101457, .F. ) ;
#212697=CARTESIAN_POINT ( 'NONE',  ( 23.14999999999999503, 6.450000000011156587, -188.6499999999999488 ) ) ;
#212710=DIRECTION ( 'NONE',  ( 0.000000000000000000, 0.000000000000000000, 1.000000000000000000 ) ) ;
#212728=EDGE_LOOP ( 'NONE', ( #209235, #135032, #200603, #173195 ) ) ;
#212780=EDGE_LOOP ( 'NONE', ( #217219, #119006, #75991, #135237 ) ) ;
#212781=EDGE_LOOP ( 'NONE', ( #224028, #86032, #35955, #105544 ) ) ;
#212822=CARTESIAN_POINT ( 'NONE',  ( 23.25000000000000000, -11.74999999998883560, -197.8999999999999773 ) ) ;
#212849=ORIENTED_EDGE ( 'NONE', *, *, #198556, .T. ) ;
#212865=DIRECTION ( 'NONE',  ( 0.000000000000000000, -0.4791956752371546169, -0.8777080977375152360 ) ) ;
#212869=EDGE_CURVE ( 'NONE', #27613, #143316, #59347, .T. ) ;
#212870=CARTESIAN_POINT ( 'NONE',  ( -21.05000000000000071, -1.249999999988843369, -175.4999999999999716 ) ) ;
#212881=CARTESIAN_POINT ( 'NONE',  ( 21.07946286933444924, 0.07668384326757191061, -161.1709626809922895 ) ) ;
#212895=AXIS2_PLACEMENT_3D ( 'NONE', #29191, #184350, #166126 ) ;
#212916=CIRCLE ( 'NONE', #125607, 0.09999999999999939493 ) ;
#212963=VERTEX_POINT ( 'NONE', #205298 ) ;
#213009=DIRECTION ( 'NONE',  ( 0.000000000000000000, 0.000000000000000000, -1.000000000000000000 ) ) ;
#213071=ORIENTED_EDGE ( 'NONE', *, *, #134287, .T. ) ;
#213086=AXIS2_PLACEMENT_3D ( 'NONE', #197908, #237047, #80499 ) ;
#213116=ORIENTED_EDGE ( 'NONE', *, *, #146156, .F. ) ;
#213137=EDGE_LOOP ( 'NONE', ( #76545, #126823, #147, #118060, #84770 ) ) ;
#213144=DIRECTION ( 'NONE',  ( 1.000000000000000000, 0.000000000000000000, -0.000000000000000000 ) ) ;
#213147=DIRECTION ( 'NONE',  ( 1.000000000000000000, 0.000000000000000000, 0.000000000000000000 ) ) ;
#213159=ORIENTED_EDGE ( 'NONE', *, *, #55422, .F. ) ;
#213163=EDGE_CURVE ( 'NONE', #70620, #220627, #32608, .T. ) ;
#213172=CARTESIAN_POINT ( 'NONE',  ( -18.50000000000000000, -9.499999999988849808, -155.7499999999999716 ) ) ;
#213186=VERTEX_POINT ( 'NONE', #2943 ) ;
#213193=TOROIDAL_SURFACE ( 'NONE', #59222, 11.89999999999999858, 0.1000000000000000056 ) ;
#213199=CARTESIAN_POINT ( 'NONE',  ( -18.47690164073607022, -9.464844538001077723, -207.7013809398360422 ) ) ;
#213210=DIRECTION ( 'NONE',  ( 1.000000000000000000, -0.000000000000000000, -0.000000000000000000 ) ) ;
#213279=CIRCLE ( 'NONE', #188179, 0.4000000000000114575 ) ;
#213294=ADVANCED_FACE ( 'NONE', ( #208868 ), #26391, .T. ) ;
#213316=VERTEX_POINT ( 'NONE', #107185 ) ;
#213323=AXIS2_PLACEMENT_3D ( 'NONE', #158434, #194985, #237931 ) ;
#213330=ORIENTED_EDGE ( 'NONE', *, *, #117733, .F. ) ;
#213343=CIRCLE ( 'NONE', #121794, 12.87499999999999822 ) ;
#213387=ADVANCED_FACE ( 'NONE', ( #91492 ), #124162, .F. ) ;
#213396=DIRECTION ( 'NONE',  ( 0.000000000000000000, -1.000000000000000000, 0.000000000000000000 ) ) ;
#213400=CIRCLE ( 'NONE', #155197, 0.09999999999999939493 ) ;
#213408=CARTESIAN_POINT ( 'NONE',  ( -21.05000000000000071, 1.115600667400684642E-11, -167.4999999999999716 ) ) ;
#213426=CIRCLE ( 'NONE', #230192, 0.09999999999998898659 ) ;
#213434=ORIENTED_EDGE ( 'NONE', *, *, #89183, .F. ) ;
#213458=DIRECTION ( 'NONE',  ( 0.000000000000000000, 0.000000000000000000, -1.000000000000000000 ) ) ;
#213463=CARTESIAN_POINT ( 'NONE',  ( -20.94999999999999929, -1.835341550213255957, -179.0551512925629538 ) ) ;
#213467=EDGE_CURVE ( 'NONE', #93167, #194728, #236730, .T. ) ;
#213482=CYLINDRICAL_SURFACE ( 'NONE', #169505, 0.09999999999999939493 ) ;
#213518=ORIENTED_EDGE ( 'NONE', *, *, #236230, .T. ) ;
#213534=DIRECTION ( 'NONE',  ( 0.000000000000000000, 0.000000000000000000, -1.000000000000000000 ) ) ;
#213561=DIRECTION ( 'NONE',  ( 1.000000000000000000, 0.000000000000000000, 0.000000000000000000 ) ) ;
#213580=CARTESIAN_POINT ( 'NONE',  ( -18.59999999999999787, -1.164121893230052995, -208.9148480855715775 ) ) ;
#213586=ORIENTED_EDGE ( 'NONE', *, *, #181233, .F. ) ;
#213595=CIRCLE ( 'NONE', #1772, 0.2000000000000057288 ) ;
#213614=EDGE_LOOP ( 'NONE', ( #85098, #203586, #70106, #94050 ) ) ;
#213626=DIRECTION ( 'NONE',  ( 0.000000000000000000, 0.000000000000000000, -1.000000000000000000 ) ) ;
#213627=CIRCLE ( 'NONE', #101135, 0.09999999999999892308 ) ;
#213686=DIRECTION ( 'NONE',  ( 1.000000000000000000, 1.836970198721029934E-16, 0.000000000000000000 ) ) ;
#213687=VERTEX_POINT ( 'NONE', #205995 ) ;
#213731=CARTESIAN_POINT ( 'NONE',  ( -23.25000000000000000, 1.115600667400684642E-11, -180.2749999999999773 ) ) ;
#213789=CIRCLE ( 'NONE', #134653, 0.09999999999999860389 ) ;
#213806=DIRECTION ( 'NONE',  ( 0.000000000000000000, 0.000000000000000000, 1.000000000000000000 ) ) ;
#213833=CIRCLE ( 'NONE', #188688, 0.2000000000000057288 ) ;
#213859=LINE ( 'NONE', #193024, #26222 ) ;
#213880=CARTESIAN_POINT ( 'NONE',  ( 23.25000000000000000, -8.999999999988844479, -177.3939691226524076 ) ) ;
#213888=DIRECTION ( 'NONE',  ( 1.000000000000000000, -0.000000000000000000, -0.000000000000000000 ) ) ;
#213934=VERTEX_POINT ( 'NONE', #80230 ) ;
#213950=VERTEX_POINT ( 'NONE', #218475 ) ;
#213959=EDGE_CURVE ( 'NONE', #199601, #64710, #84068, .T. ) ;
#213965=( BOUNDED_SURFACE ( )  B_SPLINE_SURFACE ( 3, 2, ( 
 ( #230851, #88723, #247823 ),
 ( #228271, #49619, #208717 ),
 ( #186582, #165741, #189134 ),
 ( #90019, #169619, #249126 ),
 ( #131726, #70506, #26224 ),
 ( #150028, #245264, #36506 ) ),
 .UNSPECIFIED., .F., .F., .T. ) 
 B_SPLINE_SURFACE_WITH_KNOTS ( ( 4, 2, 4 ),
 ( 3, 3 ),
 ( 1.570796326794895448, 2.356194490192343505, 3.141592653589791784 ),
 ( 0.000000000000000000, 1.000000000000000000 ),
 .UNSPECIFIED. ) 
 GEOMETRIC_REPRESENTATION_ITEM ( )  RATIONAL_B_SPLINE_SURFACE ( (
 ( 1.000000000000000000, 0.7071067811865352493, 1.000000000000000000),
 ( 1.000000000000000000, 0.6611148371775361632, 1.000000000000000000),
 ( 1.000000000000000000, 0.6092287576700777807, 1.000000000000000000),
 ( 1.000000000000000000, 0.5278258667052361242, 1.000000000000000000),
 ( 1.000000000000000000, 0.4993418825340519285, 1.000000000000000000),
 ( 1.000000000000000000, 0.4999999999998459010, 1.000000000000000000) ) ) 
 REPRESENTATION_ITEM ( '' )  SURFACE ( )  );
#213998=CARTESIAN_POINT ( 'NONE',  ( 21.05000000000000071, -8.999999999988844479, -177.3939691226524076 ) ) ;
#214021=AXIS2_PLACEMENT_3D ( 'NONE', #194792, #18694, #136045 ) ;
#214055=EDGE_LOOP ( 'NONE', ( #72227, #99628, #41794, #187353 ) ) ;
#214073=CIRCLE ( 'NONE', #168343, 4.000000000000003553 ) ;
#214086=ADVANCED_FACE ( 'NONE', ( #31884 ), #214347, .T. ) ;
#214109=CARTESIAN_POINT ( 'NONE',  ( 21.14999999999999503, -0.09999999998884338825, -155.8504291924551808 ) ) ;
#214122=ORIENTED_EDGE ( 'NONE', *, *, #186846, .F. ) ;
#214138=CARTESIAN_POINT ( 'NONE',  ( 20.95512820512820440, 10.62384868372303615, -188.7499999999999716 ) ) ;
#214139=DIRECTION ( 'NONE',  ( -1.000000000000000000, 0.000000000000000000, 0.000000000000000000 ) ) ;
#214157=VECTOR ( 'NONE', #239606, 1000.000000000000000 ) ;
#214161=FACE_OUTER_BOUND ( 'NONE', #18320, .T. ) ;
#214172=TOROIDAL_SURFACE ( 'NONE', #101708, 11.65000000000000036, 0.1000000000000000056 ) ;
#214177=FACE_OUTER_BOUND ( 'NONE', #232942, .T. ) ;
#214192=CIRCLE ( 'NONE', #226649, 0.09999999999998898659 ) ;
#214220=DIRECTION ( 'NONE',  ( 0.000000000000000000, 0.000000000000000000, -1.000000000000000000 ) ) ;
#214261=ORIENTED_EDGE ( 'NONE', *, *, #14831, .T. ) ;
#214270=EDGE_CURVE ( 'NONE', #157570, #34375, #218168, .T. ) ;
#214272=AXIS2_PLACEMENT_3D ( 'NONE', #149179, #228713, #12237 ) ;
#214290=DIRECTION ( 'NONE',  ( 0.000000000000000000, -1.000000000000000000, 6.308085367188393199E-16 ) ) ;
#214305=ORIENTED_EDGE ( 'NONE', *, *, #124244, .F. ) ;
#214347=CYLINDRICAL_SURFACE ( 'NONE', #170347, 0.09999999999999939493 ) ;
#214381=ADVANCED_FACE ( 'NONE', ( #43414 ), #64262, .T. ) ;
#214441=ADVANCED_FACE ( 'NONE', ( #70709, #107233 ), #68114, .T. ) ;
#214444=ORIENTED_EDGE ( 'NONE', *, *, #85405, .F. ) ;
#214469=LINE ( 'NONE', #17547, #85917 ) ;
#214473=EDGE_CURVE ( 'NONE', #140937, #56169, #140692, .T. ) ;
#214483=CIRCLE ( 'NONE', #176918, 0.09999999999998898659 ) ;
#214513=ORIENTED_EDGE ( 'NONE', *, *, #87388, .T. ) ;
#214514=ORIENTED_EDGE ( 'NONE', *, *, #177179, .F. ) ;
#214520=DIRECTION ( 'NONE',  ( 0.000000000000000000, 0.000000000000000000, -1.000000000000000000 ) ) ;
#214527=PLANE ( 'NONE',  #123589 ) ;
#214529=VERTEX_POINT ( 'NONE', #185493 ) ;
#214530=CARTESIAN_POINT ( 'NONE',  ( 22.39999999999999858, 7.790779598384538929, -167.3999999999999773 ) ) ;
#214552=EDGE_CURVE ( 'NONE', #117379, #66806, #155386, .T. ) ;
#214635=DIRECTION ( 'NONE',  ( 0.000000000000000000, 0.4999999999999348299, -0.8660254037844762331 ) ) ;
#214688=CIRCLE ( 'NONE', #210603, 0.09999999999998898659 ) ;
#214696=EDGE_CURVE ( 'NONE', #238407, #223496, #149971, .T. ) ;
#214703=ORIENTED_EDGE ( 'NONE', *, *, #124780, .T. ) ;
#214798=DIRECTION ( 'NONE',  ( 0.000000000000000000, 0.000000000000000000, -1.000000000000000000 ) ) ;
#214809=ADVANCED_FACE ( 'NONE', ( #166942 ), #45189, .T. ) ;
#214811=CYLINDRICAL_SURFACE ( 'NONE', #42175, 0.09999999999999939493 ) ;
#214814=FACE_OUTER_BOUND ( 'NONE', #13642, .T. ) ;
#214823=EDGE_LOOP ( 'NONE', ( #122402, #124605, #143226, #139287 ) ) ;
#214861=CARTESIAN_POINT ( 'NONE',  ( 18.39999999999999858, -9.499999999988842703, -207.9146583429696307 ) ) ;
#214863=CARTESIAN_POINT ( 'NONE',  ( 18.55807992284871588, 10.32898536001801659, -206.5826683222763904 ) ) ;
#214884=EDGE_CURVE ( 'NONE', #183886, #82821, #136762, .T. ) ;
#214910=CARTESIAN_POINT ( 'NONE',  ( 20.12518398540832365, 9.975088720679844201, -175.4966682524667192 ) ) ;
#214921=EDGE_LOOP ( 'NONE', ( #211992, #151340, #17378, #134146, #94827, #199513, #158720, #14675, #84085 ) ) ;
#214934=CARTESIAN_POINT ( 'NONE',  ( 18.43709777086140988, -9.682403433465237796, -207.6568433774128266 ) ) ;
#214953=DIRECTION ( 'NONE',  ( 1.000000000000000000, 0.000000000000000000, 0.000000000000000000 ) ) ;
#214965=FACE_OUTER_BOUND ( 'NONE', #201968, .T. ) ;
#214974=ORIENTED_EDGE ( 'NONE', *, *, #188763, .T. ) ;
#214983=VERTEX_POINT ( 'NONE', #72975 ) ;
#215005=ORIENTED_EDGE ( 'NONE', *, *, #72077, .T. ) ;
#215007=EDGE_CURVE ( 'NONE', #51843, #90327, #141069, .T. ) ;
#215011=VERTEX_POINT ( 'NONE', #212466 ) ;
#215041=CARTESIAN_POINT ( 'NONE',  ( -21.05000000000000071, 14.00000000001115374, -195.5729074696174905 ) ) ;
#215128=EDGE_CURVE ( 'NONE', #163089, #225164, #220170, .T. ) ;
#215160=VERTEX_POINT ( 'NONE', #138025 ) ;
#215163=DIRECTION ( 'NONE',  ( 0.000000000000000000, -1.000000000000000000, 0.000000000000000000 ) ) ;
#215175=AXIS2_PLACEMENT_3D ( 'NONE', #70446, #247755, #146077 ) ;
#215184=ADVANCED_FACE ( 'NONE', ( #179753 ), #23266, .T. ) ;
#215185=EDGE_CURVE ( 'NONE', #7750, #213950, #149453, .T. ) ;
#215209=DIRECTION ( 'NONE',  ( -1.000000000000000000, 0.000000000000000000, 0.000000000000000000 ) ) ;
#215213=CARTESIAN_POINT ( 'NONE',  ( 23.15000000000000213, -11.48912529306489994, -197.8999999999999773 ) ) ;
#215218=ORIENTED_EDGE ( 'NONE', *, *, #81387, .T. ) ;
#215251=AXIS2_PLACEMENT_3D ( 'NONE', #145359, #149246, #150517 ) ;
#215265=ORIENTED_EDGE ( 'NONE', *, *, #254472, .F. ) ;
#215271=CARTESIAN_POINT ( 'NONE',  ( 23.14999999999998437, 4.050000000011155343, -167.4999999999999716 ) ) ;
#215294=ORIENTED_EDGE ( 'NONE', *, *, #217489, .F. ) ;
#215315=AXIS2_PLACEMENT_3D ( 'NONE', #64806, #145617, #144319 ) ;
#215316=FACE_OUTER_BOUND ( 'NONE', #229441, .T. ) ;
#215400=ORIENTED_EDGE ( 'NONE', *, *, #93816, .T. ) ;
#215416=LINE ( 'NONE', #195881, #41536 ) ;
#215418=DIRECTION ( 'NONE',  ( -1.000000000000000000, -2.952720810173289112E-16, 0.000000000000000000 ) ) ;
#215420=EDGE_CURVE ( 'NONE', #213316, #21796, #133881, .T. ) ;
#215445=EDGE_CURVE ( 'NONE', #250193, #233212, #93577, .T. ) ;
#215462=CARTESIAN_POINT ( 'NONE',  ( -23.15000000000000213, 4.250000000011156409, -179.8499999999999943 ) ) ;
#215473=VECTOR ( 'NONE', #210152, 1000.000000000000000 ) ;
#215497=AXIS2_PLACEMENT_3D ( 'NONE', #71907, #15802, #193134 ) ;
#215532=ORIENTED_EDGE ( 'NONE', *, *, #153362, .F. ) ;
#215602=AXIS2_PLACEMENT_3D ( 'NONE', #217013, #159629, #134893 ) ;
#215603=VERTEX_POINT ( 'NONE', #119470 ) ;
#215643=EDGE_CURVE ( 'NONE', #96910, #116285, #162760, .T. ) ;
#215644=CIRCLE ( 'NONE', #61543, 0.4000000000000114575 ) ;
#215673=VECTOR ( 'NONE', #115680, 1000.000000000000000 ) ;
#215678=EDGE_CURVE ( 'NONE', #75238, #79726, #125552, .T. ) ;
#215679=DIRECTION ( 'NONE',  ( 1.000000000000000000, 0.000000000000000000, -0.000000000000000000 ) ) ;
#215688=ORIENTED_EDGE ( 'NONE', *, *, #207150, .F. ) ;
#215701=CARTESIAN_POINT ( 'NONE',  ( -18.50000000000000000, -1.637172712959223952, -179.0821533654719815 ) ) ;
#215703=EDGE_CURVE ( 'NONE', #102805, #219709, #158678, .T. ) ;
#215705=VERTEX_POINT ( 'NONE', #249370 ) ;
#215721=ORIENTED_EDGE ( 'NONE', *, *, #247949, .T. ) ;
#215732=CARTESIAN_POINT ( 'NONE',  ( 21.05000000000000071, 5.900000000011162093, -190.7809002353436085 ) ) ;
#215734=CARTESIAN_POINT ( 'NONE',  ( 23.25000000000000000, -11.74999999998883560, -179.6499999999999773 ) ) ;
#215758=AXIS2_PLACEMENT_3D ( 'NONE', #158681, #40019, #161224 ) ;
#215771=CARTESIAN_POINT ( 'NONE',  ( 21.05000000000000071, 10.62872031401550288, -175.1649135690876165 ) ) ;
#215796=CARTESIAN_POINT ( 'NONE',  ( -18.39999999999999858, -9.682403433465239573, -207.6568433774127413 ) ) ;
#215803=ORIENTED_EDGE ( 'NONE', *, *, #46203, .T. ) ;
#215804=VERTEX_POINT ( 'NONE', #70310 ) ;
#215838=VERTEX_POINT ( 'NONE', #50682 ) ;
#215932=EDGE_CURVE ( 'NONE', #95676, #35026, #118454, .T. ) ;
#215943=DIRECTION ( 'NONE',  ( 2.557131231893037478E-16, -0.8660254037844385966, 0.5000000000000003331 ) ) ;
#215956=CIRCLE ( 'NONE', #186980, 0.2000000000000057288 ) ;
#215960=DIRECTION ( 'NONE',  ( 0.000000000000000000, 0.000000000000000000, -1.000000000000000000 ) ) ;
#215973=CARTESIAN_POINT ( 'NONE',  ( 18.59999999999999076, 6.550000000011156231, -188.6499999999999488 ) ) ;
#215979=CARTESIAN_POINT ( 'NONE',  ( 23.15000000000000213, -9.499999999988848032, -177.3939691226524076 ) ) ;
#215985=EDGE_LOOP ( 'NONE', ( #5571, #52746, #183561, #23824 ) ) ;
#215996=CARTESIAN_POINT ( 'NONE',  ( -18.59999999999999787, -1.866714910046153308, -179.2526752462819672 ) ) ;
#216002=CARTESIAN_POINT ( 'NONE',  ( 20.94999999999999929, 4.850467289730776344, -188.9657325909983001 ) ) ;
#216004=VERTEX_POINT ( 'NONE', #35095 ) ;
#216017=DIRECTION ( 'NONE',  ( 0.000000000000000000, -0.9908441862701411473, 0.1350103645453267498 ) ) ;
#216021=CARTESIAN_POINT ( 'NONE',  ( 23.24999999999999289, 6.450000000011156587, -188.6499999999999488 ) ) ;
#216055=CARTESIAN_POINT ( 'NONE',  ( 22.39999999999999503, 0.1000000000111554016, -159.7092204016265669 ) ) ;
#216076=VECTOR ( 'NONE', #39891, 1000.000000000000000 ) ;
#216089=AXIS2_PLACEMENT_3D ( 'NONE', #58883, #154211, #214139 ) ;
#216093=ORIENTED_EDGE ( 'NONE', *, *, #221140, .T. ) ;
#216110=( BOUNDED_SURFACE ( )  B_SPLINE_SURFACE ( 3, 2, ( 
 ( #167984, #247481, #10165 ),
 ( #248779, #38715, #16599 ),
 ( #75295, #120844, #41304 ),
 ( #58251, #137785, #253889 ),
 ( #136496, #217318, #234328 ),
 ( #255127, #157409, #76538 ) ),
 .UNSPECIFIED., .F., .F., .F. ) 
 B_SPLINE_SURFACE_WITH_KNOTS ( ( 4, 2, 4 ),
 ( 3, 3 ),
 ( 0.0001300404313046571046, 0.0003183318589266621477, 0.0005066232865486671637 ),
 ( 0.000000000000000000, 1.000000000000000000 ),
 .UNSPECIFIED. ) 
 GEOMETRIC_REPRESENTATION_ITEM ( )  RATIONAL_B_SPLINE_SURFACE ( (
 ( 1.000000000000000000, 0.7071067811865475727, 1.000000000000000000),
 ( 1.000000000000000000, 0.7625113560541822988, 1.000000000000000000),
 ( 1.000000000000000000, 0.8126073484686407999, 1.000000000000000000),
 ( 1.000000000000000000, 0.8923049332734508399, 1.000000000000000000),
 ( 1.000000000000000000, 0.9231914937768306295, 1.000000000000000000),
 ( 1.000000000000000000, 0.9238795325112714174, 1.000000000000000000) ) ) 
 REPRESENTATION_ITEM ( '' )  SURFACE ( )  );
#216135=CARTESIAN_POINT ( 'NONE',  ( -20.85000000000000142, -1.263275465206102233, -208.9018646667463770 ) ) ;
#216140=CARTESIAN_POINT ( 'NONE',  ( 18.50596464788227280, 10.30632246271648889, -206.5041836778895572 ) ) ;
#216243=EDGE_CURVE ( 'NONE', #50465, #133529, #113683, .T. ) ;
#216247=EDGE_LOOP ( 'NONE', ( #51986, #104405, #256010, #73992 ) ) ;
#216269=DIRECTION ( 'NONE',  ( -0.000000000000000000, -0.000000000000000000, 1.000000000000000000 ) ) ;
#216290=DIRECTION ( 'NONE',  ( 0.000000000000000000, -0.000000000000000000, 1.000000000000000000 ) ) ;
#216298=CARTESIAN_POINT ( 'NONE',  ( 18.59999999999999432, -1.162701749926853712, -175.5999999999999659 ) ) ;
#216306=ORIENTED_EDGE ( 'NONE', *, *, #29838, .T. ) ;
#216308=CARTESIAN_POINT ( 'NONE',  ( -23.25000000000000000, 1.115600667400684642E-11, -200.9999999999999432 ) ) ;
#216325=VECTOR ( 'NONE', #1606, 1000.000000000000000 ) ;
#216341=B_SPLINE_CURVE_WITH_KNOTS ( 'NONE', 3,
 ( #40083, #164818, #243056, #64434, #107398, #185661, #149121, #25324, #65708, #186973, #44868, #119608, #103531, #145232, #184361, #7016 ),
 .UNSPECIFIED., .F., .F.,
 ( 4, 3, 3, 3, 3, 4 ),
 ( 0.000000000000000000, 3.357088238232317244E-05, 6.714213034886757942E-05, 0.0001007408646120921551, 0.0001343627955914185768, 0.0001573956632895995484 ),
 .UNSPECIFIED. ) ;
#216342=DIRECTION ( 'NONE',  ( 0.000000000000000000, -0.000000000000000000, 1.000000000000000000 ) ) ;
#216364=CARTESIAN_POINT ( 'NONE',  ( -20.94999999999999929, 1.115600667400684642E-11, -200.9999999999999432 ) ) ;
#216375=CARTESIAN_POINT ( 'NONE',  ( 22.50927854361889047, -0.1008580735143998902, -155.7504328739730397 ) ) ;
#216390=CARTESIAN_POINT ( 'NONE',  ( -18.59999999999999787, 9.150000000011157653, -179.8499999999999943 ) ) ;
#216394=VECTOR ( 'NONE', #98937, 1000.000000000000114 ) ;
#216397=VECTOR ( 'NONE', #229945, 1000.000000000000000 ) ;
#216418=EDGE_LOOP ( 'NONE', ( #238978, #233112, #21299, #245580 ) ) ;
#216445=DIRECTION ( 'NONE',  ( 0.000000000000000000, 2.891205793294679805E-16, -1.000000000000000000 ) ) ;
#216470=CARTESIAN_POINT ( 'NONE',  ( 20.85000000000000142, -11.64999999998883595, -198.0999999999999659 ) ) ;
#216521=CARTESIAN_POINT ( 'NONE',  ( -21.05000000000000071, 1.835341550235567887, -179.0551512925629538 ) ) ;
#216537=ORIENTED_EDGE ( 'NONE', *, *, #239703, .F. ) ;
#216602=CARTESIAN_POINT ( 'NONE',  ( -18.50000000000000000, 1.115600667400684642E-11, -167.4999999999999716 ) ) ;
#216607=ORIENTED_EDGE ( 'NONE', *, *, #9143, .T. ) ;
#216610=DIRECTION ( 'NONE',  ( 1.000000000000000000, 0.000000000000000000, 0.000000000000000000 ) ) ;
#216621=ORIENTED_EDGE ( 'NONE', *, *, #183604, .T. ) ;
#216626=CARTESIAN_POINT ( 'NONE',  ( -21.05000000000000071, -11.64999999998884483, -170.3999999999999773 ) ) ;
#216627=DIRECTION ( 'NONE',  ( 1.000000000000000000, 2.952720810173289112E-16, -0.000000000000000000 ) ) ;
#216632=CARTESIAN_POINT ( 'NONE',  ( -21.65000000000000213, 7.750000000011155521, -179.8499999999999943 ) ) ;
#216640=ORIENTED_EDGE ( 'NONE', *, *, #39785, .F. ) ;
#216645=CARTESIAN_POINT ( 'NONE',  ( 23.14999999999998437, -4.049999999988842525, -167.4999999999999716 ) ) ;
#216649=DIRECTION ( 'NONE',  ( 1.000000000000000000, 3.265361837132813093E-16, -0.000000000000000000 ) ) ;
#216668=ORIENTED_EDGE ( 'NONE', *, *, #204103, .T. ) ;
#216675=ORIENTED_EDGE ( 'NONE', *, *, #136555, .T. ) ;
#216680=LINE ( 'NONE', #253227, #230659 ) ;
#216684=DIRECTION ( 'NONE',  ( 1.000000000000000000, 3.265361837132813093E-16, -0.000000000000000000 ) ) ;
#216702=EDGE_CURVE ( 'NONE', #83655, #23197, #213833, .T. ) ;
#216713=CARTESIAN_POINT ( 'NONE',  ( -18.51555513499475580, -9.352657054492611977, -174.6951698956958978 ) ) ;
#216714=CARTESIAN_POINT ( 'NONE',  ( -18.50000000000000000, -9.499999999988849808, -175.5999999999999659 ) ) ;
#216728=CARTESIAN_POINT ( 'NONE',  ( -18.59999999999999787, 9.250000000011157297, -179.7499999999999716 ) ) ;
#216767=ORIENTED_EDGE ( 'NONE', *, *, #116594, .T. ) ;
#216801=ORIENTED_EDGE ( 'NONE', *, *, #224204, .F. ) ;
#216813=CARTESIAN_POINT ( 'NONE',  ( 21.97500000000000497, 9.750000000011153745, -179.8499999999999943 ) ) ;
#216825=AXIS2_PLACEMENT_3D ( 'NONE', #74705, #175095, #75949 ) ;
#216870=EDGE_CURVE ( 'NONE', #138993, #105545, #33854, .T. ) ;
#216877=ORIENTED_EDGE ( 'NONE', *, *, #30889, .T. ) ;
#216929=ADVANCED_FACE ( 'NONE', ( #50772 ), #5687, .T. ) ;
#216945=DIRECTION ( 'NONE',  ( 1.000000000000000000, 0.000000000000000000, 0.000000000000000000 ) ) ;
#216965=AXIS2_PLACEMENT_3D ( 'NONE', #248156, #69538, #55063 ) ;
#216967=AXIS2_PLACEMENT_3D ( 'NONE', #64062, #22393, #185300 ) ;
#216969=DIRECTION ( 'NONE',  ( 2.715809747126116508E-16, -1.000000000000000000, 0.000000000000000000 ) ) ;
#216997=CARTESIAN_POINT ( 'NONE',  ( -20.64999999999999858, 7.150000000011155876, -179.7499999999999716 ) ) ;
#217001=AXIS2_PLACEMENT_3D ( 'NONE', #115194, #194757, #70965 ) ;
#217008=EDGE_LOOP ( 'NONE', ( #119517, #50088, #111979, #118143 ) ) ;
#217011=DIRECTION ( 'NONE',  ( 0.000000000000000000, 0.000000000000000000, -1.000000000000000000 ) ) ;
#217013=CARTESIAN_POINT ( 'NONE',  ( -23.15000000000000213, 2.000000000011154189, -180.7246219227620543 ) ) ;
#217018=ORIENTED_EDGE ( 'NONE', *, *, #219388, .F. ) ;
#217057=ORIENTED_EDGE ( 'NONE', *, *, #46189, .T. ) ;
#217077=CARTESIAN_POINT ( 'NONE',  ( 20.95378194480896639, 10.53491199155394220, -175.0650541481478228 ) ) ;
#217109=ORIENTED_EDGE ( 'NONE', *, *, #52470, .T. ) ;
#217142=EDGE_LOOP ( 'NONE', ( #123955, #234283, #191091, #131407 ) ) ;
#217148=DIRECTION ( 'NONE',  ( 0.000000000000000000, 0.000000000000000000, -1.000000000000000000 ) ) ;
#217158=ORIENTED_EDGE ( 'NONE', *, *, #46742, .T. ) ;
#217164=AXIS2_PLACEMENT_3D ( 'NONE', #242515, #62606, #241253 ) ;
#217180=CARTESIAN_POINT ( 'NONE',  ( 18.59999999999999076, 6.650000000011155876, -188.7499999999999716 ) ) ;
#217181=EDGE_CURVE ( 'NONE', #119689, #135869, #172366, .T. ) ;
#217188=VECTOR ( 'NONE', #185013, 1000.000000000000114 ) ;
#217217=FACE_OUTER_BOUND ( 'NONE', #179712, .T. ) ;
#217219=ORIENTED_EDGE ( 'NONE', *, *, #15899, .F. ) ;
#217244=AXIS2_PLACEMENT_3D ( 'NONE', #18772, #215679, #116601 ) ;
#217259=DIRECTION ( 'NONE',  ( 1.000000000000000000, 2.952720810173289112E-16, -0.000000000000000000 ) ) ;
#217278=CARTESIAN_POINT ( 'NONE',  ( 18.59999999999999432, -9.480686695267811714, -207.9411151687578183 ) ) ;
#217296=DIRECTION ( 'NONE',  ( 0.000000000000000000, -0.9654727137038715545, 0.2605042016806676242 ) ) ;
#217318=CARTESIAN_POINT ( 'NONE',  ( 21.05000000000000071, 0.05148288189269902698, -161.1998201820867394 ) ) ;
#217335=AXIS2_PLACEMENT_3D ( 'NONE', #204563, #226687, #246269 ) ;
#217343=EDGE_LOOP ( 'NONE', ( #12496, #181086, #2392, #237685 ) ) ;
#217361=AXIS2_PLACEMENT_3D ( 'NONE', #38888, #197932, #178412 ) ;
#217374=CARTESIAN_POINT ( 'NONE',  ( -23.15000000000000213, 1.115626384983466744E-11, -198.8999999999999773 ) ) ;
#217413=DIRECTION ( 'NONE',  ( 1.734723475976817507E-14, -1.000000000000000000, 0.000000000000000000 ) ) ;
#217427=CYLINDRICAL_SURFACE ( 'NONE', #5940, 0.5000000000000004441 ) ;
#217432=CARTESIAN_POINT ( 'NONE',  ( -20.00857864376270001, 9.150000000011157653, -179.8499999999999943 ) ) ;
#217437=UNCERTAINTY_MEASURE_WITH_UNIT (LENGTH_MEASURE( 1.000000000000000082E-05 ), #43531, 'distance_accuracy_value', 'NONE');
#217438=CARTESIAN_POINT ( 'NONE',  ( -23.15000000000000213, 11.65000000001115588, -188.8499999999999659 ) ) ;
#217442=DIRECTION ( 'NONE',  ( 0.000000000000000000, -1.000000000000000000, -2.891205793294679805E-16 ) ) ;
#217445=AXIS2_PLACEMENT_3D ( 'NONE', #246404, #203431, #44363 ) ;
#217457=CARTESIAN_POINT ( 'NONE',  ( 20.97107704358301916, 8.875478152032441059, -176.0589732293892382 ) ) ;
#217471=DIRECTION ( 'NONE',  ( 1.000000000000000000, 0.000000000000000000, 0.000000000000000000 ) ) ;
#217481=CARTESIAN_POINT ( 'NONE',  ( 18.59999999999999432, -9.480686695267811714, -207.9411151687578183 ) ) ;
#217489=EDGE_CURVE ( 'NONE', #114560, #77502, #76814, .T. ) ;
#217490=DIRECTION ( 'NONE',  ( -1.000000000000000000, 0.000000000000000000, 0.000000000000000000 ) ) ;
#217502=ORIENTED_EDGE ( 'NONE', *, *, #188313, .F. ) ;
#217510=AXIS2_PLACEMENT_3D ( 'NONE', #192685, #34921, #173163 ) ;
#217513=ORIENTED_EDGE ( 'NONE', *, *, #82955, .F. ) ;
#217560=DIRECTION ( 'NONE',  ( 1.000000000000000000, -0.000000000000000000, -0.000000000000000000 ) ) ;
#217561=CARTESIAN_POINT ( 'NONE',  ( -18.59999999999999787, 1.115600667400684642E-11, -200.9999999999999432 ) ) ;
#217565=ORIENTED_EDGE ( 'NONE', *, *, #138949, .T. ) ;
#217582=DIRECTION ( 'NONE',  ( 0.000000000000000000, 0.000000000000000000, -1.000000000000000000 ) ) ;
#217613=DIRECTION ( 'NONE',  ( 0.000000000000000000, 0.000000000000000000, -1.000000000000000000 ) ) ;
#217632=DIRECTION ( 'NONE',  ( 1.000000000000000000, 0.000000000000000000, 0.000000000000000000 ) ) ;
#217662=ADVANCED_FACE ( 'NONE', ( #67183 ), #11061, .T. ) ;
#217703=CARTESIAN_POINT ( 'NONE',  ( -22.50000000000000000, 1.115600667400684642E-11, -167.4999999999999716 ) ) ;
#217755=ADVANCED_FACE ( 'NONE', ( #14928 ), #39644, .T. ) ;
#217777=LINE ( 'NONE', #155296, #251724 ) ;
#217798=DIRECTION ( 'NONE',  ( -1.000000000000000000, 0.000000000000000000, 0.000000000000000000 ) ) ;
#217812=ORIENTED_EDGE ( 'NONE', *, *, #31721, .T. ) ;
#217871=DIRECTION ( 'NONE',  ( 0.000000000000000000, 0.000000000000000000, -1.000000000000000000 ) ) ;
#217878=CARTESIAN_POINT ( 'NONE',  ( -21.05000000000000071, 0.09779029131994597390, -161.2421853895238542 ) ) ;
#217964=FACE_OUTER_BOUND ( 'NONE', #17106, .T. ) ;
#217975=CARTESIAN_POINT ( 'NONE',  ( -18.60000000000000142, -9.321008403350132809, -174.7359382490778614 ) ) ;
#218002=DIRECTION ( 'NONE',  ( -1.000000000000000000, -0.000000000000000000, -0.000000000000000000 ) ) ;
#218004=DIRECTION ( 'NONE',  ( 0.000000000000000000, 0.000000000000000000, 1.000000000000000000 ) ) ;
#218010=ORIENTED_EDGE ( 'NONE', *, *, #197371, .T. ) ;
#218014=DIRECTION ( 'NONE',  ( 1.000000000000000000, 2.952720810173289112E-16, -0.000000000000000000 ) ) ;
#218024=CARTESIAN_POINT ( 'NONE',  ( -22.50000000000000000, 1.115600667400684642E-11, -167.4999999999999716 ) ) ;
#218052=CARTESIAN_POINT ( 'NONE',  ( -22.01447462590972748, 7.263800201241075172, -167.4009629999404183 ) ) ;
#218077=DIRECTION ( 'NONE',  ( -1.000000000000000000, 0.000000000000000000, 0.000000000000000000 ) ) ;
#218080=VERTEX_POINT ( 'NONE', #146390 ) ;
#218081=EDGE_CURVE ( 'NONE', #195524, #251640, #30666, .T. ) ;
#218097=EDGE_LOOP ( 'NONE', ( #127945, #31805, #256811, #90449 ) ) ;
#218100=CARTESIAN_POINT ( 'NONE',  ( 21.14999999999999503, -11.64999999998883595, -170.3999999999999773 ) ) ;
#218131=ORIENTED_EDGE ( 'NONE', *, *, #176572, .T. ) ;
#218141=CARTESIAN_POINT ( 'NONE',  ( -20.54999999999999716, -8.999999999988844479, -191.5060308773475413 ) ) ;
#218143=VECTOR ( 'NONE', #142274, 1000.000000000000000 ) ;
#218168=LINE ( 'NONE', #142495, #199137 ) ;
#218207=FACE_OUTER_BOUND ( 'NONE', #255845, .T. ) ;
#218212=CIRCLE ( 'NONE', #105790, 0.8750000000000007772 ) ;
#218231=EDGE_CURVE ( 'NONE', #169886, #245309, #137133, .T. ) ;
#218247=SPHERICAL_SURFACE ( 'NONE', #95249, 0.1000000000000000056 ) ;
#218254=CARTESIAN_POINT ( 'NONE',  ( -22.49436431346200038, 11.64995094766461392, -167.4330964702777180 ) ) ;
#218263=CARTESIAN_POINT ( 'NONE',  ( 22.60000000000000142, 0.1008583691098682150, -155.7504328765105868 ) ) ;
#218304=EDGE_CURVE ( 'NONE', #159614, #38886, #23636, .T. ) ;
#218317=CARTESIAN_POINT ( 'NONE',  ( 21.33487959338958362, 6.725558151922348848, -167.4999999999999716 ) ) ;
#218321=CARTESIAN_POINT ( 'NONE',  ( 20.94999999999999929, -8.999999999988842703, -191.5060308773475128 ) ) ;
#218333=CARTESIAN_POINT ( 'NONE',  ( 20.95429693346638444, 10.54330487990667820, -175.0608825383128533 ) ) ;
#218344=DIRECTION ( 'NONE',  ( 1.000000000000000000, 0.000000000000000000, 0.000000000000000000 ) ) ;
#218346=AXIS2_PLACEMENT_3D ( 'NONE', #150161, #13210, #129296 ) ;
#218351=ORIENTED_EDGE ( 'NONE', *, *, #88255, .T. ) ;
#218358=CARTESIAN_POINT ( 'NONE',  ( 23.14999999999999858, 1.115600667400684642E-11, -200.9999999999999432 ) ) ;
#218409=AXIS2_PLACEMENT_3D ( 'NONE', #60799, #118224, #197753 ) ;
#218411=( BOUNDED_CURVE ( )  B_SPLINE_CURVE ( 3, ( #156079, #139004, #99883, #179479 ),
 .UNSPECIFIED., .F., .F. ) 
 B_SPLINE_CURVE_WITH_KNOTS ( ( 4, 4 ),
 ( 3.192897208853993529, 4.712388980384689674 ),
 .UNSPECIFIED. ) 
 CURVE ( )  GEOMETRIC_REPRESENTATION_ITEM ( )  RATIONAL_B_SPLINE_CURVE ( ( 1.000000000000000000, 0.8166740347213228279, 0.8166740347213228279, 1.000000000000000000 ) ) 
 REPRESENTATION_ITEM ( '' )  );
#218419=DIRECTION ( 'NONE',  ( 0.7071067811865474617, 0.7071067811865474617, -0.000000000000000000 ) ) ;
#218430=EDGE_CURVE ( 'NONE', #32118, #252758, #168245, .T. ) ;
#218453=CARTESIAN_POINT ( 'NONE',  ( 18.59999999999999076, 10.20857864377385127, -188.8499999999999659 ) ) ;
#218473=DIRECTION ( 'NONE',  ( -3.787827842127535236E-15, 0.7397360091702777085, 0.6728971962616808744 ) ) ;
#218475=CARTESIAN_POINT ( 'NONE',  ( -18.59999999999999787, -9.480686695267820596, -207.9411151687578183 ) ) ;
#218494=DIRECTION ( 'NONE',  ( -0.000000000000000000, 1.000000000000000000, 2.891205793294679805E-16 ) ) ;
#218499=DIRECTION ( 'NONE',  ( 0.000000000000000000, -0.4999999999999478195, -0.8660254037844686836 ) ) ;
#218508=DIRECTION ( 'NONE',  ( 0.000000000000000000, 0.000000000000000000, -1.000000000000000000 ) ) ;
#218522=AXIS2_PLACEMENT_3D ( 'NONE', #99887, #180751, #156083 ) ;
#218537=CIRCLE ( 'NONE', #14589, 0.1000000000000096922 ) ;
#218549=DIRECTION ( 'NONE',  ( 0.000000000000000000, 0.000000000000000000, 1.000000000000000000 ) ) ;
#218583=VERTEX_POINT ( 'NONE', #136465 ) ;
#218608=ORIENTED_EDGE ( 'NONE', *, *, #218926, .F. ) ;
#218631=ORIENTED_EDGE ( 'NONE', *, *, #46203, .F. ) ;
#218639=DIRECTION ( 'NONE',  ( 0.000000000000000000, 1.000000000000000000, 0.000000000000000000 ) ) ;
#218644=ORIENTED_EDGE ( 'NONE', *, *, #216870, .F. ) ;
#218649=ORIENTED_EDGE ( 'NONE', *, *, #187537, .F. ) ;
#218660=ADVANCED_FACE ( 'NONE', ( #224984 ), #101159, .T. ) ;
#218685=DIRECTION ( 'NONE',  ( -1.000000000000000000, 0.000000000000000000, 0.000000000000000000 ) ) ;
#218694=DIRECTION ( 'NONE',  ( 0.000000000000000000, 0.000000000000000000, -1.000000000000000000 ) ) ;
#218696=EDGE_CURVE ( 'NONE', #177630, #231520, #106321, .T. ) ;
#218721=DIRECTION ( 'NONE',  ( 0.000000000000000000, 0.000000000000000000, -1.000000000000000000 ) ) ;
#218759=ORIENTED_EDGE ( 'NONE', *, *, #222397, .T. ) ;
#218782=ORIENTED_EDGE ( 'NONE', *, *, #209506, .T. ) ;
#218785=ORIENTED_EDGE ( 'NONE', *, *, #84544, .F. ) ;
#218795=TOROIDAL_SURFACE ( 'NONE', #6988, 12.97499999999999609, 0.1000000000000000056 ) ;
#218800=DIRECTION ( 'NONE',  ( 1.000000000000000000, 0.000000000000000000, 0.000000000000000000 ) ) ;
#218808=ORIENTED_EDGE ( 'NONE', *, *, #52879, .T. ) ;
#218819=LINE ( 'NONE', #119758, #85865 ) ;
#218851=CARTESIAN_POINT ( 'NONE',  ( -20.64999999999999858, 2.500000000011154633, -187.7753780772378889 ) ) ;
#218868=EDGE_CURVE ( 'NONE', #12339, #190986, #68616, .T. ) ;
#218880=CARTESIAN_POINT ( 'NONE',  ( 23.15000000000000213, -11.74999999998883560, -197.8999999999999773 ) ) ;
#218889=DIRECTION ( 'NONE',  ( 0.000000000000000000, 0.000000000000000000, -1.000000000000000000 ) ) ;
#218926=EDGE_CURVE ( 'NONE', #204622, #151116, #118515, .T. ) ;
#218927=CARTESIAN_POINT ( 'NONE',  ( 18.59999999999999787, 1.851028230152016674, -179.1539132694224463 ) ) ;
#218929=EDGE_CURVE ( 'NONE', #137741, #96910, #200627, .T. ) ;
#218954=DIRECTION ( 'NONE',  ( -1.000000000000000000, -0.000000000000000000, -0.000000000000000000 ) ) ;
#218991=DIRECTION ( 'NONE',  ( 1.000000000000000000, -0.000000000000000000, -0.000000000000000000 ) ) ;
#219038=EDGE_LOOP ( 'NONE', ( #55115, #219281, #114817, #115671 ) ) ;
#219068=DIRECTION ( 'NONE',  ( 1.000000000000000000, -0.000000000000000000, -0.000000000000000000 ) ) ;
#219108=CARTESIAN_POINT ( 'NONE',  ( -22.39999999999999858, 7.790779598384560245, -167.4999999999999716 ) ) ;
#219132=CARTESIAN_POINT ( 'NONE',  ( -23.15000000000000213, 11.75000000001116263, -179.6499999999999773 ) ) ;
#219134=DIRECTION ( 'NONE',  ( 1.000000000000000000, -0.000000000000000000, -0.000000000000000000 ) ) ;
#219159=ORIENTED_EDGE ( 'NONE', *, *, #808, .F. ) ;
#219171=ORIENTED_EDGE ( 'NONE', *, *, #257809, .T. ) ;
#219193=CARTESIAN_POINT ( 'NONE',  ( 20.95512820512820440, 10.62384868372303615, -175.1649135690875880 ) ) ;
#219194=B_SPLINE_CURVE_WITH_KNOTS ( 'NONE', 3,
 ( #219108, #180016, #100430, #103010, #19652, #242533, #82148 ),
 .UNSPECIFIED., .F., .F.,
 ( 4, 3, 4 ),
 ( 0.000000000000000000, 0.0009834301579439998740, 0.001767853679402675614 ),
 .UNSPECIFIED. ) ;
#219216=DIRECTION ( 'NONE',  ( 1.000000000000000000, 0.000000000000000000, 0.000000000000000000 ) ) ;
#219222=VERTEX_POINT ( 'NONE', #44361 ) ;
#219252=CIRCLE ( 'NONE', #65132, 0.09999999999998898659 ) ;
#219256=CARTESIAN_POINT ( 'NONE',  ( -20.85000000000000142, 11.65000000001115232, -200.9999999999999432 ) ) ;
#219273=ORIENTED_EDGE ( 'NONE', *, *, #199185, .T. ) ;
#219277=CARTESIAN_POINT ( 'NONE',  ( -18.51991288638513566, -9.392436789662129470, -174.6432664039591600 ) ) ;
#219281=ORIENTED_EDGE ( 'NONE', *, *, #42730, .T. ) ;
#219284=CARTESIAN_POINT ( 'NONE',  ( -23.15000000000000213, 1.115600667400684642E-11, -200.9999999999999432 ) ) ;
#219297=CIRCLE ( 'NONE', #90105, 0.09999999999998715472 ) ;
#219311=EDGE_CURVE ( 'NONE', #117760, #52759, #201881, .T. ) ;
#219347=EDGE_CURVE ( 'NONE', #135358, #190027, #126447, .T. ) ;
#219364=DIRECTION ( 'NONE',  ( -1.000000000000000000, 0.000000000000000000, 0.000000000000000000 ) ) ;
#219376=CARTESIAN_POINT ( 'NONE',  ( 20.94999999999999929, -8.730841121484166578, -191.4019252810156217 ) ) ;
#219379=CARTESIAN_POINT ( 'NONE',  ( 18.50000000000000000, -9.399999999988823518, -174.7972597596632340 ) ) ;
#219388=EDGE_CURVE ( 'NONE', #255868, #42929, #190292, .T. ) ;
#219416=ORIENTED_EDGE ( 'NONE', *, *, #118507, .T. ) ;
#219432=ORIENTED_EDGE ( 'NONE', *, *, #54123, .T. ) ;
#219461=LINE ( 'NONE', #222019, #18177 ) ;
#219493=ADVANCED_FACE ( 'NONE', ( #129029 ), #131583, .F. ) ;
#219500=CARTESIAN_POINT ( 'NONE',  ( -22.59999999999999787, 0.1008583691098682150, -155.7504328765105868 ) ) ;
#219508=DIRECTION ( 'NONE',  ( -1.000000000000000000, 0.000000000000000000, 0.000000000000000000 ) ) ;
#219523=EDGE_LOOP ( 'NONE', ( #171302, #205725, #245506, #231375 ) ) ;
#219526=AXIS2_PLACEMENT_3D ( 'NONE', #235894, #156410, #134224 ) ;
#219532=EDGE_CURVE ( 'NONE', #103174, #213687, #67601, .T. ) ;
#219546=ADVANCED_FACE ( 'NONE', ( #144562 ), #164152, .F. ) ;
#219569=DIRECTION ( 'NONE',  ( -1.000000000000000000, -2.952720810173289112E-16, 0.000000000000000000 ) ) ;
#219590=DIRECTION ( 'NONE',  ( -1.000000000000000000, 0.000000000000000000, 0.000000000000000000 ) ) ;
#219602=LINE ( 'NONE', #97055, #159518 ) ;
#219623=CARTESIAN_POINT ( 'NONE',  ( 21.05095171578076574, 8.776179878782192745, -179.6658732766378535 ) ) ;
#219627=CARTESIAN_POINT ( 'NONE',  ( -21.55000000000000071, 7.350000000011155166, -179.7499999999999716 ) ) ;
#219676=CYLINDRICAL_SURFACE ( 'NONE', #222034, 0.1000000000000098310 ) ;
#219693=EDGE_CURVE ( 'NONE', #232936, #23864, #251373, .T. ) ;
#219709=VERTEX_POINT ( 'NONE', #12796 ) ;
#219710=FACE_OUTER_BOUND ( 'NONE', #10742, .T. ) ;
#219721=ORIENTED_EDGE ( 'NONE', *, *, #165798, .F. ) ;
#219832=ORIENTED_EDGE ( 'NONE', *, *, #109994, .F. ) ;
#219835=CARTESIAN_POINT ( 'NONE',  ( 21.05000000000000071, 1.360870587203197646, -175.5729979270909382 ) ) ;
#219837=TOROIDAL_SURFACE ( 'NONE', #128285, 0.6000000000000009770, 0.1000000000000000056 ) ;
#219888=AXIS2_PLACEMENT_3D ( 'NONE', #223644, #2030, #81554 ) ;
#219890=VECTOR ( 'NONE', #142606, 1000.000000000000000 ) ;
#219917=CIRCLE ( 'NONE', #157604, 0.09999999999999864553 ) ;
#219925=EDGE_LOOP ( 'NONE', ( #239108, #108306, #127002, #209108, #87085, #45571 ) ) ;
#219942=CIRCLE ( 'NONE', #57614, 0.8750000000000007772 ) ;
#219963=ORIENTED_EDGE ( 'NONE', *, *, #167176, .F. ) ;
#219980=ORIENTED_EDGE ( 'NONE', *, *, #141792, .F. ) ;
#220011=EDGE_CURVE ( 'NONE', #196293, #7452, #56648, .T. ) ;
#220013=ORIENTED_EDGE ( 'NONE', *, *, #87388, .F. ) ;
#220032=DIRECTION ( 'NONE',  ( 1.000000000000000000, 0.000000000000000000, 0.000000000000000000 ) ) ;
#220048=TOROIDAL_SURFACE ( 'NONE', #111918, 11.70000000000000107, 0.1000000000000000056 ) ;
#220049=CARTESIAN_POINT ( 'NONE',  ( 20.44999100639894962, 10.43971070322319683, -175.2590757259704901 ) ) ;
#220070=CARTESIAN_POINT ( 'NONE',  ( -23.15000000000000213, 1.115600667400684642E-11, -200.9999999999999432 ) ) ;
#220110=VERTEX_POINT ( 'NONE', #151683 ) ;
#220113=ADVANCED_FACE ( 'NONE', ( #31737 ), #210348, .T. ) ;
#220129=ORIENTED_EDGE ( 'NONE', *, *, #217489, .T. ) ;
#220135=EDGE_CURVE ( 'NONE', #10380, #63695, #127419, .T. ) ;
#220136=CARTESIAN_POINT ( 'NONE',  ( -21.05000000000000071, -11.48912529306490349, -170.5999999999999659 ) ) ;
#220145=DIRECTION ( 'NONE',  ( -1.000000000000000000, -0.000000000000000000, -0.000000000000000000 ) ) ;
#220170=CIRCLE ( 'NONE', #178695, 0.09999999999999363565 ) ;
#220172=ORIENTED_EDGE ( 'NONE', *, *, #168825, .T. ) ;
#220178=CARTESIAN_POINT ( 'NONE',  ( -18.59999999999999787, -1.149570369564537842, -208.8159124845019221 ) ) ;
#220180=AXIS2_PLACEMENT_3D ( 'NONE', #64946, #224017, #166660 ) ;
#220195=CARTESIAN_POINT ( 'NONE',  ( 23.14999999999999858, 5.000000000011153745, -179.9052660189130677 ) ) ;
#220203=ADVANCED_FACE ( 'NONE', ( #94232 ), #253304, .F. ) ;
#220230=AXIS2_PLACEMENT_3D ( 'NONE', #216632, #174994, #256997 ) ;
#220250=ADVANCED_FACE ( 'NONE', ( #40725 ), #262, .T. ) ;
#220259=CARTESIAN_POINT ( 'NONE',  ( -20.64999999999999858, 4.350000000011156054, -179.7499999999999716 ) ) ;
#220263=EDGE_CURVE ( 'NONE', #107478, #34312, #81076, .T. ) ;
#220285=ORIENTED_EDGE ( 'NONE', *, *, #250256, .F. ) ;
#220329=FACE_OUTER_BOUND ( 'NONE', #43155, .T. ) ;
#220331=LINE ( 'NONE', #58650, #124464 ) ;
#220339=EDGE_LOOP ( 'NONE', ( #234308, #98450, #111148, #132823 ) ) ;
#220343=EDGE_CURVE ( 'NONE', #25429, #58178, #199785, .T. ) ;
#220366=ORIENTED_EDGE ( 'NONE', *, *, #9995, .T. ) ;
#220381=DIRECTION ( 'NONE',  ( 0.000000000000000000, 0.000000000000000000, -1.000000000000000000 ) ) ;
#220384=ORIENTED_EDGE ( 'NONE', *, *, #28063, .F. ) ;
#220390=FACE_OUTER_BOUND ( 'NONE', #235376, .T. ) ;
#220454=VERTEX_POINT ( 'NONE', #54793 ) ;
#220457=VERTEX_POINT ( 'NONE', #131776 ) ;
#220473=CARTESIAN_POINT ( 'NONE',  ( 21.53551880898956838, 6.784797761427480367, -167.4010302654283180 ) ) ;
#220484=CIRCLE ( 'NONE', #112170, 0.2000000000000057288 ) ;
#220486=CARTESIAN_POINT ( 'NONE',  ( -21.05000000000000071, 0.03175835306662712354, -161.2411528769235929 ) ) ;
#220490=CARTESIAN_POINT ( 'NONE',  ( -21.14999999999999858, 11.65000000001115588, -174.2838656629781156 ) ) ;
#220513=DIRECTION ( 'NONE',  ( 0.000000000000000000, 0.000000000000000000, -1.000000000000000000 ) ) ;
#220541=DIRECTION ( 'NONE',  ( -0.000000000000000000, 0.6132151058540549204, -0.7899159663865520375 ) ) ;
#220546=DIRECTION ( 'NONE',  ( -3.265361837132813093E-16, 1.000000000000000000, 0.000000000000000000 ) ) ;
#220563=CARTESIAN_POINT ( 'NONE',  ( 18.50000000000000000, -9.399999999988843058, -207.8820418481726620 ) ) ;
#220565=DIRECTION ( 'NONE',  ( -0.000000000000000000, 0.8660254037844502539, 0.4999999999999799050 ) ) ;
#220589=CARTESIAN_POINT ( 'NONE',  ( 18.59999999999999076, 1.115600667400684642E-11, -200.9999999999999432 ) ) ;
#220611=AXIS2_PLACEMENT_3D ( 'NONE', #162672, #122260, #161399 ) ;
#220627=VERTEX_POINT ( 'NONE', #99041 ) ;
#220657=CARTESIAN_POINT ( 'NONE',  ( -23.15000000000000213, -8.999999999988846255, -177.3939691226524076 ) ) ;
#220665=ORIENTED_EDGE ( 'NONE', *, *, #82955, .T. ) ;
#220741=EDGE_CURVE ( 'NONE', #117253, #184932, #224142, .T. ) ;
#220749=ORIENTED_EDGE ( 'NONE', *, *, #224421, .F. ) ;
#220763=EDGE_CURVE ( 'NONE', #191501, #196430, #115302, .T. ) ;
#220801=CYLINDRICAL_SURFACE ( 'NONE', #82717, 0.1000000000000098310 ) ;
#220824=VECTOR ( 'NONE', #184891, 1000.000000000000000 ) ;
#220834=LINE ( 'NONE', #164730, #64907 ) ;
#220855=ORIENTED_EDGE ( 'NONE', *, *, #134512, .F. ) ;
#220898=CARTESIAN_POINT ( 'NONE',  ( 22.50000000000000000, 0.1000000000111554016, -155.8504291924551808 ) ) ;
#220931=ADVANCED_FACE ( 'NONE', ( #188881 ), #251418, .F. ) ;
#220961=ORIENTED_EDGE ( 'NONE', *, *, #177110, .T. ) ;
#220965=CIRCLE ( 'NONE', #4297, 11.75000000000000000 ) ;
#221029=DIRECTION ( 'NONE',  ( 0.7071067811865388020, -0.7071067811865561215, 0.000000000000000000 ) ) ;
#221039=VERTEX_POINT ( 'NONE', #178327 ) ;
#221061=DIRECTION ( 'NONE',  ( 0.000000000000000000, 0.000000000000000000, -1.000000000000000000 ) ) ;
#221082=CARTESIAN_POINT ( 'NONE',  ( -21.05000000000000071, -1.835341550213255957, -179.0551512925629538 ) ) ;
#221095=DIRECTION ( 'NONE',  ( 1.000000000000000000, 3.265361837132813093E-16, -0.000000000000000000 ) ) ;
#221129=DIRECTION ( 'NONE',  ( 1.000000000000000000, 0.000000000000000000, 0.000000000000000000 ) ) ;
#221130=ORIENTED_EDGE ( 'NONE', *, *, #39785, .T. ) ;
#221140=EDGE_CURVE ( 'NONE', #162728, #199385, #57705, .T. ) ;
#221195=ORIENTED_EDGE ( 'NONE', *, *, #42703, .T. ) ;
#221244=CARTESIAN_POINT ( 'NONE',  ( 18.59999999999999076, 10.20857864377385127, -188.7499999999999716 ) ) ;
#221307=CARTESIAN_POINT ( 'NONE',  ( 20.41140022480670879, 10.41043084241175087, -175.1150013036360349 ) ) ;
#221325=AXIS2_PLACEMENT_3D ( 'NONE', #123073, #22706, #40986 ) ;
#221369=CYLINDRICAL_SURFACE ( 'NONE', #56012, 0.09999999999998898659 ) ;
#221382=ORIENTED_EDGE ( 'NONE', *, *, #176846, .F. ) ;
#221401=CARTESIAN_POINT ( 'NONE',  ( 18.39999999999999858, -9.599999999988845900, -207.6001893912220169 ) ) ;
#221415=DIRECTION ( 'NONE',  ( 0.000000000000000000, 0.000000000000000000, -1.000000000000000000 ) ) ;
#221424=ORIENTED_EDGE ( 'NONE', *, *, #37561, .T. ) ;
#221433=DIRECTION ( 'NONE',  ( 2.659396599871503635E-15, 0.6132151058540549204, -0.7899159663865520375 ) ) ;
#221446=EDGE_LOOP ( 'NONE', ( #101502, #200752, #211718, #156086 ) ) ;
#221449=CARTESIAN_POINT ( 'NONE',  ( -20.54999999999999716, 2.000000000011154189, -180.2246219227620543 ) ) ;
#221458=CARTESIAN_POINT ( 'NONE',  ( 18.59999999999999787, -1.362429037182151470, -208.8888812479211765 ) ) ;
#221478=FACE_OUTER_BOUND ( 'NONE', #252444, .T. ) ;
#221481=FACE_OUTER_BOUND ( 'NONE', #196271, .T. ) ;
#221526=DIRECTION ( 'NONE',  ( -1.000000000000000000, 0.000000000000000000, 0.000000000000000000 ) ) ;
#221532=CARTESIAN_POINT ( 'NONE',  ( 21.30000000000002558, 1.115600667400684642E-11, -167.4999999999999716 ) ) ;
#221547=ADVANCED_FACE ( 'NONE', ( #201400 ), #104834, .T. ) ;
#221580=ORIENTED_EDGE ( 'NONE', *, *, #164931, .F. ) ;
#221603=VECTOR ( 'NONE', #110928, 1000.000000000000000 ) ;
#221612=ORIENTED_EDGE ( 'NONE', *, *, #38695, .T. ) ;
#221627=CARTESIAN_POINT ( 'NONE',  ( -18.50000000000000000, 11.65000000001115232, -174.5148057706539930 ) ) ;
#221646=CARTESIAN_POINT ( 'NONE',  ( 20.95512840106819752, 10.62384869378447583, -179.7024792207988071 ) ) ;
#221651=CARTESIAN_POINT ( 'NONE',  ( -23.25000000000000000, 2.000000000011154189, -187.7753780772378889 ) ) ;
#221674=VERTEX_POINT ( 'NONE', #206548 ) ;
#221684=CYLINDRICAL_SURFACE ( 'NONE', #143333, 11.80000000000000426 ) ;
#221697=ORIENTED_EDGE ( 'NONE', *, *, #110503, .T. ) ;
#221754=ORIENTED_EDGE ( 'NONE', *, *, #16367, .T. ) ;
#221760=CARTESIAN_POINT ( 'NONE',  ( 20.94999999999999929, 1.115600667400684642E-11, -200.9999999999999432 ) ) ;
#221837=DIRECTION ( 'NONE',  ( -3.265361837132813093E-16, 1.000000000000000000, 0.000000000000000000 ) ) ;
#221893=AXIS2_PLACEMENT_3D ( 'NONE', #1861, #99672, #137527 ) ;
#221897=AXIS2_PLACEMENT_3D ( 'NONE', #117104, #173277, #213626 ) ;
#221921=AXIS2_PLACEMENT_3D ( 'NONE', #256379, #140333, #216017 ) ;
#221929=CIRCLE ( 'NONE', #209475, 0.09999999999999939493 ) ;
#221930=CARTESIAN_POINT ( 'NONE',  ( 18.58703555225034165, -9.406336740777783589, -174.6249446412465716 ) ) ;
#221940=EDGE_CURVE ( 'NONE', #177487, #22985, #219917, .T. ) ;
#221969=ADVANCED_FACE ( 'NONE', ( #104225 ), #115870, .F. ) ;
#221973=ORIENTED_EDGE ( 'NONE', *, *, #76952, .F. ) ;
#221980=AXIS2_PLACEMENT_3D ( 'NONE', #25705, #90795, #6119 ) ;
#221986=CIRCLE ( 'NONE', #142881, 1.900000000000012790 ) ;
#221999=EDGE_LOOP ( 'NONE', ( #206654, #119605, #252238, #29590 ) ) ;
#222002=DIRECTION ( 'NONE',  ( 1.000000000000000000, -0.000000000000000000, -0.000000000000000000 ) ) ;
#222019=CARTESIAN_POINT ( 'NONE',  ( -18.50000000000000000, -26.43935341558978891, -185.6415086075074328 ) ) ;
#222023=ORIENTED_EDGE ( 'NONE', *, *, #19743, .T. ) ;
#222032=ORIENTED_EDGE ( 'NONE', *, *, #251492, .F. ) ;
#222034=AXIS2_PLACEMENT_3D ( 'NONE', #41078, #134988, #44912 ) ;
#222048=CARTESIAN_POINT ( 'NONE',  ( -22.39999999999999858, -0.1008583690875579364, -155.7504328765105868 ) ) ;
#222061=EDGE_CURVE ( 'NONE', #6622, #70888, #92373, .T. ) ;
#222112=CARTESIAN_POINT ( 'NONE',  ( 20.94999999999999574, 6.550000000011159784, -177.3438220896831012 ) ) ;
#222138=DIRECTION ( 'NONE',  ( 0.000000000000000000, 0.000000000000000000, 1.000000000000000000 ) ) ;
#222161=CARTESIAN_POINT ( 'NONE',  ( 23.14999999999999858, 1.115600667400684642E-11, -200.9999999999999432 ) ) ;
#222210=CARTESIAN_POINT ( 'NONE',  ( 20.95568717954149562, 10.60199405390297400, -175.1025083682686159 ) ) ;
#222240=VECTOR ( 'NONE', #183315, 1000.000000000000000 ) ;
#222253=AXIS2_PLACEMENT_3D ( 'NONE', #135436, #74232, #152475 ) ;
#222273=DIRECTION ( 'NONE',  ( 1.000000000000000000, 0.000000000000000000, 0.000000000000000000 ) ) ;
#222283=ORIENTED_EDGE ( 'NONE', *, *, #84670, .T. ) ;
#222286=ORIENTED_EDGE ( 'NONE', *, *, #4302, .T. ) ;
#222295=VERTEX_POINT ( 'NONE', #16712 ) ;
#222309=AXIS2_PLACEMENT_3D ( 'NONE', #109223, #49257, #15292 ) ;
#222352=EDGE_CURVE ( 'NONE', #257429, #4495, #45312, .T. ) ;
#222370=VECTOR ( 'NONE', #158301, 1000.000000000000000 ) ;
#222386=CARTESIAN_POINT ( 'NONE',  ( -23.15000000000000213, 4.250000000011156409, -188.7499999999999716 ) ) ;
#222389=CARTESIAN_POINT ( 'NONE',  ( -23.15000000000000213, 11.65000000001115588, -179.7499999999999716 ) ) ;
#222397=EDGE_CURVE ( 'NONE', #224848, #96608, #128523, .T. ) ;
#222407=CARTESIAN_POINT ( 'NONE',  ( -20.15000000000000568, 9.291421356248463326, -179.7499999999999716 ) ) ;
#222438=DIRECTION ( 'NONE',  ( -0.000000000000000000, 1.000000000000000000, -0.000000000000000000 ) ) ;
#222453=DIRECTION ( 'NONE',  ( 0.000000000000000000, 0.000000000000000000, -1.000000000000000000 ) ) ;
#222492=DIRECTION ( 'NONE',  ( 1.000000000000000000, 0.000000000000000000, 0.000000000000000000 ) ) ;
#222513=AXIS2_PLACEMENT_3D ( 'NONE', #72388, #112782, #189747 ) ;
#222522=CARTESIAN_POINT ( 'NONE',  ( 23.14999999999998437, 1.115600667400684642E-11, -167.4999999999999716 ) ) ;
#222527=ORIENTED_EDGE ( 'NONE', *, *, #136757, .F. ) ;
#222535=CARTESIAN_POINT ( 'NONE',  ( 18.49999999999998934, 19.85039924724470950, -169.7803030578013477 ) ) ;
#222545=DIRECTION ( 'NONE',  ( 0.000000000000000000, 4.510281037540195239E-13, 1.000000000000000000 ) ) ;
#222565=CARTESIAN_POINT ( 'NONE',  ( -23.25000000000000000, -11.64999999998884483, -197.9999999999999432 ) ) ;
#222567=ORIENTED_EDGE ( 'NONE', *, *, #24385, .T. ) ;
#222571=PRODUCT_DEFINITION_CONTEXT ( 'detailed design', #42461, 'design' ) ;
#222584=ORIENTED_EDGE ( 'NONE', *, *, #109214, .F. ) ;
#222586=CARTESIAN_POINT ( 'NONE',  ( 20.97250901189795513, 10.62456803371303593, -175.1645457169669555 ) ) ;
#222595=ORIENTED_EDGE ( 'NONE', *, *, #24379, .F. ) ;
#222603=CIRCLE ( 'NONE', #193437, 0.09999999999999230338 ) ;
#222629=ORIENTED_EDGE ( 'NONE', *, *, #2199, .F. ) ;
#222656=DIRECTION ( 'NONE',  ( -0.000000000000000000, -1.000000000000000000, 6.308085367188393199E-16 ) ) ;
#222693=ORIENTED_EDGE ( 'NONE', *, *, #64657, .F. ) ;
#222714=ORIENTED_EDGE ( 'NONE', *, *, #153945, .F. ) ;
#222716=ORIENTED_EDGE ( 'NONE', *, *, #233309, .F. ) ;
#222731=CARTESIAN_POINT ( 'NONE',  ( -2.995603634470891112E-16, 6.650000000011155876, -188.7499999999999716 ) ) ;
#222758=CARTESIAN_POINT ( 'NONE',  ( 18.48197441911631955, -9.517954794695798526, -207.8902116422065092 ) ) ;
#222773=CARTESIAN_POINT ( 'NONE',  ( -21.04999999999676774, 6.497017786442108367, -167.5145456905664219 ) ) ;
#222781=ADVANCED_FACE ( 'NONE', ( #236701 ), #115666, .T. ) ;
#222795=DIRECTION ( 'NONE',  ( 0.000000000000000000, 0.000000000000000000, -1.000000000000000000 ) ) ;
#222806=CIRCLE ( 'NONE', #101986, 0.1000000000000001860 ) ;
#222817=VERTEX_POINT ( 'NONE', #166211 ) ;
#222842=CIRCLE ( 'NONE', #39721, 0.09999999999999939493 ) ;
#222868=DIRECTION ( 'NONE',  ( 1.000000000000000000, 0.000000000000000000, -0.000000000000000000 ) ) ;
#222875=LINE ( 'NONE', #117371, #116084 ) ;
#222882=CIRCLE ( 'NONE', #35487, 0.09999999999999178990 ) ;
#222925=ORIENTED_EDGE ( 'NONE', *, *, #66364, .T. ) ;
#222927=AXIS2_PLACEMENT_3D ( 'NONE', #121134, #216342, #200642 ) ;
#222943=DIRECTION ( 'NONE',  ( 1.000000000000000000, 0.000000000000000000, -0.000000000000000000 ) ) ;
#222952=EDGE_LOOP ( 'NONE', ( #9730, #155783, #181207, #134407, #84437, #125124, #108799 ) ) ;
#222958=ORIENTED_EDGE ( 'NONE', *, *, #5488, .F. ) ;
#223009=DIRECTION ( 'NONE',  ( 0.000000000000000000, 0.000000000000000000, -1.000000000000000000 ) ) ;
#223039=ADVANCED_FACE ( 'NONE', ( #16115 ), #116479, .F. ) ;
#223047=ORIENTED_EDGE ( 'NONE', *, *, #152746, .T. ) ;
#223059=ORIENTED_EDGE ( 'NONE', *, *, #83448, .F. ) ;
#223073=CIRCLE ( 'NONE', #110648, 0.09999999999998898659 ) ;
#223106=EDGE_LOOP ( 'NONE', ( #59377, #13220, #244334, #165896 ) ) ;
#223113=LINE ( 'NONE', #225660, #28953 ) ;
#223117=CARTESIAN_POINT ( 'NONE',  ( 18.42636655943171320, -9.496944315759474620, -207.6090805711554879 ) ) ;
#223157=CARTESIAN_POINT ( 'NONE',  ( 18.59999999999999432, -1.835859311432481045, -212.5044391687984842 ) ) ;
#223183=EDGE_CURVE ( 'NONE', #236853, #26557, #107469, .T. ) ;
#223185=LINE ( 'NONE', #146217, #257522 ) ;
#223220=AXIS2_PLACEMENT_3D ( 'NONE', #231869, #53211, #132771 ) ;
#223232=EDGE_LOOP ( 'NONE', ( #103084, #81420, #171846, #203448 ) ) ;
#223339=ORIENTED_EDGE ( 'NONE', *, *, #39156, .T. ) ;
#223350=AXIS2_PLACEMENT_3D ( 'NONE', #207993, #71052, #106276 ) ;
#223354=VERTEX_POINT ( 'NONE', #121201 ) ;
#223357=DIRECTION ( 'NONE',  ( 0.000000000000000000, -0.8068669527897506244, -0.5907332058516622242 ) ) ;
#223389=CARTESIAN_POINT ( 'NONE',  ( 18.59999999999999076, 11.65000000001115943, -192.3499999999999659 ) ) ;
#223429=VECTOR ( 'NONE', #8162, 1000.000000000000114 ) ;
#223434=CARTESIAN_POINT ( 'NONE',  ( -22.50000000000000000, 11.65000000001115588, -167.4999999999999716 ) ) ;
#223450=CARTESIAN_POINT ( 'NONE',  ( 18.59999999999999076, -1.835859311432481045, -212.5044391687984842 ) ) ;
#223452=EDGE_CURVE ( 'NONE', #232431, #32139, #57570, .T. ) ;
#223490=DIRECTION ( 'NONE',  ( 0.000000000000000000, 1.000000000000000000, 0.000000000000000000 ) ) ;
#223496=VERTEX_POINT ( 'NONE', #25444 ) ;
#223497=DIRECTION ( 'NONE',  ( 0.000000000000000000, -1.000000000000000000, 0.000000000000000000 ) ) ;
#223509=VECTOR ( 'NONE', #88010, 1000.000000000000000 ) ;
#223514=VERTEX_POINT ( 'NONE', #201489 ) ;
#223520=DIRECTION ( 'NONE',  ( 0.000000000000000000, 0.000000000000000000, -1.000000000000000000 ) ) ;
#223522=VECTOR ( 'NONE', #88424, 1000.000000000000000 ) ;
#223529=TOROIDAL_SURFACE ( 'NONE', #215175, 0.2000000000000000111, 0.1000000000000000056 ) ;
#223572=DIRECTION ( 'NONE',  ( 0.000000000000000000, 0.000000000000000000, -1.000000000000000000 ) ) ;
#223582=EDGE_CURVE ( 'NONE', #7699, #132399, #68415, .T. ) ;
#223599=DIRECTION ( 'NONE',  ( 0.000000000000000000, -0.8700118002898359348, 0.4930308989875165082 ) ) ;
#223600=DIRECTION ( 'NONE',  ( 0.000000000000000000, -1.000000000000000000, -0.000000000000000000 ) ) ;
#223644=CARTESIAN_POINT ( 'NONE',  ( 22.39999999999999503, 0.1000000000111554016, -161.2499999999999716 ) ) ;
#223679=CARTESIAN_POINT ( 'NONE',  ( -18.50000000000000000, -1.164121893230052995, -208.9148480855715775 ) ) ;
#223702=DIRECTION ( 'NONE',  ( 1.836970198721029934E-16, -1.000000000000000000, -0.000000000000000000 ) ) ;
#223746=DIRECTION ( 'NONE',  ( 0.000000000000000000, 0.000000000000000000, -1.000000000000000000 ) ) ;
#223758=FACE_OUTER_BOUND ( 'NONE', #126299, .T. ) ;
#223776=CARTESIAN_POINT ( 'NONE',  ( 18.49999999999999289, 10.49142135624846439, -192.3499999999999659 ) ) ;
#223805=CARTESIAN_POINT ( 'NONE',  ( 20.99780126800918723, 11.60538868788781031, -194.0873525717054804 ) ) ;
#223813=DIRECTION ( 'NONE',  ( 0.000000000000000000, -1.000000000000000000, 0.000000000000000000 ) ) ;
#223833=CARTESIAN_POINT ( 'NONE',  ( 21.04999999999999716, 8.872080675388932747, -176.0210474188342005 ) ) ;
#223834=ADVANCED_FACE ( 'NONE', ( #239044 ), #257265, .F. ) ;
#223849=DIRECTION ( 'NONE',  ( -1.000000000000000000, 0.000000000000000000, 0.000000000000000000 ) ) ;
#223864=DIRECTION ( 'NONE',  ( -0.000000000000000000, -0.000000000000000000, 1.000000000000000000 ) ) ;
#223877=CARTESIAN_POINT ( 'NONE',  ( 20.19326291200817280, 10.15606098791077017, -175.2618618076036228 ) ) ;
#223911=VERTEX_POINT ( 'NONE', #82503 ) ;
#223964=ORIENTED_EDGE ( 'NONE', *, *, #242505, .T. ) ;
#224007=FACE_OUTER_BOUND ( 'NONE', #11196, .T. ) ;
#224017=DIRECTION ( 'NONE',  ( 0.000000000000000000, 1.000000000000000000, 0.000000000000000000 ) ) ;
#224028=ORIENTED_EDGE ( 'NONE', *, *, #6841, .F. ) ;
#224043=CARTESIAN_POINT ( 'NONE',  ( 18.43630871534867666, -9.679800874791856913, -207.6606320679839541 ) ) ;
#224044=EDGE_CURVE ( 'NONE', #249596, #160190, #20370, .T. ) ;
#224051=CARTESIAN_POINT ( 'NONE',  ( 18.59999999999999076, 11.65000000001115943, -192.3499999999999659 ) ) ;
#224054=FACE_OUTER_BOUND ( 'NONE', #35980, .T. ) ;
#224079=LINE ( 'NONE', #126265, #194665 ) ;
#224084=CARTESIAN_POINT ( 'NONE',  ( 20.85000000000000142, -1.835859311432481045, -212.6044391687984785 ) ) ;
#224107=CARTESIAN_POINT ( 'NONE',  ( 20.94999999999999929, 1.115649653272650466E-11, -196.9999999999999432 ) ) ;
#224127=ORIENTED_EDGE ( 'NONE', *, *, #245504, .T. ) ;
#224139=CARTESIAN_POINT ( 'NONE',  ( -18.59999999999999787, -1.164121893230052995, -208.9148480855715775 ) ) ;
#224142=LINE ( 'NONE', #6384, #236122 ) ;
#224181=DIRECTION ( 'NONE',  ( 0.000000000000000000, -0.9915357197604971473, 0.1298341882519111479 ) ) ;
#224204=EDGE_CURVE ( 'NONE', #75721, #68978, #60085, .T. ) ;
#224222=CARTESIAN_POINT ( 'NONE',  ( -20.85000000000000142, -1.736705739456431807, -212.5174225876236846 ) ) ;
#224236=DIRECTION ( 'NONE',  ( 0.000000000000000000, 0.000000000000000000, -1.000000000000000000 ) ) ;
#224237=CYLINDRICAL_SURFACE ( 'NONE', #175358, 0.09999999999998898659 ) ;
#224240=AXIS2_PLACEMENT_3D ( 'NONE', #236849, #154784, #76488 ) ;
#224258=AXIS2_PLACEMENT_3D ( 'NONE', #226377, #47748, #187298 ) ;
#224264=EDGE_CURVE ( 'NONE', #90934, #114385, #66336, .T. ) ;
#224284=ORIENTED_EDGE ( 'NONE', *, *, #44094, .F. ) ;
#224289=EDGE_LOOP ( 'NONE', ( #169809, #179495, #84077 ) ) ;
#224312=EDGE_CURVE ( 'NONE', #38886, #22668, #199628, .T. ) ;
#224320=ORIENTED_EDGE ( 'NONE', *, *, #171225, .F. ) ;
#224322=CIRCLE ( 'NONE', #145204, 11.90000000000000391 ) ;
#224363=ORIENTED_EDGE ( 'NONE', *, *, #72564, .T. ) ;
#224365=ORIENTED_EDGE ( 'NONE', *, *, #210536, .T. ) ;
#224367=ORIENTED_EDGE ( 'NONE', *, *, #194805, .T. ) ;
#224407=DIRECTION ( 'NONE',  ( 0.000000000000000000, 1.000000000000000000, 0.000000000000000000 ) ) ;
#224409=AXIS2_PLACEMENT_3D ( 'NONE', #125522, #145071, #5549 ) ;
#224417=CARTESIAN_POINT ( 'NONE',  ( -20.54999999999999716, 4.350000000011156054, -184.2499999999999716 ) ) ;
#224419=CARTESIAN_POINT ( 'NONE',  ( -20.54999999999999716, 4.350000000011156054, -188.6499999999999488 ) ) ;
#224421=EDGE_CURVE ( 'NONE', #48432, #255690, #204048, .T. ) ;
#224466=EDGE_LOOP ( 'NONE', ( #241562, #22903, #77066, #140978 ) ) ;
#224471=CARTESIAN_POINT ( 'NONE',  ( -23.25000000000000000, 1.115600667400684642E-11, -200.9999999999999432 ) ) ;
#224509=VERTEX_POINT ( 'NONE', #112084 ) ;
#224514=EDGE_CURVE ( 'NONE', #167246, #201908, #99788, .T. ) ;
#224519=CIRCLE ( 'NONE', #57898, 11.69999999999998863 ) ;
#224540=AXIS2_PLACEMENT_3D ( 'NONE', #138565, #61635, #198567 ) ;
#224557=EDGE_CURVE ( 'NONE', #218583, #59445, #174662, .T. ) ;
#224564=CARTESIAN_POINT ( 'NONE',  ( -20.54999999999999716, -8.999999999988844479, -191.1060308773475356 ) ) ;
#224612=ORIENTED_EDGE ( 'NONE', *, *, #97318, .F. ) ;
#224613=DIRECTION ( 'NONE',  ( 3.616040088954497272E-32, -1.224646799147352961E-16, 1.000000000000000000 ) ) ;
#224614=ADVANCED_FACE ( 'NONE', ( #41541 ), #76781, .F. ) ;
#224650=DIRECTION ( 'NONE',  ( 0.000000000000000000, 0.000000000000000000, -1.000000000000000000 ) ) ;
#224661=VECTOR ( 'NONE', #1107, 1000.000000000000000 ) ;
#224710=ORIENTED_EDGE ( 'NONE', *, *, #198383, .F. ) ;
#224749=AXIS2_PLACEMENT_3D ( 'NONE', #132316, #63683, #33261 ) ;
#224757=CARTESIAN_POINT ( 'NONE',  ( 21.11747605621531321, 8.778708005504054057, -179.7445631697897568 ) ) ;
#224759=AXIS2_PLACEMENT_3D ( 'NONE', #230877, #13106, #52199 ) ;
#224766=ORIENTED_EDGE ( 'NONE', *, *, #161719, .T. ) ;
#224769=DIRECTION ( 'NONE',  ( 0.000000000000000000, 0.1575844902526835067, 0.9875055080513738259 ) ) ;
#224848=VERTEX_POINT ( 'NONE', #63638 ) ;
#224888=ORIENTED_EDGE ( 'NONE', *, *, #38185, .F. ) ;
#224890=AXIS2_PLACEMENT_3D ( 'NONE', #232416, #116313, #255763 ) ;
#224902=DIRECTION ( 'NONE',  ( 0.000000000000000000, 0.000000000000000000, -1.000000000000000000 ) ) ;
#224904=CARTESIAN_POINT ( 'NONE',  ( -18.59999999999999787, 11.75000000001115552, -200.9999999999999432 ) ) ;
#224962=ORIENTED_EDGE ( 'NONE', *, *, #225667, .T. ) ;
#224969=TOROIDAL_SURFACE ( 'NONE', #50191, 0.2000000000000000111, 0.1000000000000000056 ) ;
#224984=FACE_OUTER_BOUND ( 'NONE', #57318, .T. ) ;
#224996=EDGE_CURVE ( 'NONE', #202617, #99286, #145787, .T. ) ;
#225000=EDGE_CURVE ( 'NONE', #184932, #7699, #87524, .T. ) ;
#225034=CARTESIAN_POINT ( 'NONE',  ( -18.59999999999999787, -1.162701749926853712, -175.5999999999999659 ) ) ;
#225039=EDGE_LOOP ( 'NONE', ( #146617, #26241, #136523, #240983 ) ) ;
#225066=EDGE_CURVE ( 'NONE', #14833, #254925, #62605, .T. ) ;
#225153=ORIENTED_EDGE ( 'NONE', *, *, #208280, .T. ) ;
#225164=VERTEX_POINT ( 'NONE', #169867 ) ;
#225173=CIRCLE ( 'NONE', #79619, 4.300000000000025580 ) ;
#225179=ORIENTED_EDGE ( 'NONE', *, *, #113555, .T. ) ;
#225193=VERTEX_POINT ( 'NONE', #68149 ) ;
#225194=CARTESIAN_POINT ( 'NONE',  ( 22.39999999999999503, 11.75000000001116263, -167.3999999999999773 ) ) ;
#225216=DIRECTION ( 'NONE',  ( 0.000000000000000000, 0.000000000000000000, -1.000000000000000000 ) ) ;
#225245=ADVANCED_FACE ( 'NONE', ( #57553 ), #255727, .F. ) ;
#225260=ORIENTED_EDGE ( 'NONE', *, *, #67051, .F. ) ;
#225263=( BOUNDED_CURVE ( )  B_SPLINE_CURVE ( 3, ( #57282, #19475, #74342, #55993 ),
 .UNSPECIFIED., .F., .F. ) 
 B_SPLINE_CURVE_WITH_KNOTS ( ( 4, 4 ),
 ( 0.06456096931748307732, 3.077031684272310219 ),
 .UNSPECIFIED. ) 
 CURVE ( )  GEOMETRIC_REPRESENTATION_ITEM ( )  RATIONAL_B_SPLINE_CURVE ( ( 1.000000000000000000, 0.3763440860215093164, 0.3763440860215093164, 1.000000000000000000 ) ) 
 REPRESENTATION_ITEM ( '' )  );
#225288=DIRECTION ( 'NONE',  ( 1.000000000000000000, 0.000000000000000000, 0.000000000000000000 ) ) ;
#225301=ORIENTED_EDGE ( 'NONE', *, *, #249325, .T. ) ;
#225317=CARTESIAN_POINT ( 'NONE',  ( 18.47135592147651195, -9.471088613254559974, -207.6835949398434309 ) ) ;
#225335=ADVANCED_FACE ( 'NONE', ( #52419 ), #131971, .T. ) ;
#225336=LINE ( 'NONE', #84513, #109256 ) ;
#225387=CARTESIAN_POINT ( 'NONE',  ( -20.85000000000000142, 7.021664781911246322, -204.8335654018972605 ) ) ;
#225406=ADVANCED_FACE ( 'NONE', ( #199678 ), #21041, .T. ) ;
#225422=CARTESIAN_POINT ( 'NONE',  ( 20.94999999999999929, 11.65000000001115943, -200.9999999999999432 ) ) ;
#225424=EDGE_CURVE ( 'NONE', #48432, #156856, #158668, .T. ) ;
#225433=DIRECTION ( 'NONE',  ( 0.000000000000000000, -0.9908441862701782288, 0.1350103645450542456 ) ) ;
#225438=EDGE_CURVE ( 'NONE', #176002, #54306, #62782, .T. ) ;
#225445=CIRCLE ( 'NONE', #113039, 0.1000000000000000472 ) ;
#225454=CARTESIAN_POINT ( 'NONE',  ( 23.24999999999999645, 5.000000000011153745, -179.9052660189130677 ) ) ;
#225473=CARTESIAN_POINT ( 'NONE',  ( -23.25000000000000000, -11.74999999998884448, -197.8999999999999773 ) ) ;
#225485=DIRECTION ( 'NONE',  ( 2.557131231893036985E-16, -0.8660254037844383745, 0.5000000000000003331 ) ) ;
#225486=DIRECTION ( 'NONE',  ( 1.000000000000000000, -0.000000000000000000, -0.000000000000000000 ) ) ;
#225489=CARTESIAN_POINT ( 'NONE',  ( 21.12400247839510925, 10.72148804404153921, -179.7500000000000000 ) ) ;
#225546=AXIS2_PLACEMENT_3D ( 'NONE', #155640, #235143, #136012 ) ;
#225550=ORIENTED_EDGE ( 'NONE', *, *, #112736, .F. ) ;
#225559=DIRECTION ( 'NONE',  ( 0.000000000000000000, 0.000000000000000000, 1.000000000000000000 ) ) ;
#225566=DIRECTION ( 'NONE',  ( 0.000000000000000000, 0.000000000000000000, 1.000000000000000000 ) ) ;
#225574=ORIENTED_EDGE ( 'NONE', *, *, #119219, .T. ) ;
#225584=ORIENTED_EDGE ( 'NONE', *, *, #178298, .T. ) ;
#225593=ORIENTED_EDGE ( 'NONE', *, *, #148829, .T. ) ;
#225599=AXIS2_PLACEMENT_3D ( 'NONE', #153952, #191778, #78200 ) ;
#225604=DIRECTION ( 'NONE',  ( 1.000000000000000000, 0.000000000000000000, 0.000000000000000000 ) ) ;
#225622=CIRCLE ( 'NONE', #196599, 0.09999999999998898659 ) ;
#225647=CARTESIAN_POINT ( 'NONE',  ( 20.94999999999999929, -1.349153571964892606, -208.7874973355898476 ) ) ;
#225660=CARTESIAN_POINT ( 'NONE',  ( -20.54999999999999716, 4.350000000011156054, -188.7499999999999716 ) ) ;
#225661=CIRCLE ( 'NONE', #179915, 4.099999999999992539 ) ;
#225667=EDGE_CURVE ( 'NONE', #194728, #52702, #205059, .T. ) ;
#225699=DIRECTION ( 'NONE',  ( 0.000000000000000000, -1.000000000000000000, -2.891205793294679805E-16 ) ) ;
#225707=ORIENTED_EDGE ( 'NONE', *, *, #170241, .F. ) ;
#225730=EDGE_CURVE ( 'NONE', #95420, #164666, #17627, .T. ) ;
#225737=CARTESIAN_POINT ( 'NONE',  ( -20.64999999999999858, 1.115600667400684642E-11, -180.3749999999999716 ) ) ;
#225741=CIRCLE ( 'NONE', #217361, 0.09999999999999939493 ) ;
#225757=ADVANCED_FACE ( 'NONE', ( #93822 ), #38499, .T. ) ;
#225770=AXIS2_PLACEMENT_3D ( 'NONE', #119868, #40348, #184948 ) ;
#225802=EDGE_CURVE ( 'NONE', #35026, #59716, #188328, .T. ) ;
#225810=VECTOR ( 'NONE', #258005, 1000.000000000000000 ) ;
#225813=CARTESIAN_POINT ( 'NONE',  ( -18.54260524012575928, -9.624219390062513924, -207.7407730457709079 ) ) ;
#225826=DIRECTION ( 'NONE',  ( 0.000000000000000000, 0.000000000000000000, 1.000000000000000000 ) ) ;
#225839=ORIENTED_EDGE ( 'NONE', *, *, #113359, .T. ) ;
#225863=DIRECTION ( 'NONE',  ( 1.000000000000000000, -0.000000000000000000, -0.000000000000000000 ) ) ;
#225868=EDGE_CURVE ( 'NONE', #252063, #221674, #241058, .T. ) ;
#225904=ORIENTED_EDGE ( 'NONE', *, *, #236912, .T. ) ;
#225911=DIRECTION ( 'NONE',  ( 0.000000000000000000, 0.000000000000000000, -1.000000000000000000 ) ) ;
#225938=DIRECTION ( 'NONE',  ( -1.000000000000000000, 0.000000000000000000, 0.000000000000000000 ) ) ;
#225941=DIRECTION ( 'NONE',  ( -1.000000000000000000, 0.000000000000000000, 0.000000000000000000 ) ) ;
#225950=DIRECTION ( 'NONE',  ( 0.000000000000000000, -1.000000000000000000, -2.891205793294679805E-16 ) ) ;
#225962=ORIENTED_EDGE ( 'NONE', *, *, #118369, .T. ) ;
#226024=ADVANCED_FACE ( 'NONE', ( #67534 ), #226594, .T. ) ;
#226026=CARTESIAN_POINT ( 'NONE',  ( -20.85000000000000142, 7.021664781911246322, -204.8335654018972605 ) ) ;
#226037=DIRECTION ( 'NONE',  ( 0.000000000000000000, -0.9915357197604971473, 0.1298341882519111479 ) ) ;
#226046=CARTESIAN_POINT ( 'NONE',  ( -22.48660254037843487, 11.65000000001115588, -167.4499999999999886 ) ) ;
#226101=CARTESIAN_POINT ( 'NONE',  ( -18.59999999999999787, -1.687074390080403941, -154.6854270334582964 ) ) ;
#226124=DIRECTION ( 'NONE',  ( 0.000000000000000000, 0.000000000000000000, -1.000000000000000000 ) ) ;
#226129=CARTESIAN_POINT ( 'NONE',  ( 21.05000000000000071, 1.115600667400684642E-11, -167.4999999999999716 ) ) ;
#226141=ORIENTED_EDGE ( 'NONE', *, *, #173235, .F. ) ;
#226162=LINE ( 'NONE', #89249, #125543 ) ;
#226164=CARTESIAN_POINT ( 'NONE',  ( -23.15000000000000213, -8.999999999988844479, -191.1060308773475356 ) ) ;
#226183=EDGE_LOOP ( 'NONE', ( #247344, #211810, #231426, #201850 ) ) ;
#226203=ORIENTED_EDGE ( 'NONE', *, *, #138949, .F. ) ;
#226206=CARTESIAN_POINT ( 'NONE',  ( 18.59999999999999432, 1.162701749949165642, -175.5999999999999659 ) ) ;
#226223=EDGE_CURVE ( 'NONE', #25429, #16283, #130350, .T. ) ;
#226243=AXIS2_PLACEMENT_3D ( 'NONE', #247687, #69071, #148601 ) ;
#226252=CARTESIAN_POINT ( 'NONE',  ( 23.14999999999999858, 1.115600667400684642E-11, -204.9999999999999716 ) ) ;
#226274=ORIENTED_EDGE ( 'NONE', *, *, #212335, .T. ) ;
#226297=CARTESIAN_POINT ( 'NONE',  ( -18.59999999999999787, 1.250000000011155299, -175.4999999999999716 ) ) ;
#226325=ORIENTED_EDGE ( 'NONE', *, *, #198119, .T. ) ;
#226340=EDGE_CURVE ( 'NONE', #148316, #91171, #105574, .T. ) ;
#226377=CARTESIAN_POINT ( 'NONE',  ( -18.50000000000000000, -1.835341550213255957, -179.0551512925629538 ) ) ;
#226390=DIRECTION ( 'NONE',  ( -0.7071067811865474617, -0.7071067811865474617, -0.000000000000000000 ) ) ;
#226396=ORIENTED_EDGE ( 'NONE', *, *, #18720, .T. ) ;
#226409=AXIS2_PLACEMENT_3D ( 'NONE', #198407, #216684, #220546 ) ;
#226425=CARTESIAN_POINT ( 'NONE',  ( -23.25000000000000000, 10.33248238083634440, -206.5948465439131496 ) ) ;
#226434=ORIENTED_EDGE ( 'NONE', *, *, #21741, .F. ) ;
#226438=AXIS2_PLACEMENT_3D ( 'NONE', #36368, #254087, #170771 ) ;
#226450=ORIENTED_EDGE ( 'NONE', *, *, #60961, .T. ) ;
#226456=CIRCLE ( 'NONE', #118353, 4.149999999999999467 ) ;
#226535=ORIENTED_EDGE ( 'NONE', *, *, #49124, .F. ) ;
#226544=ORIENTED_EDGE ( 'NONE', *, *, #30559, .T. ) ;
#226594=CYLINDRICAL_SURFACE ( 'NONE', #209467, 0.09999999999998898659 ) ;
#226608=CARTESIAN_POINT ( 'NONE',  ( 18.44208962362927551, -9.552340496896620792, -207.8421730554641442 ) ) ;
#226649=AXIS2_PLACEMENT_3D ( 'NONE', #225387, #153286, #232807 ) ;
#226669=CARTESIAN_POINT ( 'NONE',  ( -18.59999999999999787, -9.499999999988842703, -179.6499999999999773 ) ) ;
#226687=DIRECTION ( 'NONE',  ( 0.000000000000000000, 0.000000000000000000, 1.000000000000000000 ) ) ;
#226702=DIRECTION ( 'NONE',  ( 4.408576920032447355E-17, -0.1350103645451876666, 0.9908441862701600211 ) ) ;
#226708=DIRECTION ( 'NONE',  ( 1.000000000000000000, 0.000000000000000000, 0.000000000000000000 ) ) ;
#226726=AXIS2_PLACEMENT_3D ( 'NONE', #71409, #233051, #213458 ) ;
#226729=DIRECTION ( 'NONE',  ( 1.000000000000000000, 0.000000000000000000, 0.000000000000000000 ) ) ;
#226735=FACE_OUTER_BOUND ( 'NONE', #118724, .T. ) ;
#226765=EDGE_LOOP ( 'NONE', ( #60395, #468, #163349, #145592 ) ) ;
#226771=CIRCLE ( 'NONE', #189186, 0.09999999999998898659 ) ;
#226775=AXIS2_PLACEMENT_3D ( 'NONE', #38909, #121029, #4865 ) ;
#226781=ORIENTED_EDGE ( 'NONE', *, *, #157878, .T. ) ;
#226815=DIRECTION ( 'NONE',  ( 1.000000000000000000, 0.000000000000000000, 0.000000000000000000 ) ) ;
#226831=B_SPLINE_CURVE_WITH_KNOTS ( 'NONE', 3,
 ( #164484, #257407, #65368, #158405, #237902, #59220 ),
 .UNSPECIFIED., .F., .F.,
 ( 4, 2, 4 ),
 ( 0.000000000000000000, 0.0001496588209255837190, 0.0002993176418511674379 ),
 .UNSPECIFIED. ) ;
#226834=ORIENTED_EDGE ( 'NONE', *, *, #177148, .T. ) ;
#226840=VERTEX_POINT ( 'NONE', #117479 ) ;
#226843=EDGE_LOOP ( 'NONE', ( #34140, #209969, #1600 ) ) ;
#226863=DIRECTION ( 'NONE',  ( -1.000000000000000000, 0.000000000000000000, 0.000000000000000000 ) ) ;
#226864=AXIS2_PLACEMENT_3D ( 'NONE', #226922, #48284, #34845 ) ;
#226865=DIRECTION ( 'NONE',  ( 1.000000000000000000, -0.000000000000000000, -0.000000000000000000 ) ) ;
#226878=CARTESIAN_POINT ( 'NONE',  ( -21.05000000000000071, 1.115600667400684642E-11, -167.4999999999999716 ) ) ;
#226886=VERTEX_POINT ( 'NONE', #120072 ) ;
#226899=LINE ( 'NONE', #131653, #227434 ) ;
#226922=CARTESIAN_POINT ( 'NONE',  ( -20.64999999999999858, 1.115600667400684642E-11, -167.4999999999999716 ) ) ;
#226937=AXIS2_PLACEMENT_3D ( 'NONE', #19401, #173384, #195494 ) ;
#226939=EDGE_LOOP ( 'NONE', ( #126939, #51577, #33089, #65231 ) ) ;
#226963=DIRECTION ( 'NONE',  ( -0.000000000000000000, -0.1350103645451876666, -0.9908441862701600211 ) ) ;
#226968=FACE_OUTER_BOUND ( 'NONE', #246939, .T. ) ;
#226972=ORIENTED_EDGE ( 'NONE', *, *, #52609, .T. ) ;
#227011=DIRECTION ( 'NONE',  ( 0.000000000000000000, 0.9654727137038715545, 0.2605042016806676242 ) ) ;
#227016=DIRECTION ( 'NONE',  ( 0.000000000000000000, 1.000000000000000000, 0.000000000000000000 ) ) ;
#227033=CYLINDRICAL_SURFACE ( 'NONE', #256005, 0.09999999999998898659 ) ;
#227057=EDGE_CURVE ( 'NONE', #146076, #184932, #111698, .T. ) ;
#227059=CARTESIAN_POINT ( 'NONE',  ( -21.05000000000000426, -0.02103547652896323866, -161.1955441780523586 ) ) ;
#227081=CARTESIAN_POINT ( 'NONE',  ( 18.46947024752506294, -9.509297157144905199, -174.4866894486979447 ) ) ;
#227083=AXIS2_PLACEMENT_3D ( 'NONE', #147340, #44406, #3977 ) ;
#227097=EDGE_CURVE ( 'NONE', #250193, #122594, #101848, .T. ) ;
#227098=EDGE_CURVE ( 'NONE', #141186, #196430, #56058, .T. ) ;
#227142=DIRECTION ( 'NONE',  ( 0.000000000000000000, 0.000000000000000000, 1.000000000000000000 ) ) ;
#227167=DIRECTION ( 'NONE',  ( 1.000000000000000000, 0.000000000000000000, 0.000000000000000000 ) ) ;
#227173=DIRECTION ( 'NONE',  ( 0.000000000000000000, 0.000000000000000000, -1.000000000000000000 ) ) ;
#227175=DIRECTION ( 'NONE',  ( 0.000000000000000000, -0.6728971962617388280, -0.7397360091702248619 ) ) ;
#227193=EDGE_CURVE ( 'NONE', #128029, #244617, #226771, .T. ) ;
#227205=DIRECTION ( 'NONE',  ( 0.000000000000000000, 0.000000000000000000, -1.000000000000000000 ) ) ;
#227209=CIRCLE ( 'NONE', #114794, 7.800000000000001599 ) ;
#227217=DIRECTION ( 'NONE',  ( 0.000000000000000000, -0.8660254037844411501, -0.4999999999999956701 ) ) ;
#227223=FACE_OUTER_BOUND ( 'NONE', #104000, .T. ) ;
#227277=ORIENTED_EDGE ( 'NONE', *, *, #206951, .F. ) ;
#227281=CARTESIAN_POINT ( 'NONE',  ( -22.39999999999999858, 1.115600667400684642E-11, -159.7092204016265384 ) ) ;
#227290=VERTEX_POINT ( 'NONE', #139250 ) ;
#227306=AXIS2_PLACEMENT_3D ( 'NONE', #145948, #204633, #126393 ) ;
#227316=TOROIDAL_SURFACE ( 'NONE', #148209, 0.6000000000000009770, 0.1000000000000000056 ) ;
#227323=AXIS2_PLACEMENT_3D ( 'NONE', #101617, #181215, #82062 ) ;
#227327=DIRECTION ( 'NONE',  ( 1.000000000000000000, 0.000000000000000000, 0.000000000000000000 ) ) ;
#227354=CARTESIAN_POINT ( 'NONE',  ( 20.94999999999999929, 1.115600667400684642E-11, -200.9999999999999432 ) ) ;
#227364=DIRECTION ( 'NONE',  ( 1.000000000000000000, -0.000000000000000000, -0.000000000000000000 ) ) ;
#227370=DIRECTION ( 'NONE',  ( 0.000000000000000000, 0.000000000000000000, -1.000000000000000000 ) ) ;
#227391=ORIENTED_EDGE ( 'NONE', *, *, #109360, .F. ) ;
#227399=CIRCLE ( 'NONE', #194106, 11.64999999999999325 ) ;
#227434=VECTOR ( 'NONE', #127814, 1000.000000000000114 ) ;
#227455=DIRECTION ( 'NONE',  ( 0.000000000000000000, 6.505213034913742890E-15, -1.000000000000000000 ) ) ;
#227513=EDGE_CURVE ( 'NONE', #147926, #146255, #252480, .T. ) ;
#227518=ORIENTED_EDGE ( 'NONE', *, *, #13962, .T. ) ;
#227519=CIRCLE ( 'NONE', #194254, 0.6000000000000015321 ) ;
#227523=DIRECTION ( 'NONE',  ( 0.000000000000000000, -0.9908441862701782288, -0.1350103645450542456 ) ) ;
#227526=DIRECTION ( 'NONE',  ( -1.000000000000000000, 0.000000000000000000, 0.000000000000000000 ) ) ;
#227531=CARTESIAN_POINT ( 'NONE',  ( -20.94999999999999929, 1.115600667400684642E-11, -200.9999999999999432 ) ) ;
#227535=EDGE_LOOP ( 'NONE', ( #222958, #202678, #98654, #204050 ) ) ;
#227542=LINE ( 'NONE', #25511, #48603 ) ;
#227585=EDGE_CURVE ( 'NONE', #249408, #206366, #131093, .T. ) ;
#227623=CARTESIAN_POINT ( 'NONE',  ( -20.93302460841142931, 10.31565961587945424, -206.5364194119177625 ) ) ;
#227658=ORIENTED_EDGE ( 'NONE', *, *, #240487, .F. ) ;
#227665=CARTESIAN_POINT ( 'NONE',  ( -21.44999999999999929, 7.350000000011155166, -188.6499999999999488 ) ) ;
#227683=DIRECTION ( 'NONE',  ( 0.000000000000000000, 0.9908441862701600211, -0.1350103645451876666 ) ) ;
#227692=CARTESIAN_POINT ( 'NONE',  ( -22.59999999999999787, 11.74956712350054566, -167.3991416309012550 ) ) ;
#227715=VECTOR ( 'NONE', #225950, 1000.000000000000000 ) ;
#227722=CIRCLE ( 'NONE', #240232, 0.09999999999998898659 ) ;
#227735=LINE ( 'NONE', #209460, #43354 ) ;
#227737=EDGE_CURVE ( 'NONE', #219709, #239082, #106233, .T. ) ;
#227755=CIRCLE ( 'NONE', #136151, 0.09999999999998898659 ) ;
#227765=VERTEX_POINT ( 'NONE', #240632 ) ;
#227783=CARTESIAN_POINT ( 'NONE',  ( -21.14999999999999858, 11.75000000001115552, -174.2261306360591675 ) ) ;
#227814=ADVANCED_FACE ( 'NONE', ( #110104 ), #8451, .F. ) ;
#227818=AXIS2_PLACEMENT_3D ( 'NONE', #114670, #48585, #86401 ) ;
#227898=CARTESIAN_POINT ( 'NONE',  ( -20.00857864376270001, 9.250000000011157297, -188.6499999999999488 ) ) ;
#227913=CARTESIAN_POINT ( 'NONE',  ( 18.41815437325347204, -9.498709853130270275, -207.6039458388019341 ) ) ;
#227916=EDGE_LOOP ( 'NONE', ( #59160, #93416, #37996, #150556 ) ) ;
#227965=EDGE_CURVE ( 'NONE', #7452, #175979, #39729, .T. ) ;
#227997=AXIS2_PLACEMENT_3D ( 'NONE', #207404, #113421, #148710 ) ;
#228008=CARTESIAN_POINT ( 'NONE',  ( 22.39999999999999503, 11.65000000001116298, -167.3999999999999773 ) ) ;
#228016=CYLINDRICAL_SURFACE ( 'NONE', #7381, 0.09999999999999939493 ) ;
#228031=ORIENTED_EDGE ( 'NONE', *, *, #77638, .T. ) ;
#228068=AXIS2_PLACEMENT_3D ( 'NONE', #161952, #25013, #245326 ) ;
#228081=AXIS2_PLACEMENT_3D ( 'NONE', #67853, #11764, #148697 ) ;
#228093=AXIS2_PLACEMENT_3D ( 'NONE', #115288, #194856, #16219 ) ;
#228119=FACE_OUTER_BOUND ( 'NONE', #169588, .T. ) ;
#228138=DIRECTION ( 'NONE',  ( 1.000000000000000000, -0.000000000000000000, -0.000000000000000000 ) ) ;
#228139=EDGE_CURVE ( 'NONE', #135650, #199385, #248029, .T. ) ;
#228156=ORIENTED_EDGE ( 'NONE', *, *, #225066, .F. ) ;
#228244=DIRECTION ( 'NONE',  ( 1.000000000000000000, 0.000000000000000000, 0.000000000000000000 ) ) ;
#228254=AXIS2_PLACEMENT_3D ( 'NONE', #2949, #45942, #201162 ) ;
#228255=AXIS2_PLACEMENT_3D ( 'NONE', #172544, #229897, #132082 ) ;
#228271=CARTESIAN_POINT ( 'NONE',  ( -21.05000000000000071, 11.63687328911514030, -174.3217592133248957 ) ) ;
#228290=CARTESIAN_POINT ( 'NONE',  ( -20.85000000000000142, 10.33248238083634440, -206.5948465439131496 ) ) ;
#228295=FACE_OUTER_BOUND ( 'NONE', #62717, .T. ) ;
#228308=CARTESIAN_POINT ( 'NONE',  ( -20.54999999999999716, 7.150000000011155876, -179.7499999999999716 ) ) ;
#228312=FACE_OUTER_BOUND ( 'NONE', #187042, .T. ) ;
#228314=EDGE_CURVE ( 'NONE', #97822, #99579, #91449, .T. ) ;
#228318=DIRECTION ( 'NONE',  ( 1.000000000000000000, 0.000000000000000000, 0.000000000000000000 ) ) ;
#228323=CARTESIAN_POINT ( 'NONE',  ( -20.94999999999999929, 7.021664781911246322, -204.6335654018972434 ) ) ;
#228348=CARTESIAN_POINT ( 'NONE',  ( 21.05000000000000071, 10.42338541492406279, -174.9920519238700649 ) ) ;
#228356=ADVANCED_FACE ( 'NONE', ( #85716 ), #227316, .T. ) ;
#228422=EDGE_LOOP ( 'NONE', ( #109822, #89784, #47645, #104396 ) ) ;
#228424=CIRCLE ( 'NONE', #195108, 11.65000000000000036 ) ;
#228432=ADVANCED_FACE ( 'NONE', ( #28394 ), #114305, .F. ) ;
#228445=ORIENTED_EDGE ( 'NONE', *, *, #106269, .F. ) ;
#228450=ORIENTED_EDGE ( 'NONE', *, *, #196112, .F. ) ;
#228451=CARTESIAN_POINT ( 'NONE',  ( 23.14999999999999503, 11.65000000001116298, -188.8499999999999659 ) ) ;
#228455=CIRCLE ( 'NONE', #7885, 0.09999999999999344136 ) ;
#228470=EDGE_LOOP ( 'NONE', ( #19411, #214122, #121931, #171403 ) ) ;
#228477=CARTESIAN_POINT ( 'NONE',  ( 18.49999999999999645, -1.162701749926855266, -175.5999999999999659 ) ) ;
#228484=CYLINDRICAL_SURFACE ( 'NONE', #151476, 7.899999999999990585 ) ;
#228508=EDGE_CURVE ( 'NONE', #68874, #220110, #243837, .T. ) ;
#228513=CARTESIAN_POINT ( 'NONE',  ( -20.94999999999999929, 1.116121084443477685E-11, -170.3999999999999488 ) ) ;
#228537=EDGE_LOOP ( 'NONE', ( #177583, #255713, #14669, #177070 ) ) ;
#228556=CARTESIAN_POINT ( 'NONE',  ( -23.25000000000000000, 1.115600667400684642E-11, -204.8999999999999488 ) ) ;
#228593=VECTOR ( 'NONE', #10297, 1000.000000000000000 ) ;
#228613=ORIENTED_EDGE ( 'NONE', *, *, #33126, .T. ) ;
#228616=LINE ( 'NONE', #26566, #175001 ) ;
#228617=EDGE_CURVE ( 'NONE', #14186, #75721, #20367, .T. ) ;
#228652=ORIENTED_EDGE ( 'NONE', *, *, #235370, .T. ) ;
#228674=DIRECTION ( 'NONE',  ( 0.000000000000000000, 0.000000000000000000, -1.000000000000000000 ) ) ;
#228713=DIRECTION ( 'NONE',  ( 0.000000000000000000, 1.000000000000000000, -6.308085367188393199E-16 ) ) ;
#228727=CIRCLE ( 'NONE', #187213, 0.09999999999998898659 ) ;
#228740=DIRECTION ( 'NONE',  ( -3.265361837132813093E-16, 1.000000000000000000, 0.000000000000000000 ) ) ;
#228758=AXIS2_PLACEMENT_3D ( 'NONE', #113821, #193386, #214220 ) ;
#228805=ORIENTED_EDGE ( 'NONE', *, *, #13943, .F. ) ;
#228813=ORIENTED_EDGE ( 'NONE', *, *, #125109, .T. ) ;
#228816=EDGE_CURVE ( 'NONE', #88113, #126189, #135903, .T. ) ;
#228841=ORIENTED_EDGE ( 'NONE', *, *, #60474, .T. ) ;
#228846=CYLINDRICAL_SURFACE ( 'NONE', #107285, 12.87499999999999822 ) ;
#228850=ORIENTED_EDGE ( 'NONE', *, *, #71235, .T. ) ;
#228907=EDGE_LOOP ( 'NONE', ( #223339, #195129, #65376, #251459 ) ) ;
#228941=CARTESIAN_POINT ( 'NONE',  ( 18.49999999999999289, 6.450000000011156587, -188.6499999999999488 ) ) ;
#228979=ADVANCED_FACE ( 'NONE', ( #210541 ), #48610, .F. ) ;
#228990=VERTEX_POINT ( 'NONE', #74909 ) ;
#228994=AXIS2_PLACEMENT_3D ( 'NONE', #140910, #180039, #61362 ) ;
#229011=VECTOR ( 'NONE', #251568, 1000.000000000000000 ) ;
#229020=EDGE_LOOP ( 'NONE', ( #198790, #68099, #220855, #248193, #157433 ) ) ;
#229022=DIRECTION ( 'NONE',  ( 0.000000000000000000, -0.4930308989874718772, -0.8700118002898612479 ) ) ;
#229040=CIRCLE ( 'NONE', #87357, 0.1000000000000089567 ) ;
#229052=ADVANCED_FACE ( 'NONE', ( #20055 ), #77420, .T. ) ;
#229122=EDGE_CURVE ( 'NONE', #183971, #176002, #123005, .T. ) ;
#229127=CARTESIAN_POINT ( 'NONE',  ( -22.49510344025093644, 0.06712767820541533370, -155.8500298948856937 ) ) ;
#229131=CARTESIAN_POINT ( 'NONE',  ( -22.39999999999999858, 7.790779598384560245, -167.3999999999999773 ) ) ;
#229145=CARTESIAN_POINT ( 'NONE',  ( 21.05000000000000426, 10.56275983746217761, -174.9568139579185981 ) ) ;
#229152=EDGE_CURVE ( 'NONE', #12777, #140846, #36172, .T. ) ;
#229155=ORIENTED_EDGE ( 'NONE', *, *, #28558, .F. ) ;
#229208=AXIS2_PLACEMENT_3D ( 'NONE', #153247, #132359, #201014 ) ;
#229218=DIRECTION ( 'NONE',  ( 0.000000000000000000, 0.2605042016806672911, -0.9654727137038716656 ) ) ;
#229224=ORIENTED_EDGE ( 'NONE', *, *, #238295, .T. ) ;
#229234=DIRECTION ( 'NONE',  ( 0.000000000000000000, 1.224646799142185182E-16, 1.000000000000000000 ) ) ;
#229244=CARTESIAN_POINT ( 'NONE',  ( -18.59999999999999787, -9.480686695267820596, -207.9411151687578183 ) ) ;
#229256=ORIENTED_EDGE ( 'NONE', *, *, #124581, .F. ) ;
#229262=EDGE_CURVE ( 'NONE', #41250, #254925, #191984, .T. ) ;
#229311=VERTEX_POINT ( 'NONE', #10755 ) ;
#229353=CARTESIAN_POINT ( 'NONE',  ( 20.04142135623730070, 11.75000000001115907, -188.8499999999999659 ) ) ;
#229362=CARTESIAN_POINT ( 'NONE',  ( -21.05000000000000071, 6.300000000011169554, -167.5999999999999659 ) ) ;
#229372=CARTESIAN_POINT ( 'NONE',  ( -20.54999999999999716, 1.925233644870972816, -180.2302435331260995 ) ) ;
#229373=AXIS2_PLACEMENT_3D ( 'NONE', #22201, #1315, #144680 ) ;
#229419=PLANE ( 'NONE',  #237901 ) ;
#229424=VECTOR ( 'NONE', #176345, 1000.000000000000000 ) ;
#229441=EDGE_LOOP ( 'NONE', ( #135209, #162825, #206380, #198062, #119491 ) ) ;
#229457=AXIS2_PLACEMENT_3D ( 'NONE', #256141, #133695, #234073 ) ;
#229496=EDGE_LOOP ( 'NONE', ( #222925, #200894, #5217, #45287 ) ) ;
#229499=CARTESIAN_POINT ( 'NONE',  ( 21.05000000000000071, -8.999999999988842703, -191.1060308773475072 ) ) ;
#229511=DIRECTION ( 'NONE',  ( 0.000000000000000000, 0.000000000000000000, -1.000000000000000000 ) ) ;
#229520=ORIENTED_EDGE ( 'NONE', *, *, #87458, .F. ) ;
#229554=EDGE_CURVE ( 'NONE', #6055, #230164, #111351, .T. ) ;
#229581=FACE_OUTER_BOUND ( 'NONE', #196656, .T. ) ;
#229585=ORIENTED_EDGE ( 'NONE', *, *, #114546, .T. ) ;
#229595=CARTESIAN_POINT ( 'NONE',  ( 20.95224633520496127, 8.900522166568386240, -175.9932764479212324 ) ) ;
#229608=DIRECTION ( 'NONE',  ( -1.000000000000000000, -1.836970198721029934E-16, -0.000000000000000000 ) ) ;
#229625=CYLINDRICAL_SURFACE ( 'NONE', #23359, 11.75000000000001066 ) ;
#229629=DIRECTION ( 'NONE',  ( 1.000000000000000000, 0.000000000000000000, -0.000000000000000000 ) ) ;
#229649=ORIENTED_EDGE ( 'NONE', *, *, #141602, .T. ) ;
#229651=DIRECTION ( 'NONE',  ( -1.000000000000000000, -0.000000000000000000, -0.000000000000000000 ) ) ;
#229689=AXIS2_PLACEMENT_3D ( 'NONE', #24034, #103526, #243052 ) ;
#229691=DIRECTION ( 'NONE',  ( 0.000000000000000000, 0.000000000000000000, -1.000000000000000000 ) ) ;
#229712=CARTESIAN_POINT ( 'NONE',  ( 20.97224591636399538, 10.62515341617478271, -179.7499259046635416 ) ) ;
#229714=ORIENTED_EDGE ( 'NONE', *, *, #222352, .T. ) ;
#229723=CARTESIAN_POINT ( 'NONE',  ( -21.05000000000000071, 1.115600667400684642E-11, -189.2999999999999545 ) ) ;
#229764=ORIENTED_EDGE ( 'NONE', *, *, #234440, .F. ) ;
#229795=FACE_OUTER_BOUND ( 'NONE', #249916, .T. ) ;
#229801=ORIENTED_EDGE ( 'NONE', *, *, #118940, .T. ) ;
#229817=AXIS2_PLACEMENT_3D ( 'NONE', #50925, #228318, #212608 ) ;
#229841=AXIS2_PLACEMENT_3D ( 'NONE', #162224, #98324, #256092 ) ;
#229897=DIRECTION ( 'NONE',  ( 0.000000000000000000, -1.000000000000000000, 0.000000000000000000 ) ) ;
#229907=ADVANCED_FACE ( 'NONE', ( #256708 ), #15707, .T. ) ;
#229945=DIRECTION ( 'NONE',  ( 1.000000000000000000, -0.000000000000000000, -0.000000000000000000 ) ) ;
#229989=FACE_OUTER_BOUND ( 'NONE', #108927, .T. ) ;
#230011=DIRECTION ( 'NONE',  ( -1.000000000000000000, -7.304098846218134667E-16, 0.000000000000000000 ) ) ;
#230039=ADVANCED_FACE ( 'NONE', ( #242324 ), #119739, .T. ) ;
#230049=AXIS2_PLACEMENT_3D ( 'NONE', #110291, #85554, #127296 ) ;
#230052=ORIENTED_EDGE ( 'NONE', *, *, #169629, .F. ) ;
#230081=DIRECTION ( 'NONE',  ( 1.000000000000000000, 0.000000000000000000, 0.000000000000000000 ) ) ;
#230099=FACE_OUTER_BOUND ( 'NONE', #33880, .T. ) ;
#230139=AXIS2_PLACEMENT_3D ( 'NONE', #189222, #229629, #210073 ) ;
#230145=CARTESIAN_POINT ( 'NONE',  ( 20.95512820512820440, 8.876151316299269567, -179.6499999999999773 ) ) ;
#230158=FACE_OUTER_BOUND ( 'NONE', #80370, .T. ) ;
#230164=VERTEX_POINT ( 'NONE', #189735 ) ;
#230176=ORIENTED_EDGE ( 'NONE', *, *, #96959, .T. ) ;
#230186=ORIENTED_EDGE ( 'NONE', *, *, #136692, .F. ) ;
#230187=CIRCLE ( 'NONE', #9421, 6.258578643762724880 ) ;
#230192=AXIS2_PLACEMENT_3D ( 'NONE', #124728, #204246, #245962 ) ;
#230196=LINE ( 'NONE', #148101, #15923 ) ;
#230234=TOROIDAL_SURFACE ( 'NONE', #51140, 2.100000000000002309, 0.1000000000000000056 ) ;
#230299=EDGE_LOOP ( 'NONE', ( #106993, #151416, #46411 ) ) ;
#230342=PLANE ( 'NONE',  #65903 ) ;
#230351=LINE ( 'NONE', #11316, #119726 ) ;
#230395=AXIS2_PLACEMENT_3D ( 'NONE', #196347, #155972, #235466 ) ;
#230420=CARTESIAN_POINT ( 'NONE',  ( 21.05000000000000071, 10.42338541492406279, -174.9920519238700649 ) ) ;
#230452=ORIENTED_EDGE ( 'NONE', *, *, #204028, .T. ) ;
#230505=CARTESIAN_POINT ( 'NONE',  ( 20.94999999999999929, 6.550000000011156231, -179.6499999999999773 ) ) ;
#230534=FACE_OUTER_BOUND ( 'NONE', #159932, .T. ) ;
#230552=AXIS2_PLACEMENT_3D ( 'NONE', #52157, #169604, #75614 ) ;
#230571=DIRECTION ( 'NONE',  ( 0.000000000000000000, 0.000000000000000000, 1.000000000000000000 ) ) ;
#230573=VECTOR ( 'NONE', #131984, 1000.000000000000000 ) ;
#230611=DIRECTION ( 'NONE',  ( 1.000000000000000000, -0.000000000000000000, 0.000000000000000000 ) ) ;
#230614=VECTOR ( 'NONE', #223600, 1000.000000000000000 ) ;
#230659=VECTOR ( 'NONE', #175042, 1000.000000000000000 ) ;
#230725=ORIENTED_EDGE ( 'NONE', *, *, #73864, .F. ) ;
#230802=PLANE ( 'NONE',  #145459 ) ;
#230806=CARTESIAN_POINT ( 'NONE',  ( -22.39999999999999858, 7.790779598384560245, -167.3999999999999773 ) ) ;
#230813=EDGE_CURVE ( 'NONE', #185697, #61007, #111146, .T. ) ;
#230815=EDGE_CURVE ( 'NONE', #34312, #165621, #182727, .T. ) ;
#230818=ORIENTED_EDGE ( 'NONE', *, *, #235370, .F. ) ;
#230837=CARTESIAN_POINT ( 'NONE',  ( 22.45463910399148233, 1.026727559903827787E-11, -155.8504291898206020 ) ) ;
#230851=CARTESIAN_POINT ( 'NONE',  ( -21.05000000000000071, 11.65000000001115055, -174.2838656629781156 ) ) ;
#230855=DIRECTION ( 'NONE',  ( 1.734723475976817507E-14, 0.000000000000000000, -1.000000000000000000 ) ) ;
#230877=CARTESIAN_POINT ( 'NONE',  ( -18.59999999999999787, 7.021664781911246322, -204.8335654018972605 ) ) ;
#230882=EDGE_LOOP ( 'NONE', ( #102723, #208212, #41981, #180328 ) ) ;
#230884=VECTOR ( 'NONE', #206433, 999.9999999999998863 ) ;
#230888=DIRECTION ( 'NONE',  ( 0.000000000000000000, -0.9887567792719341719, -0.1495327102803664099 ) ) ;
#230902=CARTESIAN_POINT ( 'NONE',  ( 20.85000000000000142, 1.115600667400684642E-11, -200.9999999999999432 ) ) ;
#230944=EDGE_CURVE ( 'NONE', #152584, #114560, #15497, .T. ) ;
#230959=ORIENTED_EDGE ( 'NONE', *, *, #194805, .F. ) ;
#231016=EDGE_CURVE ( 'NONE', #29625, #34439, #109481, .T. ) ;
#231017=FACE_OUTER_BOUND ( 'NONE', #257697, .T. ) ;
#231020=LINE ( 'NONE', #32838, #159597 ) ;
#231041=CARTESIAN_POINT ( 'NONE',  ( -22.39999999999999858, 11.75000000001115552, -167.3999999999999773 ) ) ;
#231123=CARTESIAN_POINT ( 'NONE',  ( -18.59999999999999787, -1.162701749926853712, -175.4999999999999716 ) ) ;
#231226=CARTESIAN_POINT ( 'NONE',  ( 20.94999999999999929, 11.65000000001115943, -194.2161343370218560 ) ) ;
#231227=CARTESIAN_POINT ( 'NONE',  ( -23.15000000000000213, 11.75000000001115552, -155.7499999999999716 ) ) ;
#231233=ORIENTED_EDGE ( 'NONE', *, *, #144352, .F. ) ;
#231240=DIRECTION ( 'NONE',  ( 1.000000000000000000, 0.000000000000000000, 0.000000000000000000 ) ) ;
#231247=DIRECTION ( 'NONE',  ( 1.000000000000000000, -7.304098846218134667E-16, 0.000000000000000000 ) ) ;
#231281=CYLINDRICAL_SURFACE ( 'NONE', #22932, 0.5000000000000004441 ) ;
#231283=ORIENTED_EDGE ( 'NONE', *, *, #31925, .T. ) ;
#231304=EDGE_CURVE ( 'NONE', #215838, #41810, #240509, .T. ) ;
#231307=EDGE_CURVE ( 'NONE', #68890, #252758, #82255, .T. ) ;
#231314=VECTOR ( 'NONE', #104148, 1000.000000000000000 ) ;
#231375=ORIENTED_EDGE ( 'NONE', *, *, #30576, .T. ) ;
#231382=ORIENTED_EDGE ( 'NONE', *, *, #46092, .F. ) ;
#231402=FACE_OUTER_BOUND ( 'NONE', #73984, .T. ) ;
#231426=ORIENTED_EDGE ( 'NONE', *, *, #91763, .F. ) ;
#231438=ADVANCED_FACE ( 'NONE', ( #21990 ), #4942, .T. ) ;
#231447=CARTESIAN_POINT ( 'NONE',  ( 21.11345278033245165, 8.882122073382985761, -179.7460221707566745 ) ) ;
#231500=DIRECTION ( 'NONE',  ( 1.000000000000000000, -0.000000000000000000, -0.000000000000000000 ) ) ;
#231512=CARTESIAN_POINT ( 'NONE',  ( -18.44448725179915627, -9.490081715472170387, -207.6289602940624661 ) ) ;
#231520=VERTEX_POINT ( 'NONE', #24564 ) ;
#231531=AXIS2_PLACEMENT_3D ( 'NONE', #205110, #42217, #240413 ) ;
#231533=DIRECTION ( 'NONE',  ( 0.000000000000000000, 0.3738317757009345654, 0.9274965247785492695 ) ) ;
#231545=LINE ( 'NONE', #174175, #165277 ) ;
#231547=VERTEX_POINT ( 'NONE', #11408 ) ;
#231562=CARTESIAN_POINT ( 'NONE',  ( 18.39999999999999858, -9.599999999988845900, -207.7001893912220112 ) ) ;
#231565=VECTOR ( 'NONE', #189622, 1000.000000000000000 ) ;
#231577=EDGE_CURVE ( 'NONE', #42095, #239004, #30995, .T. ) ;
#231620=LINE ( 'NONE', #111656, #155418 ) ;
#231660=ORIENTED_EDGE ( 'NONE', *, *, #122583, .F. ) ;
#231707=CIRCLE ( 'NONE', #248448, 0.09999999999998898659 ) ;
#231730=EDGE_LOOP ( 'NONE', ( #140803, #137210, #1978, #205159 ) ) ;
#231738=ORIENTED_EDGE ( 'NONE', *, *, #126881, .T. ) ;
#231774=EDGE_LOOP ( 'NONE', ( #19305, #215803, #175932, #154359 ) ) ;
#231777=ORIENTED_EDGE ( 'NONE', *, *, #4982, .T. ) ;
#231827=CARTESIAN_POINT ( 'NONE',  ( 21.05000000000000426, -0.01681986837452507932, -161.1925747804345974 ) ) ;
#231846=DIRECTION ( 'NONE',  ( 1.000000000000000000, 0.000000000000000000, 0.000000000000000000 ) ) ;
#231869=CARTESIAN_POINT ( 'NONE',  ( 21.14999999999999858, 11.65000000001116298, -179.6499999999999773 ) ) ;
#231871=ADVANCED_FACE ( 'NONE', ( #116307 ), #193268, .T. ) ;
#231872=VECTOR ( 'NONE', #60436, 1000.000000000000000 ) ;
#231878=DIRECTION ( 'NONE',  ( 1.000000000000000000, -0.000000000000000000, -0.000000000000000000 ) ) ;
#231894=LINE ( 'NONE', #212329, #245065 ) ;
#231905=CIRCLE ( 'NONE', #235581, 0.09999999999999939493 ) ;
#231911=ORIENTED_EDGE ( 'NONE', *, *, #194184, .T. ) ;
#231955=DIRECTION ( 'NONE',  ( 0.000000000000000000, 0.000000000000000000, -1.000000000000000000 ) ) ;
#231962=CARTESIAN_POINT ( 'NONE',  ( -18.39999999999999858, -9.682403433465244902, -207.6568433774127413 ) ) ;
#231970=DIRECTION ( 'NONE',  ( 2.952720810173289112E-16, -1.000000000000000000, 0.000000000000000000 ) ) ;
#231981=CIRCLE ( 'NONE', #248705, 11.80000000000000426 ) ;
#232017=EDGE_LOOP ( 'NONE', ( #52397, #176734 ) ) ;
#232052=ORIENTED_EDGE ( 'NONE', *, *, #33740, .T. ) ;
#232078=EDGE_CURVE ( 'NONE', #13363, #9380, #116180, .T. ) ;
#232095=VERTEX_POINT ( 'NONE', #19778 ) ;
#232141=AXIS2_PLACEMENT_3D ( 'NONE', #38722, #180799, #62134 ) ;
#232176=ADVANCED_FACE ( 'NONE', ( #46999 ), #186915, .F. ) ;
#232196=DIRECTION ( 'NONE',  ( -1.000000000000000000, -0.000000000000000000, 0.000000000000000000 ) ) ;
#232202=AXIS2_PLACEMENT_3D ( 'NONE', #94436, #149307, #73629 ) ;
#232228=ADVANCED_FACE ( 'NONE', ( #103128 ), #108292, .T. ) ;
#232239=CYLINDRICAL_SURFACE ( 'NONE', #94202, 0.09999999999999939493 ) ;
#232247=VERTEX_POINT ( 'NONE', #6608 ) ;
#232257=AXIS2_PLACEMENT_3D ( 'NONE', #222161, #102204, #103506 ) ;
#232345=CARTESIAN_POINT ( 'NONE',  ( -23.25000000000000000, -1.149570369564537842, -208.8159124845019221 ) ) ;
#232351=CARTESIAN_POINT ( 'NONE',  ( 21.46681500598108272, 1.115539681028482333E-11, -160.6424888405743729 ) ) ;
#232358=AXIS2_PLACEMENT_3D ( 'NONE', #66236, #68811, #126192 ) ;
#232371=CIRCLE ( 'NONE', #215758, 0.09999999999998898659 ) ;
#232379=LINE ( 'NONE', #56266, #200768 ) ;
#232380=EDGE_LOOP ( 'NONE', ( #212399, #69003, #63282, #143981 ) ) ;
#232410=ADVANCED_FACE ( 'NONE', ( #22036 ), #158996, .T. ) ;
#232416=CARTESIAN_POINT ( 'NONE',  ( 23.14999999999999858, 4.775700934590591196, -189.1512318959539982 ) ) ;
#232431=VERTEX_POINT ( 'NONE', #235922 ) ;
#232438=FACE_OUTER_BOUND ( 'NONE', #237483, .T. ) ;
#232469=CARTESIAN_POINT ( 'NONE',  ( 18.52928932188133970, 10.27928932189250411, -192.2499999999999716 ) ) ;
#232482=AXIS2_PLACEMENT_3D ( 'NONE', #78667, #139922, #120420 ) ;
#232546=DIRECTION ( 'NONE',  ( 0.000000000000000000, -1.000000000000000000, 0.000000000000000000 ) ) ;
#232551=ORIENTED_EDGE ( 'NONE', *, *, #76044, .T. ) ;
#232553=ORIENTED_EDGE ( 'NONE', *, *, #194858, .T. ) ;
#232559=ORIENTED_EDGE ( 'NONE', *, *, #253274, .F. ) ;
#232563=TOROIDAL_SURFACE ( 'NONE', #119953, 11.65000000000000036, 0.1000000000000000056 ) ;
#232613=CARTESIAN_POINT ( 'NONE',  ( 20.85000000000000142, -11.74999999998883560, -198.0999999999999659 ) ) ;
#232617=CYLINDRICAL_SURFACE ( 'NONE', #240877, 0.09999999999998898659 ) ;
#232626=CARTESIAN_POINT ( 'NONE',  ( 18.59999999999999787, 5.900000000011102586, -177.7190997646563915 ) ) ;
#232667=CARTESIAN_POINT ( 'NONE',  ( 18.49999999999999289, 7.021664781911246322, -204.8335654018972605 ) ) ;
#232683=AXIS2_PLACEMENT_3D ( 'NONE', #56602, #59167, #198716 ) ;
#232686=ADVANCED_FACE ( 'NONE', ( #193942 ), #216110, .T. ) ;
#232721=LINE ( 'NONE', #199709, #99653 ) ;
#232772=CARTESIAN_POINT ( 'NONE',  ( -18.49999999999999645, -9.321008403350157678, -174.7359382490778330 ) ) ;
#232780=DIRECTION ( 'NONE',  ( 0.000000000000000000, 0.000000000000000000, 1.000000000000000000 ) ) ;
#232784=VERTEX_POINT ( 'NONE', #21718 ) ;
#232791=ORIENTED_EDGE ( 'NONE', *, *, #190396, .T. ) ;
#232804=EDGE_CURVE ( 'NONE', #4264, #205992, #74521, .T. ) ;
#232807=DIRECTION ( 'NONE',  ( 0.000000000000000000, 0.000000000000000000, 1.000000000000000000 ) ) ;
#232820=FACE_OUTER_BOUND ( 'NONE', #248171, .T. ) ;
#232848=DIRECTION ( 'NONE',  ( 0.000000000000000000, 1.000000000000000000, 2.891205793294679805E-16 ) ) ;
#232874=CARTESIAN_POINT ( 'NONE',  ( -23.25000000000000000, 11.65000000001115588, -155.7499999999999716 ) ) ;
#232877=ORIENTED_EDGE ( 'NONE', *, *, #34121, .F. ) ;
#232880=ORIENTED_EDGE ( 'NONE', *, *, #398, .T. ) ;
#232882=AXIS2_PLACEMENT_3D ( 'NONE', #138097, #117277, #255442 ) ;
#232887=ORIENTED_EDGE ( 'NONE', *, *, #190036, .F. ) ;
#232936=VERTEX_POINT ( 'NONE', #153246 ) ;
#232942=EDGE_LOOP ( 'NONE', ( #130863, #216801, #8504, #156849 ) ) ;
#232943=DIRECTION ( 'NONE',  ( 0.000000000000000000, -1.000000000000000000, 0.000000000000000000 ) ) ;
#232953=ORIENTED_EDGE ( 'NONE', *, *, #25509, .T. ) ;
#232962=VECTOR ( 'NONE', #173266, 1000.000000000000000 ) ;
#232973=ORIENTED_EDGE ( 'NONE', *, *, #137508, .T. ) ;
#232995=LINE ( 'NONE', #133866, #40909 ) ;
#232998=CARTESIAN_POINT ( 'NONE',  ( 18.49999999999998934, 6.550000000011156231, -188.7499999999999716 ) ) ;
#233013=ORIENTED_EDGE ( 'NONE', *, *, #179698, .T. ) ;
#233019=ORIENTED_EDGE ( 'NONE', *, *, #79639, .F. ) ;
#233040=CARTESIAN_POINT ( 'NONE',  ( 23.15000000000000213, -9.499999999988844479, -191.1060308773475072 ) ) ;
#233043=DIRECTION ( 'NONE',  ( -1.000000000000000000, -0.000000000000000000, -0.000000000000000000 ) ) ;
#233051=DIRECTION ( 'NONE',  ( -1.000000000000000000, -0.000000000000000000, -0.000000000000000000 ) ) ;
#233079=FACE_OUTER_BOUND ( 'NONE', #254184, .T. ) ;
#233094=DIRECTION ( 'NONE',  ( 0.7070776581708965169, 0.000000000000000000, 0.7071359030027827286 ) ) ;
#233112=ORIENTED_EDGE ( 'NONE', *, *, #123477, .F. ) ;
#233115=ADVANCED_FACE ( 'NONE', ( #56635 ), #253577, .F. ) ;
#233124=CARTESIAN_POINT ( 'NONE',  ( -23.25000000000000000, 5.950000000011163692, -190.6942976949651438 ) ) ;
#233178=DIRECTION ( 'NONE',  ( -6.938893903907222856E-15, 1.000000000000000000, 0.000000000000000000 ) ) ;
#233194=AXIS2_PLACEMENT_3D ( 'NONE', #8405, #244429, #226124 ) ;
#233212=VERTEX_POINT ( 'NONE', #85184 ) ;
#233277=ORIENTED_EDGE ( 'NONE', *, *, #136528, .T. ) ;
#233290=DIRECTION ( 'NONE',  ( 0.000000000000000000, 0.000000000000000000, -1.000000000000000000 ) ) ;
#233291=EDGE_LOOP ( 'NONE', ( #189283, #214974, #228450, #233803, #22523, #181844, #888 ) ) ;
#233294=CIRCLE ( 'NONE', #137396, 0.1000000000000000472 ) ;
#233309=EDGE_CURVE ( 'NONE', #154602, #16613, #183347, .T. ) ;
#233313=CIRCLE ( 'NONE', #224890, 0.09999999999999749367 ) ;
#233370=VERTEX_POINT ( 'NONE', #91648 ) ;
#233396=ORIENTED_EDGE ( 'NONE', *, *, #119219, .F. ) ;
#233407=CARTESIAN_POINT ( 'NONE',  ( 22.49999999999999645, 0.04562336060741833954, -155.8494956614523517 ) ) ;
#233421=CYLINDRICAL_SURFACE ( 'NONE', #207886, 0.09999999999999939493 ) ;
#233498=DIRECTION ( 'NONE',  ( -0.000000000000000000, -0.000000000000000000, -1.000000000000000000 ) ) ;
#233504=VECTOR ( 'NONE', #34818, 1000.000000000000227 ) ;
#233517=DIRECTION ( 'NONE',  ( -0.000000000000000000, -0.4791956752371546169, -0.8777080977375152360 ) ) ;
#233558=ORIENTED_EDGE ( 'NONE', *, *, #245504, .F. ) ;
#233564=CARTESIAN_POINT ( 'NONE',  ( 19.97071067811864609, 11.72071067812981404, -192.2499999999999716 ) ) ;
#233566=ADVANCED_FACE ( 'NONE', ( #74694 ), #19508, .T. ) ;
#233574=CARTESIAN_POINT ( 'NONE',  ( 22.49999999999999645, 11.64987090377452184, -167.4174801091270126 ) ) ;
#233576=ORIENTED_EDGE ( 'NONE', *, *, #118348, .T. ) ;
#233603=DIRECTION ( 'NONE',  ( 0.000000000000000000, 1.224646799142185182E-16, 1.000000000000000000 ) ) ;
#233635=ORIENTED_EDGE ( 'NONE', *, *, #87684, .T. ) ;
#233647=FACE_OUTER_BOUND ( 'NONE', #240789, .T. ) ;
#233763=AXIS2_PLACEMENT_3D ( 'NONE', #48612, #245549, #46043 ) ;
#233766=DIRECTION ( 'NONE',  ( 7.304098846218134667E-16, -1.000000000000000000, 0.000000000000000000 ) ) ;
#233770=CARTESIAN_POINT ( 'NONE',  ( -20.85000000000000142, -1.835859311432481045, -212.5044391687984842 ) ) ;
#233803=ORIENTED_EDGE ( 'NONE', *, *, #216870, .T. ) ;
#233835=ORIENTED_EDGE ( 'NONE', *, *, #201806, .T. ) ;
#233845=CIRCLE ( 'NONE', #200522, 0.09999999999999749367 ) ;
#233897=ORIENTED_EDGE ( 'NONE', *, *, #53760, .T. ) ;
#233918=CIRCLE ( 'NONE', #179767, 0.09999999999998898659 ) ;
#233952=DIRECTION ( 'NONE',  ( 0.000000000000000000, 0.01562499999998609446, -0.9998779222360101304 ) ) ;
#233973=EDGE_CURVE ( 'NONE', #31369, #17415, #154518, .T. ) ;
#233980=DIRECTION ( 'NONE',  ( -2.557131231893036985E-16, 0.8660254037844384856, -0.5000000000000002220 ) ) ;
#233982=CARTESIAN_POINT ( 'NONE',  ( -20.94999999999999929, -1.164121893230052995, -208.7148480855715604 ) ) ;
#233990=CARTESIAN_POINT ( 'NONE',  ( 21.40925344232283223, 0.09895018863080314031, -160.8414811406095453 ) ) ;
#233992=DIRECTION ( 'NONE',  ( -1.000000000000000000, 0.000000000000000000, 0.000000000000000000 ) ) ;
#234027=DIRECTION ( 'NONE',  ( 0.000000000000000000, -0.9999631594459056361, -0.008583690987124413183 ) ) ;
#234041=CARTESIAN_POINT ( 'NONE',  ( 20.12500000000000000, 9.750000000011153745, -188.7499999999999716 ) ) ;
#234045=EDGE_LOOP ( 'NONE', ( #56037, #23911, #234134, #30675 ) ) ;
#234053=FACE_OUTER_BOUND ( 'NONE', #204665, .T. ) ;
#234054=CARTESIAN_POINT ( 'NONE',  ( -18.45140287520617761, -9.486077739518407270, -207.6405231266861051 ) ) ;
#234062=DIRECTION ( 'NONE',  ( 1.000000000000000000, 0.000000000000000000, 0.000000000000000000 ) ) ;
#234064=ORIENTED_EDGE ( 'NONE', *, *, #140249, .F. ) ;
#234073=DIRECTION ( 'NONE',  ( 0.000000000000000000, 0.000000000000000000, -1.000000000000000000 ) ) ;
#234076=DIRECTION ( 'NONE',  ( -4.408576920032448588E-17, 0.1350103645451876944, 0.9908441862701601321 ) ) ;
#234109=CARTESIAN_POINT ( 'NONE',  ( 18.49999999999999645, 1.115600667400684642E-11, -200.9999999999999432 ) ) ;
#234134=ORIENTED_EDGE ( 'NONE', *, *, #161923, .F. ) ;
#234142=FACE_OUTER_BOUND ( 'NONE', #175087, .T. ) ;
#234150=CARTESIAN_POINT ( 'NONE',  ( -21.05000000000000071, -11.48912529306489994, -197.9999999999999432 ) ) ;
#234151=DIRECTION ( 'NONE',  ( -1.000000000000000000, 0.000000000000000000, 0.000000000000000000 ) ) ;
#234152=EDGE_CURVE ( 'NONE', #249408, #157570, #192380, .T. ) ;
#234156=CARTESIAN_POINT ( 'NONE',  ( -21.05000000000000426, 6.332272273946816910, -167.5375360632856427 ) ) ;
#234169=CARTESIAN_POINT ( 'NONE',  ( -23.25000000000000000, -9.599999999988838795, -191.1060308773475072 ) ) ;
#234175=VERTEX_POINT ( 'NONE', #13743 ) ;
#234203=ORIENTED_EDGE ( 'NONE', *, *, #93184, .T. ) ;
#234204=VECTOR ( 'NONE', #49486, 1000.000000000000000 ) ;
#234216=ADVANCED_FACE ( 'NONE', ( #138778 ), #245830, .F. ) ;
#234229=CARTESIAN_POINT ( 'NONE',  ( -20.94999999999999929, 11.65000000001115055, -194.2161343370218560 ) ) ;
#234237=ADVANCED_FACE ( 'NONE', ( #35894 ), #21466, .T. ) ;
#234271=ORIENTED_EDGE ( 'NONE', *, *, #181626, .T. ) ;
#234283=ORIENTED_EDGE ( 'NONE', *, *, #126451, .T. ) ;
#234303=AXIS2_PLACEMENT_3D ( 'NONE', #104799, #103534, #61866 ) ;
#234308=ORIENTED_EDGE ( 'NONE', *, *, #45496, .T. ) ;
#234328=CARTESIAN_POINT ( 'NONE',  ( 21.05000000000000071, 0.03201369319884249387, -161.2411572764626158 ) ) ;
#234343=AXIS2_PLACEMENT_3D ( 'NONE', #111489, #94482, #171495 ) ;
#234349=ORIENTED_EDGE ( 'NONE', *, *, #240256, .T. ) ;
#234352=ORIENTED_EDGE ( 'NONE', *, *, #147689, .T. ) ;
#234381=CARTESIAN_POINT ( 'NONE',  ( -20.54999999999999716, 2.000000000011154189, -187.7753780772378889 ) ) ;
#234415=CARTESIAN_POINT ( 'NONE',  ( 23.15000000000000213, -12.41227409413852811, -197.9999999999999432 ) ) ;
#234419=CARTESIAN_POINT ( 'NONE',  ( 21.05000000000000071, 5.000000000011153745, -188.5947339810868755 ) ) ;
#234420=CARTESIAN_POINT ( 'NONE',  ( 18.50016250449482413, 10.29766095125173386, -206.4743663933278697 ) ) ;
#234422=DIRECTION ( 'NONE',  ( 0.000000000000000000, 0.000000000000000000, -1.000000000000000000 ) ) ;
#234425=CYLINDRICAL_SURFACE ( 'NONE', #18650, 0.09999999999998898659 ) ;
#234440=EDGE_CURVE ( 'NONE', #222817, #8158, #121393, .T. ) ;
#234464=FACE_OUTER_BOUND ( 'NONE', #120610, .T. ) ;
#234476=AXIS2_PLACEMENT_3D ( 'NONE', #195122, #176834, #192536 ) ;
#234484=AXIS2_PLACEMENT_3D ( 'NONE', #8787, #145708, #107877 ) ;
#234530=CARTESIAN_POINT ( 'NONE',  ( 18.59999999999999787, -1.835341550213255957, -179.0551512925629538 ) ) ;
#234534=CARTESIAN_POINT ( 'NONE',  ( -20.07928932188135107, 9.220710678129810489, -188.6499999999999488 ) ) ;
#234600=CARTESIAN_POINT ( 'NONE',  ( 21.05000000000000071, 1.115600667400684642E-11, -198.0999999999999659 ) ) ;
#234659=VECTOR ( 'NONE', #133255, 1000.000000000000000 ) ;
#234738=CYLINDRICAL_SURFACE ( 'NONE', #8876, 12.87499999999999822 ) ;
#234759=CARTESIAN_POINT ( 'NONE',  ( 23.14999999999999503, 11.65000000001116298, -193.9851942293460070 ) ) ;
#234763=AXIS2_PLACEMENT_3D ( 'NONE', #191239, #253730, #12596 ) ;
#234784=VERTEX_POINT ( 'NONE', #128946 ) ;
#234799=AXIS2_PLACEMENT_3D ( 'NONE', #19616, #177425, #134390 ) ;
#234822=DIRECTION ( 'NONE',  ( 0.000000000000000000, 0.000000000000000000, -1.000000000000000000 ) ) ;
#234835=AXIS2_PLACEMENT_3D ( 'NONE', #59810, #58536, #156412 ) ;
#234843=EDGE_CURVE ( 'NONE', #143156, #191501, #254755, .T. ) ;
#234885=EDGE_LOOP ( 'NONE', ( #39691, #64623, #53922, #159969 ) ) ;
#234897=VERTEX_POINT ( 'NONE', #123181 ) ;
#234902=VERTEX_POINT ( 'NONE', #159739 ) ;
#234906=CARTESIAN_POINT ( 'NONE',  ( 22.00356870070926973, 7.976845382617315661E-12, -160.2457576382639672 ) ) ;
#234911=DIRECTION ( 'NONE',  ( 0.000000000000000000, 0.000000000000000000, 1.000000000000000000 ) ) ;
#234936=CARTESIAN_POINT ( 'NONE',  ( -20.54999999999999716, 7.150000000011155876, -179.8499999999999943 ) ) ;
#234939=CARTESIAN_POINT ( 'NONE',  ( -18.59999999999999787, -1.835859311432481045, -212.5044391687984842 ) ) ;
#234966=DIRECTION ( 'NONE',  ( 0.000000000000000000, -0.01283462868042125823, -0.9999176327611367654 ) ) ;
#235001=PLANE ( 'NONE',  #157049 ) ;
#235012=CARTESIAN_POINT ( 'NONE',  ( 21.14999999999999858, 1.115600667400684642E-11, -160.9593430482987344 ) ) ;
#235014=LINE ( 'NONE', #112506, #165219 ) ;
#235015=AXIS2_PLACEMENT_3D ( 'NONE', #221651, #222943, #144690 ) ;
#235021=CARTESIAN_POINT ( 'NONE',  ( 19.96984138294323330, 11.75000000001115197, -192.2245720712021466 ) ) ;
#235032=TOROIDAL_SURFACE ( 'NONE', #205985, 0.2000000000000000111, 0.1000000000000000056 ) ;
#235068=DIRECTION ( 'NONE',  ( -0.000000000000000000, 0.000000000000000000, -1.000000000000000000 ) ) ;
#235082=CIRCLE ( 'NONE', #164343, 0.09999999999999911737 ) ;
#235084=CARTESIAN_POINT ( 'NONE',  ( -21.07928932188134041, 6.328516656404449492, -167.4011048543455615 ) ) ;
#235141=DIRECTION ( 'NONE',  ( -1.000000000000000000, 0.000000000000000000, 0.000000000000000000 ) ) ;
#235143=DIRECTION ( 'NONE',  ( 0.000000000000000000, -0.1350103645451876944, -0.9908441862701601321 ) ) ;
#235158=ADVANCED_FACE ( 'NONE', ( #135994 ), #17362, .T. ) ;
#235179=ORIENTED_EDGE ( 'NONE', *, *, #223452, .T. ) ;
#235182=ORIENTED_EDGE ( 'NONE', *, *, #158046, .T. ) ;
#235193=AXIS2_PLACEMENT_3D ( 'NONE', #181439, #141022, #82286 ) ;
#235213=VERTEX_POINT ( 'NONE', #155620 ) ;
#235250=CARTESIAN_POINT ( 'NONE',  ( 20.94999675878240808, 10.29307482169071264, -206.4586421466940180 ) ) ;
#235261=DIRECTION ( 'NONE',  ( -1.000000000000000000, -0.000000000000000000, -0.000000000000000000 ) ) ;
#235272=AXIS2_PLACEMENT_3D ( 'NONE', #2594, #100400, #104253 ) ;
#235315=ORIENTED_EDGE ( 'NONE', *, *, #89789, .T. ) ;
#235325=DIRECTION ( 'NONE',  ( 1.000000000000000000, 0.000000000000000000, 0.000000000000000000 ) ) ;
#235327=AXIS2_PLACEMENT_3D ( 'NONE', #207629, #131921, #108504 ) ;
#235333=CARTESIAN_POINT ( 'NONE',  ( -18.39999999999999858, -9.499999999988849808, -207.6001893912220169 ) ) ;
#235358=DIRECTION ( 'NONE',  ( 0.000000000000000000, -0.9908441862701782288, 0.1350103645450542456 ) ) ;
#235368=LINE ( 'NONE', #112869, #125988 ) ;
#235370=EDGE_CURVE ( 'NONE', #154991, #95624, #66981, .T. ) ;
#235376=EDGE_LOOP ( 'NONE', ( #132667, #212087, #122413, #164351, #59547, #254856, #61802, #123577, #119808, #49784, #156905, #195765 ) ) ;
#235452=AXIS2_PLACEMENT_3D ( 'NONE', #24000, #145194, #66952 ) ;
#235466=DIRECTION ( 'NONE',  ( 0.000000000000000000, 0.000000000000000000, 1.000000000000000000 ) ) ;
#235498=VERTEX_POINT ( 'NONE', #112307 ) ;
#235502=LINE ( 'NONE', #193829, #243664 ) ;
#235507=ORIENTED_EDGE ( 'NONE', *, *, #35591, .T. ) ;
#235514=CARTESIAN_POINT ( 'NONE',  ( -20.94999999999999929, 11.63687328911530727, -194.1782407866749622 ) ) ;
#235553=ORIENTED_EDGE ( 'NONE', *, *, #6834, .T. ) ;
#235581=AXIS2_PLACEMENT_3D ( 'NONE', #187559, #209665, #250077 ) ;
#235602=DIRECTION ( 'NONE',  ( -1.000000000000000000, 0.000000000000000000, 0.000000000000000000 ) ) ;
#235652=DIRECTION ( 'NONE',  ( 1.000000000000000000, 2.952720810173289112E-16, -0.000000000000000000 ) ) ;
#235655=DIRECTION ( 'NONE',  ( 1.000000000000000000, 0.000000000000000000, -0.000000000000000000 ) ) ;
#235688=AXIS2_PLACEMENT_3D ( 'NONE', #218024, #79796, #57674 ) ;
#235703=DIRECTION ( 'NONE',  ( 1.000000000000000000, 1.734723475976817507E-14, 0.000000000000000000 ) ) ;
#235716=VECTOR ( 'NONE', #88563, 1000.000000000000000 ) ;
#235741=EDGE_LOOP ( 'NONE', ( #57071, #165985, #222714, #103729 ) ) ;
#235762=CIRCLE ( 'NONE', #56666, 0.4000000000000114575 ) ;
#235768=EDGE_LOOP ( 'NONE', ( #90431, #222567, #3869, #27122 ) ) ;
#235824=DIRECTION ( 'NONE',  ( 1.000000000000000000, -0.000000000000000000, -0.000000000000000000 ) ) ;
#235833=EDGE_CURVE ( 'NONE', #199092, #157944, #5147, .T. ) ;
#235838=CARTESIAN_POINT ( 'NONE',  ( -21.08134388332232589, 0.07581891751813138458, -161.1653194194820173 ) ) ;
#235852=EDGE_LOOP ( 'NONE', ( #229714, #184071, #73604 ) ) ;
#235876=DIRECTION ( 'NONE',  ( 0.000000000000000000, 0.4999999999999478195, 0.8660254037844686836 ) ) ;
#235887=FACE_OUTER_BOUND ( 'NONE', #155787, .T. ) ;
#235894=CARTESIAN_POINT ( 'NONE',  ( 23.14999999999999858, 5.950000000011160139, -190.6942976949651438 ) ) ;
#235899=CARTESIAN_POINT ( 'NONE',  ( -18.50000000000000000, 3.912899247244609580, -178.9818229730109351 ) ) ;
#235907=AXIS2_PLACEMENT_3D ( 'NONE', #5615, #163443, #137764 ) ;
#235922=CARTESIAN_POINT ( 'NONE',  ( 21.05000000000000071, -8.663551401857999323, -191.4758988819326646 ) ) ;
#235923=DIRECTION ( 'NONE',  ( 0.000000000000000000, 0.000000000000000000, -1.000000000000000000 ) ) ;
#236008=CARTESIAN_POINT ( 'NONE',  ( 22.57320508075688537, 11.65000000001115588, -167.4999999999999716 ) ) ;
#236011=CARTESIAN_POINT ( 'NONE',  ( -18.59999999999999787, 10.33248238083634440, -206.5948465439131496 ) ) ;
#236025=CYLINDRICAL_SURFACE ( 'NONE', #12041, 0.09999999999998898659 ) ;
#236054=DIRECTION ( 'NONE',  ( 0.000000000000000000, 0.8660254037844309360, -0.5000000000000134337 ) ) ;
#236055=CARTESIAN_POINT ( 'NONE',  ( -18.59999999999999787, 1.115600667400684642E-11, -167.4999999999999716 ) ) ;
#236085=EDGE_LOOP ( 'NONE', ( #234349, #187091 ) ) ;
#236118=DIRECTION ( 'NONE',  ( 1.000000000000000000, 0.000000000000000000, 0.000000000000000000 ) ) ;
#236119=VECTOR ( 'NONE', #72150, 1000.000000000000000 ) ;
#236122=VECTOR ( 'NONE', #108064, 1000.000000000000000 ) ;
#236125=EDGE_CURVE ( 'NONE', #48866, #103901, #1695, .T. ) ;
#236130=DIRECTION ( 'NONE',  ( -0.000000000000000000, 0.000000000000000000, -1.000000000000000000 ) ) ;
#236172=ORIENTED_EDGE ( 'NONE', *, *, #146154, .F. ) ;
#236195=CYLINDRICAL_SURFACE ( 'NONE', #220230, 0.09999999999999939493 ) ;
#236199=CARTESIAN_POINT ( 'NONE',  ( 18.49999999999999289, 11.75000000001115907, -175.5999999999999659 ) ) ;
#236210=CARTESIAN_POINT ( 'NONE',  ( -18.50000000000000000, 9.350000000011156942, -188.8499999999999659 ) ) ;
#236230=EDGE_CURVE ( 'NONE', #63249, #192876, #90808, .T. ) ;
#236236=EDGE_LOOP ( 'NONE', ( #165678, #229224, #241966, #216877 ) ) ;
#236246=DIRECTION ( 'NONE',  ( -1.000000000000000000, 0.000000000000000000, 0.000000000000000000 ) ) ;
#236250=LINE ( 'NONE', #162838, #56301 ) ;
#236253=FACE_OUTER_BOUND ( 'NONE', #54895, .T. ) ;
#236263=LINE ( 'NONE', #213, #195521 ) ;
#236285=EDGE_CURVE ( 'NONE', #147926, #107466, #193260, .T. ) ;
#236300=ORIENTED_EDGE ( 'NONE', *, *, #96847, .F. ) ;
#236321=DIRECTION ( 'NONE',  ( -0.000000000000000000, 1.000000000000000000, -0.000000000000000000 ) ) ;
#236354=ORIENTED_EDGE ( 'NONE', *, *, #44584, .T. ) ;
#236381=DIRECTION ( 'NONE',  ( -1.000000000000000000, -0.000000000000000000, -0.000000000000000000 ) ) ;
#236406=VERTEX_POINT ( 'NONE', #672 ) ;
#236416=DIRECTION ( 'NONE',  ( 0.000000000000000000, 0.000000000000000000, 1.000000000000000000 ) ) ;
#236423=CARTESIAN_POINT ( 'NONE',  ( 21.05000000000000071, -8.999999999988844479, -177.3939691226524076 ) ) ;
#236446=DIRECTION ( 'NONE',  ( 0.000000000000000000, 0.000000000000000000, -1.000000000000000000 ) ) ;
#236488=ORIENTED_EDGE ( 'NONE', *, *, #79639, .T. ) ;
#236496=ORIENTED_EDGE ( 'NONE', *, *, #4873, .F. ) ;
#236504=ADVANCED_FACE ( 'NONE', ( #206302 ), #240603, .F. ) ;
#236516=AXIS2_PLACEMENT_3D ( 'NONE', #91726, #81129, #219364 ) ;
#236527=PRODUCT_DEFINITION ( 'UNKNOWN', '', #252954, #222571 ) ;
#236528=CARTESIAN_POINT ( 'NONE',  ( 20.94403535211772294, 10.30632246271647467, -206.5041836778895288 ) ) ;
#236534=CARTESIAN_POINT ( 'NONE',  ( -18.50016250449483479, 10.29766095125276415, -206.4743663933275855 ) ) ;
#236540=ORIENTED_EDGE ( 'NONE', *, *, #24385, .F. ) ;
#236553=DIRECTION ( 'NONE',  ( -1.000000000000000000, 0.000000000000000000, 0.000000000000000000 ) ) ;
#236574=DIRECTION ( 'NONE',  ( -1.000000000000000000, -7.304098846218134667E-16, 0.000000000000000000 ) ) ;
#236581=CYLINDRICAL_SURFACE ( 'NONE', #59111, 0.09999999999999939493 ) ;
#236598=VERTEX_POINT ( 'NONE', #113615 ) ;
#236612=AXIS2_PLACEMENT_3D ( 'NONE', #245330, #86215, #66690 ) ;
#236615=CARTESIAN_POINT ( 'NONE',  ( 20.94999999999999929, -9.399999999988844834, -191.1060308773475072 ) ) ;
#236633=CYLINDRICAL_SURFACE ( 'NONE', #221893, 11.75000000000001066 ) ;
#236639=CARTESIAN_POINT ( 'NONE',  ( 21.05000000000000071, 6.650000000011155876, -177.5170271704400022 ) ) ;
#236654=ADVANCED_FACE ( 'NONE', ( #17107, #96590 ), #255645, .F. ) ;
#236656=AXIS2_PLACEMENT_3D ( 'NONE', #44286, #168121, #243755 ) ;
#236687=B_SPLINE_CURVE_WITH_KNOTS ( 'NONE', 3,
 ( #3801, #44222, #166762, #104162, #183729, #83302, #2495 ),
 .UNSPECIFIED., .F., .F.,
 ( 4, 3, 4 ),
 ( 0.000000000000000000, 3.357501770814691602E-05, 5.199112466349472097E-05 ),
 .UNSPECIFIED. ) ;
#236701=FACE_OUTER_BOUND ( 'NONE', #3440, .T. ) ;
#236730=CIRCLE ( 'NONE', #103454, 0.1000000000000002554 ) ;
#236753=ORIENTED_EDGE ( 'NONE', *, *, #88180, .F. ) ;
#236755=ORIENTED_EDGE ( 'NONE', *, *, #109633, .T. ) ;
#236763=AXIS2_PLACEMENT_3D ( 'NONE', #21640, #22943, #102413 ) ;
#236799=ORIENTED_EDGE ( 'NONE', *, *, #21293, .T. ) ;
#236809=DIRECTION ( 'NONE',  ( -1.000000000000000000, 0.000000000000000000, 0.000000000000000000 ) ) ;
#236810=AXIS2_PLACEMENT_3D ( 'NONE', #46764, #185010, #24679 ) ;
#236825=EDGE_LOOP ( 'NONE', ( #229585, #187319, #132808, #252185 ) ) ;
#236849=CARTESIAN_POINT ( 'NONE',  ( -23.25000000000000000, 1.115600667400684642E-11, -167.4999999999999716 ) ) ;
#236853=VERTEX_POINT ( 'NONE', #169477 ) ;
#236886=VERTEX_POINT ( 'NONE', #183860 ) ;
#236902=CARTESIAN_POINT ( 'NONE',  ( 23.14999999999999503, 6.450000000011156587, -179.8499999999999943 ) ) ;
#236912=EDGE_CURVE ( 'NONE', #150045, #222817, #146008, .T. ) ;
#236950=AXIS2_PLACEMENT_3D ( 'NONE', #104430, #21100, #120210 ) ;
#236967=VERTEX_POINT ( 'NONE', #234534 ) ;
#236974=CIRCLE ( 'NONE', #91236, 0.09999999999998898659 ) ;
#237004=AXIS2_PLACEMENT_3D ( 'NONE', #213580, #105138, #124762 ) ;
#237007=DIRECTION ( 'NONE',  ( 1.000000000000000000, -0.000000000000000000, -0.000000000000000000 ) ) ;
#237027=DIRECTION ( 'NONE',  ( 0.000000000000000000, 1.000000000000000000, 0.000000000000000000 ) ) ;
#237038=VERTEX_POINT ( 'NONE', #192858 ) ;
#237047=DIRECTION ( 'NONE',  ( 1.000000000000000000, 0.000000000000000000, 0.000000000000000000 ) ) ;
#237075=CIRCLE ( 'NONE', #253623, 7.899999999999990585 ) ;
#237107=ORIENTED_EDGE ( 'NONE', *, *, #161238, .F. ) ;
#237192=DIRECTION ( 'NONE',  ( 1.000000000000000000, 2.952720810173289112E-16, -0.000000000000000000 ) ) ;
#237208=DIRECTION ( 'NONE',  ( 0.000000000000000000, 0.000000000000000000, -1.000000000000000000 ) ) ;
#237224=FACE_OUTER_BOUND ( 'NONE', #211478, .T. ) ;
#237228=VERTEX_POINT ( 'NONE', #158877 ) ;
#237235=EDGE_CURVE ( 'NONE', #232247, #86058, #31345, .T. ) ;
#237251=CYLINDRICAL_SURFACE ( 'NONE', #33548, 0.09999999999999939493 ) ;
#237255=EDGE_CURVE ( 'NONE', #64290, #223354, #61023, .T. ) ;
#237299=EDGE_LOOP ( 'NONE', ( #142593, #199809, #75849, #246283 ) ) ;
#237301=ORIENTED_EDGE ( 'NONE', *, *, #215420, .F. ) ;
#237340=ORIENTED_EDGE ( 'NONE', *, *, #90668, .F. ) ;
#237355=ORIENTED_EDGE ( 'NONE', *, *, #76171, .T. ) ;
#237360=DIRECTION ( 'NONE',  ( 0.000000000000000000, 1.598721155460228258E-14, -1.000000000000000000 ) ) ;
#237378=DIRECTION ( 'NONE',  ( 1.000000000000000000, -0.000000000000000000, -0.000000000000000000 ) ) ;
#237411=CARTESIAN_POINT ( 'NONE',  ( 19.97071067811864609, 11.72071067812981404, -192.1499999999999488 ) ) ;
#237428=CIRCLE ( 'NONE', #224749, 0.09999999999999892308 ) ;
#237454=DIRECTION ( 'NONE',  ( 0.000000000000000000, 0.000000000000000000, 1.000000000000000000 ) ) ;
#237475=ORIENTED_EDGE ( 'NONE', *, *, #20288, .F. ) ;
#237483=EDGE_LOOP ( 'NONE', ( #31319, #211500, #126621, #37836 ) ) ;
#237487=EDGE_LOOP ( 'NONE', ( #65989, #121708, #239286, #15093 ) ) ;
#237544=DIRECTION ( 'NONE',  ( 0.000000000000000000, 0.000000000000000000, 1.000000000000000000 ) ) ;
#237550=CARTESIAN_POINT ( 'NONE',  ( -23.25000000000000000, 7.021664781911246322, -204.8335654018972605 ) ) ;
#237558=DIRECTION ( 'NONE',  ( -0.000000000000000000, 0.8660254037844383745, -0.5000000000000003331 ) ) ;
#237561=CARTESIAN_POINT ( 'NONE',  ( 18.46905048506371472, -9.473744257371233601, -207.6759862922554021 ) ) ;
#237578=CARTESIAN_POINT ( 'NONE',  ( 21.10257677756356998, 0.02495074957913955352, -161.1016182574672655 ) ) ;
#237685=ORIENTED_EDGE ( 'NONE', *, *, #115781, .T. ) ;
#237715=CARTESIAN_POINT ( 'NONE',  ( 21.05000000000000071, 1.115600667400684642E-11, -205.0999999999999375 ) ) ;
#237751=ORIENTED_EDGE ( 'NONE', *, *, #232804, .T. ) ;
#237754=EDGE_CURVE ( 'NONE', #73463, #121293, #81510, .T. ) ;
#237807=AXIS2_PLACEMENT_3D ( 'NONE', #178629, #181185, #238568 ) ;
#237846=CARTESIAN_POINT ( 'NONE',  ( -23.25000000000000000, -8.999999999988844479, -191.1060308773475356 ) ) ;
#237874=CYLINDRICAL_SURFACE ( 'NONE', #153468, 0.09999999999998898659 ) ;
#237901=AXIS2_PLACEMENT_3D ( 'NONE', #151171, #209860, #31257 ) ;
#237902=CARTESIAN_POINT ( 'NONE',  ( 21.08489247129320887, 8.877675190881227252, -179.8500000000000227 ) ) ;
#237908=ADVANCED_FACE ( 'NONE', ( #25038 ), #208792, .F. ) ;
#237914=DIRECTION ( 'NONE',  ( 1.000000000000000000, 0.000000000000000000, 0.000000000000000000 ) ) ;
#237931=DIRECTION ( 'NONE',  ( 0.000000000000000000, 0.000000000000000000, -1.000000000000000000 ) ) ;
#237957=EDGE_LOOP ( 'NONE', ( #71560, #228613, #111809, #224320 ) ) ;
#238012=EDGE_CURVE ( 'NONE', #187086, #115342, #56625, .T. ) ;
#238017=EDGE_LOOP ( 'NONE', ( #186787, #193893, #95240, #228805 ) ) ;
#238028=DIRECTION ( 'NONE',  ( -0.7071067811865475727, -0.7071067811865475727, 0.000000000000000000 ) ) ;
#238061=ORIENTED_EDGE ( 'NONE', *, *, #42030, .T. ) ;
#238072=EDGE_LOOP ( 'NONE', ( #167103, #41753, #59106 ) ) ;
#238079=EDGE_CURVE ( 'NONE', #178529, #178867, #156777, .T. ) ;
#238080=CARTESIAN_POINT ( 'NONE',  ( -20.96428641294188111, 11.75000000001171863, -194.1748931779392535 ) ) ;
#238144=DIRECTION ( 'NONE',  ( 0.000000000000000000, 0.4999999999999478195, -0.8660254037844686836 ) ) ;
#238160=DIRECTION ( 'NONE',  ( 0.000000000000000000, 1.000000000000000000, 0.000000000000000000 ) ) ;
#238175=DIRECTION ( 'NONE',  ( 0.000000000000000000, 1.000000000000000000, 1.224646799147353207E-16 ) ) ;
#238181=ORIENTED_EDGE ( 'NONE', *, *, #53311, .F. ) ;
#238200=EDGE_LOOP ( 'NONE', ( #136385, #78670, #34858, #179327 ) ) ;
#238295=EDGE_CURVE ( 'NONE', #147404, #22985, #112528, .T. ) ;
#238307=CARTESIAN_POINT ( 'NONE',  ( 20.04142135623730070, 11.75000000001115907, -192.1499999999999488 ) ) ;
#238329=AXIS2_PLACEMENT_3D ( 'NONE', #95832, #37190, #18881 ) ;
#238337=ORIENTED_EDGE ( 'NONE', *, *, #42330, .F. ) ;
#238373=EDGE_CURVE ( 'NONE', #205992, #15539, #106849, .T. ) ;
#238384=ADVANCED_FACE ( 'NONE', ( #52532 ), #119334, .F. ) ;
#238388=ORIENTED_EDGE ( 'NONE', *, *, #40302, .F. ) ;
#238406=DIRECTION ( 'NONE',  ( 0.000000000000000000, 0.000000000000000000, -1.000000000000000000 ) ) ;
#238407=VERTEX_POINT ( 'NONE', #257111 ) ;
#238413=VERTEX_POINT ( 'NONE', #215462 ) ;
#238416=CARTESIAN_POINT ( 'NONE',  ( -21.09316766718153247, 0.03926340232583241247, -161.1298466875252586 ) ) ;
#238430=EDGE_CURVE ( 'NONE', #190383, #36747, #181876, .T. ) ;
#238432=DIRECTION ( 'NONE',  ( 0.000000000000000000, -0.8777080977375715243, 0.4791956752370512551 ) ) ;
#238436=CYLINDRICAL_SURFACE ( 'NONE', #201721, 0.09999999999999939493 ) ;
#238469=ORIENTED_EDGE ( 'NONE', *, *, #152203, .F. ) ;
#238503=EDGE_LOOP ( 'NONE', ( #31799, #6818, #185595, #171765, #166497, #251545, #160457, #225153, #34324, #254955, #123924 ) ) ;
#238513=CARTESIAN_POINT ( 'NONE',  ( 18.59999999999999076, -1.835859311432481045, -212.6044391687984785 ) ) ;
#238548=DIRECTION ( 'NONE',  ( 0.000000000000000000, 0.000000000000000000, 1.000000000000000000 ) ) ;
#238568=DIRECTION ( 'NONE',  ( -1.000000000000000000, 0.000000000000000000, 0.000000000000000000 ) ) ;
#238575=DIRECTION ( 'NONE',  ( -3.265361837132813093E-16, 1.000000000000000000, 0.000000000000000000 ) ) ;
#238579=CONICAL_SURFACE ( 'NONE', #126132, 4.049999999999998046, 0.7853981633974604915 ) ;
#238593=CARTESIAN_POINT ( 'NONE',  ( -21.14999999999999858, -0.09999999998884338825, -155.8504291924551808 ) ) ;
#238639=ORIENTED_EDGE ( 'NONE', *, *, #76201, .T. ) ;
#238657=CARTESIAN_POINT ( 'NONE',  ( -18.59999999999999787, 11.75000000001115197, -188.8499999999999659 ) ) ;
#238680=CIRCLE ( 'NONE', #34681, 4.000000000000003553 ) ;
#238716=ADVANCED_FACE ( 'NONE', ( #69253 ), #207000, .T. ) ;
#238738=CIRCLE ( 'NONE', #205575, 0.09999999999998898659 ) ;
#238799=CARTESIAN_POINT ( 'NONE',  ( 20.85000000000000142, 1.115600667400684642E-11, -200.9999999999999432 ) ) ;
#238812=CARTESIAN_POINT ( 'NONE',  ( -21.05000000000000071, -11.64999999998884306, -197.9999999999999432 ) ) ;
#238837=CARTESIAN_POINT ( 'NONE',  ( 20.94999999999999574, -11.48912529306490349, -170.3999999999999773 ) ) ;
#238844=AXIS2_PLACEMENT_3D ( 'NONE', #216470, #233498, #134354 ) ;
#238893=EDGE_CURVE ( 'NONE', #29024, #178529, #57130, .T. ) ;
#238894=AXIS2_PLACEMENT_3D ( 'NONE', #162917, #28570, #66360 ) ;
#238936=ADVANCED_FACE ( 'NONE', ( #53524 ), #157807, .F. ) ;
#238938=FACE_OUTER_BOUND ( 'NONE', #190565, .T. ) ;
#238945=DIRECTION ( 'NONE',  ( 1.000000000000000000, 0.000000000000000000, 0.000000000000000000 ) ) ;
#238978=ORIENTED_EDGE ( 'NONE', *, *, #52839, .T. ) ;
#238996=ORIENTED_EDGE ( 'NONE', *, *, #95931, .T. ) ;
#239004=VERTEX_POINT ( 'NONE', #100325 ) ;
#239044=FACE_OUTER_BOUND ( 'NONE', #212728, .T. ) ;
#239060=AXIS2_PLACEMENT_3D ( 'NONE', #82103, #162974, #122560 ) ;
#239065=VECTOR ( 'NONE', #230011, 1000.000000000000000 ) ;
#239082=VERTEX_POINT ( 'NONE', #186318 ) ;
#239085=VERTEX_POINT ( 'NONE', #147178 ) ;
#239108=ORIENTED_EDGE ( 'NONE', *, *, #25915, .T. ) ;
#239124=ORIENTED_EDGE ( 'NONE', *, *, #177611, .F. ) ;
#239148=ORIENTED_EDGE ( 'NONE', *, *, #67282, .F. ) ;
#239156=SURFACE_STYLE_FILL_AREA ( #80036 ) ;
#239193=DIRECTION ( 'NONE',  ( 1.000000000000000000, 0.000000000000000000, 0.000000000000000000 ) ) ;
#239196=AXIS2_PLACEMENT_3D ( 'NONE', #148176, #223849, #165180 ) ;
#239212=ORIENTED_EDGE ( 'NONE', *, *, #95844, .T. ) ;
#239216=SPHERICAL_SURFACE ( 'NONE', #112738, 0.1000000000000000056 ) ;
#239233=CARTESIAN_POINT ( 'NONE',  ( 20.95420533658165141, 10.54586447477073285, -175.0675060206932017 ) ) ;
#239254=CARTESIAN_POINT ( 'NONE',  ( 18.39999999999999858, -9.499999999988842703, -174.5320693966996259 ) ) ;
#239286=ORIENTED_EDGE ( 'NONE', *, *, #194858, .F. ) ;
#239305=ORIENTED_EDGE ( 'NONE', *, *, #173448, .T. ) ;
#239340=ORIENTED_EDGE ( 'NONE', *, *, #65461, .F. ) ;
#239391=EDGE_CURVE ( 'NONE', #91171, #207624, #142992, .T. ) ;
#239400=EDGE_CURVE ( 'NONE', #7699, #108752, #163876, .T. ) ;
#239411=ORIENTED_EDGE ( 'NONE', *, *, #3589, .T. ) ;
#239419=CIRCLE ( 'NONE', #197706, 0.09999999999999939493 ) ;
#239429=DIRECTION ( 'NONE',  ( -1.000000000000000000, 0.000000000000000000, 0.000000000000000000 ) ) ;
#239477=AXIS2_PLACEMENT_3D ( 'NONE', #69821, #91920, #176308 ) ;
#239508=CIRCLE ( 'NONE', #202091, 0.5000000000000004441 ) ;
#239543=ORIENTED_EDGE ( 'NONE', *, *, #81113, .T. ) ;
#239558=CARTESIAN_POINT ( 'NONE',  ( -22.59999999999999787, 0.1000000000111554016, -155.8504291924551808 ) ) ;
#239562=DIRECTION ( 'NONE',  ( 0.000000000000000000, 0.000000000000000000, 1.000000000000000000 ) ) ;
#239572=ADVANCED_FACE ( 'NONE', ( #176413 ), #120314, .F. ) ;
#239605=AXIS2_PLACEMENT_3D ( 'NONE', #138649, #156990, #20042 ) ;
#239606=DIRECTION ( 'NONE',  ( -1.000000000000000000, -0.000000000000000000, -0.000000000000000000 ) ) ;
#239668=AXIS2_PLACEMENT_3D ( 'NONE', #187538, #169274, #109245 ) ;
#239678=DIRECTION ( 'NONE',  ( 1.000000000000000000, 0.000000000000000000, 0.000000000000000000 ) ) ;
#239680=DIRECTION ( 'NONE',  ( -1.836970198721029934E-16, 1.000000000000000000, 0.000000000000000000 ) ) ;
#239690=DIRECTION ( 'NONE',  ( 0.000000000000000000, 0.9998779222360102414, 0.01562499999996356907 ) ) ;
#239700=DIRECTION ( 'NONE',  ( 1.000000000000000000, -0.000000000000000000, -0.000000000000000000 ) ) ;
#239703=EDGE_CURVE ( 'NONE', #82701, #169886, #5422, .T. ) ;
#239734=CIRCLE ( 'NONE', #14897, 0.5000000000000004441 ) ;
#239736=ORIENTED_EDGE ( 'NONE', *, *, #48184, .T. ) ;
#239806=CARTESIAN_POINT ( 'NONE',  ( -18.50000000000000000, -9.399999999988850163, -207.8820418481726335 ) ) ;
#239828=CARTESIAN_POINT ( 'NONE',  ( 18.59999999999999787, -1.835341550213255957, -179.0551512925629538 ) ) ;
#239841=EDGE_CURVE ( 'NONE', #123700, #125534, #86387, .T. ) ;
#239847=DIRECTION ( 'NONE',  ( 1.000000000000000000, 0.000000000000000000, 0.000000000000000000 ) ) ;
#239850=CIRCLE ( 'NONE', #123315, 0.1000000000000001027 ) ;
#239899=DIRECTION ( 'NONE',  ( 1.000000000000000000, -0.000000000000000000, -0.000000000000000000 ) ) ;
#239922=CARTESIAN_POINT ( 'NONE',  ( -20.54999999999999716, 1.115625160336667635E-11, -202.9999999999999716 ) ) ;
#239934=ORIENTED_EDGE ( 'NONE', *, *, #77872, .F. ) ;
#239951=AXIS2_PLACEMENT_3D ( 'NONE', #136737, #18081, #118492 ) ;
#239958=CARTESIAN_POINT ( 'NONE',  ( 20.94999999999999574, 10.47338541492405994, -175.0786544642485012 ) ) ;
#240023=ORIENTED_EDGE ( 'NONE', *, *, #45863, .T. ) ;
#240062=CARTESIAN_POINT ( 'NONE',  ( 20.46382478191415188, 10.59862044130854031, -175.1778144693454635 ) ) ;
#240075=DIRECTION ( 'NONE',  ( 0.000000000000000000, 0.000000000000000000, -1.000000000000000000 ) ) ;
#240087=TOROIDAL_SURFACE ( 'NONE', #90207, 0.2000000000000000111, 0.1000000000000000056 ) ;
#240120=PLANE ( 'NONE',  #210853 ) ;
#240146=AXIS2_PLACEMENT_3D ( 'NONE', #167387, #227327, #29175 ) ;
#240222=EDGE_CURVE ( 'NONE', #196293, #249408, #110662, .T. ) ;
#240228=EDGE_LOOP ( 'NONE', ( #211104, #8826, #87010, #15629 ) ) ;
#240232=AXIS2_PLACEMENT_3D ( 'NONE', #171285, #92970, #194679 ) ;
#240233=ADVANCED_FACE ( 'NONE', ( #205904 ), #89799, .F. ) ;
#240256=EDGE_CURVE ( 'NONE', #61925, #14880, #169791, .T. ) ;
#240261=CARTESIAN_POINT ( 'NONE',  ( -23.25000000000000000, -11.64999999998884483, -197.8999999999999773 ) ) ;
#240266=DIRECTION ( 'NONE',  ( 0.000000000000000000, 0.000000000000000000, 1.000000000000000000 ) ) ;
#240268=DIRECTION ( 'NONE',  ( 1.000000000000000000, 0.000000000000000000, -0.000000000000000000 ) ) ;
#240284=ORIENTED_EDGE ( 'NONE', *, *, #195970, .F. ) ;
#240292=EDGE_LOOP ( 'NONE', ( #149842, #143740, #220665, #225260 ) ) ;
#240293=AXIS2_PLACEMENT_3D ( 'NONE', #25216, #86420, #126867 ) ;
#240334=CIRCLE ( 'NONE', #165309, 3.899999999999999467 ) ;
#240346=VECTOR ( 'NONE', #10970, 1000.000000000000000 ) ;
#240365=DIRECTION ( 'NONE',  ( 1.224646799147353207E-16, 1.000000000000000000, 0.000000000000000000 ) ) ;
#240407=CARTESIAN_POINT ( 'NONE',  ( -18.50000972452446035, 10.29326151435326508, -206.4592822510414578 ) ) ;
#240413=DIRECTION ( 'NONE',  ( 1.000000000000000000, 0.000000000000000000, 0.000000000000000000 ) ) ;
#240446=AXIS2_PLACEMENT_3D ( 'NONE', #19965, #179056, #156921 ) ;
#240467=DIRECTION ( 'NONE',  ( 0.000000000000000000, -1.000000000000000000, 0.000000000000000000 ) ) ;
#240487=EDGE_CURVE ( 'NONE', #14558, #67305, #139181, .T. ) ;
#240509=CIRCLE ( 'NONE', #248893, 0.1000000000000008937 ) ;
#240531=ORIENTED_EDGE ( 'NONE', *, *, #59714, .F. ) ;
#240558=ADVANCED_FACE ( 'NONE', ( #163912 ), #124789, .F. ) ;
#240603=SPHERICAL_SURFACE ( 'NONE', #210014, 0.1000000000000000056 ) ;
#240631=EDGE_CURVE ( 'NONE', #57292, #44391, #98990, .T. ) ;
#240632=CARTESIAN_POINT ( 'NONE',  ( -22.59999999999999787, 0.1008583691098682150, -155.7504328765105868 ) ) ;
#240649=ORIENTED_EDGE ( 'NONE', *, *, #43838, .T. ) ;
#240653=LINE ( 'NONE', #101088, #144103 ) ;
#240658=CARTESIAN_POINT ( 'NONE',  ( -21.14999999999999858, 11.75000000001115552, -174.2838656629781156 ) ) ;
#240748=EDGE_CURVE ( 'NONE', #238413, #20839, #58056, .T. ) ;
#240755=DIRECTION ( 'NONE',  ( 0.9880948137434723000, 0.1538461538461484146, -0.000000000000000000 ) ) ;
#240761=LINE ( 'NONE', #178240, #187878 ) ;
#240762=DIRECTION ( 'NONE',  ( 1.000000000000000000, 0.000000000000000000, 0.000000000000000000 ) ) ;
#240765=LINE ( 'NONE', #85487, #64889 ) ;
#240788=DIRECTION ( 'NONE',  ( -1.000000000000000000, -0.000000000000000000, 0.000000000000000000 ) ) ;
#240789=EDGE_LOOP ( 'NONE', ( #175565, #212517, #68758, #69732 ) ) ;
#240793=FACE_OUTER_BOUND ( 'NONE', #162661, .T. ) ;
#240799=ORIENTED_EDGE ( 'NONE', *, *, #209469, .T. ) ;
#240803=EDGE_CURVE ( 'NONE', #12339, #152450, #193743, .T. ) ;
#240826=DIRECTION ( 'NONE',  ( 1.000000000000000000, -0.000000000000000000, -0.000000000000000000 ) ) ;
#240834=AXIS2_PLACEMENT_3D ( 'NONE', #16901, #177277, #235923 ) ;
#240866=ORIENTED_EDGE ( 'NONE', *, *, #161398, .F. ) ;
#240868=AXIS2_PLACEMENT_3D ( 'NONE', #22435, #103206, #39439 ) ;
#240877=AXIS2_PLACEMENT_3D ( 'NONE', #50093, #72244, #35706 ) ;
#240890=CARTESIAN_POINT ( 'NONE',  ( 21.05000000000000071, -11.64999999998883595, -167.4999999999999432 ) ) ;
#240892=LINE ( 'NONE', #158810, #173506 ) ;
#240895=DIRECTION ( 'NONE',  ( 0.000000000000000000, 0.000000000000000000, 1.000000000000000000 ) ) ;
#240929=EDGE_CURVE ( 'NONE', #182355, #219709, #91013, .T. ) ;
#240939=CARTESIAN_POINT ( 'NONE',  ( -23.25000000000000000, 1.115600667400684642E-11, -200.9999999999999432 ) ) ;
#240946=ADVANCED_FACE ( 'NONE', ( #219710 ), #121921, .F. ) ;
#240950=ORIENTED_EDGE ( 'NONE', *, *, #87684, .F. ) ;
#240963=EDGE_CURVE ( 'NONE', #172274, #133, #120085, .T. ) ;
#240981=ORIENTED_EDGE ( 'NONE', *, *, #220135, .T. ) ;
#240983=ORIENTED_EDGE ( 'NONE', *, *, #49033, .F. ) ;
#241012=DIRECTION ( 'NONE',  ( 0.000000000000000000, 1.000000000000000000, 0.000000000000000000 ) ) ;
#241016=CYLINDRICAL_SURFACE ( 'NONE', #118799, 0.09999999999999939493 ) ;
#241018=AXIS2_PLACEMENT_3D ( 'NONE', #127231, #168968, #170258 ) ;
#241033=EDGE_CURVE ( 'NONE', #122253, #48993, #65878, .T. ) ;
#241058=LINE ( 'NONE', #221449, #13555 ) ;
#241059=CARTESIAN_POINT ( 'NONE',  ( -20.64999999999999858, 4.350000000011156054, -188.6499999999999488 ) ) ;
#241072=EDGE_CURVE ( 'NONE', #148316, #177021, #207554, .T. ) ;
#241080=AXIS2_PLACEMENT_3D ( 'NONE', #58935, #199791, #198477 ) ;
#241109=CARTESIAN_POINT ( 'NONE',  ( -20.94999999999999929, 1.115600667400684642E-11, -167.4999999999999716 ) ) ;
#241133=CARTESIAN_POINT ( 'NONE',  ( -21.05000000000000071, -11.39257802169451672, -170.5739495798319183 ) ) ;
#241221=ORIENTED_EDGE ( 'NONE', *, *, #26455, .T. ) ;
#241231=DIRECTION ( 'NONE',  ( 0.000000000000000000, 0.000000000000000000, -1.000000000000000000 ) ) ;
#241253=DIRECTION ( 'NONE',  ( 0.7071067811865388020, -0.7071067811865561215, 0.000000000000000000 ) ) ;
#241267=VECTOR ( 'NONE', #72072, 1000.000000000000000 ) ;
#241282=VECTOR ( 'NONE', #196242, 1000.000000000000000 ) ;
#241320=CARTESIAN_POINT ( 'NONE',  ( 22.37643362114956247, 7.625789993969535274, -167.4009186263185995 ) ) ;
#241322=CARTESIAN_POINT ( 'NONE',  ( 19.99999999999998934, 11.75000000001115552, -188.8499999999999659 ) ) ;
#241345=DIRECTION ( 'NONE',  ( 0.000000000000000000, 1.000000000000000000, 0.000000000000000000 ) ) ;
#241372=AXIS2_PLACEMENT_3D ( 'NONE', #60852, #38746, #37470 ) ;
#241389=CARTESIAN_POINT ( 'NONE',  ( 20.94999999999999929, 11.65000000001115943, -194.2161343370218560 ) ) ;
#241464=AXIS2_PLACEMENT_3D ( 'NONE', #183880, #49506, #27415 ) ;
#241473=FACE_OUTER_BOUND ( 'NONE', #119481, .T. ) ;
#241490=AXIS2_PLACEMENT_3D ( 'NONE', #165637, #88622, #10408 ) ;
#241493=EDGE_LOOP ( 'NONE', ( #146356, #226203, #121147, #29783 ) ) ;
#241515=DIRECTION ( 'NONE',  ( 0.000000000000000000, 0.000000000000000000, 1.000000000000000000 ) ) ;
#241526=CYLINDRICAL_SURFACE ( 'NONE', #159992, 0.09999999999998898659 ) ;
#241540=AXIS2_PLACEMENT_3D ( 'NONE', #178199, #93494, #16548 ) ;
#241562=ORIENTED_EDGE ( 'NONE', *, *, #78955, .T. ) ;
#241567=EDGE_LOOP ( 'NONE', ( #153654, #14768, #72427, #118728 ) ) ;
#241572=ADVANCED_FACE ( 'NONE', ( #240793 ), #101561, .T. ) ;
#241582=ORIENTED_EDGE ( 'NONE', *, *, #107064, .T. ) ;
#241606=CIRCLE ( 'NONE', #204170, 0.5000000000000004441 ) ;
#241630=DIRECTION ( 'NONE',  ( 0.000000000000000000, -0.8660254037844383745, 0.5000000000000003331 ) ) ;
#241683=DIRECTION ( 'NONE',  ( 0.000000000000000000, -0.3738317757009345654, 0.9274965247785492695 ) ) ;
#241684=LINE ( 'NONE', #139990, #71469 ) ;
#241741=FACE_OUTER_BOUND ( 'NONE', #73176, .T. ) ;
#241749=DIRECTION ( 'NONE',  ( 0.000000000000000000, 0.000000000000000000, -1.000000000000000000 ) ) ;
#241774=AXIS2_PLACEMENT_3D ( 'NONE', #135024, #193746, #72529 ) ;
#241785=CIRCLE ( 'NONE', #62734, 0.09999999999998898659 ) ;
#241794=SURFACE_STYLE_FILL_AREA ( #162280 ) ;
#241798=CARTESIAN_POINT ( 'NONE',  ( 20.95462737510932882, 10.55678195165489441, -175.0699500565622486 ) ) ;
#241803=DIRECTION ( 'NONE',  ( 1.000000000000000000, 0.000000000000000000, 0.000000000000000000 ) ) ;
#241818=EDGE_CURVE ( 'NONE', #36019, #219709, #216341, .T. ) ;
#241838=AXIS2_PLACEMENT_3D ( 'NONE', #204802, #220541, #60160 ) ;
#241848=EDGE_CURVE ( 'NONE', #78009, #66095, #157884, .T. ) ;
#241874=VERTEX_POINT ( 'NONE', #129548 ) ;
#241875=AXIS2_PLACEMENT_3D ( 'NONE', #57295, #155172, #56003 ) ;
#241883=EDGE_CURVE ( 'NONE', #199092, #135643, #91384, .T. ) ;
#241906=TOROIDAL_SURFACE ( 'NONE', #129507, 0.2000000000000000111, 0.1000000000000000056 ) ;
#241919=CARTESIAN_POINT ( 'NONE',  ( 18.49999999999999645, -1.835859311432484375, -212.5044391687984842 ) ) ;
#241931=ORIENTED_EDGE ( 'NONE', *, *, #72732, .F. ) ;
#241935=EDGE_CURVE ( 'NONE', #252199, #140280, #95470, .T. ) ;
#241959=AXIS2_PLACEMENT_3D ( 'NONE', #57978, #234062, #119275 ) ;
#241963=EDGE_CURVE ( 'NONE', #87080, #236598, #138493, .T. ) ;
#241964=TOROIDAL_SURFACE ( 'NONE', #137330, 0.2000000000000000111, 0.1000000000000000056 ) ;
#241965=AXIS2_PLACEMENT_3D ( 'NONE', #226164, #123256, #224902 ) ;
#241966=ORIENTED_EDGE ( 'NONE', *, *, #167142, .T. ) ;
#241994=CARTESIAN_POINT ( 'NONE',  ( 21.05000000000000071, -8.999999999988842703, -191.6060308773475072 ) ) ;
#242026=VECTOR ( 'NONE', #119737, 999.9999999999998863 ) ;
#242107=ORIENTED_EDGE ( 'NONE', *, *, #47782, .T. ) ;
#242128=CARTESIAN_POINT ( 'NONE',  ( 21.14999999999999858, 11.65000000001115943, -179.6499999999999773 ) ) ;
#242139=VERTEX_POINT ( 'NONE', #225737 ) ;
#242193=EDGE_CURVE ( 'NONE', #195524, #141132, #79053, .T. ) ;
#242197=CARTESIAN_POINT ( 'NONE',  ( 23.14999999999998792, 11.65000000001115588, -167.4999999999999716 ) ) ;
#242211=DIRECTION ( 'NONE',  ( 0.000000000000000000, 0.000000000000000000, -1.000000000000000000 ) ) ;
#242218=ORIENTED_EDGE ( 'NONE', *, *, #182721, .T. ) ;
#242220=DIRECTION ( 'NONE',  ( 1.000000000000000000, -0.000000000000000000, -0.000000000000000000 ) ) ;
#242250=CIRCLE ( 'NONE', #25782, 0.5000000000000004441 ) ;
#242262=CARTESIAN_POINT ( 'NONE',  ( 21.14999999999999858, 6.650000000011155876, -179.7499999999999716 ) ) ;
#242283=VERTEX_POINT ( 'NONE', #53548 ) ;
#242287=VERTEX_POINT ( 'NONE', #212634 ) ;
#242324=FACE_OUTER_BOUND ( 'NONE', #248939, .T. ) ;
#242330=CARTESIAN_POINT ( 'NONE',  ( 18.41832399655381280, -9.682403266662619856, -207.6568436200278143 ) ) ;
#242343=CARTESIAN_POINT ( 'NONE',  ( -21.14999999999999858, 11.65000000001115232, -167.4999999999999716 ) ) ;
#242361=CARTESIAN_POINT ( 'NONE',  ( -18.59999999999999787, -1.851617760457748618, -212.6031897196036198 ) ) ;
#242401=DIRECTION ( 'NONE',  ( 0.000000000000000000, 0.000000000000000000, -1.000000000000000000 ) ) ;
#242425=AXIS2_PLACEMENT_3D ( 'NONE', #121565, #143652, #1564 ) ;
#242458=DIRECTION ( 'NONE',  ( -2.252264143451594314E-15, -0.1298341882520124002, -0.9915357197604841577 ) ) ;
#242475=ORIENTED_EDGE ( 'NONE', *, *, #5209, .T. ) ;
#242489=VECTOR ( 'NONE', #126617, 1000.000000000000000 ) ;
#242498=TOROIDAL_SURFACE ( 'NONE', #46667, 0.2000000000000000111, 0.1000000000000000056 ) ;
#242499=ADVANCED_FACE ( 'NONE', ( #157829 ), #96498, .F. ) ;
#242505=EDGE_CURVE ( 'NONE', #215603, #175396, #122520, .T. ) ;
#242515=CARTESIAN_POINT ( 'NONE',  ( -20.15000000000000568, 9.291421356248463326, -179.8499999999999943 ) ) ;
#242524=AXIS2_PLACEMENT_3D ( 'NONE', #216813, #38207, #117721 ) ;
#242533=CARTESIAN_POINT ( 'NONE',  ( -21.33487959338958362, 6.725558151922345296, -167.4999999999999716 ) ) ;
#242538=CARTESIAN_POINT ( 'NONE',  ( -20.94999999999999929, 1.115600667400684642E-11, -200.9999999999999432 ) ) ;
#242560=ORIENTED_EDGE ( 'NONE', *, *, #202681, .F. ) ;
#242588=CARTESIAN_POINT ( 'NONE',  ( -21.05000000000000071, -0.08579911626282435422, -161.0860211185119795 ) ) ;
#242603=ADVANCED_FACE ( 'NONE', ( #84614 ), #46799, .F. ) ;
#242643=ADVANCED_FACE ( 'NONE', ( #32427 ), #29250, .F. ) ;
#242648=DIRECTION ( 'NONE',  ( -1.000000000000000000, -0.000000000000000000, -0.000000000000000000 ) ) ;
#242653=CIRCLE ( 'NONE', #255057, 0.09999999999999939493 ) ;
#242668=DIRECTION ( 'NONE',  ( 1.000000000000000000, 0.000000000000000000, 0.000000000000000000 ) ) ;
#242683=VECTOR ( 'NONE', #219134, 1000.000000000000000 ) ;
#242688=FACE_OUTER_BOUND ( 'NONE', #156744, .T. ) ;
#242723=DIRECTION ( 'NONE',  ( 0.000000000000000000, 0.000000000000000000, 1.000000000000000000 ) ) ;
#242758=DIRECTION ( 'NONE',  ( 1.000000000000000000, -0.000000000000000000, -0.000000000000000000 ) ) ;
#242783=ORIENTED_EDGE ( 'NONE', *, *, #6458, .T. ) ;
#242811=FACE_OUTER_BOUND ( 'NONE', #100176, .T. ) ;
#242829=FACE_OUTER_BOUND ( 'NONE', #73051, .T. ) ;
#242848=CARTESIAN_POINT ( 'NONE',  ( 21.08489834409762054, 10.62232389474667293, -179.8499999999999943 ) ) ;
#242886=ORIENTED_EDGE ( 'NONE', *, *, #38695, .F. ) ;
#242931=DIRECTION ( 'NONE',  ( 1.000000000000000000, 0.000000000000000000, 0.000000000000000000 ) ) ;
#242966=CARTESIAN_POINT ( 'NONE',  ( -22.48660254037843487, 11.65000000001115588, -167.4499999999999886 ) ) ;
#243000=DIRECTION ( 'NONE',  ( 0.000000000000000000, 0.000000000000000000, 1.000000000000000000 ) ) ;
#243009=CARTESIAN_POINT ( 'NONE',  ( -18.59999999999999787, -1.263275465206102233, -208.9018646667463770 ) ) ;
#243044=CARTESIAN_POINT ( 'NONE',  ( 21.13920837816993270, 8.783247050131068434, -179.7499999999999716 ) ) ;
#243052=DIRECTION ( 'NONE',  ( 0.000000000000000000, -1.000000000000000000, 0.000000000000000000 ) ) ;
#243053=DIRECTION ( 'NONE',  ( 0.000000000000000000, 0.000000000000000000, -1.000000000000000000 ) ) ;
#243056=CARTESIAN_POINT ( 'NONE',  ( 21.05193202509564898, 10.72393601970834354, -179.6725346033257154 ) ) ;
#243061=DIRECTION ( 'NONE',  ( 0.000000000000000000, 0.1298341882520022972, 0.9915357197604853789 ) ) ;
#243080=DIRECTION ( 'NONE',  ( -1.000000000000000000, 9.012599976028471648E-15, 6.882867235861662930E-14 ) ) ;
#243084=CARTESIAN_POINT ( 'NONE',  ( 18.53317502108576420, 10.32263460347359718, -206.5605957968671760 ) ) ;
#243119=ORIENTED_EDGE ( 'NONE', *, *, #241935, .F. ) ;
#243140=AXIS2_PLACEMENT_3D ( 'NONE', #210587, #233992, #252265 ) ;
#243166=EDGE_CURVE ( 'NONE', #226840, #5761, #4600, .T. ) ;
#243191=VERTEX_POINT ( 'NONE', #11234 ) ;
#243259=CARTESIAN_POINT ( 'NONE',  ( -23.25000000000000000, 4.350000000011156054, -179.6499999999999773 ) ) ;
#243270=ORIENTED_EDGE ( 'NONE', *, *, #36871, .F. ) ;
#243273=DIRECTION ( 'NONE',  ( 1.000000000000000000, 0.000000000000000000, -0.000000000000000000 ) ) ;
#243282=ORIENTED_EDGE ( 'NONE', *, *, #144941, .T. ) ;
#243293=AXIS2_PLACEMENT_3D ( 'NONE', #39205, #194424, #56153 ) ;
#243386=AXIS2_PLACEMENT_3D ( 'NONE', #85460, #142879, #64649 ) ;
#243436=DIRECTION ( 'NONE',  ( 1.000000000000000000, -0.000000000000000000, -0.000000000000000000 ) ) ;
#243489=ORIENTED_EDGE ( 'NONE', *, *, #5843, .F. ) ;
#243514=CARTESIAN_POINT ( 'NONE',  ( -2.995603634470891112E-16, -11.74999999998884448, -188.7499999999999716 ) ) ;
#243522=ORIENTED_EDGE ( 'NONE', *, *, #225000, .F. ) ;
#243542=CIRCLE ( 'NONE', #118485, 0.09999999999999892308 ) ;
#243565=CARTESIAN_POINT ( 'NONE',  ( 18.59999999999999432, -1.135018845899022466, -208.7169768834322952 ) ) ;
#243590=ORIENTED_EDGE ( 'NONE', *, *, #197371, .F. ) ;
#243591=SPHERICAL_SURFACE ( 'NONE', #196827, 0.1000000000000000056 ) ;
#243628=CYLINDRICAL_SURFACE ( 'NONE', #51017, 0.09999999999999939493 ) ;
#243647=DIRECTION ( 'NONE',  ( 1.000000000000000000, 2.952720810173289112E-16, -0.000000000000000000 ) ) ;
#243664=VECTOR ( 'NONE', #115558, 1000.000000000000000 ) ;
#243695=CARTESIAN_POINT ( 'NONE',  ( -21.14999999999999858, 1.115600667400684642E-11, -161.2414213562372538 ) ) ;
#243698=TOROIDAL_SURFACE ( 'NONE', #106291, 0.9750000000000019762, 0.1000000000000000056 ) ;
#243720=DIRECTION ( 'NONE',  ( -1.000000000000000000, 0.000000000000000000, 0.000000000000000000 ) ) ;
#243726=CARTESIAN_POINT ( 'NONE',  ( 22.39999999999999503, 1.115600667400684642E-11, -155.8504291924551808 ) ) ;
#243754=CIRCLE ( 'NONE', #239668, 0.09999999999998898659 ) ;
#243755=DIRECTION ( 'NONE',  ( 0.000000000000000000, 0.000000000000000000, -1.000000000000000000 ) ) ;
#243797=CARTESIAN_POINT ( 'NONE',  ( 21.04116576186311605, 10.62466307876251292, -179.8285817686277426 ) ) ;
#243834=EDGE_CURVE ( 'NONE', #66095, #164666, #117241, .T. ) ;
#243837=B_SPLINE_CURVE_WITH_KNOTS ( 'NONE', 3,
 ( #150865, #173046, #110451, #251234, #229127, #174334, #73931, #111745, #109156, #188706, #53045, #10072, #152181, #191315, #34804, #75209 ),
 .UNSPECIFIED., .F., .F.,
 ( 4, 3, 3, 3, 3, 4 ),
 ( 0.000000000000000000, 2.209075297430758666E-05, 5.594258369009633163E-05, 8.979524372342017908E-05, 0.0001236472815274585488, 0.0001574990747609553653 ),
 .UNSPECIFIED. ) ;
#243881=ORIENTED_EDGE ( 'NONE', *, *, #62410, .F. ) ;
#243898=LINE ( 'NONE', #24886, #206981 ) ;
#243941=ADVANCED_FACE ( 'NONE', ( #119680 ), #97500, .T. ) ;
#243942=CARTESIAN_POINT ( 'NONE',  ( -20.85000000000000142, -1.164121893230052995, -208.8148480855715832 ) ) ;
#243944=ADVANCED_FACE ( 'NONE', ( #136646 ), #58936, .T. ) ;
#243997=ORIENTED_EDGE ( 'NONE', *, *, #251396, .F. ) ;
#244002=FACE_OUTER_BOUND ( 'NONE', #211463, .T. ) ;
#244013=DIRECTION ( 'NONE',  ( 1.000000000000000000, 0.000000000000000000, 0.000000000000000000 ) ) ;
#244037=ORIENTED_EDGE ( 'NONE', *, *, #45863, .F. ) ;
#244067=VECTOR ( 'NONE', #178159, 1000.000000000000000 ) ;
#244109=CARTESIAN_POINT ( 'NONE',  ( -18.50000000000000000, -9.480686695267820596, -207.9411151687577899 ) ) ;
#244158=AXIS2_PLACEMENT_3D ( 'NONE', #12882, #140483, #178371 ) ;
#244172=ORIENTED_EDGE ( 'NONE', *, *, #153689, .T. ) ;
#244191=ORIENTED_EDGE ( 'NONE', *, *, #249823, .F. ) ;
#244243=FACE_OUTER_BOUND ( 'NONE', #36703, .T. ) ;
#244259=ORIENTED_EDGE ( 'NONE', *, *, #147446, .F. ) ;
#244301=CARTESIAN_POINT ( 'NONE',  ( -20.54999999999999716, -11.74999999998884626, -179.8499999999999943 ) ) ;
#244325=DIRECTION ( 'NONE',  ( 0.000000000000000000, -4.163336342344333240E-14, -1.000000000000000000 ) ) ;
#244331=EDGE_CURVE ( 'NONE', #239085, #231547, #254950, .T. ) ;
#244334=ORIENTED_EDGE ( 'NONE', *, *, #35591, .F. ) ;
#244335=DIRECTION ( 'NONE',  ( 0.000000000000000000, -0.1568667991644714932, 0.9876197685951274563 ) ) ;
#244353=CARTESIAN_POINT ( 'NONE',  ( 18.46921299892753510, -9.509378177812612520, -174.4865787093704341 ) ) ;
#244355=( BOUNDED_SURFACE ( )  B_SPLINE_SURFACE ( 3, 2, ( 
 ( #234229, #116861, #156012 ),
 ( #235514, #238080, #175571 ),
 ( #55564, #253785, #73918 ),
 ( #157299, #17740, #15209 ),
 ( #137683, #56849, #115572 ),
 ( #59415, #255022, #196389 ) ),
 .UNSPECIFIED., .F., .F., .F. ) 
 B_SPLINE_SURFACE_WITH_KNOTS ( ( 4, 2, 4 ),
 ( 3, 3 ),
 ( 1.570796326794897668, 2.356194490192346169, 3.141592653589794448 ),
 ( 0.000000000000000000, 1.000000000000000000 ),
 .UNSPECIFIED. ) 
 GEOMETRIC_REPRESENTATION_ITEM ( )  RATIONAL_B_SPLINE_SURFACE ( (
 ( 1.000000000000000000, 0.7071067811865475727, 1.000000000000000000),
 ( 1.000000000000000000, 0.6611148371756124797, 1.000000000000000000),
 ( 1.000000000000000000, 0.6092287576726203024, 1.000000000000000000),
 ( 1.000000000000000000, 0.5278258667029250839, 1.000000000000000000),
 ( 1.000000000000000000, 0.4993418825354254964, 1.000000000000000000),
 ( 1.000000000000000000, 0.5000000000000260902, 1.000000000000000000) ) ) 
 REPRESENTATION_ITEM ( '' )  SURFACE ( )  );
#244381=DIRECTION ( 'NONE',  ( 1.000000000000000000, 0.000000000000000000, 0.000000000000000000 ) ) ;
#244387=CIRCLE ( 'NONE', #227818, 0.4000000000000114575 ) ;
#244408=VECTOR ( 'NONE', #164444, 1000.000000000000000 ) ;
#244410=CIRCLE ( 'NONE', #198622, 0.1999999999999987899 ) ;
#244429=DIRECTION ( 'NONE',  ( 1.000000000000000000, 0.000000000000000000, -0.000000000000000000 ) ) ;
#244434=DIRECTION ( 'NONE',  ( 0.000000000000000000, -1.000000000000000000, 0.000000000000000000 ) ) ;
#244464=ORIENTED_EDGE ( 'NONE', *, *, #249621, .F. ) ;
#244467=AXIS2_PLACEMENT_3D ( 'NONE', #160527, #38013, #77106 ) ;
#244469=ADVANCED_FACE ( 'NONE', ( #196317 ), #176784, .T. ) ;
#244472=CARTESIAN_POINT ( 'NONE',  ( -18.50000000000000000, 9.250000000011157297, -188.8499999999999659 ) ) ;
#244547=EDGE_CURVE ( 'NONE', #7750, #202760, #184227, .T. ) ;
#244571=EDGE_LOOP ( 'NONE', ( #234064, #211568, #85032, #119269 ) ) ;
#244577=ADVANCED_FACE ( 'NONE', ( #164906 ), #124503, .F. ) ;
#244617=VERTEX_POINT ( 'NONE', #149214 ) ;
#244622=CARTESIAN_POINT ( 'NONE',  ( -20.94788355080263997, 10.30207779525983547, -206.4895520716781903 ) ) ;
#244636=DIRECTION ( 'NONE',  ( 1.000000000000000000, 0.000000000000000000, 0.000000000000000000 ) ) ;
#244643=AXIS2_PLACEMENT_3D ( 'NONE', #186151, #60092, #101763 ) ;
#244658=DIRECTION ( 'NONE',  ( 0.000000000000000000, 0.000000000000000000, -1.000000000000000000 ) ) ;
#244663=DIRECTION ( 'NONE',  ( -1.000000000000000000, 0.000000000000000000, 0.000000000000000000 ) ) ;
#244680=EDGE_CURVE ( 'NONE', #34439, #135650, #90491, .T. ) ;
#244721=CARTESIAN_POINT ( 'NONE',  ( 18.59999999999999432, -1.261786168553869603, -175.5864989635454378 ) ) ;
#244727=CARTESIAN_POINT ( 'NONE',  ( 20.74897398619109268, 10.59569302167756888, -175.1793114562568974 ) ) ;
#244729=CARTESIAN_POINT ( 'NONE',  ( -23.25000000000000000, -8.999999999988844479, -191.1060308773475356 ) ) ;
#244830=AXIS2_PLACEMENT_3D ( 'NONE', #175606, #217259, #159897 ) ;
#244858=CARTESIAN_POINT ( 'NONE',  ( 18.39999999999999858, -9.399999999988843058, -155.7499999999999716 ) ) ;
#244898=CARTESIAN_POINT ( 'NONE',  ( 18.39999999999999858, -9.499999999988844479, -207.9221498493303670 ) ) ;
#244943=CARTESIAN_POINT ( 'NONE',  ( 23.14999999999999858, 5.000000000011153745, -188.5947339810868755 ) ) ;
#244944=EDGE_CURVE ( 'NONE', #114560, #178866, #101651, .T. ) ;
#244963=CARTESIAN_POINT ( 'NONE',  ( -20.54999999999999716, 7.250000000011155521, -179.7499999999999716 ) ) ;
#244990=ORIENTED_EDGE ( 'NONE', *, *, #109633, .F. ) ;
#245005=LINE ( 'NONE', #66373, #256197 ) ;
#245018=CARTESIAN_POINT ( 'NONE',  ( -20.54999999999999716, 7.150000000011155876, -184.2499999999999716 ) ) ;
#245045=EDGE_CURVE ( 'NONE', #102805, #118647, #153336, .T. ) ;
#245061=CARTESIAN_POINT ( 'NONE',  ( 21.05000000000000071, -0.09999999998884338825, -160.9593430482987344 ) ) ;
#245065=VECTOR ( 'NONE', #209746, 1000.000000000000000 ) ;
#245080=FACE_OUTER_BOUND ( 'NONE', #134944, .T. ) ;
#245123=ORIENTED_EDGE ( 'NONE', *, *, #68389, .F. ) ;
#245143=CARTESIAN_POINT ( 'NONE',  ( -22.39999999999999858, 1.115488181425289271E-11, -155.8504291924551808 ) ) ;
#245149=ORIENTED_EDGE ( 'NONE', *, *, #45510, .F. ) ;
#245151=EDGE_CURVE ( 'NONE', #64290, #205292, #185075, .T. ) ;
#245161=ORIENTED_EDGE ( 'NONE', *, *, #54687, .F. ) ;
#245168=ORIENTED_EDGE ( 'NONE', *, *, #100979, .T. ) ;
#245176=ADVANCED_FACE ( 'NONE', ( #231017 ), #208227, .T. ) ;
#245181=AXIS2_PLACEMENT_3D ( 'NONE', #91121, #111985, #191540 ) ;
#245213=DIRECTION ( 'NONE',  ( 0.000000000000000000, 0.000000000000000000, -1.000000000000000000 ) ) ;
#245215=DIRECTION ( 'NONE',  ( 0.000000000000000000, 4.336808689942494997E-15, -1.000000000000000000 ) ) ;
#245226=CYLINDRICAL_SURFACE ( 'NONE', #228081, 0.09999999999998898659 ) ;
#245244=DIRECTION ( 'NONE',  ( 1.000000000000000000, 0.000000000000000000, 0.000000000000000000 ) ) ;
#245247=CARTESIAN_POINT ( 'NONE',  ( -20.00857864376270001, 9.150000000011157653, -188.6499999999999488 ) ) ;
#245251=EDGE_LOOP ( 'NONE', ( #88846, #106364, #49892, #108238 ) ) ;
#245264=CARTESIAN_POINT ( 'NONE',  ( -20.94999999999999929, 11.75000000001120171, -174.3416006898970636 ) ) ;
#245271=DIRECTION ( 'NONE',  ( 2.952720810173289112E-16, -1.000000000000000000, 0.000000000000000000 ) ) ;
#245278=CARTESIAN_POINT ( 'NONE',  ( 18.49999999999999645, 1.835341550235567887, -179.0551512925629538 ) ) ;
#245304=CYLINDRICAL_SURFACE ( 'NONE', #163289, 0.09999999999998898659 ) ;
#245309=VERTEX_POINT ( 'NONE', #149755 ) ;
#245312=DIRECTION ( 'NONE',  ( 0.000000000000000000, -0.8777080977375715243, 0.4791956752370512551 ) ) ;
#245319=DIRECTION ( 'NONE',  ( 0.000000000000000000, 0.000000000000000000, -1.000000000000000000 ) ) ;
#245325=DIRECTION ( 'NONE',  ( 0.000000000000000000, 0.000000000000000000, 1.000000000000000000 ) ) ;
#245326=DIRECTION ( 'NONE',  ( 1.000000000000000000, 0.000000000000000000, 0.000000000000000000 ) ) ;
#245330=CARTESIAN_POINT ( 'NONE',  ( 23.14999999999999503, 11.65000000001116298, -193.9851942293460070 ) ) ;
#245333=ORIENTED_EDGE ( 'NONE', *, *, #28481, .T. ) ;
#245341=AXIS2_PLACEMENT_3D ( 'NONE', #202029, #2522, #256801 ) ;
#245351=CARTESIAN_POINT ( 'NONE',  ( -23.25000000000000000, -1.164121893230052995, -208.9148480855715775 ) ) ;
#245367=CARTESIAN_POINT ( 'NONE',  ( 18.59999999999996945, 7.021664781911246322, -204.8335654018972605 ) ) ;
#245372=EDGE_LOOP ( 'NONE', ( #178203, #245535, #193839, #181657 ) ) ;
#245417=CARTESIAN_POINT ( 'NONE',  ( -18.36527282682029494, -9.500000599982218574, -207.9221489645163388 ) ) ;
#245420=VERTEX_POINT ( 'NONE', #58305 ) ;
#245432=CARTESIAN_POINT ( 'NONE',  ( 22.59999985501178799, 11.74986979301414003, -167.4344013302003873 ) ) ;
#245436=EDGE_LOOP ( 'NONE', ( #116903, #83908, #27994, #201446 ) ) ;
#245484=DIRECTION ( 'NONE',  ( 3.265361837132813093E-16, -1.000000000000000000, -0.000000000000000000 ) ) ;
#245485=EDGE_LOOP ( 'NONE', ( #78960, #61837 ) ) ;
#245504=EDGE_CURVE ( 'NONE', #147015, #157637, #197149, .T. ) ;
#245506=ORIENTED_EDGE ( 'NONE', *, *, #146673, .F. ) ;
#245513=CARTESIAN_POINT ( 'NONE',  ( 21.05000000000000071, 5.850000000011105428, -177.6324972242779268 ) ) ;
#245535=ORIENTED_EDGE ( 'NONE', *, *, #22685, .T. ) ;
#245549=DIRECTION ( 'NONE',  ( -1.000000000000000000, -3.265361837132813093E-16, 0.000000000000000000 ) ) ;
#245580=ORIENTED_EDGE ( 'NONE', *, *, #111898, .F. ) ;
#245583=SURFACE_SIDE_STYLE ('',( #239156 ) ) ;
#245647=EDGE_LOOP ( 'NONE', ( #181397, #121857, #233019, #118854 ) ) ;
#245650=ORIENTED_EDGE ( 'NONE', *, *, #110029, .F. ) ;
#245672=ADVANCED_FACE ( 'NONE', ( #122766 ), #93098, .T. ) ;
#245682=ORIENTED_EDGE ( 'NONE', *, *, #151848, .F. ) ;
#245691=DIRECTION ( 'NONE',  ( 0.000000000000000000, 1.000000000000000000, 0.000000000000000000 ) ) ;
#245716=LINE ( 'NONE', #205283, #187991 ) ;
#245728=EDGE_CURVE ( 'NONE', #113374, #71995, #34879, .T. ) ;
#245752=ORIENTED_EDGE ( 'NONE', *, *, #120059, .T. ) ;
#245755=DIRECTION ( 'NONE',  ( 0.000000000000000000, -1.000000000000000000, 0.000000000000000000 ) ) ;
#245788=DIRECTION ( 'NONE',  ( 0.000000000000000000, 0.000000000000000000, -1.000000000000000000 ) ) ;
#245790=ORIENTED_EDGE ( 'NONE', *, *, #247990, .F. ) ;
#245800=CARTESIAN_POINT ( 'NONE',  ( -20.12071067811865888, 9.320710678129810134, -179.8499999999999943 ) ) ;
#245822=CARTESIAN_POINT ( 'NONE',  ( 18.49999999999996803, 7.070967871809997973, -204.7465642218682547 ) ) ;
#245830=( BOUNDED_SURFACE ( )  B_SPLINE_SURFACE ( 3, 2, ( 
 ( #20170, #215771, #80088 ),
 ( #159681, #154570, #56679 ),
 ( #573, #120567, #157126 ),
 ( #99665, #177964, #218333 ),
 ( #100925, #17574, #97084 ),
 ( #78824, #60554, #39754 ) ),
 .UNSPECIFIED., .F., .F., .F. ) 
 B_SPLINE_SURFACE_WITH_KNOTS ( ( 4, 2, 4 ),
 ( 3, 3 ),
 ( 6.719893378898281297E-05, 0.0002757154632485351252, 0.0004842319927080873969 ),
 ( 0.000000000000000000, 1.000000000000000000 ),
 .UNSPECIFIED. ) 
 GEOMETRIC_REPRESENTATION_ITEM ( )  RATIONAL_B_SPLINE_SURFACE ( (
 ( 1.000000000000000000, 0.7250110520819756932, 1.000000000000000000),
 ( 1.000000000000000000, 0.7277932058380179869, 1.000000000000000000),
 ( 1.000000000000000000, 0.7278452872589651346, 1.000000000000000000),
 ( 1.000000000000000000, 0.7221445671577162440, 1.000000000000000000),
 ( 1.000000000000000000, 0.7163662143757810741, 1.000000000000000000),
 ( 1.000000000000000000, 0.7071067811866325048, 1.000000000000000000) ) ) 
 REPRESENTATION_ITEM ( '' )  SURFACE ( )  );
#245840=EDGE_LOOP ( 'NONE', ( #165131, #228841, #250306, #84776 ) ) ;
#245853=CARTESIAN_POINT ( 'NONE',  ( -20.64999999999999858, 4.350000000011156054, -179.8499999999999943 ) ) ;
#245878=AXIS2_PLACEMENT_3D ( 'NONE', #168681, #150363, #129508 ) ;
#245887=ORIENTED_EDGE ( 'NONE', *, *, #170640, .T. ) ;
#245915=DIRECTION ( 'NONE',  ( -1.836970198721029934E-16, 1.000000000000000000, 0.000000000000000000 ) ) ;
#245930=CARTESIAN_POINT ( 'NONE',  ( 18.49999999999999289, 10.20857864609425825, -192.2025068656295446 ) ) ;
#245932=VECTOR ( 'NONE', #89708, 1000.000000000000000 ) ;
#245951=DIRECTION ( 'NONE',  ( 0.000000000000000000, 0.000000000000000000, -1.000000000000000000 ) ) ;
#245952=EDGE_CURVE ( 'NONE', #160946, #102524, #112203, .T. ) ;
#245953=EDGE_CURVE ( 'NONE', #64282, #85751, #28844, .T. ) ;
#245956=CIRCLE ( 'NONE', #87705, 11.80000000000000426 ) ;
#245962=DIRECTION ( 'NONE',  ( 0.000000000000000000, 0.000000000000000000, -1.000000000000000000 ) ) ;
#245965=ADVANCED_FACE ( 'NONE', ( #151315 ), #233421, .T. ) ;
#245969=CIRCLE ( 'NONE', #83609, 0.09999999999999939493 ) ;
#245993=CARTESIAN_POINT ( 'NONE',  ( 20.95263205890668345, 8.895740107905178107, -175.9895084069416384 ) ) ;
#246043=CARTESIAN_POINT ( 'NONE',  ( -20.64999999999999858, 2.000000000011154189, -180.2246219227620543 ) ) ;
#246145=ORIENTED_EDGE ( 'NONE', *, *, #130936, .T. ) ;
#246172=VECTOR ( 'NONE', #51872, 1000.000000000000000 ) ;
#246179=VERTEX_POINT ( 'NONE', #19496 ) ;
#246188=ADVANCED_FACE ( 'NONE', ( #188827 ), #8131, .F. ) ;
#246194=CARTESIAN_POINT ( 'NONE',  ( 18.49999999999999645, -9.480686695267806385, -207.9411151687578183 ) ) ;
#246207=CARTESIAN_POINT ( 'NONE',  ( -21.93340585900942941, 1.115541036281197940E-11, -160.1758529778945501 ) ) ;
#246235=LINE ( 'NONE', #46731, #12863 ) ;
#246237=CARTESIAN_POINT ( 'NONE',  ( 20.04142135623730070, 11.65000000001115943, -192.1499999999999488 ) ) ;
#246269=DIRECTION ( 'NONE',  ( 1.000000000000000000, 0.000000000000000000, 0.000000000000000000 ) ) ;
#246277=DIRECTION ( 'NONE',  ( 0.000000000000000000, -0.000000000000000000, -1.000000000000000000 ) ) ;
#246283=ORIENTED_EDGE ( 'NONE', *, *, #28558, .T. ) ;
#246303=DIRECTION ( 'NONE',  ( 0.000000000000000000, -0.8068669527897506244, -0.5907332058516622242 ) ) ;
#246308=DIRECTION ( 'NONE',  ( -0.000000000000000000, 0.1350103645451876666, 0.9908441862701600211 ) ) ;
#246323=ORIENTED_EDGE ( 'NONE', *, *, #214884, .T. ) ;
#246370=CARTESIAN_POINT ( 'NONE',  ( 21.08804281139612868, 10.62183430185230826, -179.8499999673788068 ) ) ;
#246394=ADVANCED_FACE ( 'NONE', ( #230534 ), #54443, .T. ) ;
#246401=ORIENTED_EDGE ( 'NONE', *, *, #178239, .F. ) ;
#246404=CARTESIAN_POINT ( 'NONE',  ( -20.85000000000000142, -1.164121893230052995, -208.7148480855715604 ) ) ;
#246431=ORIENTED_EDGE ( 'NONE', *, *, #250256, .T. ) ;
#246435=CIRCLE ( 'NONE', #208841, 0.09999999999998898659 ) ;
#246457=CARTESIAN_POINT ( 'NONE',  ( 20.94999999999999574, 1.835341550235569663, -179.0551512925629538 ) ) ;
#246458=ORIENTED_EDGE ( 'NONE', *, *, #219532, .T. ) ;
#246495=ADVANCED_FACE ( 'NONE', ( #77849 ), #62156, .T. ) ;
#246535=FACE_OUTER_BOUND ( 'NONE', #203445, .T. ) ;
#246538=EDGE_CURVE ( 'NONE', #63066, #85197, #187382, .T. ) ;
#246563=ADVANCED_FACE ( 'NONE', ( #81670 ), #59544, .F. ) ;
#246601=DIRECTION ( 'NONE',  ( 0.000000000000000000, 0.9654727137038726648, -0.2605042016806632943 ) ) ;
#246605=CIRCLE ( 'NONE', #179987, 0.09999999999998898659 ) ;
#246606=DIRECTION ( 'NONE',  ( 1.000000000000000000, -0.000000000000000000, -0.000000000000000000 ) ) ;
#246621=CARTESIAN_POINT ( 'NONE',  ( -21.05000000000000071, 0.09779029131994770863, -161.2421853895238542 ) ) ;
#246648=CARTESIAN_POINT ( 'NONE',  ( 18.59999999999999432, 1.637172712981537659, -179.0821533654719815 ) ) ;
#246670=ORIENTED_EDGE ( 'NONE', *, *, #103030, .F. ) ;
#246698=DIRECTION ( 'NONE',  ( -1.000000000000000000, 0.000000000000000000, 0.000000000000000000 ) ) ;
#246743=VECTOR ( 'NONE', #141832, 1000.000000000000000 ) ;
#246745=VERTEX_POINT ( 'NONE', #73725 ) ;
#246767=VECTOR ( 'NONE', #125200, 1000.000000000000000 ) ;
#246768=CIRCLE ( 'NONE', #21937, 0.09999999999999484301 ) ;
#246788=CIRCLE ( 'NONE', #242524, 0.09999999999998898659 ) ;
#246808=CARTESIAN_POINT ( 'NONE',  ( -21.55000000000000426, 7.750000000011159074, -188.6499999999999488 ) ) ;
#246888=CARTESIAN_POINT ( 'NONE',  ( -18.59999999999999787, 11.65000000001115232, -188.8499999999999659 ) ) ;
#246910=CYLINDRICAL_SURFACE ( 'NONE', #152668, 0.09999999999999864553 ) ;
#246934=CARTESIAN_POINT ( 'NONE',  ( -22.00411653962160585, 7.253442868381348774, -167.4009618942313864 ) ) ;
#246937=ORIENTED_EDGE ( 'NONE', *, *, #21445, .T. ) ;
#246939=EDGE_LOOP ( 'NONE', ( #83772, #189713, #210237, #125637 ) ) ;
#246941=DIRECTION ( 'NONE',  ( -1.000000000000000000, 7.304098846218133681E-16, -4.217023435051677994E-16 ) ) ;
#246946=TOROIDAL_SURFACE ( 'NONE', #209349, 0.6000000000000013101, 0.1000000000000000056 ) ;
#246979=CARTESIAN_POINT ( 'NONE',  ( -18.58671080940900211, -9.406932858815471477, -174.6241544649046489 ) ) ;
#246993=CARTESIAN_POINT ( 'NONE',  ( -23.15000000000000213, 11.65000000001115588, -188.8499999999999659 ) ) ;
#247018=EDGE_CURVE ( 'NONE', #41810, #229311, #116817, .T. ) ;
#247020=ORIENTED_EDGE ( 'NONE', *, *, #241935, .T. ) ;
#247037=VECTOR ( 'NONE', #218889, 1000.000000000000000 ) ;
#247065=DIRECTION ( 'NONE',  ( 0.7071067811865475727, 0.7071067811865475727, 2.044391222244500083E-16 ) ) ;
#247100=CARTESIAN_POINT ( 'NONE',  ( 20.86777300164944648, 10.33200063080771969, -206.5931674956642610 ) ) ;
#247106=CIRCLE ( 'NONE', #43129, 0.09999999999998898659 ) ;
#247146=VECTOR ( 'NONE', #218419, 1000.000000000000114 ) ;
#247151=ORIENTED_EDGE ( 'NONE', *, *, #27256, .T. ) ;
#247176=CARTESIAN_POINT ( 'NONE',  ( 21.97500000000000497, 9.750000000011153745, -188.7499999999999716 ) ) ;
#247181=ORIENTED_EDGE ( 'NONE', *, *, #29314, .T. ) ;
#247187=CARTESIAN_POINT ( 'NONE',  ( -20.94999027547553894, 10.29326151435327219, -206.4592822510414578 ) ) ;
#247220=AXIS2_PLACEMENT_3D ( 'NONE', #202285, #79737, #23676 ) ;
#247266=DIRECTION ( 'NONE',  ( 0.000000000000000000, 0.000000000000000000, 1.000000000000000000 ) ) ;
#247272=DIRECTION ( 'NONE',  ( -0.000000000000000000, 1.000000000000000000, -1.224646799147352961E-16 ) ) ;
#247274=ORIENTED_EDGE ( 'NONE', *, *, #56101, .T. ) ;
#247279=DIRECTION ( 'NONE',  ( 0.000000000000000000, 0.000000000000000000, -1.000000000000000000 ) ) ;
#247285=LINE ( 'NONE', #226425, #38900 ) ;
#247329=ORIENTED_EDGE ( 'NONE', *, *, #46232, .F. ) ;
#247335=DIRECTION ( 'NONE',  ( 0.000000000000000000, 0.000000000000000000, 1.000000000000000000 ) ) ;
#247336=EDGE_LOOP ( 'NONE', ( #47531, #13067, #96246, #219721 ) ) ;
#247344=ORIENTED_EDGE ( 'NONE', *, *, #257792, .T. ) ;
#247347=EDGE_CURVE ( 'NONE', #143316, #29024, #125395, .T. ) ;
#247363=CARTESIAN_POINT ( 'NONE',  ( -23.25000000000000000, 11.65000000001115588, -155.7499999999999716 ) ) ;
#247438=DIRECTION ( 'NONE',  ( 0.000000000000000000, -1.000000000000000000, 0.000000000000000000 ) ) ;
#247481=CARTESIAN_POINT ( 'NONE',  ( 21.05000000000000071, 1.115488181425289110E-11, -160.9593430482987344 ) ) ;
#247489=DIRECTION ( 'NONE',  ( 1.000000000000000000, 0.000000000000000000, 0.000000000000000000 ) ) ;
#247497=DIRECTION ( 'NONE',  ( 1.000000000000000000, 0.000000000000000000, 0.000000000000000000 ) ) ;
#247522=EDGE_CURVE ( 'NONE', #62638, #154602, #207157, .T. ) ;
#247532=EDGE_CURVE ( 'NONE', #158708, #57292, #21527, .T. ) ;
#247542=CIRCLE ( 'NONE', #168480, 0.09999999999998898659 ) ;
#247566=DIRECTION ( 'NONE',  ( 1.000000000000000000, 0.000000000000000000, 0.000000000000000000 ) ) ;
#247574=CARTESIAN_POINT ( 'NONE',  ( 22.48508240969612615, 0.04627641452807085970, -155.8499892684264125 ) ) ;
#247604=CARTESIAN_POINT ( 'NONE',  ( 23.24999999999999645, 1.115600667400684642E-11, -200.9999999999999432 ) ) ;
#247632=EDGE_CURVE ( 'NONE', #185697, #94619, #31117, .T. ) ;
#247635=DIRECTION ( 'NONE',  ( 0.000000000000000000, 0.9908441862701782288, -0.1350103645450542456 ) ) ;
#247687=CARTESIAN_POINT ( 'NONE',  ( 18.49999999999999289, 6.650000000011155876, -188.6499999999999488 ) ) ;
#247700=AXIS2_PLACEMENT_3D ( 'NONE', #142383, #125403, #160706 ) ;
#247729=DIRECTION ( 'NONE',  ( 1.000000000000000000, -0.000000000000000000, -0.000000000000000000 ) ) ;
#247755=DIRECTION ( 'NONE',  ( -1.836970198721029934E-16, 1.000000000000000000, 0.000000000000000000 ) ) ;
#247788=DIRECTION ( 'NONE',  ( 1.000000000000000000, 0.000000000000000000, 0.000000000000000000 ) ) ;
#247797=ORIENTED_EDGE ( 'NONE', *, *, #30030, .T. ) ;
#247823=CARTESIAN_POINT ( 'NONE',  ( -21.14999999999999858, 11.75000000001115197, -174.2838656629781156 ) ) ;
#247859=CARTESIAN_POINT ( 'NONE',  ( 18.49999999999999645, -1.135018845899022466, -208.7169768834322952 ) ) ;
#247867=VERTEX_POINT ( 'NONE', #179590 ) ;
#247883=ORIENTED_EDGE ( 'NONE', *, *, #28456, .T. ) ;
#247930=CARTESIAN_POINT ( 'NONE',  ( -21.05000000000000071, 1.162701749949165642, -175.5999999999999659 ) ) ;
#247949=EDGE_CURVE ( 'NONE', #246745, #117026, #67318, .T. ) ;
#247950=LINE ( 'NONE', #69341, #32172 ) ;
#247990=EDGE_CURVE ( 'NONE', #77502, #184791, #142303, .T. ) ;
#248010=DIRECTION ( 'NONE',  ( 1.000000000000000000, -0.000000000000000000, -0.000000000000000000 ) ) ;
#248021=CARTESIAN_POINT ( 'NONE',  ( -20.94999999999999929, -1.849153571964891274, -212.6059666197970159 ) ) ;
#248029=LINE ( 'NONE', #8153, #210409 ) ;
#248056=ORIENTED_EDGE ( 'NONE', *, *, #201434, .F. ) ;
#248094=EDGE_CURVE ( 'NONE', #54306, #199182, #242250, .T. ) ;
#248120=LINE ( 'NONE', #190753, #241267 ) ;
#248122=DIRECTION ( 'NONE',  ( -0.000000000000000000, -0.000000000000000000, 1.000000000000000000 ) ) ;
#248126=ORIENTED_EDGE ( 'NONE', *, *, #109994, .T. ) ;
#248133=CARTESIAN_POINT ( 'NONE',  ( -23.15000000000000213, 1.115600667400684642E-11, -200.9999999999999432 ) ) ;
#248134=LINE ( 'NONE', #69521, #81899 ) ;
#248156=CARTESIAN_POINT ( 'NONE',  ( 23.25000000000000000, -11.74999999998883560, -155.7499999999999716 ) ) ;
#248171=EDGE_LOOP ( 'NONE', ( #144253, #197834, #180180, #191924 ) ) ;
#248175=CIRCLE ( 'NONE', #223220, 0.09999999999999939493 ) ;
#248182=VECTOR ( 'NONE', #129205, 1000.000000000000000 ) ;
#248193=ORIENTED_EDGE ( 'NONE', *, *, #195457, .F. ) ;
#248203=CARTESIAN_POINT ( 'NONE',  ( 20.96428641294170703, 11.75000000001150013, -194.1748931779407030 ) ) ;
#248254=CIRCLE ( 'NONE', #90025, 0.09999999999998898659 ) ;
#248259=CYLINDRICAL_SURFACE ( 'NONE', #214272, 0.09999999999998898659 ) ;
#248342=EDGE_CURVE ( 'NONE', #42612, #130077, #37906, .T. ) ;
#248378=ORIENTED_EDGE ( 'NONE', *, *, #30025, .T. ) ;
#248408=ORIENTED_EDGE ( 'NONE', *, *, #193042, .T. ) ;
#248448=AXIS2_PLACEMENT_3D ( 'NONE', #192355, #133659, #232780 ) ;
#248478=DIRECTION ( 'NONE',  ( 0.000000000000000000, 0.000000000000000000, 1.000000000000000000 ) ) ;
#248509=CARTESIAN_POINT ( 'NONE',  ( 21.05000000000041638, 6.344359042055009112, -167.4851443651052989 ) ) ;
#248510=AXIS2_PLACEMENT_3D ( 'NONE', #68263, #250737, #87794 ) ;
#248547=CARTESIAN_POINT ( 'NONE',  ( -22.49533356619862445, 11.65000000631534149, -167.4348774196772069 ) ) ;
#248579=AXIS2_PLACEMENT_3D ( 'NONE', #34316, #74741, #151703 ) ;
#248585=CARTESIAN_POINT ( 'NONE',  ( 21.00000000000000000, 9.750000000011153745, -179.7499999999999716 ) ) ;
#248588=CARTESIAN_POINT ( 'NONE',  ( 21.05000000000000071, 1.115600667400684642E-11, -200.9999999999999432 ) ) ;
#248645=CARTESIAN_POINT ( 'NONE',  ( -21.05000000000000071, 1.835341550235567887, -179.1551512925629197 ) ) ;
#248698=AXIS2_PLACEMENT_3D ( 'NONE', #166587, #47875, #136375 ) ;
#248705=AXIS2_PLACEMENT_3D ( 'NONE', #22521, #60328, #40810 ) ;
#248713=CARTESIAN_POINT ( 'NONE',  ( 21.05000000000000071, 6.650000000011155876, -179.6499999999999773 ) ) ;
#248729=FACE_OUTER_BOUND ( 'NONE', #98091, .T. ) ;
#248750=AXIS2_PLACEMENT_3D ( 'NONE', #229131, #203142, #105288 ) ;
#248768=VECTOR ( 'NONE', #156372, 1000.000000000000000 ) ;
#248779=CARTESIAN_POINT ( 'NONE',  ( 21.13435531349819740, 1.115515320630192923E-11, -161.0062789364080515 ) ) ;
#248784=ORIENTED_EDGE ( 'NONE', *, *, #170682, .T. ) ;
#248796=DIRECTION ( 'NONE',  ( 0.000000000000000000, -1.000000000000000000, 0.000000000000000000 ) ) ;
#248847=VECTOR ( 'NONE', #17212, 1000.000000000000114 ) ;
#248865=CARTESIAN_POINT ( 'NONE',  ( 22.49066049874202022, 0.05634325154338429287, -155.8499877624828400 ) ) ;
#248871=CARTESIAN_POINT ( 'NONE',  ( -18.59999999999999787, 9.250000000011157297, -188.6499999999999488 ) ) ;
#248877=CARTESIAN_POINT ( 'NONE',  ( 20.94999999999999574, 1.835341550235567887, -179.1551512925629197 ) ) ;
#248886=EDGE_CURVE ( 'NONE', #102524, #216004, #154618, .T. ) ;
#248887=DIRECTION ( 'NONE',  ( 0.000000000000000000, 0.000000000000000000, 1.000000000000000000 ) ) ;
#248893=AXIS2_PLACEMENT_3D ( 'NONE', #174685, #115951, #156385 ) ;
#248894=AXIS2_PLACEMENT_3D ( 'NONE', #56532, #175269, #155698 ) ;
#248900=EDGE_LOOP ( 'NONE', ( #58514, #231777, #42874, #203069 ) ) ;
#248939=EDGE_LOOP ( 'NONE', ( #153973, #247181, #110617, #238996 ) ) ;
#248957=CYLINDRICAL_SURFACE ( 'NONE', #40127, 0.09999999999999817368 ) ;
#248969=EDGE_CURVE ( 'NONE', #145941, #215011, #146198, .T. ) ;
#248975=CARTESIAN_POINT ( 'NONE',  ( 20.94999999999999929, -1.162701749926853712, -175.3999999999999773 ) ) ;
#248983=LINE ( 'NONE', #192856, #234204 ) ;
#249030=CARTESIAN_POINT ( 'NONE',  ( -20.94999999999999929, 11.65000000001115232, -200.9999999999999432 ) ) ;
#249042=AXIS2_PLACEMENT_3D ( 'NONE', #59598, #139133, #218685 ) ;
#249067=VECTOR ( 'NONE', #97155, 1000.000000000000000 ) ;
#249077=ORIENTED_EDGE ( 'NONE', *, *, #81242, .F. ) ;
#249126=CARTESIAN_POINT ( 'NONE',  ( -21.05439746398122836, 11.75000000001115197, -174.4899164874849760 ) ) ;
#249134=ORIENTED_EDGE ( 'NONE', *, *, #210346, .T. ) ;
#249142=AXIS2_PLACEMENT_3D ( 'NONE', #219284, #177633, #257084 ) ;
#249164=DIRECTION ( 'NONE',  ( 0.000000000000000000, 1.000000000000000000, 0.000000000000000000 ) ) ;
#249169=CARTESIAN_POINT ( 'NONE',  ( 21.05000000000000071, -11.74999999998883560, -170.3999999999999773 ) ) ;
#249177=CARTESIAN_POINT ( 'NONE',  ( 20.94999999999999929, -11.64999999998883595, -197.9999999999999432 ) ) ;
#249208=EDGE_CURVE ( 'NONE', #102524, #251277, #6942, .T. ) ;
#249214=CARTESIAN_POINT ( 'NONE',  ( 20.94999999999999929, -1.164121893230052995, -208.9148480855715775 ) ) ;
#249216=ORIENTED_EDGE ( 'NONE', *, *, #18668, .T. ) ;
#249226=CARTESIAN_POINT ( 'NONE',  ( -23.15000000000000213, 1.115600667400684642E-11, -200.9999999999999432 ) ) ;
#249256=ORIENTED_EDGE ( 'NONE', *, *, #218696, .T. ) ;
#249268=DIRECTION ( 'NONE',  ( -0.000000000000000000, 1.000000000000000000, 0.000000000000000000 ) ) ;
#249323=CARTESIAN_POINT ( 'NONE',  ( 21.30000000000002558, 1.115600667400684642E-11, -171.5499999999999829 ) ) ;
#249325=EDGE_CURVE ( 'NONE', #151116, #19947, #38251, .T. ) ;
#249348=ORIENTED_EDGE ( 'NONE', *, *, #3230, .T. ) ;
#249356=CARTESIAN_POINT ( 'NONE',  ( -20.64999999999999858, 2.000000000011154189, -187.7753780772378889 ) ) ;
#249370=CARTESIAN_POINT ( 'NONE',  ( -21.64999999999999858, 7.350000000011155166, -188.7499999999999716 ) ) ;
#249372=DIRECTION ( 'NONE',  ( -1.000000000000000000, 0.000000000000000000, 0.000000000000000000 ) ) ;
#249378=CARTESIAN_POINT ( 'NONE',  ( 21.05000000000000071, 1.349084418638171412, -175.4864989635454435 ) ) ;
#249396=ORIENTED_EDGE ( 'NONE', *, *, #148750, .F. ) ;
#249400=EDGE_LOOP ( 'NONE', ( #233635, #86041, #150391, #186912 ) ) ;
#249408=VERTEX_POINT ( 'NONE', #69901 ) ;
#249413=CARTESIAN_POINT ( 'NONE',  ( -21.14999999999999858, -11.74999999998884448, -170.3999999999999773 ) ) ;
#249473=ORIENTED_EDGE ( 'NONE', *, *, #150030, .T. ) ;
#249496=CARTESIAN_POINT ( 'NONE',  ( 21.05000000000000071, 11.60000000001116049, -194.0717967697244717 ) ) ;
#249505=TOROIDAL_SURFACE ( 'NONE', #236810, 4.099999999999999645, 0.1000000000000000056 ) ;
#249512=DIRECTION ( 'NONE',  ( 0.000000000000000000, -1.000000000000000000, 0.000000000000000000 ) ) ;
#249517=ADVANCED_FACE ( 'NONE', ( #94561 ), #179581, .T. ) ;
#249524=DIRECTION ( 'NONE',  ( 1.000000000000000000, 0.000000000000000000, 0.000000000000000000 ) ) ;
#249531=EDGE_LOOP ( 'NONE', ( #61843, #98588, #33255, #156270, #255114 ) ) ;
#249591=EDGE_CURVE ( 'NONE', #202185, #199945, #117535, .T. ) ;
#249596=VERTEX_POINT ( 'NONE', #65717 ) ;
#249599=AXIS2_PLACEMENT_3D ( 'NONE', #44829, #142622, #124377 ) ;
#249602=ADVANCED_FACE ( 'NONE', ( #46150 ), #213193, .T. ) ;
#249606=ORIENTED_EDGE ( 'NONE', *, *, #127659, .F. ) ;
#249621=EDGE_CURVE ( 'NONE', #22716, #232095, #95255, .T. ) ;
#249631=DIRECTION ( 'NONE',  ( 0.000000000000000000, 0.4999999999999956701, -0.8660254037844411501 ) ) ;
#249641=DIRECTION ( 'NONE',  ( -3.469446951953605354E-14, 1.000000000000000000, 0.000000000000000000 ) ) ;
#249713=CARTESIAN_POINT ( 'NONE',  ( 21.13461538461538680, 8.885417037985614996, -179.8499999999999943 ) ) ;
#249722=CIRCLE ( 'NONE', #224759, 0.09999999999998898659 ) ;
#249725=EDGE_LOOP ( 'NONE', ( #233576, #256764, #121281, #254005 ) ) ;
#249728=EDGE_CURVE ( 'NONE', #191282, #223911, #47421, .T. ) ;
#249753=CARTESIAN_POINT ( 'NONE',  ( -18.43473496883423124, -9.494952410988105385, -174.5458715722282079 ) ) ;
#249765=AXIS2_PLACEMENT_3D ( 'NONE', #56307, #38070, #177596 ) ;
#249767=CARTESIAN_POINT ( 'NONE',  ( -20.54999999999999716, 1.115600667400684642E-11, -200.9999999999999432 ) ) ;
#249801=DIRECTION ( 'NONE',  ( 1.000000000000000000, 0.000000000000000000, 0.000000000000000000 ) ) ;
#249823=EDGE_CURVE ( 'NONE', #199182, #145487, #200743, .T. ) ;
#249851=ORIENTED_EDGE ( 'NONE', *, *, #138552, .F. ) ;
#249855=VERTEX_POINT ( 'NONE', #255863 ) ;
#249916=EDGE_LOOP ( 'NONE', ( #39220, #234203, #175805, #43625, #149559, #175164, #80838, #139643 ) ) ;
#249978=CARTESIAN_POINT ( 'NONE',  ( 20.94999999999999929, 1.115600667400684642E-11, -200.9999999999999432 ) ) ;
#249979=AXIS2_PLACEMENT_3D ( 'NONE', #207765, #171233, #70829 ) ;
#249984=VECTOR ( 'NONE', #235261, 1000.000000000000000 ) ;
#250004=DIRECTION ( 'NONE',  ( 0.000000000000000000, 0.000000000000000000, 1.000000000000000000 ) ) ;
#250014=CARTESIAN_POINT ( 'NONE',  ( -21.14999999999999858, 1.115600667400684642E-11, -167.4999999999999716 ) ) ;
#250040=AXIS2_PLACEMENT_3D ( 'NONE', #179837, #217632, #23346 ) ;
#250057=CARTESIAN_POINT ( 'NONE',  ( 21.05000000000000071, -1.835341550213257733, -179.0551512925629538 ) ) ;
#250077=DIRECTION ( 'NONE',  ( 1.000000000000000000, 0.000000000000000000, 0.000000000000000000 ) ) ;
#250094=ORIENTED_EDGE ( 'NONE', *, *, #139109, .T. ) ;
#250193=VERTEX_POINT ( 'NONE', #228348 ) ;
#250208=VERTEX_POINT ( 'NONE', #186661 ) ;
#250232=EDGE_CURVE ( 'NONE', #224509, #59445, #146913, .T. ) ;
#250256=EDGE_CURVE ( 'NONE', #209275, #202001, #63537, .T. ) ;
#250279=VERTEX_POINT ( 'NONE', #256825 ) ;
#250287=CARTESIAN_POINT ( 'NONE',  ( 21.05000000000000071, 1.115600667400684642E-11, -167.4999999999999716 ) ) ;
#250292=ORIENTED_EDGE ( 'NONE', *, *, #96901, .T. ) ;
#250294=DIRECTION ( 'NONE',  ( 0.000000000000000000, 0.000000000000000000, -1.000000000000000000 ) ) ;
#250306=ORIENTED_EDGE ( 'NONE', *, *, #48453, .T. ) ;
#250317=FACE_OUTER_BOUND ( 'NONE', #114260, .T. ) ;
#250324=EDGE_CURVE ( 'NONE', #159944, #26762, #221929, .T. ) ;
#250356=TOROIDAL_SURFACE ( 'NONE', #241965, 0.6000000000000004219, 0.1000000000000000056 ) ;
#250367=CARTESIAN_POINT ( 'NONE',  ( 23.15000000000000213, -8.596261682231828516, -191.5498724828496790 ) ) ;
#250386=DIRECTION ( 'NONE',  ( 0.000000000000000000, 0.000000000000000000, -1.000000000000000000 ) ) ;
#250387=DIRECTION ( 'NONE',  ( -1.000000000000000000, 0.000000000000000000, 0.000000000000000000 ) ) ;
#250443=DIRECTION ( 'NONE',  ( -1.000000000000000000, -0.000000000000000000, -0.000000000000000000 ) ) ;
#250461=ADVANCED_FACE ( 'NONE', ( #226735 ), #87216, .T. ) ;
#250479=DIRECTION ( 'NONE',  ( 0.000000000000000000, 0.000000000000000000, -1.000000000000000000 ) ) ;
#250483=ORIENTED_EDGE ( 'NONE', *, *, #177624, .F. ) ;
#250500=CARTESIAN_POINT ( 'NONE',  ( -23.25000000000000000, -11.64999999998884483, -167.4999999999999432 ) ) ;
#250529=ORIENTED_EDGE ( 'NONE', *, *, #35283, .T. ) ;
#250530=CYLINDRICAL_SURFACE ( 'NONE', #122589, 2.000000000000001776 ) ;
#250538=ORIENTED_EDGE ( 'NONE', *, *, #249728, .T. ) ;
#250552=DIRECTION ( 'NONE',  ( 1.000000000000000000, 0.000000000000000000, 0.000000000000000000 ) ) ;
#250608=ORIENTED_EDGE ( 'NONE', *, *, #69926, .F. ) ;
#250624=DIRECTION ( 'NONE',  ( 0.000000000000000000, -0.9999176327611369874, 0.01283462868041987913 ) ) ;
#250673=AXIS2_PLACEMENT_3D ( 'NONE', #205102, #105998, #166029 ) ;
#250698=ORIENTED_EDGE ( 'NONE', *, *, #244547, .T. ) ;
#250702=CARTESIAN_POINT ( 'NONE',  ( -22.57320508075687115, 11.75000000001115552, -167.4999999999999716 ) ) ;
#250708=DIRECTION ( 'NONE',  ( 0.000000000000000000, 0.000000000000000000, -1.000000000000000000 ) ) ;
#250737=DIRECTION ( 'NONE',  ( -1.000000000000000000, 0.000000000000000000, -0.000000000000000000 ) ) ;
#250775=CYLINDRICAL_SURFACE ( 'NONE', #159377, 0.09999999999999939493 ) ;
#250778=DIRECTION ( 'NONE',  ( 0.000000000000000000, 0.000000000000000000, -1.000000000000000000 ) ) ;
#250789=LINE ( 'NONE', #133420, #257727 ) ;
#250796=ORIENTED_EDGE ( 'NONE', *, *, #166097, .F. ) ;
#250804=ORIENTED_EDGE ( 'NONE', *, *, #180911, .T. ) ;
#250842=CIRCLE ( 'NONE', #209154, 0.5000000000000004441 ) ;
#250853=FACE_OUTER_BOUND ( 'NONE', #211493, .T. ) ;
#250878=EDGE_CURVE ( 'NONE', #33844, #181739, #53908, .T. ) ;
#250886=ORIENTED_EDGE ( 'NONE', *, *, #48648, .T. ) ;
#250942=FACE_OUTER_BOUND ( 'NONE', #58727, .T. ) ;
#250961=LINE ( 'NONE', #35808, #49627 ) ;
#250972=CIRCLE ( 'NONE', #46969, 3.999999999999999112 ) ;
#250998=CIRCLE ( 'NONE', #196852, 12.97499999999998721 ) ;
#251006=CARTESIAN_POINT ( 'NONE',  ( 23.24999999999999289, 11.65000000001116298, -179.6499999999999773 ) ) ;
#251072=CARTESIAN_POINT ( 'NONE',  ( -18.59999999999999787, 11.65000000001115232, -174.5148057706539930 ) ) ;
#251078=DIRECTION ( 'NONE',  ( 0.000000000000000000, 0.000000000000000000, -1.000000000000000000 ) ) ;
#251081=CARTESIAN_POINT ( 'NONE',  ( -2.995603634470891112E-16, -11.74999999998884448, -192.2499999999999716 ) ) ;
#251118=FACE_OUTER_BOUND ( 'NONE', #134543, .T. ) ;
#251149=ADVANCED_FACE ( 'NONE', ( #82418 ), #241526, .T. ) ;
#251169=AXIS2_PLACEMENT_3D ( 'NONE', #117692, #76005, #201081 ) ;
#251224=CONICAL_SURFACE ( 'NONE', #230395, 4.049999999999998046, 0.7853981633974604915 ) ;
#251234=CARTESIAN_POINT ( 'NONE',  ( -22.49756042579671700, 0.07804633702833754794, -155.8501350388976334 ) ) ;
#251237=CARTESIAN_POINT ( 'NONE',  ( 23.24999999999999645, 1.115600667400684642E-11, -200.9999999999999432 ) ) ;
#251261=EDGE_LOOP ( 'NONE', ( #109217, #15150, #18302, #61988 ) ) ;
#251267=DIRECTION ( 'NONE',  ( 1.000000000000000000, 0.000000000000000000, 0.000000000000000000 ) ) ;
#251275=CARTESIAN_POINT ( 'NONE',  ( 21.46681500593265213, 6.857511159395772715, -167.4999999999999432 ) ) ;
#251277=VERTEX_POINT ( 'NONE', #250500 ) ;
#251278=DIRECTION ( 'NONE',  ( 1.000000000000000000, 0.000000000000000000, 0.000000000000000000 ) ) ;
#251282=ORIENTED_EDGE ( 'NONE', *, *, #56101, .F. ) ;
#251302=EDGE_CURVE ( 'NONE', #34375, #42715, #101666, .T. ) ;
#251345=LINE ( 'NONE', #175692, #123175 ) ;
#251373=LINE ( 'NONE', #252645, #10547 ) ;
#251376=ORIENTED_EDGE ( 'NONE', *, *, #81437, .F. ) ;
#251382=TOROIDAL_SURFACE ( 'NONE', #226409, 0.2000000000000000111, 0.1000000000000000056 ) ;
#251396=EDGE_CURVE ( 'NONE', #42929, #50099, #30807, .T. ) ;
#251418=CYLINDRICAL_SURFACE ( 'NONE', #169528, 11.80000000000000426 ) ;
#251422=CARTESIAN_POINT ( 'NONE',  ( 22.57320508075687115, 11.75000000001115552, -167.4999999999999716 ) ) ;
#251428=CARTESIAN_POINT ( 'NONE',  ( 21.05000000000000071, 5.000000000011153745, -189.0947339810868755 ) ) ;
#251446=EDGE_CURVE ( 'NONE', #166015, #68443, #176134, .T. ) ;
#251459=ORIENTED_EDGE ( 'NONE', *, *, #203835, .F. ) ;
#251468=DIRECTION ( 'NONE',  ( 1.000000000000000000, 0.000000000000000000, 0.000000000000000000 ) ) ;
#251480=ORIENTED_EDGE ( 'NONE', *, *, #227513, .F. ) ;
#251482=ORIENTED_EDGE ( 'NONE', *, *, #168872, .T. ) ;
#251492=EDGE_CURVE ( 'NONE', #236853, #215160, #217777, .T. ) ;
#251494=CARTESIAN_POINT ( 'NONE',  ( -21.05000000000000071, -11.48912529306490349, -170.3999999999999773 ) ) ;
#251530=DIRECTION ( 'NONE',  ( 0.000000000000000000, 4.336808689942494997E-15, -1.000000000000000000 ) ) ;
#251545=ORIENTED_EDGE ( 'NONE', *, *, #140278, .T. ) ;
#251568=DIRECTION ( 'NONE',  ( -1.000000000000000000, -0.000000000000000000, -0.000000000000000000 ) ) ;
#251611=VERTEX_POINT ( 'NONE', #221627 ) ;
#251615=EDGE_CURVE ( 'NONE', #219222, #64828, #101858, .T. ) ;
#251617=CIRCLE ( 'NONE', #10213, 6.258578643762696458 ) ;
#251621=DIRECTION ( 'NONE',  ( 0.000000000000000000, 0.000000000000000000, -1.000000000000000000 ) ) ;
#251640=VERTEX_POINT ( 'NONE', #88536 ) ;
#251667=CARTESIAN_POINT ( 'NONE',  ( -21.14999999999999858, 1.115600667400684642E-11, -167.4999999999999716 ) ) ;
#251698=TOROIDAL_SURFACE ( 'NONE', #122534, 11.65000000000000036, 0.1000000000000000056 ) ;
#251724=VECTOR ( 'NONE', #199549, 1000.000000000000000 ) ;
#251734=DIRECTION ( 'NONE',  ( 0.000000000000000000, 0.000000000000000000, -1.000000000000000000 ) ) ;
#251782=DIRECTION ( 'NONE',  ( 0.000000000000000000, -0.9915357197604972583, 0.1298341882519109536 ) ) ;
#251812=ORIENTED_EDGE ( 'NONE', *, *, #77638, .F. ) ;
#251886=AXIS2_PLACEMENT_3D ( 'NONE', #118908, #159324, #199734 ) ;
#251927=CIRCLE ( 'NONE', #6407, 0.2000000000000057288 ) ;
#251959=DIRECTION ( 'NONE',  ( 0.000000000000000000, -0.000000000000000000, -1.000000000000000000 ) ) ;
#251979=AXIS2_PLACEMENT_3D ( 'NONE', #90741, #47759, #152041 ) ;
#251992=ORIENTED_EDGE ( 'NONE', *, *, #94403, .F. ) ;
#252013=ORIENTED_EDGE ( 'NONE', *, *, #97318, .T. ) ;
#252046=CARTESIAN_POINT ( 'NONE',  ( 21.05000000000000071, 11.75000000001115907, -193.9851942293460070 ) ) ;
#252061=FACE_OUTER_BOUND ( 'NONE', #113411, .T. ) ;
#252063=VERTEX_POINT ( 'NONE', #246043 ) ;
#252067=DIRECTION ( 'NONE',  ( -7.304098846218134667E-16, -1.000000000000000000, 0.000000000000000000 ) ) ;
#252076=EDGE_LOOP ( 'NONE', ( #2181, #166270, #200178, #131950, #180582 ) ) ;
#252088=ORIENTED_EDGE ( 'NONE', *, *, #61793, .F. ) ;
#252120=DIRECTION ( 'NONE',  ( -1.000000000000000000, -0.000000000000000000, -0.000000000000000000 ) ) ;
#252177=DIRECTION ( 'NONE',  ( 0.000000000000000000, -0.1350103645451876666, 0.9908441862701600211 ) ) ;
#252182=VERTEX_POINT ( 'NONE', #89515 ) ;
#252185=ORIENTED_EDGE ( 'NONE', *, *, #183844, .T. ) ;
#252199=VERTEX_POINT ( 'NONE', #176790 ) ;
#252214=ADVANCED_FACE ( 'NONE', ( #55498 ), #171672, .T. ) ;
#252222=CARTESIAN_POINT ( 'NONE',  ( 23.14999999999999858, 1.115600667400684642E-11, -200.9999999999999432 ) ) ;
#252238=ORIENTED_EDGE ( 'NONE', *, *, #15574, .F. ) ;
#252265=DIRECTION ( 'NONE',  ( 0.000000000000000000, 0.000000000000000000, 1.000000000000000000 ) ) ;
#252298=CARTESIAN_POINT ( 'NONE',  ( -18.46946985241279648, -9.509317228700149727, -174.4866625654999552 ) ) ;
#252301=DIRECTION ( 'NONE',  ( 1.000000000000000000, 0.000000000000000000, 0.000000000000000000 ) ) ;
#252401=VECTOR ( 'NONE', #131826, 1000.000000000000000 ) ;
#252415=CARTESIAN_POINT ( 'NONE',  ( 23.24999999999999645, -3.899999999988843502, -200.9999999999999432 ) ) ;
#252444=EDGE_LOOP ( 'NONE', ( #62995, #232052, #24539, #247797, #201006 ) ) ;
#252480=LINE ( 'NONE', #128709, #89392 ) ;
#252490=EDGE_LOOP ( 'NONE', ( #99505, #153811, #168342, #82557 ) ) ;
#252503=LINE ( 'NONE', #75192, #210987 ) ;
#252540=DIRECTION ( 'NONE',  ( 0.000000000000000000, 1.000000000000000000, 0.000000000000000000 ) ) ;
#252581=( GEOMETRIC_REPRESENTATION_CONTEXT ( 3 ) GLOBAL_UNCERTAINTY_ASSIGNED_CONTEXT ( ( #217437 ) ) GLOBAL_UNIT_ASSIGNED_CONTEXT ( ( #43531, #78771, #203868 ) ) REPRESENTATION_CONTEXT ( 'NONE', 'WORKASPACE' ) );
#252594=ORIENTED_EDGE ( 'NONE', *, *, #187803, .T. ) ;
#252599=CARTESIAN_POINT ( 'NONE',  ( 21.05000000000000071, 10.72371710471867701, -167.4999999999999716 ) ) ;
#252602=DIRECTION ( 'NONE',  ( 0.000000000000000000, 1.000000000000000000, 0.000000000000000000 ) ) ;
#252607=DIRECTION ( 'NONE',  ( 0.000000000000000000, 0.000000000000000000, 1.000000000000000000 ) ) ;
#252632=ORIENTED_EDGE ( 'NONE', *, *, #22593, .F. ) ;
#252645=CARTESIAN_POINT ( 'NONE',  ( -20.94999999999999929, 5.900000000011162093, -190.7809002353436085 ) ) ;
#252681=SPHERICAL_SURFACE ( 'NONE', #75668, 0.1000000000000000056 ) ;
#252682=LINE ( 'NONE', #10251, #86676 ) ;
#252692=FACE_OUTER_BOUND ( 'NONE', #87672, .T. ) ;
#252726=EDGE_CURVE ( 'NONE', #152124, #169487, #185640, .T. ) ;
#252734=LINE ( 'NONE', #136637, #101875 ) ;
#252758=VERTEX_POINT ( 'NONE', #247859 ) ;
#252778=AXIS2_PLACEMENT_3D ( 'NONE', #213880, #37841, #215163 ) ;
#252795=EDGE_CURVE ( 'NONE', #172330, #48880, #73250, .T. ) ;
#252796=VERTEX_POINT ( 'NONE', #131761 ) ;
#252797=EDGE_CURVE ( 'NONE', #52702, #108203, #186619, .T. ) ;
#252802=FACE_OUTER_BOUND ( 'NONE', #12001, .T. ) ;
#252817=DIRECTION ( 'NONE',  ( 2.952720810173289112E-16, -1.000000000000000000, 0.000000000000000000 ) ) ;
#252820=VERTEX_POINT ( 'NONE', #191774 ) ;
#252821=ORIENTED_EDGE ( 'NONE', *, *, #177394, .F. ) ;
#252933=CARTESIAN_POINT ( 'NONE',  ( 20.94999999999999929, 8.776282895303628706, -176.0586289951409071 ) ) ;
#252947=CARTESIAN_POINT ( 'NONE',  ( -23.15000000000000213, 2.600000000011156054, -180.7246219227620543 ) ) ;
#252954=PRODUCT_DEFINITION_FORMATION_WITH_SPECIFIED_SOURCE ( 'ANY', '', #170204, .NOT_KNOWN. ) ;
#252976=TOROIDAL_SURFACE ( 'NONE', #3164, 11.65000000000000036, 0.1000000000000000056 ) ;
#252983=CARTESIAN_POINT ( 'NONE',  ( 21.05000000000000071, 1.115600667400684642E-11, -167.4999999999999716 ) ) ;
#253004=VECTOR ( 'NONE', #48294, 1000.000000000000000 ) ;
#253024=VERTEX_POINT ( 'NONE', #206972 ) ;
#253060=PLANE ( 'NONE',  #62648 ) ;
#253071=ORIENTED_EDGE ( 'NONE', *, *, #81242, .T. ) ;
#253091=EDGE_LOOP ( 'NONE', ( #125387, #152934, #208864, #21788, #47061 ) ) ;
#253142=CARTESIAN_POINT ( 'NONE',  ( 20.04142135623731136, 11.75000000001116085, -192.2671572875253219 ) ) ;
#253153=ORIENTED_EDGE ( 'NONE', *, *, #204103, .F. ) ;
#253163=DIRECTION ( 'NONE',  ( 0.000000000000000000, -1.734723475976757554E-14, -1.000000000000000000 ) ) ;
#253176=EDGE_LOOP ( 'NONE', ( #151546, #240649, #9946, #158297, #220172, #193908, #199339, #153292, #3532, #175916 ) ) ;
#253208=TOROIDAL_SURFACE ( 'NONE', #111572, 0.2000000000000000111, 0.1000000000000000056 ) ;
#253212=AXIS2_PLACEMENT_3D ( 'NONE', #52185, #54760, #134288 ) ;
#253227=CARTESIAN_POINT ( 'NONE',  ( -21.05000000000000071, -1.851028230129704522, -179.1539132694224463 ) ) ;
#253240=DIRECTION ( 'NONE',  ( 0.000000000000000000, 0.000000000000000000, -1.000000000000000000 ) ) ;
#253245=LINE ( 'NONE', #214138, #190987 ) ;
#253253=DIRECTION ( 'NONE',  ( 0.000000000000000000, -0.8777080977375715243, 0.4791956752370512551 ) ) ;
#253261=ADVANCED_FACE ( 'NONE', ( #217217 ), #38606, .T. ) ;
#253267=ORIENTED_EDGE ( 'NONE', *, *, #177174, .T. ) ;
#253274=EDGE_CURVE ( 'NONE', #236886, #117760, #240653, .T. ) ;
#253279=CARTESIAN_POINT ( 'NONE',  ( 19.75857864376269291, 11.75000000001116263, -192.3499999999999659 ) ) ;
#253284=CYLINDRICAL_SURFACE ( 'NONE', #216825, 0.09999999999998898659 ) ;
#253299=VECTOR ( 'NONE', #253329, 1000.000000000000000 ) ;
#253304=PLANE ( 'NONE',  #181777 ) ;
#253311=CARTESIAN_POINT ( 'NONE',  ( 21.07928932188134397, 6.328516656404459262, -167.4011048543455615 ) ) ;
#253329=DIRECTION ( 'NONE',  ( 1.000000000000000000, 7.304098846218133681E-16, -4.217023435051677501E-16 ) ) ;
#253333=AXIS2_PLACEMENT_3D ( 'NONE', #194351, #15717, #174810 ) ;
#253471=CARTESIAN_POINT ( 'NONE',  ( 20.94999999999999929, 6.650000000011155876, -179.6499999999999773 ) ) ;
#253482=VECTOR ( 'NONE', #87063, 1000.000000000000000 ) ;
#253538=CARTESIAN_POINT ( 'NONE',  ( -18.50000000000000000, 9.250000000011157297, -188.6499999999999488 ) ) ;
#253547=CIRCLE ( 'NONE', #237004, 0.09999999999998898659 ) ;
#253549=DIRECTION ( 'NONE',  ( 0.000000000000000000, 0.000000000000000000, 1.000000000000000000 ) ) ;
#253577=PLANE ( 'NONE',  #33360 ) ;
#253584=DIRECTION ( 'NONE',  ( 3.265361837132813093E-16, -1.000000000000000000, -0.000000000000000000 ) ) ;
#253588=ORIENTED_EDGE ( 'NONE', *, *, #229554, .T. ) ;
#253595=ADVANCED_FACE ( 'NONE', ( #257290 ), #176549, .T. ) ;
#253623=AXIS2_PLACEMENT_3D ( 'NONE', #83149, #220145, #204407 ) ;
#253627=CARTESIAN_POINT ( 'NONE',  ( 21.05000000000000071, 6.258847123090474973, -167.4682416469444206 ) ) ;
#253628=FACE_OUTER_BOUND ( 'NONE', #89431, .T. ) ;
#253632=EDGE_CURVE ( 'NONE', #136769, #126189, #222842, .T. ) ;
#253640=CARTESIAN_POINT ( 'NONE',  ( -18.50000000000000000, -9.399999999988850163, -174.7972597596632625 ) ) ;
#253674=CARTESIAN_POINT ( 'NONE',  ( -18.50000000000000000, 9.350000000011156942, -179.8499999999999943 ) ) ;
#253691=ORIENTED_EDGE ( 'NONE', *, *, #114407, .F. ) ;
#253692=DIRECTION ( 'NONE',  ( 1.000000000000000000, 0.000000000000000000, 0.000000000000000000 ) ) ;
#253704=LINE ( 'NONE', #54221, #247146 ) ;
#253710=CARTESIAN_POINT ( 'NONE',  ( -20.94999999999999929, -11.48912529306489994, -197.8999999999999773 ) ) ;
#253730=DIRECTION ( 'NONE',  ( 0.000000000000000000, 0.1350103645451904977, -0.9908441862701596881 ) ) ;
#253748=DIRECTION ( 'NONE',  ( 0.7071067811865474617, 0.7071067811865474617, 0.000000000000000000 ) ) ;
#253749=CARTESIAN_POINT ( 'NONE',  ( -18.50000000000000000, 11.75000000001115197, -155.7499999999999716 ) ) ;
#253766=ORIENTED_EDGE ( 'NONE', *, *, #31925, .F. ) ;
#253771=ORIENTED_EDGE ( 'NONE', *, *, #9033, .F. ) ;
#253772=DIRECTION ( 'NONE',  ( 1.000000000000000000, 0.000000000000000000, 0.000000000000000000 ) ) ;
#253777=EDGE_LOOP ( 'NONE', ( #197631, #72662, #253267, #187937, #43010 ) ) ;
#253785=CARTESIAN_POINT ( 'NONE',  ( -20.99551997958277383, 11.75000000001053202, -194.1516591376910128 ) ) ;
#253830=ORIENTED_EDGE ( 'NONE', *, *, #232078, .F. ) ;
#253845=CARTESIAN_POINT ( 'NONE',  ( -21.07928932188134041, 6.328516656404449492, -167.4011048543455615 ) ) ;
#253889=CARTESIAN_POINT ( 'NONE',  ( 21.05000000000000071, -0.02138556592634376433, -161.1950388873158317 ) ) ;
#253919=DIRECTION ( 'NONE',  ( 0.000000000000000000, -0.8660254037844412611, -0.4999999999999956701 ) ) ;
#253933=EDGE_CURVE ( 'NONE', #50484, #163089, #254444, .T. ) ;
#253941=VERTEX_POINT ( 'NONE', #216626 ) ;
#253963=FACE_OUTER_BOUND ( 'NONE', #42732, .T. ) ;
#253994=ADVANCED_FACE ( 'NONE', ( #45693 ), #103077, .F. ) ;
#254005=ORIENTED_EDGE ( 'NONE', *, *, #166301, .F. ) ;
#254040=AXIS2_PLACEMENT_3D ( 'NONE', #27293, #246308, #225433 ) ;
#254053=CIRCLE ( 'NONE', #145711, 0.09999999999999484301 ) ;
#254084=DIRECTION ( 'NONE',  ( -1.000000000000000000, -3.265361837132813093E-16, 0.000000000000000000 ) ) ;
#254085=ORIENTED_EDGE ( 'NONE', *, *, #108814, .F. ) ;
#254087=DIRECTION ( 'NONE',  ( 1.000000000000000000, 0.000000000000000000, 0.000000000000000000 ) ) ;
#254128=CARTESIAN_POINT ( 'NONE',  ( 21.00000000000000000, 9.750000000011153745, -179.8499999999999943 ) ) ;
#254149=CARTESIAN_POINT ( 'NONE',  ( 18.49999999999999645, -1.164121893230052995, -208.9148480855715775 ) ) ;
#254184=EDGE_LOOP ( 'NONE', ( #166721, #131014, #209800, #216537 ) ) ;
#254244=AXIS2_PLACEMENT_3D ( 'NONE', #198114, #75627, #116027 ) ;
#254289=CARTESIAN_POINT ( 'NONE',  ( -23.15000000000000213, 11.65000000001115588, -193.9851942293460070 ) ) ;
#254337=CIRCLE ( 'NONE', #241875, 0.09999999999998898659 ) ;
#254345=CYLINDRICAL_SURFACE ( 'NONE', #46780, 0.09999999999999939493 ) ;
#254379=CARTESIAN_POINT ( 'NONE',  ( 22.57320508075688537, 11.75000000001115552, -167.4999999999999432 ) ) ;
#254402=AXIS2_PLACEMENT_3D ( 'NONE', #160649, #61525, #10544 ) ;
#254415=AXIS2_PLACEMENT_3D ( 'NONE', #121338, #20942, #125160 ) ;
#254428=CARTESIAN_POINT ( 'NONE',  ( 21.93340585900761397, 1.115541036281197940E-11, -160.1758529778929301 ) ) ;
#254435=CARTESIAN_POINT ( 'NONE',  ( -18.59999999999999787, -1.164121893230052995, -208.9148480855715775 ) ) ;
#254440=VERTEX_POINT ( 'NONE', #144135 ) ;
#254444=LINE ( 'NONE', #57538, #81523 ) ;
#254446=AXIS2_PLACEMENT_3D ( 'NONE', #137988, #119751, #96294 ) ;
#254464=EDGE_CURVE ( 'NONE', #5761, #20715, #65180, .T. ) ;
#254472=EDGE_CURVE ( 'NONE', #8977, #38476, #227542, .T. ) ;
#254531=ADVANCED_FACE ( 'NONE', ( #250942 ), #191017, .T. ) ;
#254573=CARTESIAN_POINT ( 'NONE',  ( 21.08078803292165659, 6.333012964448272442, -167.4208140128421860 ) ) ;
#254577=VERTEX_POINT ( 'NONE', #154469 ) ;
#254640=EDGE_CURVE ( 'NONE', #97822, #123700, #219297, .T. ) ;
#254681=EDGE_LOOP ( 'NONE', ( #43032, #72517, #115000 ) ) ;
#254691=VERTEX_POINT ( 'NONE', #136118 ) ;
#254716=ADVANCED_FACE ( 'NONE', ( #18764 ), #61269, .T. ) ;
#254717=CIRCLE ( 'NONE', #229817, 0.5000000000000004441 ) ;
#254721=EDGE_LOOP ( 'NONE', ( #28644, #204973, #230818, #197310 ) ) ;
#254754=CARTESIAN_POINT ( 'NONE',  ( -18.59999999999999787, 11.65000000001115232, -179.6499999999999773 ) ) ;
#254755=CIRCLE ( 'NONE', #184075, 0.1000000000000001860 ) ;
#254756=CARTESIAN_POINT ( 'NONE',  ( 18.49999999999999289, 10.20857864377385127, -188.8499999999999659 ) ) ;
#254783=LINE ( 'NONE', #257340, #137539 ) ;
#254835=LINE ( 'NONE', #234041, #3252 ) ;
#254846=CARTESIAN_POINT ( 'NONE',  ( -18.50000000000000000, -9.399999999988850163, -207.8820418481726335 ) ) ;
#254856=ORIENTED_EDGE ( 'NONE', *, *, #240803, .T. ) ;
#254866=CARTESIAN_POINT ( 'NONE',  ( 18.59999999999999432, 1.728086936805619311, -154.3844350051677452 ) ) ;
#254873=TOROIDAL_SURFACE ( 'NONE', #134122, 0.9750000000000019762, 0.1000000000000000056 ) ;
#254918=DIRECTION ( 'NONE',  ( 0.000000000000000000, 0.000000000000000000, -1.000000000000000000 ) ) ;
#254922=AXIS2_PLACEMENT_3D ( 'NONE', #15063, #58002, #171586 ) ;
#254924=AXIS2_PLACEMENT_3D ( 'NONE', #10185, #88397, #89692 ) ;
#254925=VERTEX_POINT ( 'NONE', #238812 ) ;
#254937=DIRECTION ( 'NONE',  ( 1.000000000000000000, 0.000000000000000000, 0.000000000000000000 ) ) ;
#254947=CARTESIAN_POINT ( 'NONE',  ( -21.05000000000000071, 6.540656951712397138, -167.5999999999999659 ) ) ;
#254950=LINE ( 'NONE', #98461, #96723 ) ;
#254951=CARTESIAN_POINT ( 'NONE',  ( 20.94999999999999929, 5.000000000011153745, -189.0947339810868755 ) ) ;
#254955=ORIENTED_EDGE ( 'NONE', *, *, #207240, .T. ) ;
#254960=CARTESIAN_POINT ( 'NONE',  ( -23.25000000000000000, 4.350000000011156054, -179.8499999999999943 ) ) ;
#255020=CIRCLE ( 'NONE', #188626, 0.1999999999999987899 ) ;
#255022=CARTESIAN_POINT ( 'NONE',  ( -21.05000000000000071, 11.75000000001115197, -194.1583993101029080 ) ) ;
#255047=ORIENTED_EDGE ( 'NONE', *, *, #128, .F. ) ;
#255057=AXIS2_PLACEMENT_3D ( 'NONE', #95008, #155018, #118443 ) ;
#255088=DIRECTION ( 'NONE',  ( 0.000000000000000000, 0.000000000000000000, -1.000000000000000000 ) ) ;
#255114=ORIENTED_EDGE ( 'NONE', *, *, #67121, .F. ) ;
#255127=CARTESIAN_POINT ( 'NONE',  ( 21.07928932188134397, 0.09889514566578838650, -161.1714833436012668 ) ) ;
#255133=FACE_OUTER_BOUND ( 'NONE', #193227, .T. ) ;
#255198=FACE_OUTER_BOUND ( 'NONE', #229496, .T. ) ;
#255201=CARTESIAN_POINT ( 'NONE',  ( 23.24999999999999289, 6.650000000011155876, -179.8499999999999943 ) ) ;
#255211=CARTESIAN_POINT ( 'NONE',  ( -21.05000000000000071, 11.75000000001115552, -193.9851942293460070 ) ) ;
#255228=CYLINDRICAL_SURFACE ( 'NONE', #18821, 0.1000000000000098310 ) ;
#255283=TOROIDAL_SURFACE ( 'NONE', #234484, 0.2000000000000000111, 0.1000000000000000056 ) ;
#255307=VECTOR ( 'NONE', #166509, 1000.000000000000000 ) ;
#255321=ORIENTED_EDGE ( 'NONE', *, *, #44655, .F. ) ;
#255353=CARTESIAN_POINT ( 'NONE',  ( -21.08035267497491816, 0.08268862478717949049, -161.1682931602169049 ) ) ;
#255422=DIRECTION ( 'NONE',  ( 0.000000000000000000, -1.000000000000000000, -1.897661533703519897E-16 ) ) ;
#255425=EDGE_CURVE ( 'NONE', #152513, #179560, #55983, .T. ) ;
#255442=DIRECTION ( 'NONE',  ( 1.000000000000000000, 0.000000000000000000, 0.000000000000000000 ) ) ;
#255474=ADVANCED_FACE ( 'NONE', ( #221478 ), #46700, .F. ) ;
#255494=CIRCLE ( 'NONE', #89136, 7.900000000000000355 ) ;
#255529=AXIS2_PLACEMENT_3D ( 'NONE', #220070, #60983, #166228 ) ;
#255532=AXIS2_PLACEMENT_3D ( 'NONE', #166811, #230611, #6410 ) ;
#255536=CIRCLE ( 'NONE', #201413, 0.09999999999998898659 ) ;
#255539=EDGE_CURVE ( 'NONE', #88951, #169154, #109298, .T. ) ;
#255569=FACE_OUTER_BOUND ( 'NONE', #109516, .T. ) ;
#255571=EDGE_LOOP ( 'NONE', ( #97829, #143141, #243590, #81704 ) ) ;
#255573=CARTESIAN_POINT ( 'NONE',  ( 21.00000000000000000, 9.750000000011153745, -179.8499999999999943 ) ) ;
#255588=ORIENTED_EDGE ( 'NONE', *, *, #134574, .F. ) ;
#255606=ADVANCED_FACE ( 'NONE', ( #224054 ), #243628, .T. ) ;
#255645=PLANE ( 'NONE',  #39529 ) ;
#255665=CARTESIAN_POINT ( 'NONE',  ( 20.85000000000000142, 7.120270961708750512, -204.6595630418393057 ) ) ;
#255690=VERTEX_POINT ( 'NONE', #169270 ) ;
#255692=CARTESIAN_POINT ( 'NONE',  ( 21.53752568622134334, 0.09897446127763709356, -160.7131921254513998 ) ) ;
#255713=ORIENTED_EDGE ( 'NONE', *, *, #82862, .F. ) ;
#255727=CYLINDRICAL_SURFACE ( 'NONE', #191810, 0.09999999999998898659 ) ;
#255763=DIRECTION ( 'NONE',  ( 0.000000000000000000, 0.3738317757009345654, 0.9274965247785492695 ) ) ;
#255780=VERTEX_POINT ( 'NONE', #75293 ) ;
#255845=EDGE_LOOP ( 'NONE', ( #154103, #188687, #138244, #175611 ) ) ;
#255855=CARTESIAN_POINT ( 'NONE',  ( -23.25000000000000000, 4.250000000011156409, -188.6499999999999488 ) ) ;
#255863=CARTESIAN_POINT ( 'NONE',  ( -20.94999999999999929, 10.29270135741298731, -206.4573618871519045 ) ) ;
#255868=VERTEX_POINT ( 'NONE', #165069 ) ;
#255951=CARTESIAN_POINT ( 'NONE',  ( -21.07928932188134041, 1.115600667400684642E-11, -167.4999999999999716 ) ) ;
#255952=CARTESIAN_POINT ( 'NONE',  ( -18.59999999999999787, 9.150000000011157653, -188.6499999999999488 ) ) ;
#255973=ORIENTED_EDGE ( 'NONE', *, *, #230944, .T. ) ;
#256005=AXIS2_PLACEMENT_3D ( 'NONE', #109646, #69267, #146207 ) ;
#256010=ORIENTED_EDGE ( 'NONE', *, *, #136528, .F. ) ;
#256049=CARTESIAN_POINT ( 'NONE',  ( -18.53317502108577486, 10.32263460347359363, -206.5605957968671760 ) ) ;
#256092=DIRECTION ( 'NONE',  ( 1.000000000000000000, 0.000000000000000000, 0.000000000000000000 ) ) ;
#256109=VECTOR ( 'NONE', #201495, 1000.000000000000000 ) ;
#256132=VERTEX_POINT ( 'NONE', #60195 ) ;
#256141=CARTESIAN_POINT ( 'NONE',  ( -20.64999999999999858, 2.000000000011154189, -187.7753780772378889 ) ) ;
#256166=CARTESIAN_POINT ( 'NONE',  ( -23.25000000000000000, 1.115600667400684642E-11, -208.8999999999999488 ) ) ;
#256194=ORIENTED_EDGE ( 'NONE', *, *, #64657, .T. ) ;
#256197=VECTOR ( 'NONE', #145891, 1000.000000000000000 ) ;
#256214=CARTESIAN_POINT ( 'NONE',  ( 20.94999999999999929, 5.000000000011153745, -188.5947339810868755 ) ) ;
#256225=CARTESIAN_POINT ( 'NONE',  ( -23.25000000000000000, -0.09999999998884338825, -155.8504291924551808 ) ) ;
#256272=CARTESIAN_POINT ( 'NONE',  ( 20.94999999999999574, 1.162701749949165642, -175.5999999999999659 ) ) ;
#256312=CIRCLE ( 'NONE', #177324, 4.049999999999998046 ) ;
#256347=CYLINDRICAL_SURFACE ( 'NONE', #67066, 0.09999999999999939493 ) ;
#256366=ADVANCED_FACE ( 'NONE', ( #152472 ), #84699, .F. ) ;
#256369=CARTESIAN_POINT ( 'NONE',  ( 20.94999999999999574, 14.00000000001115730, -172.9270925303825095 ) ) ;
#256379=CARTESIAN_POINT ( 'NONE',  ( 18.59999999999999432, -1.162701749926855266, -175.5999999999999659 ) ) ;
#256401=DIRECTION ( 'NONE',  ( 1.000000000000000000, -0.000000000000000000, -0.000000000000000000 ) ) ;
#256409=FACE_OUTER_BOUND ( 'NONE', #132250, .T. ) ;
#256461=EDGE_CURVE ( 'NONE', #85452, #98329, #238680, .T. ) ;
#256483=DIRECTION ( 'NONE',  ( 0.000000000000000000, 0.9999631594459056361, -0.008583690987128059571 ) ) ;
#256591=EDGE_LOOP ( 'NONE', ( #103738, #109760, #53686 ) ) ;
#256623=AXIS2_PLACEMENT_3D ( 'NONE', #69895, #169015, #189825 ) ;
#256659=FACE_OUTER_BOUND ( 'NONE', #133212, .T. ) ;
#256667=AXIS2_PLACEMENT_3D ( 'NONE', #117844, #219508, #177850 ) ;
#256708=FACE_OUTER_BOUND ( 'NONE', #161487, .T. ) ;
#256714=ADVANCED_FACE ( 'NONE', ( #53346 ), #113947, .T. ) ;
#256753=DIRECTION ( 'NONE',  ( 0.000000000000000000, 0.000000000000000000, 1.000000000000000000 ) ) ;
#256761=AXIS2_PLACEMENT_3D ( 'NONE', #158671, #136485, #2115 ) ;
#256763=EDGE_CURVE ( 'NONE', #159614, #121293, #193084, .T. ) ;
#256764=ORIENTED_EDGE ( 'NONE', *, *, #47858, .F. ) ;
#256801=DIRECTION ( 'NONE',  ( 1.000000000000000000, 0.000000000000000000, 0.000000000000000000 ) ) ;
#256811=ORIENTED_EDGE ( 'NONE', *, *, #220741, .T. ) ;
#256825=CARTESIAN_POINT ( 'NONE',  ( 23.24999999999999645, 5.600000000011153389, -188.5947339810868755 ) ) ;
#256842=AXIS2_PLACEMENT_3D ( 'NONE', #201251, #181706, #57877 ) ;
#256902=CARTESIAN_POINT ( 'NONE',  ( -21.05000000000000071, 1.115600667400684642E-11, -167.4999999999999716 ) ) ;
#256906=ORIENTED_EDGE ( 'NONE', *, *, #88429, .F. ) ;
#256919=ORIENTED_EDGE ( 'NONE', *, *, #108550, .T. ) ;
#256945=EDGE_LOOP ( 'NONE', ( #32854, #5404, #75334, #176954 ) ) ;
#256956=ORIENTED_EDGE ( 'NONE', *, *, #143253, .T. ) ;
#256993=ORIENTED_EDGE ( 'NONE', *, *, #131843, .F. ) ;
#256997=DIRECTION ( 'NONE',  ( -1.000000000000000000, -8.673617379884087537E-15, 0.000000000000000000 ) ) ;
#257037=DIRECTION ( 'NONE',  ( -1.000000000000000000, -0.000000000000000000, -0.000000000000000000 ) ) ;
#257048=ORIENTED_EDGE ( 'NONE', *, *, #216702, .T. ) ;
#257052=DIRECTION ( 'NONE',  ( 1.000000000000000000, 0.000000000000000000, -0.000000000000000000 ) ) ;
#257084=DIRECTION ( 'NONE',  ( 0.000000000000000000, 0.000000000000000000, -1.000000000000000000 ) ) ;
#257086=CARTESIAN_POINT ( 'NONE',  ( 21.05000000000000071, 1.115600667400684642E-11, -179.6499999999999773 ) ) ;
#257089=DIRECTION ( 'NONE',  ( -1.000000000000000000, 0.000000000000000000, 0.000000000000000000 ) ) ;
#257111=CARTESIAN_POINT ( 'NONE',  ( 22.47071067811865319, 7.720074744509199505, -167.4009075452973434 ) ) ;
#257148=EDGE_CURVE ( 'NONE', #22668, #38886, #22572, .T. ) ;
#257169=DIRECTION ( 'NONE',  ( 0.000000000000000000, 0.000000000000000000, 1.000000000000000000 ) ) ;
#257175=DIRECTION ( 'NONE',  ( 0.000000000000000000, 0.000000000000000000, -1.000000000000000000 ) ) ;
#257186=ADVANCED_FACE ( 'NONE', ( #200251 ), #161131, .F. ) ;
#257209=( BOUNDED_SURFACE ( )  B_SPLINE_SURFACE ( 3, 2, ( 
 ( #11409, #53082, #49233 ),
 ( #8833, #32271, #150907 ),
 ( #73970, #33574, #251275 ),
 ( #92204, #212180, #173089 ) ),
 .UNSPECIFIED., .F., .F., .F. ) 
 B_SPLINE_SURFACE_WITH_KNOTS ( ( 4, 4 ),
 ( 3, 3 ),
 ( 0.04058434257139475337, 0.04256401539001600232 ),
 ( 0.000000000000000000, 1.000000000000000000 ),
 .UNSPECIFIED. ) 
 GEOMETRIC_REPRESENTATION_ITEM ( )  RATIONAL_B_SPLINE_SURFACE ( (
 ( 1.000000000000000000, 0.7103081912007809251, 1.000000000000000000),
 ( 1.000000000000000000, 0.7104998333556865608, 1.000000000000000000),
 ( 1.000000000000000000, 0.7107238315753950930, 1.000000000000000000),
 ( 1.000000000000000000, 0.7110073749539780330, 1.000000000000000000) ) ) 
 REPRESENTATION_ITEM ( '' )  SURFACE ( )  );
#257212=EDGE_CURVE ( 'NONE', #90455, #249596, #144985, .T. ) ;
#257262=ORIENTED_EDGE ( 'NONE', *, *, #117445, .F. ) ;
#257265=PLANE ( 'NONE',  #128693 ) ;
#257290=FACE_OUTER_BOUND ( 'NONE', #40558, .T. ) ;
#257292=ORIENTED_EDGE ( 'NONE', *, *, #12563, .F. ) ;
#257304=CARTESIAN_POINT ( 'NONE',  ( -23.25000000000000000, 11.75000000001115552, -179.6499999999999773 ) ) ;
#257306=DIRECTION ( 'NONE',  ( 1.000000000000000000, 0.000000000000000000, 0.000000000000000000 ) ) ;
#257340=CARTESIAN_POINT ( 'NONE',  ( 23.25000000000000355, -22.45632476061176774, -174.2938984477315785 ) ) ;
#257357=EDGE_LOOP ( 'NONE', ( #74013, #209766, #239934, #34126 ) ) ;
#257361=ADVANCED_FACE ( 'NONE', ( #145401 ), #26778, .F. ) ;
#257398=ADVANCED_FACE ( 'NONE', ( #86693 ), #39532, .F. ) ;
#257407=CARTESIAN_POINT ( 'NONE',  ( 20.95512820512820795, 8.876151316299273120, -179.7001728591287133 ) ) ;
#257427=DIRECTION ( 'NONE',  ( 0.000000000000000000, 0.000000000000000000, -1.000000000000000000 ) ) ;
#257429=VERTEX_POINT ( 'NONE', #68454 ) ;
#257446=FACE_OUTER_BOUND ( 'NONE', #138986, .T. ) ;
#257448=CARTESIAN_POINT ( 'NONE',  ( 20.95520789717937404, 10.57693059939611224, -175.0802329738748142 ) ) ;
#257461=ORIENTED_EDGE ( 'NONE', *, *, #3637, .T. ) ;
#257464=CARTESIAN_POINT ( 'NONE',  ( -20.54999999999999716, 2.000000000011154189, -180.7246219227620543 ) ) ;
#257522=VECTOR ( 'NONE', #67974, 1000.000000000000000 ) ;
#257527=ORIENTED_EDGE ( 'NONE', *, *, #59661, .F. ) ;
#257540=DIRECTION ( 'NONE',  ( 1.000000000000000000, -0.000000000000000000, -0.000000000000000000 ) ) ;
#257562=AXIS2_PLACEMENT_3D ( 'NONE', #157009, #233952, #56564 ) ;
#257576=AXIS2_PLACEMENT_3D ( 'NONE', #13119, #32718, #9253 ) ;
#257620=VERTEX_POINT ( 'NONE', #146056 ) ;
#257624=VERTEX_POINT ( 'NONE', #165651 ) ;
#257683=CARTESIAN_POINT ( 'NONE',  ( -20.64999999999999858, 2.000000000011154189, -187.7753780772378889 ) ) ;
#257697=EDGE_LOOP ( 'NONE', ( #170329, #244464, #209211, #126751 ) ) ;
#257727=VECTOR ( 'NONE', #72177, 1000.000000000000000 ) ;
#257735=FACE_OUTER_BOUND ( 'NONE', #170409, .T. ) ;
#257770=ORIENTED_EDGE ( 'NONE', *, *, #215678, .T. ) ;
#257788=CARTESIAN_POINT ( 'NONE',  ( -18.50000000000000000, 7.021664781911246322, -204.8335654018972605 ) ) ;
#257792=EDGE_CURVE ( 'NONE', #197017, #25429, #52136, .T. ) ;
#257805=CARTESIAN_POINT ( 'NONE',  ( -23.15000000000000213, 2.000000000011154189, -188.3753780772378548 ) ) ;
#257809=EDGE_CURVE ( 'NONE', #160946, #216004, #131251, .T. ) ;
#257847=ORIENTED_EDGE ( 'NONE', *, *, #194937, .T. ) ;
#257861=CARTESIAN_POINT ( 'NONE',  ( 21.05000000000000071, 6.350000000011161383, -177.3438220896831012 ) ) ;
#257868=CARTESIAN_POINT ( 'NONE',  ( -23.25000000000000000, -11.74999999998884448, -197.8999999999999773 ) ) ;
#257878=SPHERICAL_SURFACE ( 'NONE', #110273, 0.1000000000000000056 ) ;
#257900=ORIENTED_EDGE ( 'NONE', *, *, #177419, .T. ) ;
#257902=DIRECTION ( 'NONE',  ( 0.000000000000000000, 0.000000000000000000, -1.000000000000000000 ) ) ;
#257905=ORIENTED_EDGE ( 'NONE', *, *, #224996, .F. ) ;
#257910=ORIENTED_EDGE ( 'NONE', *, *, #115659, .F. ) ;
#257925=LINE ( 'NONE', #208292, #152409 ) ;
#257959=ADVANCED_FACE ( 'NONE', ( #121096 ), #241016, .F. ) ;
#257966=FACE_OUTER_BOUND ( 'NONE', #249725, .T. ) ;
#257978=CARTESIAN_POINT ( 'NONE',  ( -23.25000000000000000, -1.249999999988843369, -208.8004807544150481 ) ) ;
#257984=CARTESIAN_POINT ( 'NONE',  ( 20.85000000000000142, -1.835859311432481045, -212.5044391687984842 ) ) ;
#257985=ORIENTED_EDGE ( 'NONE', *, *, #67359, .T. ) ;
#258005=DIRECTION ( 'NONE',  ( 1.000000000000000000, -0.000000000000000000, -0.000000000000000000 ) ) ;
#258006=ADVANCED_FACE ( 'NONE', ( #183607 ), #152127, .F. ) ;
#258010=DIRECTION ( 'NONE',  ( 0.000000000000000000, 0.6728971962617388280, 0.7397360091702248619 ) ) ;
#258013=ORIENTED_EDGE ( 'NONE', *, *, #52609, .F. ) ;
#258036=DIRECTION ( 'NONE',  ( -1.000000000000000000, 0.000000000000000000, 0.000000000000000000 ) ) ;
#258067=AXIS2_PLACEMENT_3D ( 'NONE', #125302, #86134, #106999 ) ;
ENDSEC;
END-ISO-10303-21;
